ISO-10303-21;
HEADER;
FILE_DESCRIPTION (('STEP AP214'),
    '1' );
FILE_NAME ('Injection Molded Chain Links 11.step',
    '2026-10-08T22:59:04',
    ( '' ),
    ( '' ),
    'SwSTEP 2.0',
    'SolidWorks 2020',
    '' );
FILE_SCHEMA (( 'AUTOMOTIVE_DESIGN' ));
ENDSEC;

DATA;
#24=ORIENTED_EDGE ( 'NONE', *, *, #246973, .F. ) ;
#31=ORIENTED_EDGE ( 'NONE', *, *, #146192, .F. ) ;
#79=CARTESIAN_POINT ( 'NONE',  ( -20.54999999999999716, 87.75000000001259082, -191.1731074845242517 ) ) ;
#90=ORIENTED_EDGE ( 'NONE', *, *, #88866, .F. ) ;
#95=CARTESIAN_POINT ( 'NONE',  ( -18.50000000000000000, 76.00000000001244871, -170.0231074845243597 ) ) ;
#119=ORIENTED_EDGE ( 'NONE', *, *, #90031, .T. ) ;
#141=LINE ( 'NONE', #80958, #244386 ) ;
#158=AXIS2_PLACEMENT_3D ( 'NONE', #230625, #35020, #51950 ) ;
#176=VERTEX_POINT ( 'NONE', #31196 ) ;
#181=LINE ( 'NONE', #1467, #236049 ) ;
#184=DIRECTION ( 'NONE',  ( -1.000000000000000000, 2.952720810173289112E-16, 2.061873921506763405E-30 ) ) ;
#191=CARTESIAN_POINT ( 'NONE',  ( 18.49999999999999289, 69.55000000001277272, -215.2731074845244166 ) ) ;
#196=EDGE_CURVE ( 'NONE', #151569, #28788, #226776, .T. ) ;
#203=FACE_OUTER_BOUND ( 'NONE', #140613, .T. ) ;
#211=CARTESIAN_POINT ( 'NONE',  ( -23.15000000000000213, 74.00000000001254818, -183.2477294072864709 ) ) ;
#264=ADVANCED_FACE ( 'NONE', ( #17990 ), #237050, .T. ) ;
#271=DIRECTION ( 'NONE',  ( 3.265361837132813093E-16, 1.000000000000000000, 6.982962677686266711E-15 ) ) ;
#288=FACE_OUTER_BOUND ( 'NONE', #250177, .T. ) ;
#296=CARTESIAN_POINT ( 'NONE',  ( 22.50927854361892244, 76.10085807354055021, -215.2726746105512348 ) ) ;
#308=CARTESIAN_POINT ( 'NONE',  ( -23.25000000000000000, 76.00000000001264766, -199.4731074845243484 ) ) ;
#348=CARTESIAN_POINT ( 'NONE',  ( 20.95000000000000284, 64.36312671090941251, -176.8448666978491985 ) ) ;
#431=CARTESIAN_POINT ( 'NONE',  ( -18.59999999999999787, 64.25000000001244871, -170.0231074845244166 ) ) ;
#446=EDGE_CURVE ( 'NONE', #92780, #16498, #242176, .T. ) ;
#450=CARTESIAN_POINT ( 'NONE',  ( 21.05000000000000071, 69.74218538953655866, -203.6208977758331855 ) ) ;
#463=DIRECTION ( 'NONE',  ( -1.000000000000000000, 0.000000000000000000, -0.000000000000000000 ) ) ;
#474=EDGE_LOOP ( 'NONE', ( #173375, #214797, #80010, #38035 ) ) ;
#487=AXIS2_PLACEMENT_3D ( 'NONE', #75647, #218977, #256772 ) ;
#505=CARTESIAN_POINT ( 'NONE',  ( -18.40000000000000213, 85.50000000001242029, -163.4229180933022860 ) ) ;
#509=EDGE_CURVE ( 'NONE', #239043, #160419, #536, .T. ) ;
#512=EDGE_LOOP ( 'NONE', ( #80460, #76518, #125761, #137091, #11787, #28045, #59353 ) ) ;
#530=AXIS2_PLACEMENT_3D ( 'NONE', #16682, #154923, #256492 ) ;
#536=CIRCLE ( 'NONE', #105450, 0.09999999999998898659 ) ;
#545=ORIENTED_EDGE ( 'NONE', *, *, #247092, .F. ) ;
#556=DIRECTION ( 'NONE',  ( 0.000000000000000000, 6.982962677686267499E-15, -1.000000000000000000 ) ) ;
#559=CARTESIAN_POINT ( 'NONE',  ( -21.14999999999999858, 64.35000000001262777, -196.7392418215462726 ) ) ;
#566=DIRECTION ( 'NONE',  ( 0.000000000000000000, 0.000000000000000000, -1.000000000000000000 ) ) ;
#577=DIRECTION ( 'NONE',  ( 0.000000000000000000, -7.172728831056617961E-15, 1.000000000000000000 ) ) ;
#592=( BOUNDED_SURFACE ( )  B_SPLINE_SURFACE ( 3, 2, ( 
 ( #139194, #218736, #199202 ),
 ( #179650, #4506, #84001 ),
 ( #64499, #144017, #44937 ),
 ( #124484, #145299, #244407 ),
 ( #65778, #224842, #130882 ),
 ( #30529, #129613, #87880 ) ),
 .UNSPECIFIED., .F., .F., .F. ) 
 B_SPLINE_SURFACE_WITH_KNOTS ( ( 4, 2, 4 ),
 ( 3, 3 ),
 ( 0.0001342700090130149982, 0.0002909192928057525150, 0.0004475685765984900046 ),
 ( 0.000000000000000000, 1.000000000000000000 ),
 .UNSPECIFIED. ) 
 GEOMETRIC_REPRESENTATION_ITEM ( )  RATIONAL_B_SPLINE_SURFACE ( (
 ( 1.000000000000000000, 0.7250110520819876836, 1.000000000000000000),
 ( 1.000000000000000000, 0.7257599279122789460, 1.000000000000000000),
 ( 1.000000000000000000, 0.7137594617299418687, 1.000000000000000000),
 ( 1.000000000000000000, 0.6959270178795029516, 1.000000000000000000),
 ( 1.000000000000000000, 0.6919879549349066128, 1.000000000000000000),
 ( 1.000000000000000000, 0.7071067811865494601, 1.000000000000000000) ) ) 
 REPRESENTATION_ITEM ( '' )  SURFACE ( )  );
#597=AXIS2_PLACEMENT_3D ( 'NONE', #30263, #69391, #11991 ) ;
#611=VERTEX_POINT ( 'NONE', #153398 ) ;
#619=DIRECTION ( 'NONE',  ( -2.578261006436899437E-14, -0.1350103645451973811, 0.9908441862701586889 ) ) ;
#622=CARTESIAN_POINT ( 'NONE',  ( -21.05000000000000071, 76.25610579210490414, -203.5580039261966760 ) ) ;
#650=ORIENTED_EDGE ( 'NONE', *, *, #214860, .F. ) ;
#654=VERTEX_POINT ( 'NONE', #97177 ) ;
#670=VERTEX_POINT ( 'NONE', #54237 ) ;
#687=EDGE_CURVE ( 'NONE', #34471, #187182, #9630, .T. ) ;
#700=EDGE_CURVE ( 'NONE', #10156, #141625, #51297, .T. ) ;
#702=CARTESIAN_POINT ( 'NONE',  ( 20.04142135623731136, 64.25000000001250555, -178.8731074845244393 ) ) ;
#717=CARTESIAN_POINT ( 'NONE',  ( 20.94999999999999929, 77.36242903720570041, -162.1342262366031548 ) ) ;
#733=EDGE_LOOP ( 'NONE', ( #232923, #215789, #253052, #35694 ) ) ;
#751=CIRCLE ( 'NONE', #108925, 0.09999999999998898659 ) ;
#761=DIRECTION ( 'NONE',  ( 1.224646799147353207E-16, -1.000000000000000000, -6.982962677686266711E-15 ) ) ;
#778=DIRECTION ( 'NONE',  ( -2.342056488767301376E-15, 0.1350103645451974088, -0.9908441862701587999 ) ) ;
#788=VECTOR ( 'NONE', #158193, 1000.000000000000000 ) ;
#796=CARTESIAN_POINT ( 'NONE',  ( 18.48413544395647534, 85.66430403364030610, -163.3400024914861888 ) ) ;
#800=ADVANCED_FACE ( 'NONE', ( #141486 ), #137617, .F. ) ;
#821=CARTESIAN_POINT ( 'NONE',  ( 22.42196299218230493, 75.99755832602546946, -215.1727191871738398 ) ) ;
#839=CIRCLE ( 'NONE', #250650, 2.000000000000001776 ) ;
#848=ORIENTED_EDGE ( 'NONE', *, *, #73889, .F. ) ;
#859=AXIS2_PLACEMENT_3D ( 'NONE', #123694, #27188, #143234 ) ;
#868=EDGE_CURVE ( 'NONE', #145080, #106770, #13915, .T. ) ;
#944=CARTESIAN_POINT ( 'NONE',  ( -20.94999999999999929, 76.25610579210490414, -203.5580039261966760 ) ) ;
#964=CARTESIAN_POINT ( 'NONE',  ( 18.59999999999999076, 69.45000000001252261, -182.2731074845244166 ) ) ;
#995=CARTESIAN_POINT ( 'NONE',  ( -22.59999999999999787, 64.25043287652329127, -203.6239658536231616 ) ) ;
#1012=AXIS2_PLACEMENT_3D ( 'NONE', #50416, #71315, #248640 ) ;
#1035=CARTESIAN_POINT ( 'NONE',  ( -20.54999999999999716, 76.00000000001244871, -170.0231074845243597 ) ) ;
#1039=CARTESIAN_POINT ( 'NONE',  ( -20.85000000000000142, 77.25000000001239187, -162.2226267301092548 ) ) ;
#1046=DIRECTION ( 'NONE',  ( -1.000000000000000000, 2.952720810173289112E-16, 2.061873921506763405E-30 ) ) ;
#1061=LINE ( 'NONE', #25789, #119140 ) ;
#1068=CARTESIAN_POINT ( 'NONE',  ( 18.59999999999999076, 68.92903212821357783, -166.2765432626560766 ) ) ;
#1069=DIRECTION ( 'NONE',  ( 1.000000000000000000, 0.000000000000000000, 0.000000000000000000 ) ) ;
#1080=ADVANCED_FACE ( 'NONE', ( #36672 ), #154068, .F. ) ;
#1087=EDGE_LOOP ( 'NONE', ( #140736, #240001, #225855, #36280 ) ) ;
#1103=EDGE_CURVE ( 'NONE', #196419, #152244, #238187, .T. ) ;
#1116=ADVANCED_FACE ( 'NONE', ( #84706 ), #204865, .T. ) ;
#1122=SPHERICAL_SURFACE ( 'NONE', #193152, 0.1000000000000000056 ) ;
#1128=CARTESIAN_POINT ( 'NONE',  ( -18.39999999999999858, 85.60000000001241460, -163.4229180933022576 ) ) ;
#1226=CARTESIAN_POINT ( 'NONE',  ( -23.25000000000000000, 76.00000000001244871, -170.0231074845243597 ) ) ;
#1231=CYLINDRICAL_SURFACE ( 'NONE', #44591, 0.09999999999998898659 ) ;
#1232=CARTESIAN_POINT ( 'NONE',  ( 21.05000000000000071, 85.50000000001251976, -179.9170766071767389 ) ) ;
#1247=CARTESIAN_POINT ( 'NONE',  ( 21.05000000000000071, 67.22371710472012296, -191.3731074845244109 ) ) ;
#1258=EDGE_CURVE ( 'NONE', #252901, #127123, #130020, .T. ) ;
#1296=LINE ( 'NONE', #62581, #184822 ) ;
#1330=ORIENTED_EDGE ( 'NONE', *, *, #171509, .T. ) ;
#1377=ORIENTED_EDGE ( 'NONE', *, *, #102892, .F. ) ;
#1396=ORIENTED_EDGE ( 'NONE', *, *, #10929, .T. ) ;
#1406=DIRECTION ( 'NONE',  ( 0.000000000000000000, -1.000000000000000000, -7.272083257015735086E-15 ) ) ;
#1414=EDGE_LOOP ( 'NONE', ( #203161, #178221, #177205, #167831 ) ) ;
#1417=CARTESIAN_POINT ( 'NONE',  ( -20.64999999999999858, 71.65000000001253966, -182.3731074845244109 ) ) ;
#1424=ORIENTED_EDGE ( 'NONE', *, *, #36460, .F. ) ;
#1442=DIRECTION ( 'NONE',  ( -1.000000000000000000, 0.000000000000000000, -0.000000000000000000 ) ) ;
#1449=DIRECTION ( 'NONE',  ( -1.000000000000000000, 1.836970198721029934E-16, 1.282749433769087757E-30 ) ) ;
#1459=EDGE_CURVE ( 'NONE', #21234, #49859, #17775, .T. ) ;
#1464=ORIENTED_EDGE ( 'NONE', *, *, #230041, .F. ) ;
#1465=ORIENTED_EDGE ( 'NONE', *, *, #68076, .T. ) ;
#1467=CARTESIAN_POINT ( 'NONE',  ( 20.94999999999999929, 77.34915357198845243, -162.2356101489344837 ) ) ;
#1468=CARTESIAN_POINT ( 'NONE',  ( -23.15000000000000213, 64.35000000001258513, -191.3731074845244393 ) ) ;
#1473=EDGE_CURVE ( 'NONE', #233248, #67516, #20631, .T. ) ;
#1475=CARTESIAN_POINT ( 'NONE',  ( 18.59999999999997655, 77.16412189325360771, -162.1082593989527254 ) ) ;
#1490=DIRECTION ( 'NONE',  ( 0.000000000000000000, 0.000000000000000000, 1.000000000000000000 ) ) ;
#1496=CARTESIAN_POINT ( 'NONE',  ( -23.15000000000000213, 73.50000000001254818, -183.2477294072864709 ) ) ;
#1515=CARTESIAN_POINT ( 'NONE',  ( 18.59999999999999076, 65.79142135624984178, -182.2731074845244450 ) ) ;
#1556=DIRECTION ( 'NONE',  ( 1.000000000000000000, 0.000000000000000000, 0.000000000000000000 ) ) ;
#1558=CARTESIAN_POINT ( 'NONE',  ( 20.95575313997065336, 65.38544669673778742, -195.9018167825796013 ) ) ;
#1585=EDGE_LOOP ( 'NONE', ( #206508, #204425, #175251, #229716 ) ) ;
#1611=ORIENTED_EDGE ( 'NONE', *, *, #235679, .F. ) ;
#1645=EDGE_CURVE ( 'NONE', #160984, #20407, #109363, .T. ) ;
#1651=EDGE_CURVE ( 'NONE', #102497, #9837, #51694, .T. ) ;
#1660=CARTESIAN_POINT ( 'NONE',  ( -18.58693740092131108, 85.40643215026551616, -196.3982910280228111 ) ) ;
#1703=CARTESIAN_POINT ( 'NONE',  ( -21.59142135623730852, 68.15000000001259650, -191.2731074845244166 ) ) ;
#1704=ORIENTED_EDGE ( 'NONE', *, *, #47457, .F. ) ;
#1711=DIRECTION ( 'NONE',  ( 0.000000000000000000, 0.000000000000000000, 1.000000000000000000 ) ) ;
#1722=CARTESIAN_POINT ( 'NONE',  ( 20.94999999999999929, 76.00000000001244871, -170.0231074845243597 ) ) ;
#1727=CARTESIAN_POINT ( 'NONE',  ( 22.45305468355010703, 76.10085836911248691, -215.2726746080140856 ) ) ;
#1734=EDGE_CURVE ( 'NONE', #111659, #234461, #34758, .T. ) ;
#1735=CARTESIAN_POINT ( 'NONE',  ( 21.11833042828125429, 69.55435530615748974, -203.5302079935838151 ) ) ;
#1762=FACE_OUTER_BOUND ( 'NONE', #190353, .T. ) ;
#1777=ORIENTED_EDGE ( 'NONE', *, *, #186905, .F. ) ;
#1786=CARTESIAN_POINT ( 'NONE',  ( -20.54999999999999716, 71.65000000001259650, -191.1731074845243654 ) ) ;
#1793=AXIS2_PLACEMENT_3D ( 'NONE', #96958, #176557, #156997 ) ;
#1806=ADVANCED_FACE ( 'NONE', ( #218474 ), #129726, .T. ) ;
#1807=ORIENTED_EDGE ( 'NONE', *, *, #101523, .T. ) ;
#1810=ORIENTED_EDGE ( 'NONE', *, *, #7566, .F. ) ;
#1825=CARTESIAN_POINT ( 'NONE',  ( 20.94999999999999929, 84.66355140188167638, -179.5472086025916099 ) ) ;
#1841=DIRECTION ( 'NONE',  ( -0.000000000000000000, -1.000000000000000000, -8.609265936414532828E-15 ) ) ;
#1870=ORIENTED_EDGE ( 'NONE', *, *, #1459, .F. ) ;
#1893=ORIENTED_EDGE ( 'NONE', *, *, #250623, .T. ) ;
#1907=CARTESIAN_POINT ( 'NONE',  ( -23.25000000000000000, 71.65000000001259650, -191.1731074845243654 ) ) ;
#1914=CARTESIAN_POINT ( 'NONE',  ( 20.95512820512820440, 65.37615131630072085, -191.3229454651000481 ) ) ;
#1921=ADVANCED_FACE ( 'NONE', ( #168844 ), #207948, .T. ) ;
#1946=CARTESIAN_POINT ( 'NONE',  ( 21.05000000000000071, 76.00000000001267608, -203.5231074845243597 ) ) ;
#1948=CYLINDRICAL_SURFACE ( 'NONE', #15214, 0.1000000000000046685 ) ;
#1961=CARTESIAN_POINT ( 'NONE',  ( 20.52683494730046476, 67.01946918171127265, -195.0178547619902076 ) ) ;
#1971=FACE_OUTER_BOUND ( 'NONE', #116172, .T. ) ;
#1993=AXIS2_PLACEMENT_3D ( 'NONE', #142244, #183945, #61432 ) ;
#1997=ORIENTED_EDGE ( 'NONE', *, *, #246276, .F. ) ;
#1998=EDGE_CURVE ( 'NONE', #121258, #56183, #59641, .T. ) ;
#2000=CARTESIAN_POINT ( 'NONE',  ( 19.96984138294296329, 64.25000000001250555, -178.7985354133239753 ) ) ;
#2002=DIRECTION ( 'NONE',  ( 0.000000000000000000, -0.9908441862701791170, 0.1350103645450472789 ) ) ;
#2036=AXIS2_PLACEMENT_3D ( 'NONE', #33109, #70936, #89171 ) ;
#2083=CIRCLE ( 'NONE', #185278, 0.1000000000000033362 ) ;
#2096=CARTESIAN_POINT ( 'NONE',  ( 18.37172112093829668, 85.57096165225587470, -163.2063730310406697 ) ) ;
#2104=ORIENTED_EDGE ( 'NONE', *, *, #158035, .T. ) ;
#2113=ORIENTED_EDGE ( 'NONE', *, *, #171486, .F. ) ;
#2121=DIRECTION ( 'NONE',  ( 0.000000000000000000, -6.982962677686266711E-15, 1.000000000000000000 ) ) ;
#2132=CARTESIAN_POINT ( 'NONE',  ( 21.14999999999999858, 87.75000000001259082, -191.2731074845242745 ) ) ;
#2179=CARTESIAN_POINT ( 'NONE',  ( -21.33487959338958362, 69.27444184810150318, -203.5231074845243882 ) ) ;
#2184=CARTESIAN_POINT ( 'NONE',  ( 21.05000000000000071, 76.00000000001242029, -165.9231074845243654 ) ) ;
#2219=VECTOR ( 'NONE', #3106, 1000.000000000000000 ) ;
#2272=ORIENTED_EDGE ( 'NONE', *, *, #247706, .T. ) ;
#2280=EDGE_CURVE ( 'NONE', #246278, #91774, #81227, .T. ) ;
#2284=CYLINDRICAL_SURFACE ( 'NONE', #233573, 0.1000000000000028644 ) ;
#2305=ORIENTED_EDGE ( 'NONE', *, *, #186067, .F. ) ;
#2325=CARTESIAN_POINT ( 'NONE',  ( -20.54999999999999716, 76.00000000001244871, -170.0231074845243597 ) ) ;
#2402=CIRCLE ( 'NONE', #177245, 11.69999999999998863 ) ;
#2412=CARTESIAN_POINT ( 'NONE',  ( -20.94999999999999929, 77.83534155023701828, -191.9679561919613491 ) ) ;
#2425=AXIS2_PLACEMENT_3D ( 'NONE', #153513, #135160, #16531 ) ;
#2426=ORIENTED_EDGE ( 'NONE', *, *, #77999, .F. ) ;
#2433=CARTESIAN_POINT ( 'NONE',  ( -20.64999999999999858, 71.65000000001259650, -191.1731074845243654 ) ) ;
#2448=ORIENTED_EDGE ( 'NONE', *, *, #19922, .T. ) ;
#2454=FACE_OUTER_BOUND ( 'NONE', #90440, .T. ) ;
#2458=DIRECTION ( 'NONE',  ( 0.000000000000000000, -7.026728003956695223E-15, 1.000000000000000000 ) ) ;
#2506=ADVANCED_FACE ( 'NONE', ( #178670 ), #80787, .T. ) ;
#2521=FACE_OUTER_BOUND ( 'NONE', #50200, .T. ) ;
#2538=CARTESIAN_POINT ( 'NONE',  ( 21.12802099929860944, 67.21944740979039068, -191.2749174995927888 ) ) ;
#2558=ORIENTED_EDGE ( 'NONE', *, *, #78435, .T. ) ;
#2569=CARTESIAN_POINT ( 'NONE',  ( 21.06490991615909891, 65.27510865242548732, -191.3193961309912936 ) ) ;
#2587=ADVANCED_FACE ( 'NONE', ( #7543 ), #6245, .F. ) ;
#2600=ORIENTED_EDGE ( 'NONE', *, *, #135602, .T. ) ;
#2610=DIRECTION ( 'NONE',  ( -7.304098846218134667E-16, 1.000000000000000000, 6.982962677686266711E-15 ) ) ;
#2632=CIRCLE ( 'NONE', #239986, 0.1000000000000046685 ) ;
#2641=DIRECTION ( 'NONE',  ( 0.000000000000000000, -1.000000000000000000, -6.982962677686265922E-15 ) ) ;
#2692=DIRECTION ( 'NONE',  ( 0.000000000000000000, -7.272083257015735086E-15, 1.000000000000000000 ) ) ;
#2723=LINE ( 'NONE', #255733, #156151 ) ;
#2729=CARTESIAN_POINT ( 'NONE',  ( -21.59142135623730852, 68.15000000001259650, -191.1731074845243938 ) ) ;
#2739=ORIENTED_EDGE ( 'NONE', *, *, #38621, .F. ) ;
#2773=CARTESIAN_POINT ( 'NONE',  ( -18.59999999999999787, 85.52395432076518489, -163.1410904276970086 ) ) ;
#2791=CARTESIAN_POINT ( 'NONE',  ( -23.15000000000000213, 64.35000000001254250, -182.1731074845244507 ) ) ;
#2793=DIRECTION ( 'NONE',  ( -1.000000000000000000, 0.000000000000000000, 0.000000000000000000 ) ) ;
#2827=LINE ( 'NONE', #185339, #124169 ) ;
#2832=ORIENTED_EDGE ( 'NONE', *, *, #141858, .F. ) ;
#2850=CIRCLE ( 'NONE', #236092, 0.09999999999999939493 ) ;
#2864=ORIENTED_EDGE ( 'NONE', *, *, #151015, .F. ) ;
#2906=EDGE_CURVE ( 'NONE', #9660, #85698, #238128, .T. ) ;
#2910=DIRECTION ( 'NONE',  ( 0.000000000000000000, -0.7397360091702802620, 0.6728971962616779878 ) ) ;
#2919=VERTEX_POINT ( 'NONE', #7216 ) ;
#2923=DIRECTION ( 'NONE',  ( 0.000000000000000000, -1.000000000000000000, -6.860497997771532351E-15 ) ) ;
#2999=ORIENTED_EDGE ( 'NONE', *, *, #81708, .T. ) ;
#3024=AXIS2_PLACEMENT_3D ( 'NONE', #201207, #85076, #120429 ) ;
#3028=DIRECTION ( 'NONE',  ( 0.000000000000000000, 6.982962677686266711E-15, -1.000000000000000000 ) ) ;
#3061=CARTESIAN_POINT ( 'NONE',  ( -18.59999999999999787, 64.35000000001259934, -191.3731074845244393 ) ) ;
#3066=DIRECTION ( 'NONE',  ( 1.000000000000000000, 0.000000000000000000, 0.000000000000000000 ) ) ;
#3106=DIRECTION ( 'NONE',  ( -0.000000000000000000, -6.982962677686266711E-15, 1.000000000000000000 ) ) ;
#3115=EDGE_CURVE ( 'NONE', #255583, #220964, #130962, .T. ) ;
#3190=EDGE_CURVE ( 'NONE', #167877, #163056, #52762, .T. ) ;
#3207=CARTESIAN_POINT ( 'NONE',  ( -23.15000000000000213, 87.75000000001276135, -215.2731074845242745 ) ) ;
#3264=EDGE_CURVE ( 'NONE', #96501, #16498, #64510, .T. ) ;
#3272=CARTESIAN_POINT ( 'NONE',  ( 20.95512820512820440, 67.12384868372447499, -191.3731074845244109 ) ) ;
#3303=AXIS2_PLACEMENT_3D ( 'NONE', #137524, #577, #41037 ) ;
#3310=EDGE_CURVE ( 'NONE', #9515, #60454, #152023, .T. ) ;
#3351=EDGE_LOOP ( 'NONE', ( #132448, #60959, #223622 ) ) ;
#3356=VERTEX_POINT ( 'NONE', #257335 ) ;
#3367=AXIS2_PLACEMENT_3D ( 'NONE', #139042, #2121, #238167 ) ;
#3380=CARTESIAN_POINT ( 'NONE',  ( 21.05000000000000071, 69.55000000001261640, -193.5060803140843859 ) ) ;
#3412=LINE ( 'NONE', #5978, #199873 ) ;
#3432=VERTEX_POINT ( 'NONE', #107308 ) ;
#3468=ADVANCED_FACE ( 'NONE', ( #222092 ), #6925, .T. ) ;
#3469=DIRECTION ( 'NONE',  ( 0.000000000000000000, -6.982962677686266711E-15, 1.000000000000000000 ) ) ;
#3487=VECTOR ( 'NONE', #222857, 1000.000000000000000 ) ;
#3509=CARTESIAN_POINT ( 'NONE',  ( 23.24999999999999289, 69.35000000001254250, -182.3731074845244109 ) ) ;
#3522=EDGE_LOOP ( 'NONE', ( #71921, #197661, #218501, #242337 ) ) ;
#3543=DIRECTION ( 'NONE',  ( 0.000000000000000000, 0.1495327102803283015, 0.9887567792719397231 ) ) ;
#3580=AXIS2_PLACEMENT_3D ( 'NONE', #150002, #70479, #28794 ) ;
#3583=ORIENTED_EDGE ( 'NONE', *, *, #166001, .T. ) ;
#3621=CARTESIAN_POINT ( 'NONE',  ( 20.95512820512820440, 67.12384868372450342, -194.9644784893834810 ) ) ;
#3641=EDGE_CURVE ( 'NONE', #164331, #49841, #197958, .T. ) ;
#3646=DIRECTION ( 'NONE',  ( 1.000000000000000000, 0.000000000000000000, 0.000000000000000000 ) ) ;
#3660=ORIENTED_EDGE ( 'NONE', *, *, #146679, .T. ) ;
#3671=AXIS2_PLACEMENT_3D ( 'NONE', #253657, #234100, #252367 ) ;
#3688=DIRECTION ( 'NONE',  ( 0.000000000000000000, -0.1575844902526687130, -0.9875055080513762684 ) ) ;
#3707=EDGE_LOOP ( 'NONE', ( #147886, #11127, #247421, #75243, #48211 ) ) ;
#3709=ORIENTED_EDGE ( 'NONE', *, *, #153407, .F. ) ;
#3715=LINE ( 'NONE', #141943, #86577 ) ;
#3727=VERTEX_POINT ( 'NONE', #122412 ) ;
#3762=DIRECTION ( 'NONE',  ( 0.000000000000000000, -6.688090509790120484E-15, 1.000000000000000000 ) ) ;
#3767=VECTOR ( 'NONE', #32686, 1000.000000000000000 ) ;
#3808=CARTESIAN_POINT ( 'NONE',  ( 21.05000000000000071, 76.00000000001244871, -170.0231074845243597 ) ) ;
#3812=VERTEX_POINT ( 'NONE', #226623 ) ;
#3848=ORIENTED_EDGE ( 'NONE', *, *, #131238, .F. ) ;
#3858=ORIENTED_EDGE ( 'NONE', *, *, #46431, .F. ) ;
#3868=CARTESIAN_POINT ( 'NONE',  ( -20.54999999999999716, 76.00000000001246292, -171.9231074845243938 ) ) ;
#3884=DIRECTION ( 'NONE',  ( 0.000000000000000000, 1.000000000000000000, 6.982962677686266711E-15 ) ) ;
#3894=AXIS2_PLACEMENT_3D ( 'NONE', #143952, #104798, #245635 ) ;
#3895=ORIENTED_EDGE ( 'NONE', *, *, #166766, .F. ) ;
#3908=CIRCLE ( 'NONE', #212212, 11.64999999999999325 ) ;
#3913=DIRECTION ( 'NONE',  ( -0.000000000000000000, 6.982962677686266711E-15, -1.000000000000000000 ) ) ;
#3917=ORIENTED_EDGE ( 'NONE', *, *, #146920, .F. ) ;
#3918=DIRECTION ( 'NONE',  ( 1.000000000000000000, 0.000000000000000000, 0.000000000000000000 ) ) ;
#3947=AXIS2_PLACEMENT_3D ( 'NONE', #87728, #96399, #175983 ) ;
#3948=FACE_OUTER_BOUND ( 'NONE', #220229, .T. ) ;
#3970=CARTESIAN_POINT ( 'NONE',  ( 20.95512820512820440, 67.12384868372450342, -194.9644784893834810 ) ) ;
#4003=VERTEX_POINT ( 'NONE', #79093 ) ;
#4013=ORIENTED_EDGE ( 'NONE', *, *, #8450, .T. ) ;
#4039=DIRECTION ( 'NONE',  ( -0.000000000000000000, 6.982962677686266711E-15, -1.000000000000000000 ) ) ;
#4048=EDGE_CURVE ( 'NONE', #7443, #96501, #218993, .T. ) ;
#4055=EDGE_CURVE ( 'NONE', #2919, #77481, #242036, .T. ) ;
#4068=DIRECTION ( 'NONE',  ( -1.000000000000000000, -0.000000000000000000, -0.000000000000000000 ) ) ;
#4078=EDGE_CURVE ( 'NONE', #48315, #45489, #98157, .T. ) ;
#4088=EDGE_LOOP ( 'NONE', ( #66233, #92551, #202705, #247143 ) ) ;
#4167=CARTESIAN_POINT ( 'NONE',  ( -20.64999999999999858, 71.75000000001259082, -191.2731074845243882 ) ) ;
#4179=VERTEX_POINT ( 'NONE', #68547 ) ;
#4195=EDGE_CURVE ( 'NONE', #239043, #28788, #35690, .T. ) ;
#4200=AXIS2_PLACEMENT_3D ( 'NONE', #93253, #131103, #114098 ) ;
#4208=ORIENTED_EDGE ( 'NONE', *, *, #36987, .F. ) ;
#4218=CARTESIAN_POINT ( 'NONE',  ( 21.05000000000000071, 84.66355140188167638, -179.5472086025916099 ) ) ;
#4228=ORIENTED_EDGE ( 'NONE', *, *, #146920, .T. ) ;
#4292=FACE_OUTER_BOUND ( 'NONE', #27883, .T. ) ;
#4304=ADVANCED_FACE ( 'NONE', ( #76225 ), #192429, .F. ) ;
#4344=DIRECTION ( 'NONE',  ( 0.000000000000000000, 6.982962677686266711E-15, -1.000000000000000000 ) ) ;
#4346=DIRECTION ( 'NONE',  ( 0.000000000000000000, -1.000000000000000000, -6.352154140967427193E-15 ) ) ;
#4354=CARTESIAN_POINT ( 'NONE',  ( 22.39999999999999503, 75.90000000001273861, -211.3138870828977360 ) ) ;
#4443=ORIENTED_EDGE ( 'NONE', *, *, #111141, .T. ) ;
#4444=CARTESIAN_POINT ( 'NONE',  ( -18.50000000000000000, 77.86671491006991630, -191.7704322382423356 ) ) ;
#4456=AXIS2_PLACEMENT_3D ( 'NONE', #164138, #66314, #182423 ) ;
#4463=CARTESIAN_POINT ( 'NONE',  ( 18.52928932188133970, 65.72071067813116940, -178.8731074845244109 ) ) ;
#4473=FACE_OUTER_BOUND ( 'NONE', #94359, .T. ) ;
#4488=CIRCLE ( 'NONE', #150265, 0.09999999999998898659 ) ;
#4500=ORIENTED_EDGE ( 'NONE', *, *, #247571, .F. ) ;
#4504=TOROIDAL_SURFACE ( 'NONE', #33617, 0.6000000000000009770, 0.1000000000000000056 ) ;
#4506=CARTESIAN_POINT ( 'NONE',  ( 21.05000012384953223, 65.37127970113806441, -191.3451301544890271 ) ) ;
#4544=CARTESIAN_POINT ( 'NONE',  ( 21.13435531349789542, 76.00000000001271871, -210.0168285481172177 ) ) ;
#4547=ADVANCED_FACE ( 'NONE', ( #29154 ), #4951, .T. ) ;
#4556=ORIENTED_EDGE ( 'NONE', *, *, #168618, .F. ) ;
#4560=CARTESIAN_POINT ( 'NONE',  ( 21.08804582317328169, 67.12183383292068584, -191.1731076551165245 ) ) ;
#4566=CARTESIAN_POINT ( 'NONE',  ( 19.80993210785551284, 64.25000000001347189, -178.7559897356397016 ) ) ;
#4574=ADVANCED_FACE ( 'NONE', ( #225984 ), #117600, .F. ) ;
#4594=ORIENTED_EDGE ( 'NONE', *, *, #97948, .T. ) ;
#4609=ADVANCED_FACE ( 'NONE', ( #111212 ), #190783, .T. ) ;
#4629=CARTESIAN_POINT ( 'NONE',  ( 21.05000000000000071, 76.00000000001244871, -170.0231074845243597 ) ) ;
#4692=DIRECTION ( 'NONE',  ( 1.000000000000000000, 0.000000000000000000, 0.000000000000000000 ) ) ;
#4699=CARTESIAN_POINT ( 'NONE',  ( 20.94999999999999574, 74.26374286841520700, -191.9544551555068779 ) ) ;
#4705=CARTESIAN_POINT ( 'NONE',  ( 21.14250536705908345, 69.48182782313196526, -203.5231074845243882 ) ) ;
#4716=VERTEX_POINT ( 'NONE', #176342 ) ;
#4725=DIRECTION ( 'NONE',  ( 1.000000000000000000, 0.000000000000000000, 0.000000000000000000 ) ) ;
#4741=VERTEX_POINT ( 'NONE', #195903 ) ;
#4743=DIRECTION ( 'NONE',  ( 0.000000000000000000, 0.000000000000000000, 1.000000000000000000 ) ) ;
#4761=DIRECTION ( 'NONE',  ( -0.000000000000000000, 7.109473446599835262E-15, -1.000000000000000000 ) ) ;
#4838=CARTESIAN_POINT ( 'NONE',  ( -21.11101077989000530, 75.98471473109843544, -209.9467922192504830 ) ) ;
#4841=ORIENTED_EDGE ( 'NONE', *, *, #254794, .F. ) ;
#4902=EDGE_CURVE ( 'NONE', #133931, #141019, #46843, .T. ) ;
#4927=DIRECTION ( 'NONE',  ( 1.000000000000000000, 0.000000000000000000, 0.000000000000000000 ) ) ;
#4940=FACE_BOUND ( 'NONE', #195587, .T. ) ;
#4945=ORIENTED_EDGE ( 'NONE', *, *, #129543, .F. ) ;
#4949=AXIS2_PLACEMENT_3D ( 'NONE', #2433, #151606, #132011 ) ;
#4951=TOROIDAL_SURFACE ( 'NONE', #175701, 3.899999999999999467, 0.1000000000000000056 ) ;
#4988=EDGE_LOOP ( 'NONE', ( #64498, #105626, #179814, #211539 ) ) ;
#4997=ORIENTED_EDGE ( 'NONE', *, *, #167753, .T. ) ;
#5003=PLANE ( 'NONE',  #54402 ) ;
#5021=CARTESIAN_POINT ( 'NONE',  ( -21.05000000000000071, 76.00000000001267608, -203.5231074845243597 ) ) ;
#5030=EDGE_LOOP ( 'NONE', ( #14695, #138245, #135726, #191638 ) ) ;
#5083=DIRECTION ( 'NONE',  ( -2.978066053179069723E-16, -1.000000000000000000, -7.147358527629766941E-15 ) ) ;
#5092=ORIENTED_EDGE ( 'NONE', *, *, #212065, .T. ) ;
#5116=ORIENTED_EDGE ( 'NONE', *, *, #116924, .F. ) ;
#5129=DIRECTION ( 'NONE',  ( 1.000000000000000000, 0.000000000000000000, 0.000000000000000000 ) ) ;
#5157=LINE ( 'NONE', #187701, #187984 ) ;
#5168=ORIENTED_EDGE ( 'NONE', *, *, #174506, .T. ) ;
#5220=FACE_OUTER_BOUND ( 'NONE', #10923, .T. ) ;
#5223=CARTESIAN_POINT ( 'NONE',  ( -20.64999999999999858, 68.85000000001254250, -182.3731074845244109 ) ) ;
#5227=ORIENTED_EDGE ( 'NONE', *, *, #155710, .F. ) ;
#5232=DIRECTION ( 'NONE',  ( -0.000000000000000000, -1.000000000000000000, -6.982962677686266711E-15 ) ) ;
#5260=ORIENTED_EDGE ( 'NONE', *, *, #66223, .F. ) ;
#5269=EDGE_LOOP ( 'NONE', ( #3917, #73423, #72451, #48501, #135786, #131245, #1807, #203760, #223010, #75485, #240595, #144430, #181249, #67501, #196745, #142239 ) ) ;
#5294=DIRECTION ( 'NONE',  ( 0.000000000000000000, 0.000000000000000000, 1.000000000000000000 ) ) ;
#5306=DIRECTION ( 'NONE',  ( -0.000000000000000000, 7.109473446599835262E-15, -1.000000000000000000 ) ) ;
#5308=AXIS2_PLACEMENT_3D ( 'NONE', #2184, #99988, #179578 ) ;
#5346=AXIS2_PLACEMENT_3D ( 'NONE', #241271, #39229, #101705 ) ;
#5350=CARTESIAN_POINT ( 'NONE',  ( 18.39999999999999858, 85.50000000001263345, -196.4910380878246201 ) ) ;
#5393=FACE_OUTER_BOUND ( 'NONE', #178484, .T. ) ;
#5408=AXIS2_PLACEMENT_3D ( 'NONE', #72456, #75041, #172871 ) ;
#5424=AXIS2_PLACEMENT_3D ( 'NONE', #32197, #167863, #90851 ) ;
#5426=DIRECTION ( 'NONE',  ( 1.000000000000000000, 0.000000000000000000, 0.000000000000000000 ) ) ;
#5452=AXIS2_PLACEMENT_3D ( 'NONE', #94920, #75405, #174535 ) ;
#5541=ORIENTED_EDGE ( 'NONE', *, *, #47352, .T. ) ;
#5547=ORIENTED_EDGE ( 'NONE', *, *, #119274, .F. ) ;
#5548=EDGE_CURVE ( 'NONE', #71381, #37214, #65060, .T. ) ;
#5551=ADVANCED_FACE ( 'NONE', ( #89121 ), #244118, .F. ) ;
#5576=DIRECTION ( 'NONE',  ( 0.000000000000000000, 0.000000000000000000, 1.000000000000000000 ) ) ;
#5583=DIRECTION ( 'NONE',  ( 0.000000000000000000, -6.982962677686266711E-15, 1.000000000000000000 ) ) ;
#5587=LINE ( 'NONE', #42189, #232001 ) ;
#5606=CIRCLE ( 'NONE', #118061, 0.09999999999999939493 ) ;
#5635=DIRECTION ( 'NONE',  ( -1.836970198721029934E-16, -1.000000000000000000, -6.982962677686266711E-15 ) ) ;
#5644=AXIS2_PLACEMENT_3D ( 'NONE', #203006, #257799, #139162 ) ;
#5667=LINE ( 'NONE', #46097, #2219 ) ;
#5673=AXIS2_PLACEMENT_3D ( 'NONE', #230738, #74254, #93769 ) ;
#5695=AXIS2_PLACEMENT_3D ( 'NONE', #156949, #193497, #119089 ) ;
#5709=DIRECTION ( 'NONE',  ( 0.000000000000000000, -0.1350103645451945777, 0.9908441862701591329 ) ) ;
#5728=DIRECTION ( 'NONE',  ( 0.000000000000000000, 0.000000000000000000, 1.000000000000000000 ) ) ;
#5796=CARTESIAN_POINT ( 'NONE',  ( -20.85000000000000142, 76.32388570108278714, -170.0655178952103768 ) ) ;
#5805=EDGE_CURVE ( 'NONE', #221522, #152534, #94250, .T. ) ;
#5809=CARTESIAN_POINT ( 'NONE',  ( 20.77766267348356166, 65.55095760939391880, -195.9303985686467513 ) ) ;
#5819=CARTESIAN_POINT ( 'NONE',  ( 21.05000000000000071, 76.09999993531981488, -210.0011857056192071 ) ) ;
#5825=ORIENTED_EDGE ( 'NONE', *, *, #188834, .T. ) ;
#5839=CARTESIAN_POINT ( 'NONE',  ( -22.59999970745345976, 76.00935637734023942, -215.2736206921935889 ) ) ;
#5840=ADVANCED_FACE ( 'NONE', ( #229483 ), #186506, .F. ) ;
#5857=DIRECTION ( 'NONE',  ( -1.000000000000000000, 0.000000000000000000, -0.000000000000000000 ) ) ;
#5865=ORIENTED_EDGE ( 'NONE', *, *, #220751, .T. ) ;
#5869=DIRECTION ( 'NONE',  ( 0.000000000000000000, -6.938893903907222067E-15, 1.000000000000000000 ) ) ;
#5909=( BOUNDED_SURFACE ( )  B_SPLINE_SURFACE ( 3, 2, ( 
 ( #223577, #222277, #99769 ),
 ( #80197, #180625, #98466 ),
 ( #44966, #43682, #1961 ),
 ( #161068, #221013, #103622 ),
 ( #201455, #22858, #244436 ),
 ( #146601, #104891, #249593 ),
 ( #226128, #125769, #9678 ),
 ( #230013, #184462, #224863 ),
 ( #85338, #168809, #164908 ),
 ( #5809, #65803, #185756 ),
 ( #8411, #26706, #89212 ),
 ( #245733, #145333, #86622 ) ),
 .UNSPECIFIED., .F., .F., .F. ) 
 B_SPLINE_SURFACE_WITH_KNOTS ( ( 4, 2, 2, 2, 2, 4 ),
 ( 3, 3 ),
 ( 3.174653483277205090, 3.943930578431714018, 4.713207673586222946, 5.482484768740731873, 5.867123316317986337, 6.251761863895240801 ),
 ( 0.000000000000000000, 1.000000000000000000 ),
 .UNSPECIFIED. ) 
 GEOMETRIC_REPRESENTATION_ITEM ( )  RATIONAL_B_SPLINE_SURFACE ( (
 ( 1.000000000000000000, 0.8659465255642114778, 1.000000000000000000),
 ( 1.000000000000000000, 0.8648614068487343598, 1.000000000000000000),
 ( 1.000000000000000000, 0.8489031841324523597, 1.000000000000000000),
 ( 1.000000000000000000, 0.7927507630160768315, 1.000000000000000000),
 ( 1.000000000000000000, 0.7523013859006951742, 1.000000000000000000),
 ( 1.000000000000000000, 0.6616226951198839190, 1.000000000000000000),
 ( 1.000000000000000000, 0.6112214368721479163, 1.000000000000000000),
 ( 1.000000000000000000, 0.5507684314500016498, 1.000000000000000000),
 ( 1.000000000000000000, 0.5333267243152196579, 1.000000000000000000),
 ( 1.000000000000000000, 0.5084565446481067452, 1.000000000000000000),
 ( 1.000000000000000000, 0.5010722703449013160, 1.000000000000000000),
 ( 1.000000000000000000, 0.5001234037138888588, 1.000000000000000000) ) ) 
 REPRESENTATION_ITEM ( '' )  SURFACE ( )  );
#5911=FACE_OUTER_BOUND ( 'NONE', #43050, .T. ) ;
#5914=ORIENTED_EDGE ( 'NONE', *, *, #18329, .F. ) ;
#5919=CIRCLE ( 'NONE', #118588, 3.899999999999987033 ) ;
#5955=EDGE_CURVE ( 'NONE', #33564, #163131, #115226, .T. ) ;
#5963=ORIENTED_EDGE ( 'NONE', *, *, #227280, .F. ) ;
#5968=CARTESIAN_POINT ( 'NONE',  ( -21.05000000000000071, 77.83534155023701828, -191.9679561919613491 ) ) ;
#5972=DIRECTION ( 'NONE',  ( 0.000000000000000000, -7.056502275159890832E-15, 1.000000000000000000 ) ) ;
#5978=CARTESIAN_POINT ( 'NONE',  ( -18.50000000000000000, 77.68707439010432836, -216.3376804510660065 ) ) ;
#5996=DIRECTION ( 'NONE',  ( 0.000000000000000000, -7.056502275159890043E-15, 1.000000000000000000 ) ) ;
#6015=DIRECTION ( 'NONE',  ( 0.000000000000000000, -0.8660254037844387076, 0.4999999999999998335 ) ) ;
#6016=( BOUNDED_CURVE ( )  B_SPLINE_CURVE ( 3, ( #39404, #195897, #154234, #57633 ),
 .UNSPECIFIED., .F., .F. ) 
 B_SPLINE_CURVE_WITH_KNOTS ( ( 4, 4 ),
 ( 3.192897208853993085, 4.712388980384689674 ),
 .UNSPECIFIED. ) 
 CURVE ( )  GEOMETRIC_REPRESENTATION_ITEM ( )  RATIONAL_B_SPLINE_CURVE ( ( 1.000000000000000000, 0.8166740347213228279, 0.8166740347213228279, 1.000000000000000000 ) ) 
 REPRESENTATION_ITEM ( '' )  );
#6033=DIRECTION ( 'NONE',  ( 1.000000000000000000, 0.000000000000000000, 0.000000000000000000 ) ) ;
#6039=CYLINDRICAL_SURFACE ( 'NONE', #138402, 0.09999999999998898659 ) ;
#6057=EDGE_CURVE ( 'NONE', #196694, #210729, #183625, .T. ) ;
#6062=AXIS2_PLACEMENT_3D ( 'NONE', #232507, #73439, #108683 ) ;
#6110=FACE_OUTER_BOUND ( 'NONE', #203931, .T. ) ;
#6118=EDGE_CURVE ( 'NONE', #156136, #177284, #7141, .T. ) ;
#6136=EDGE_CURVE ( 'NONE', #172803, #54825, #119816, .T. ) ;
#6148=DIRECTION ( 'NONE',  ( 1.000000000000000000, 0.000000000000000000, 0.000000000000000000 ) ) ;
#6149=AXIS2_PLACEMENT_3D ( 'NONE', #115639, #130050, #114359 ) ;
#6189=CIRCLE ( 'NONE', #76929, 0.09999999999998898659 ) ;
#6196=DIRECTION ( 'NONE',  ( -1.000000000000000000, -0.000000000000000000, -0.000000000000000000 ) ) ;
#6205=VERTEX_POINT ( 'NONE', #108267 ) ;
#6207=DIRECTION ( 'NONE',  ( -1.000000000000000000, 0.000000000000000000, 0.000000000000000000 ) ) ;
#6245=CYLINDRICAL_SURFACE ( 'NONE', #84955, 0.5000000000000004441 ) ;
#6260=CARTESIAN_POINT ( 'NONE',  ( 23.25000000000000000, 87.75000000001276135, -215.2731074845242745 ) ) ;
#6277=CIRCLE ( 'NONE', #106222, 0.1000000000000009492 ) ;
#6304=CARTESIAN_POINT ( 'NONE',  ( 21.05000000000000071, 65.27628289530511552, -195.8581939154368285 ) ) ;
#6313=ORIENTED_EDGE ( 'NONE', *, *, #61052, .T. ) ;
#6316=DIRECTION ( 'NONE',  ( -0.000000000000000000, -6.982962677686266711E-15, 1.000000000000000000 ) ) ;
#6321=DIRECTION ( 'NONE',  ( 0.000000000000000000, -6.652207440891584540E-15, 1.000000000000000000 ) ) ;
#6356=DIRECTION ( 'NONE',  ( 1.000000000000000000, 0.000000000000000000, 0.000000000000000000 ) ) ;
#6388=DIRECTION ( 'NONE',  ( -1.000000000000000000, -0.000000000000000000, -0.000000000000000000 ) ) ;
#6417=ORIENTED_EDGE ( 'NONE', *, *, #255113, .T. ) ;
#6419=AXIS2_PLACEMENT_3D ( 'NONE', #86399, #246781, #103402 ) ;
#6467=DIRECTION ( 'NONE',  ( 1.000000000000000000, 0.000000000000000000, 0.000000000000000000 ) ) ;
#6521=EDGE_CURVE ( 'NONE', #14542, #228147, #214880, .T. ) ;
#6579=CARTESIAN_POINT ( 'NONE',  ( -20.94684162548481154, 64.25000000001264766, -196.6814634889770446 ) ) ;
#6596=CARTESIAN_POINT ( 'NONE',  ( -21.05000000000000071, 87.65000000001246860, -172.9231074845242802 ) ) ;
#6614=CARTESIAN_POINT ( 'NONE',  ( -23.25000000000000000, 71.75000000001259082, -191.3731074845243825 ) ) ;
#6619=CARTESIAN_POINT ( 'NONE',  ( -18.59999999999999787, 66.75000000001253397, -182.3731074845244393 ) ) ;
#6635=CARTESIAN_POINT ( 'NONE',  ( -18.54270223418607699, 85.62410550289533262, -163.2821724341169158 ) ) ;
#6656=AXIS2_PLACEMENT_3D ( 'NONE', #106149, #185713, #7061 ) ;
#6662=DIRECTION ( 'NONE',  ( -0.7071067811865475727, 0.7071067811865475727, 4.937700262164531476E-15 ) ) ;
#6666=EDGE_CURVE ( 'NONE', #196907, #165093, #235721, .T. ) ;
#6675=CARTESIAN_POINT ( 'NONE',  ( 21.30000000000002558, 76.00000000001270450, -207.5731074845243427 ) ) ;
#6699=EDGE_CURVE ( 'NONE', #145935, #165343, #240021, .T. ) ;
#6704=ORIENTED_EDGE ( 'NONE', *, *, #18212, .T. ) ;
#6712=DIRECTION ( 'NONE',  ( -1.000000000000000000, -0.000000000000000000, -0.000000000000000000 ) ) ;
#6733=FACE_OUTER_BOUND ( 'NONE', #23969, .T. ) ;
#6743=CARTESIAN_POINT ( 'NONE',  ( -22.49917693094574389, 75.91477003579109351, -215.1729032690550412 ) ) ;
#6746=VERTEX_POINT ( 'NONE', #113089 ) ;
#6765=VERTEX_POINT ( 'NONE', #173111 ) ;
#6848=ORIENTED_EDGE ( 'NONE', *, *, #237786, .T. ) ;
#6855=ORIENTED_EDGE ( 'NONE', *, *, #39267, .T. ) ;
#6860=DIRECTION ( 'NONE',  ( 1.000000000000000000, 0.000000000000000000, 0.000000000000000000 ) ) ;
#6879=VECTOR ( 'NONE', #66018, 1000.000000000000000 ) ;
#6880=AXIS2_PLACEMENT_3D ( 'NONE', #241954, #104973, #62055 ) ;
#6886=VERTEX_POINT ( 'NONE', #42216 ) ;
#6891=CARTESIAN_POINT ( 'NONE',  ( -18.46856557590793102, 85.47421590779912037, -196.4211212436419771 ) ) ;
#6917=CARTESIAN_POINT ( 'NONE',  ( -20.94999999999999929, 87.48912529308852015, -173.1231074845242688 ) ) ;
#6925=CYLINDRICAL_SURFACE ( 'NONE', #118695, 0.09999999999999939493 ) ;
#6962=DIRECTION ( 'NONE',  ( 0.000000000000000000, 0.4999999999999088507, 0.8660254037844913322 ) ) ;
#6985=DIRECTION ( 'NONE',  ( -0.000000000000000000, 0.9875055080513808203, -0.1575844902526395142 ) ) ;
#6986=EDGE_CURVE ( 'NONE', #87006, #101145, #124319, .T. ) ;
#6996=FACE_OUTER_BOUND ( 'NONE', #121391, .T. ) ;
#7002=DIRECTION ( 'NONE',  ( -1.000000000000000000, 0.000000000000000000, -0.000000000000000000 ) ) ;
#7005=PLANE ( 'NONE',  #57704 ) ;
#7033=DIRECTION ( 'NONE',  ( 0.000000000000000000, 6.467318590049456648E-15, -1.000000000000000000 ) ) ;
#7061=DIRECTION ( 'NONE',  ( 0.000000000000000000, 0.6728971962617862346, -0.7397360091701815632 ) ) ;
#7065=EDGE_CURVE ( 'NONE', #116410, #94115, #227257, .T. ) ;
#7071=AXIS2_PLACEMENT_3D ( 'NONE', #256981, #39299, #223035 ) ;
#7113=FACE_OUTER_BOUND ( 'NONE', #29039, .T. ) ;
#7132=CARTESIAN_POINT ( 'NONE',  ( 21.06277459767451887, 67.12713756174430557, -191.3191082921680959 ) ) ;
#7139=CARTESIAN_POINT ( 'NONE',  ( -18.59999999999999787, 64.35000000001245724, -170.0231074845244166 ) ) ;
#7141=CIRCLE ( 'NONE', #60739, 0.09999999999999459321 ) ;
#7142=CARTESIAN_POINT ( 'NONE',  ( 20.94999999999999929, 85.00000000001261924, -193.6291383618718385 ) ) ;
#7152=EDGE_LOOP ( 'NONE', ( #189631, #130382, #202844, #220491 ) ) ;
#7156=CARTESIAN_POINT ( 'NONE',  ( 20.94999999999999929, 76.00000000001244871, -170.0231074845243597 ) ) ;
#7163=DIRECTION ( 'NONE',  ( -0.000000000000000000, 1.000000000000000000, 6.982962677686266711E-15 ) ) ;
#7185=CARTESIAN_POINT ( 'NONE',  ( -20.94403535211772294, 65.69367753730709580, -164.5189238066348594 ) ) ;
#7196=ORIENTED_EDGE ( 'NONE', *, *, #243405, .T. ) ;
#7216=CARTESIAN_POINT ( 'NONE',  ( 21.14999999999999858, 69.35000000001259934, -191.2731074845243882 ) ) ;
#7220=VECTOR ( 'NONE', #75345, 1000.000000000000000 ) ;
#7233=DIRECTION ( 'NONE',  ( -1.000000000000000000, 0.000000000000000000, -0.000000000000000000 ) ) ;
#7258=AXIS2_PLACEMENT_3D ( 'NONE', #99228, #79667, #159246 ) ;
#7266=CARTESIAN_POINT ( 'NONE',  ( -18.59999999999999787, 85.32100840337392356, -196.2871692354464130 ) ) ;
#7283=EDGE_CURVE ( 'NONE', #197466, #36195, #28019, .T. ) ;
#7297=CARTESIAN_POINT ( 'NONE',  ( 18.59999999999999076, 69.55000000001261640, -193.5060803140843859 ) ) ;
#7305=DIRECTION ( 'NONE',  ( 0.000000000000000000, 0.000000000000000000, -1.000000000000000000 ) ) ;
#7338=DIRECTION ( 'NONE',  ( 0.000000000000000000, 1.000000000000000000, 6.982962677686266711E-15 ) ) ;
#7340=DIRECTION ( 'NONE',  ( 1.000000000000000000, 0.000000000000000000, 0.000000000000000000 ) ) ;
#7349=AXIS2_PLACEMENT_3D ( 'NONE', #218075, #139829, #39499 ) ;
#7352=ORIENTED_EDGE ( 'NONE', *, *, #149701, .F. ) ;
#7373=ORIENTED_EDGE ( 'NONE', *, *, #204842, .T. ) ;
#7387=CARTESIAN_POINT ( 'NONE',  ( -18.59999999999999787, 66.65000000001253966, -182.2731074845244166 ) ) ;
#7401=AXIS2_PLACEMENT_3D ( 'NONE', #71744, #147411, #151279 ) ;
#7429=CARTESIAN_POINT ( 'NONE',  ( -21.08035267497491816, 75.91731137523670725, -209.8548143243074264 ) ) ;
#7443=VERTEX_POINT ( 'NONE', #225648 ) ;
#7477=ORIENTED_EDGE ( 'NONE', *, *, #146192, .T. ) ;
#7486=AXIS2_PLACEMENT_3D ( 'NONE', #112548, #178970, #175130 ) ;
#7543=FACE_OUTER_BOUND ( 'NONE', #235873, .T. ) ;
#7558=VECTOR ( 'NONE', #93255, 1000.000000000000000 ) ;
#7566=EDGE_CURVE ( 'NONE', #62026, #234461, #252834, .T. ) ;
#7569=ORIENTED_EDGE ( 'NONE', *, *, #50019, .F. ) ;
#7600=CARTESIAN_POINT ( 'NONE',  ( -21.05000000000000071, 75.96824164695762249, -209.7819546076044332 ) ) ;
#7620=CARTESIAN_POINT ( 'NONE',  ( 23.14999999999999858, 76.00000000001244871, -170.0231074845243597 ) ) ;
#7621=ORIENTED_EDGE ( 'NONE', *, *, #96691, .F. ) ;
#7649=VECTOR ( 'NONE', #179943, 1000.000000000000000 ) ;
#7723=CARTESIAN_POINT ( 'NONE',  ( 18.59999999999998366, 76.00000000001244871, -170.0231074845243597 ) ) ;
#7725=AXIS2_PLACEMENT_3D ( 'NONE', #166504, #84307, #46509 ) ;
#7781=AXIS2_PLACEMENT_3D ( 'NONE', #99878, #778, #80314 ) ;
#7790=ADVANCED_FACE ( 'NONE', ( #220256 ), #257076, .T. ) ;
#7837=CIRCLE ( 'NONE', #249445, 0.1000000000000028644 ) ;
#7845=CARTESIAN_POINT ( 'NONE',  ( -20.94999999999999929, 87.41227409416235616, -200.5231074845242745 ) ) ;
#7852=ORIENTED_EDGE ( 'NONE', *, *, #79965, .T. ) ;
#7857=VERTEX_POINT ( 'NONE', #209662 ) ;
#7869=ORIENTED_EDGE ( 'NONE', *, *, #170864, .T. ) ;
#7873=EDGE_LOOP ( 'NONE', ( #39999, #120262, #11049, #39038 ) ) ;
#7874=PLANE ( 'NONE',  #156628 ) ;
#7881=TOROIDAL_SURFACE ( 'NONE', #153667, 0.2000000000000000111, 0.1000000000000000056 ) ;
#7892=CARTESIAN_POINT ( 'NONE',  ( -21.05000000000000071, 87.75000000001247713, -173.1231074845242688 ) ) ;
#7906=CIRCLE ( 'NONE', #153687, 0.09999999999998802902 ) ;
#7912=EDGE_LOOP ( 'NONE', ( #135805, #181282, #84762, #136685, #79282, #45081, #100771, #232136, #223888, #189020, #255979, #98903, #211182, #42382, #48674, #124535 ) ) ;
#7928=ORIENTED_EDGE ( 'NONE', *, *, #18329, .T. ) ;
#7930=DIRECTION ( 'NONE',  ( -1.000000000000000000, -0.000000000000000000, -0.000000000000000000 ) ) ;
#7958=DIRECTION ( 'NONE',  ( -1.000000000000000000, 0.000000000000000000, -0.000000000000000000 ) ) ;
#7993=DIRECTION ( 'NONE',  ( -1.000000000000000000, 0.000000000000000000, 0.000000000000000000 ) ) ;
#8014=CYLINDRICAL_SURFACE ( 'NONE', #183155, 0.09999999999998898659 ) ;
#8027=TOROIDAL_SURFACE ( 'NONE', #99554, 0.2000000000000000111, 0.1000000000000000056 ) ;
#8045=CIRCLE ( 'NONE', #41374, 0.1000000000000028644 ) ;
#8086=DIRECTION ( 'NONE',  ( 0.000000000000000000, 0.1350103645451946055, -0.9908441862701591329 ) ) ;
#8118=VERTEX_POINT ( 'NONE', #15334 ) ;
#8124=ORIENTED_EDGE ( 'NONE', *, *, #44046, .F. ) ;
#8125=CYLINDRICAL_SURFACE ( 'NONE', #151517, 0.09999999999999939493 ) ;
#8149=ORIENTED_EDGE ( 'NONE', *, *, #71845, .F. ) ;
#8167=ORIENTED_EDGE ( 'NONE', *, *, #131549, .F. ) ;
#8170=DIRECTION ( 'NONE',  ( 0.000000000000000000, 0.8777080977375655291, -0.4791956752370622463 ) ) ;
#8197=CARTESIAN_POINT ( 'NONE',  ( -18.41353343127310893, 85.50000000001263345, -196.4910380878245633 ) ) ;
#8202=DIRECTION ( 'NONE',  ( 1.000000000000000000, 0.000000000000000000, 0.000000000000000000 ) ) ;
#8212=ORIENTED_EDGE ( 'NONE', *, *, #127289, .T. ) ;
#8223=DIRECTION ( 'NONE',  ( -1.000000000000000000, 0.000000000000000000, 0.000000000000000000 ) ) ;
#8241=CIRCLE ( 'NONE', #87319, 0.09999999999998898659 ) ;
#8263=VERTEX_POINT ( 'NONE', #170275 ) ;
#8273=ORIENTED_EDGE ( 'NONE', *, *, #243138, .F. ) ;
#8276=DIRECTION ( 'NONE',  ( -1.000000000000000000, -0.000000000000000000, -0.000000000000000000 ) ) ;
#8285=AXIS2_PLACEMENT_3D ( 'NONE', #182203, #225144, #3543 ) ;
#8306=VECTOR ( 'NONE', #42552, 1000.000000000000000 ) ;
#8322=DIRECTION ( 'NONE',  ( 1.000000000000000000, 0.000000000000000000, 0.000000000000000000 ) ) ;
#8324=CARTESIAN_POINT ( 'NONE',  ( -18.57399277249657032, 65.66887361445387228, -164.4329845918269655 ) ) ;
#8327=CYLINDRICAL_SURFACE ( 'NONE', #32403, 0.09999999999999939493 ) ;
#8402=DIRECTION ( 'NONE',  ( 1.000000000000000000, -7.304098846218133681E-16, -4.639676173203992654E-30 ) ) ;
#8404=ORIENTED_EDGE ( 'NONE', *, *, #176839, .F. ) ;
#8411=CARTESIAN_POINT ( 'NONE',  ( 20.87631937322877462, 65.52850496324685992, -195.9433616099437927 ) ) ;
#8436=B_SPLINE_CURVE_WITH_KNOTS ( 'NONE', 3,
 ( #37919, #236090, #114864, #256887, #34083, #173609, #157891 ),
 .UNSPECIFIED., .F., .F.,
 ( 4, 3, 4 ),
 ( 0.000000000000000000, 0.0007844235214594318627, 0.001767853679404347454 ),
 .UNSPECIFIED. ) ;
#8438=EDGE_LOOP ( 'NONE', ( #8472, #257065, #25713 ) ) ;
#8439=CARTESIAN_POINT ( 'NONE',  ( 21.09787244211742419, 67.22462929267527443, -191.2838541002068666 ) ) ;
#8450=EDGE_CURVE ( 'NONE', #35186, #166912, #78422, .T. ) ;
#8472=ORIENTED_EDGE ( 'NONE', *, *, #13200, .F. ) ;
#8487=ORIENTED_EDGE ( 'NONE', *, *, #215785, .F. ) ;
#8489=PLANE ( 'NONE',  #159865 ) ;
#8601=DIRECTION ( 'NONE',  ( 1.000000000000000000, 0.000000000000000000, 0.000000000000000000 ) ) ;
#8606=CIRCLE ( 'NONE', #62778, 0.1999999999999987899 ) ;
#8621=DIRECTION ( 'NONE',  ( 0.000000000000000000, -0.9998779222360097974, 0.01562500000000363945 ) ) ;
#8626=AXIS2_PLACEMENT_3D ( 'NONE', #207408, #110856, #49601 ) ;
#8630=EDGE_LOOP ( 'NONE', ( #187142, #140200, #98638, #66259, #175709, #91850, #34871, #123145, #41679, #179427, #18883, #51049, #173763, #155058 ) ) ;
#8642=ORIENTED_EDGE ( 'NONE', *, *, #67871, .T. ) ;
#8658=CARTESIAN_POINT ( 'NONE',  ( 20.94999999999999574, 64.37928932189383602, -176.8915241368654279 ) ) ;
#8665=EDGE_CURVE ( 'NONE', #121258, #109697, #107641, .T. ) ;
#8667=CARTESIAN_POINT ( 'NONE',  ( -20.85000000000000142, 65.66751761918722252, -164.4282609406112670 ) ) ;
#8694=CARTESIAN_POINT ( 'NONE',  ( -23.15000000000000213, 64.25000000001277556, -215.2731074845244450 ) ) ;
#8709=EDGE_CURVE ( 'NONE', #78560, #125024, #7906, .T. ) ;
#8734=CYLINDRICAL_SURFACE ( 'NONE', #218974, 0.09999999999999939493 ) ;
#8743=CARTESIAN_POINT ( 'NONE',  ( -20.54999999999999716, 68.85000000001259934, -191.1731074845243938 ) ) ;
#8764=ORIENTED_EDGE ( 'NONE', *, *, #230041, .T. ) ;
#8785=CIRCLE ( 'NONE', #191973, 0.09999999999998898659 ) ;
#8790=LINE ( 'NONE', #111739, #238806 ) ;
#8794=DIRECTION ( 'NONE',  ( 0.000000000000000000, 6.982962677686266711E-15, -1.000000000000000000 ) ) ;
#8814=DIRECTION ( 'NONE',  ( 1.000000000000000000, 0.000000000000000000, 0.000000000000000000 ) ) ;
#8862=CIRCLE ( 'NONE', #208785, 0.5999999999999894307 ) ;
#8867=ADVANCED_FACE ( 'NONE', ( #176047 ), #132800, .F. ) ;
#8882=ORIENTED_EDGE ( 'NONE', *, *, #33405, .T. ) ;
#8883=DIRECTION ( 'NONE',  ( 1.000000000000000000, 0.000000000000000000, 0.000000000000000000 ) ) ;
#8884=ORIENTED_EDGE ( 'NONE', *, *, #128338, .T. ) ;
#8892=CIRCLE ( 'NONE', #37954, 7.800000000000001599 ) ;
#8894=ORIENTED_EDGE ( 'NONE', *, *, #170157, .T. ) ;
#8904=DIRECTION ( 'NONE',  ( 0.000000000000000000, 0.000000000000000000, 1.000000000000000000 ) ) ;
#8912=EDGE_CURVE ( 'NONE', #210276, #172249, #162026, .T. ) ;
#9030=CARTESIAN_POINT ( 'NONE',  ( -20.54999999999999716, 76.00000000001259082, -190.5481074845243654 ) ) ;
#9044=DIRECTION ( 'NONE',  ( 0.000000000000000000, -0.7397360091702802620, 0.6728971962616779878 ) ) ;
#9080=DIRECTION ( 'NONE',  ( 0.000000000000000000, -1.000000000000000000, -7.272083257015735086E-15 ) ) ;
#9104=ORIENTED_EDGE ( 'NONE', *, *, #202759, .F. ) ;
#9125=ORIENTED_EDGE ( 'NONE', *, *, #207561, .F. ) ;
#9133=AXIS2_PLACEMENT_3D ( 'NONE', #143556, #100547, #43186 ) ;
#9187=DIRECTION ( 'NONE',  ( 0.000000000000000000, 0.000000000000000000, -1.000000000000000000 ) ) ;
#9263=CARTESIAN_POINT ( 'NONE',  ( -20.64999999999999858, 85.00000000001261924, -193.6291383618718385 ) ) ;
#9283=CARTESIAN_POINT ( 'NONE',  ( -23.24999999999999645, 85.60000000001240039, -163.3229180933022633 ) ) ;
#9293=ORIENTED_EDGE ( 'NONE', *, *, #157619, .F. ) ;
#9327=DIRECTION ( 'NONE',  ( 0.000000000000000000, 0.000000000000000000, 1.000000000000000000 ) ) ;
#9416=ORIENTED_EDGE ( 'NONE', *, *, #83284, .F. ) ;
#9428=CIRCLE ( 'NONE', #5308, 0.09999999999998898659 ) ;
#9455=CIRCLE ( 'NONE', #225364, 0.2000000000000057288 ) ;
#9478=DIRECTION ( 'NONE',  ( 1.000000000000000000, 0.000000000000000000, 0.000000000000000000 ) ) ;
#9483=CIRCLE ( 'NONE', #26080, 0.2000000000000057288 ) ;
#9485=CYLINDRICAL_SURFACE ( 'NONE', #38223, 0.09999999999998898659 ) ;
#9501=CYLINDRICAL_SURFACE ( 'NONE', #207748, 0.09999999999998898659 ) ;
#9515=VERTEX_POINT ( 'NONE', #149445 ) ;
#9538=DIRECTION ( 'NONE',  ( 0.000000000000000000, 0.000000000000000000, -1.000000000000000000 ) ) ;
#9561=DIRECTION ( 'NONE',  ( 0.000000000000000000, 1.000000000000000000, 7.272083257015735086E-15 ) ) ;
#9583=DIRECTION ( 'NONE',  ( -1.000000000000000000, 0.000000000000000000, 0.000000000000000000 ) ) ;
#9604=ADVANCED_FACE ( 'NONE', ( #196240 ), #29142, .T. ) ;
#9613=ORIENTED_EDGE ( 'NONE', *, *, #112829, .T. ) ;
#9630=CIRCLE ( 'NONE', #17994, 0.2000000000000057288 ) ;
#9641=AXIS2_PLACEMENT_3D ( 'NONE', #87517, #154917, #194037 ) ;
#9660=VERTEX_POINT ( 'NONE', #219651 ) ;
#9678=CARTESIAN_POINT ( 'NONE',  ( 20.21567752745066215, 65.80188589878065386, -195.6404871368698082 ) ) ;
#9687=CARTESIAN_POINT ( 'NONE',  ( 21.07954640115206857, 75.93399229287285834, -209.8523951805472620 ) ) ;
#9712=CARTESIAN_POINT ( 'NONE',  ( -20.54999999999999716, 68.75000000001260503, -191.2731074845244166 ) ) ;
#9744=VECTOR ( 'NONE', #119027, 1000.000000000000000 ) ;
#9773=CIRCLE ( 'NONE', #155576, 0.09999999999998898659 ) ;
#9787=CARTESIAN_POINT ( 'NONE',  ( -21.05000000000000071, 76.00000000001267608, -203.5231074845243597 ) ) ;
#9804=( LENGTH_UNIT ( ) NAMED_UNIT ( * ) SI_UNIT ( .MILLI., .METRE. ) );
#9812=FACE_OUTER_BOUND ( 'NONE', #109630, .T. ) ;
#9816=ORIENTED_EDGE ( 'NONE', *, *, #114847, .F. ) ;
#9837=VERTEX_POINT ( 'NONE', #246919 ) ;
#9844=DIRECTION ( 'NONE',  ( 0.000000000000000000, 7.109473446599835262E-15, -1.000000000000000000 ) ) ;
#9884=DIRECTION ( 'NONE',  ( 1.000000000000000000, 0.000000000000000000, 0.000000000000000000 ) ) ;
#9891=CARTESIAN_POINT ( 'NONE',  ( 21.87500000000000355, 66.25000000001257661, -191.1731074845244223 ) ) ;
#9894=CIRCLE ( 'NONE', #226354, 12.87499999999999822 ) ;
#9919=LINE ( 'NONE', #185993, #23718 ) ;
#9921=ORIENTED_EDGE ( 'NONE', *, *, #177886, .T. ) ;
#9925=ADVANCED_FACE ( 'NONE', ( #253345 ), #151722, .F. ) ;
#9932=ORIENTED_EDGE ( 'NONE', *, *, #147323, .T. ) ;
#9938=CARTESIAN_POINT ( 'NONE',  ( -20.94999999999999929, 68.96868720525722551, -166.4139565462971007 ) ) ;
#9952=ORIENTED_EDGE ( 'NONE', *, *, #48533, .T. ) ;
#9976=CARTESIAN_POINT ( 'NONE',  ( -23.15000000000000213, 76.00000000001260503, -190.6481074845243597 ) ) ;
#9986=DIRECTION ( 'NONE',  ( 0.000000000000000000, 6.982962677686266711E-15, -1.000000000000000000 ) ) ;
#10034=FACE_OUTER_BOUND ( 'NONE', #733, .T. ) ;
#10054=CARTESIAN_POINT ( 'NONE',  ( 21.46681500593473402, 69.14248884062999423, -203.5231074845244166 ) ) ;
#10056=VERTEX_POINT ( 'NONE', #121483 ) ;
#10065=DIRECTION ( 'NONE',  ( -1.000000000000000000, 7.304098846218134667E-16, 5.100424963727255829E-30 ) ) ;
#10093=CARTESIAN_POINT ( 'NONE',  ( -20.54999999999999716, 66.65000000001253966, -182.2731074845244166 ) ) ;
#10108=ORIENTED_EDGE ( 'NONE', *, *, #18008, .T. ) ;
#10110=DIRECTION ( 'NONE',  ( 0.000000000000000000, 1.000000000000000000, 6.853228547068871147E-15 ) ) ;
#10124=ORIENTED_EDGE ( 'NONE', *, *, #231711, .T. ) ;
#10125=AXIS2_PLACEMENT_3D ( 'NONE', #80432, #256481, #239556 ) ;
#10156=VERTEX_POINT ( 'NONE', #108315 ) ;
#10170=ORIENTED_EDGE ( 'NONE', *, *, #172568, .T. ) ;
#10181=DIRECTION ( 'NONE',  ( 0.000000000000000000, -7.086529944415886769E-15, 1.000000000000000000 ) ) ;
#10184=VECTOR ( 'NONE', #236781, 1000.000000000000000 ) ;
#10191=ORIENTED_EDGE ( 'NONE', *, *, #81204, .T. ) ;
#10203=CARTESIAN_POINT ( 'NONE',  ( 20.85000000000000142, 77.83585931145600512, -158.5186683157258187 ) ) ;
#10204=CARTESIAN_POINT ( 'NONE',  ( -18.59999999999999787, 77.36242903720570041, -162.1342262366031548 ) ) ;
#10220=CARTESIAN_POINT ( 'NONE',  ( 23.25000000000000000, 87.65000000001246860, -173.1231074845242688 ) ) ;
#10268=CARTESIAN_POINT ( 'NONE',  ( -23.25000000000000000, 76.10000000001276987, -215.1726782920691505 ) ) ;
#10285=EDGE_CURVE ( 'NONE', #109096, #198292, #233912, .T. ) ;
#10310=CARTESIAN_POINT ( 'NONE',  ( -23.15000000000000213, 76.00000000001267608, -203.5231074845243597 ) ) ;
#10313=CARTESIAN_POINT ( 'NONE',  ( 21.05000000000000071, 67.22371710472015138, -194.9644784893834810 ) ) ;
#10371=ORIENTED_EDGE ( 'NONE', *, *, #232165, .T. ) ;
#10397=ORIENTED_EDGE ( 'NONE', *, *, #56143, .T. ) ;
#10409=AXIS2_PLACEMENT_3D ( 'NONE', #57363, #97761, #93937 ) ;
#10435=DIRECTION ( 'NONE',  ( 1.000000000000000000, -7.304098846218134667E-16, -5.100424963727256530E-30 ) ) ;
#10489=EDGE_CURVE ( 'NONE', #48255, #43270, #67494, .T. ) ;
#10491=DIRECTION ( 'NONE',  ( -1.000000000000000000, -0.000000000000000000, -0.000000000000000000 ) ) ;
#10522=EDGE_CURVE ( 'NONE', #103860, #242379, #88313, .T. ) ;
#10529=LINE ( 'NONE', #164464, #181981 ) ;
#10561=FACE_OUTER_BOUND ( 'NONE', #203084, .T. ) ;
#10563=DIRECTION ( 'NONE',  ( 1.000000000000000000, 0.000000000000000000, 0.000000000000000000 ) ) ;
#10593=ADVANCED_FACE ( 'NONE', ( #108005 ), #238183, .F. ) ;
#10597=EDGE_CURVE ( 'NONE', #156110, #57467, #144544, .T. ) ;
#10598=DIRECTION ( 'NONE',  ( 0.000000000000000000, 0.000000000000000000, 1.000000000000000000 ) ) ;
#10599=ADVANCED_FACE ( 'NONE', ( #207112 ), #169302, .F. ) ;
#10602=DIRECTION ( 'NONE',  ( -2.561896900575096011E-15, 0.5907332058517336115, -0.8068669527896984439 ) ) ;
#10635=EDGE_CURVE ( 'NONE', #116446, #205515, #839, .T. ) ;
#10677=AXIS2_PLACEMENT_3D ( 'NONE', #159787, #121940, #60652 ) ;
#10686=VERTEX_POINT ( 'NONE', #128861 ) ;
#10694=VECTOR ( 'NONE', #156608, 1000.000000000000000 ) ;
#10730=DIRECTION ( 'NONE',  ( 1.000000000000000000, 0.000000000000000000, 0.000000000000000000 ) ) ;
#10763=ORIENTED_EDGE ( 'NONE', *, *, #214149, .F. ) ;
#10849=VERTEX_POINT ( 'NONE', #80387 ) ;
#10850=AXIS2_PLACEMENT_3D ( 'NONE', #243544, #186146, #105284 ) ;
#10862=CARTESIAN_POINT ( 'NONE',  ( 20.86777300164944648, 65.66799936921584901, -164.4299399888601556 ) ) ;
#10863=DIRECTION ( 'NONE',  ( 0.000000000000000000, 6.982962677686266711E-15, -1.000000000000000000 ) ) ;
#10871=DIRECTION ( 'NONE',  ( 0.000000000000000000, -6.982962677686266711E-15, 1.000000000000000000 ) ) ;
#10895=SPHERICAL_SURFACE ( 'NONE', #175816, 0.1000000000000000056 ) ;
#10923=EDGE_LOOP ( 'NONE', ( #87844, #163578, #3709, #196370 ) ) ;
#10929=EDGE_CURVE ( 'NONE', #4741, #222996, #158711, .T. ) ;
#10976=DIRECTION ( 'NONE',  ( 2.952720810173289112E-16, 1.000000000000000000, 6.467318590049456648E-15 ) ) ;
#10983=CARTESIAN_POINT ( 'NONE',  ( 18.49999999999998934, 69.55000000001261640, -193.5060803140843859 ) ) ;
#11009=CIRCLE ( 'NONE', #15318, 0.1000000000000028644 ) ;
#11012=AXIS2_PLACEMENT_3D ( 'NONE', #168903, #107594, #24236 ) ;
#11021=ORIENTED_EDGE ( 'NONE', *, *, #81067, .T. ) ;
#11044=ORIENTED_EDGE ( 'NONE', *, *, #61052, .F. ) ;
#11049=ORIENTED_EDGE ( 'NONE', *, *, #251731, .T. ) ;
#11075=AXIS2_PLACEMENT_3D ( 'NONE', #104478, #49672, #47082 ) ;
#11106=AXIS2_PLACEMENT_3D ( 'NONE', #203879, #121798, #60504 ) ;
#11122=ORIENTED_EDGE ( 'NONE', *, *, #127272, .T. ) ;
#11127=ORIENTED_EDGE ( 'NONE', *, *, #132367, .F. ) ;
#11179=AXIS2_PLACEMENT_3D ( 'NONE', #216066, #196506, #217341 ) ;
#11195=ORIENTED_EDGE ( 'NONE', *, *, #189624, .T. ) ;
#11198=CIRCLE ( 'NONE', #119537, 0.09999999999998898659 ) ;
#11225=EDGE_LOOP ( 'NONE', ( #80746, #87691, #73403, #172849 ) ) ;
#11230=LINE ( 'NONE', #9938, #72949 ) ;
#11246=VECTOR ( 'NONE', #220234, 1000.000000000000000 ) ;
#11278=FACE_OUTER_BOUND ( 'NONE', #199997, .T. ) ;
#11283=ORIENTED_EDGE ( 'NONE', *, *, #164400, .F. ) ;
#11288=ORIENTED_EDGE ( 'NONE', *, *, #25162, .F. ) ;
#11318=CARTESIAN_POINT ( 'NONE',  ( -20.94999999999999929, 76.00000000001244871, -170.0231074845243597 ) ) ;
#11323=DIRECTION ( 'NONE',  ( 0.000000000000000000, 6.982962677686266711E-15, -1.000000000000000000 ) ) ;
#11338=ORIENTED_EDGE ( 'NONE', *, *, #5955, .F. ) ;
#11377=EDGE_CURVE ( 'NONE', #228673, #165186, #206165, .T. ) ;
#11378=FACE_OUTER_BOUND ( 'NONE', #34326, .T. ) ;
#11400=CIRCLE ( 'NONE', #211312, 0.1000000000000028644 ) ;
#11412=LINE ( 'NONE', #88106, #217658 ) ;
#11442=CARTESIAN_POINT ( 'NONE',  ( 23.15000000000000213, 87.48912529308852015, -173.1231074845242688 ) ) ;
#11465=ORIENTED_EDGE ( 'NONE', *, *, #10522, .T. ) ;
#11470=DIRECTION ( 'NONE',  ( 0.000000000000000000, -6.467318590049456648E-15, 1.000000000000000000 ) ) ;
#11511=CARTESIAN_POINT ( 'NONE',  ( -23.15000000000000213, 84.66355140188177586, -193.9990063664569959 ) ) ;
#11518=CARTESIAN_POINT ( 'NONE',  ( 20.94999999999999929, 69.45000000001259366, -191.3731074845244109 ) ) ;
#11547=CARTESIAN_POINT ( 'NONE',  ( -21.05000000000000071, 77.16270174995064224, -195.6231074845243540 ) ) ;
#11557=DIRECTION ( 'NONE',  ( 0.000000000000000000, 0.000000000000000000, 1.000000000000000000 ) ) ;
#11571=EDGE_LOOP ( 'NONE', ( #33582, #7621, #131263, #90824 ) ) ;
#11574=CIRCLE ( 'NONE', #44880, 0.09999999999999939493 ) ;
#11633=AXIS2_PLACEMENT_3D ( 'NONE', #31394, #109597, #130452 ) ;
#11644=CARTESIAN_POINT ( 'NONE',  ( -20.64999999999999858, 73.50000000001254818, -183.2477294072864709 ) ) ;
#11649=EDGE_CURVE ( 'NONE', #59470, #125487, #163731, .T. ) ;
#11680=ORIENTED_EDGE ( 'NONE', *, *, #146304, .F. ) ;
#11681=CARTESIAN_POINT ( 'NONE',  ( 22.47071067811865319, 76.00000000001267608, -203.5231074845243597 ) ) ;
#11732=DIRECTION ( 'NONE',  ( 0.000000000000000000, -6.982962677686266711E-15, 1.000000000000000000 ) ) ;
#11756=DIRECTION ( 'NONE',  ( 1.000000000000000000, 0.000000000000000000, 0.000000000000000000 ) ) ;
#11767=EDGE_CURVE ( 'NONE', #234183, #176065, #39039, .T. ) ;
#11770=AXIS2_PLACEMENT_3D ( 'NONE', #109810, #189371, #10730 ) ;
#11775=AXIS2_PLACEMENT_3D ( 'NONE', #139768, #77234, #254571 ) ;
#11777=LINE ( 'NONE', #191706, #116105 ) ;
#11787=ORIENTED_EDGE ( 'NONE', *, *, #179376, .T. ) ;
#11800=CARTESIAN_POINT ( 'NONE',  ( -21.44999999999999929, 68.85000000001254250, -182.3731074845244109 ) ) ;
#11815=AXIS2_PLACEMENT_3D ( 'NONE', #146208, #220629, #42007 ) ;
#11816=FACE_OUTER_BOUND ( 'NONE', #66334, .T. ) ;
#11821=CARTESIAN_POINT ( 'NONE',  ( -20.94999999999999929, 64.35000000001245724, -170.0231074845244166 ) ) ;
#11848=ORIENTED_EDGE ( 'NONE', *, *, #101714, .T. ) ;
#11863=AXIS2_PLACEMENT_3D ( 'NONE', #195923, #99342, #178946 ) ;
#11872=SPHERICAL_SURFACE ( 'NONE', #60234, 0.1000000000000000056 ) ;
#11898=FACE_OUTER_BOUND ( 'NONE', #133737, .T. ) ;
#11902=CARTESIAN_POINT ( 'NONE',  ( -18.59999999999999787, 77.16270174995064224, -195.5231074845243313 ) ) ;
#11918=ORIENTED_EDGE ( 'NONE', *, *, #79808, .T. ) ;
#11919=CARTESIAN_POINT ( 'NONE',  ( 21.05000000000000426, 69.74118280533120640, -203.5567402198580567 ) ) ;
#11922=VERTEX_POINT ( 'NONE', #74083 ) ;
#11956=CARTESIAN_POINT ( 'NONE',  ( -20.94999999999999929, 74.25000000001259082, -191.8535959266227451 ) ) ;
#11973=VERTEX_POINT ( 'NONE', #14091 ) ;
#11982=CIRCLE ( 'NONE', #241120, 0.09999999999999938105 ) ;
#11985=LINE ( 'NONE', #211444, #197766 ) ;
#11991=DIRECTION ( 'NONE',  ( 0.000000000000000000, 0.000000000000000000, -1.000000000000000000 ) ) ;
#12000=FACE_OUTER_BOUND ( 'NONE', #240551, .T. ) ;
#12006=ORIENTED_EDGE ( 'NONE', *, *, #100552, .F. ) ;
#12029=ORIENTED_EDGE ( 'NONE', *, *, #152628, .F. ) ;
#12083=EDGE_LOOP ( 'NONE', ( #234998, #83510, #151972 ) ) ;
#12124=TOROIDAL_SURFACE ( 'NONE', #220398, 11.70000000000000107, 0.1000000000000000056 ) ;
#12134=CIRCLE ( 'NONE', #195299, 0.4000000000000114575 ) ;
#12165=CARTESIAN_POINT ( 'NONE',  ( 20.94999999999999929, 65.70729864261056719, -164.5657455973725121 ) ) ;
#12184=ORIENTED_EDGE ( 'NONE', *, *, #60814, .F. ) ;
#12236=ORIENTED_EDGE ( 'NONE', *, *, #53846, .T. ) ;
#12260=FACE_OUTER_BOUND ( 'NONE', #157446, .T. ) ;
#12269=CARTESIAN_POINT ( 'NONE',  ( 20.94999999999999929, 68.97833521811233481, -166.1895420826271277 ) ) ;
#12317=AXIS2_PLACEMENT_3D ( 'NONE', #217916, #145768, #186203 ) ;
#12365=CIRCLE ( 'NONE', #74911, 0.09999999999999939493 ) ;
#12410=CARTESIAN_POINT ( 'NONE',  ( -18.54260524012575928, 85.62421939008640948, -163.2823344387538498 ) ) ;
#12414=CARTESIAN_POINT ( 'NONE',  ( 18.59999999999997655, 76.00000000001244871, -170.0231074845243597 ) ) ;
#12462=DIRECTION ( 'NONE',  ( 0.000000000000000000, -1.000000000000000000, 0.000000000000000000 ) ) ;
#12467=ORIENTED_EDGE ( 'NONE', *, *, #4048, .F. ) ;
#12471=EDGE_LOOP ( 'NONE', ( #105180, #117829, #50180 ) ) ;
#12472=LINE ( 'NONE', #105419, #109938 ) ;
#12494=AXIS2_PLACEMENT_3D ( 'NONE', #177402, #256848, #18294 ) ;
#12507=EDGE_CURVE ( 'NONE', #247920, #94393, #22651, .T. ) ;
#12515=EDGE_LOOP ( 'NONE', ( #15578, #22661, #237739, #126733 ) ) ;
#12581=EDGE_CURVE ( 'NONE', #78560, #242161, #118511, .T. ) ;
#12598=CIRCLE ( 'NONE', #249902, 0.09999999999998898659 ) ;
#12688=EDGE_LOOP ( 'NONE', ( #178491, #83741, #225508, #254335, #130102, #116298, #135066, #166249, #155602, #6417, #62670, #229536, #209261, #213371, #243772, #8124, #60667, #44797, #179157, #251132, #7852, #35044, #117291 ) ) ;
#12691=CONICAL_SURFACE ( 'NONE', #133478, 4.299999999999970512, 0.7853981633974466137 ) ;
#12707=ADVANCED_FACE ( 'NONE', ( #133415 ), #30464, .F. ) ;
#12710=ORIENTED_EDGE ( 'NONE', *, *, #247654, .F. ) ;
#12749=DIRECTION ( 'NONE',  ( -1.000000000000000000, -0.000000000000000000, -0.000000000000000000 ) ) ;
#12757=CARTESIAN_POINT ( 'NONE',  ( 20.85000000000000142, 77.85161776048127535, -158.4199177649206831 ) ) ;
#12876=FACE_OUTER_BOUND ( 'NONE', #82724, .T. ) ;
#12881=CARTESIAN_POINT ( 'NONE',  ( -20.54999999999999716, 85.00000000001261924, -194.1291383618718385 ) ) ;
#12902=DIRECTION ( 'NONE',  ( 1.000000000000000000, 0.000000000000000000, 0.000000000000000000 ) ) ;
#12904=ORIENTED_EDGE ( 'NONE', *, *, #147687, .F. ) ;
#12918=CARTESIAN_POINT ( 'NONE',  ( -20.94999999999999929, 74.83729825007462466, -195.4231074845243654 ) ) ;
#12950=DIRECTION ( 'NONE',  ( 0.000000000000000000, 0.000000000000000000, 1.000000000000000000 ) ) ;
#12952=CARTESIAN_POINT ( 'NONE',  ( 20.94999999999999929, 77.83534155023701828, -191.9679561919613491 ) ) ;
#12961=AXIS2_PLACEMENT_3D ( 'NONE', #113845, #170020, #193407 ) ;
#12962=EDGE_LOOP ( 'NONE', ( #71923, #163572, #246862, #52313 ) ) ;
#12967=VERTEX_POINT ( 'NONE', #122846 ) ;
#12969=EDGE_LOOP ( 'NONE', ( #230743, #140518, #181105, #205359 ) ) ;
#12973=DIRECTION ( 'NONE',  ( 1.000000000000000000, 0.000000000000000000, 0.000000000000000000 ) ) ;
#12982=ORIENTED_EDGE ( 'NONE', *, *, #243795, .T. ) ;
#12994=CARTESIAN_POINT ( 'NONE',  ( 21.05000000000000071, 64.35000000001267040, -203.5231074845244166 ) ) ;
#13000=CIRCLE ( 'NONE', #17269, 0.09999999999998898659 ) ;
#13034=ORIENTED_EDGE ( 'NONE', *, *, #91404, .F. ) ;
#13052=ORIENTED_EDGE ( 'NONE', *, *, #119274, .T. ) ;
#13063=DIRECTION ( 'NONE',  ( -0.000000000000000000, 0.1298341882519735979, 0.9915357197604890427 ) ) ;
#13085=DIRECTION ( 'NONE',  ( -0.000000000000000000, 1.000000000000000000, 6.982962677686266711E-15 ) ) ;
#13090=DIRECTION ( 'NONE',  ( 0.000000000000000000, -1.000000000000000000, -6.352154140967427193E-15 ) ) ;
#13091=ORIENTED_EDGE ( 'NONE', *, *, #169488, .F. ) ;
#13092=DIRECTION ( 'NONE',  ( 1.000000000000000000, -0.000000000000000000, 0.000000000000000000 ) ) ;
#13097=DIRECTION ( 'NONE',  ( 1.000000000000000000, 0.000000000000000000, 0.000000000000000000 ) ) ;
#13138=ORIENTED_EDGE ( 'NONE', *, *, #182288, .F. ) ;
#13165=CARTESIAN_POINT ( 'NONE',  ( -21.65000000000000213, 68.29142135624991283, -191.1731074845243938 ) ) ;
#13188=AXIS2_PLACEMENT_3D ( 'NONE', #16948, #217673, #93896 ) ;
#13196=EDGE_CURVE ( 'NONE', #41142, #14901, #101494, .T. ) ;
#13200=EDGE_CURVE ( 'NONE', #197466, #94008, #64133, .T. ) ;
#13225=DIRECTION ( 'NONE',  ( 0.000000000000000000, 0.9908441862701420355, 0.1350103645453197554 ) ) ;
#13232=LINE ( 'NONE', #73219, #134775 ) ;
#13236=FACE_OUTER_BOUND ( 'NONE', #12515, .T. ) ;
#13259=ORIENTED_EDGE ( 'NONE', *, *, #253384, .T. ) ;
#13273=ORIENTED_EDGE ( 'NONE', *, *, #122809, .T. ) ;
#13298=DIRECTION ( 'NONE',  ( 0.000000000000000000, 0.000000000000000000, 1.000000000000000000 ) ) ;
#13332=CYLINDRICAL_SURFACE ( 'NONE', #227690, 0.09999999999998898659 ) ;
#13339=VERTEX_POINT ( 'NONE', #8667 ) ;
#13340=CARTESIAN_POINT ( 'NONE',  ( 21.07928932188134397, 75.90110485435833709, -209.8516241409176928 ) ) ;
#13359=DIRECTION ( 'NONE',  ( 0.000000000000000000, 0.000000000000000000, 1.000000000000000000 ) ) ;
#13380=CARTESIAN_POINT ( 'NONE',  ( -21.05000000000000071, 85.51932773110506503, -196.5501311079649724 ) ) ;
#13381=AXIS2_PLACEMENT_3D ( 'NONE', #46553, #226469, #242198 ) ;
#13386=ORIENTED_EDGE ( 'NONE', *, *, #147687, .T. ) ;
#13410=FACE_OUTER_BOUND ( 'NONE', #208805, .T. ) ;
#13426=DIRECTION ( 'NONE',  ( 1.000000000000000000, -2.952720810173289112E-16, -2.061873921506763405E-30 ) ) ;
#13444=ORIENTED_EDGE ( 'NONE', *, *, #109609, .F. ) ;
#13459=ORIENTED_EDGE ( 'NONE', *, *, #199176, .T. ) ;
#13490=DIRECTION ( 'NONE',  ( 0.000000000000000000, 0.01283462868040404978, 0.9999176327611370985 ) ) ;
#13502=DIRECTION ( 'NONE',  ( 0.000000000000000000, 7.056502275159890043E-15, -1.000000000000000000 ) ) ;
#13517=EDGE_CURVE ( 'NONE', #253585, #207953, #120631, .T. ) ;
#13522=ORIENTED_EDGE ( 'NONE', *, *, #238565, .F. ) ;
#13588=DIRECTION ( 'NONE',  ( 0.000000000000000000, 7.086529944415886769E-15, -1.000000000000000000 ) ) ;
#13619=CYLINDRICAL_SURFACE ( 'NONE', #138748, 0.09999999999998898659 ) ;
#13645=FACE_OUTER_BOUND ( 'NONE', #104840, .T. ) ;
#13653=CARTESIAN_POINT ( 'NONE',  ( -20.94999999999999929, 74.16465844978819177, -191.9679561919613775 ) ) ;
#13655=DIRECTION ( 'NONE',  ( 3.469446951953635015E-14, 6.982962677686266711E-15, -1.000000000000000000 ) ) ;
#13663=DIRECTION ( 'NONE',  ( 0.000000000000000000, 7.116814260417676401E-15, -1.000000000000000000 ) ) ;
#13691=CARTESIAN_POINT ( 'NONE',  ( -20.64999999999999858, 76.00000000001244871, -170.0231074845243597 ) ) ;
#13712=VERTEX_POINT ( 'NONE', #137159 ) ;
#13730=CARTESIAN_POINT ( 'NONE',  ( -20.64999999999999858, 76.00000000001244871, -170.0231074845243597 ) ) ;
#13731=AXIS2_PLACEMENT_3D ( 'NONE', #191618, #12973, #152486 ) ;
#13755=VECTOR ( 'NONE', #127735, 1000.000000000000000 ) ;
#13759=AXIS2_PLACEMENT_3D ( 'NONE', #251549, #232016, #53358 ) ;
#13786=DIRECTION ( 'NONE',  ( -0.000000000000000000, 0.9876197685951241256, 0.1568667991644932258 ) ) ;
#13856=ORIENTED_EDGE ( 'NONE', *, *, #157775, .T. ) ;
#13889=FACE_OUTER_BOUND ( 'NONE', #183758, .T. ) ;
#13915=CIRCLE ( 'NONE', #72195, 0.09999999999998898659 ) ;
#13924=CIRCLE ( 'NONE', #26403, 0.09999999999998898659 ) ;
#13950=ORIENTED_EDGE ( 'NONE', *, *, #252491, .F. ) ;
#13994=AXIS2_PLACEMENT_3D ( 'NONE', #58863, #113726, #39360 ) ;
#14017=DIRECTION ( 'NONE',  ( 1.000000000000000000, 0.000000000000000000, 0.000000000000000000 ) ) ;
#14042=ORIENTED_EDGE ( 'NONE', *, *, #90504, .F. ) ;
#14044=CIRCLE ( 'NONE', #159779, 0.1000000000000026007 ) ;
#14091=CARTESIAN_POINT ( 'NONE',  ( -18.59999999999999787, 64.25000000001260503, -191.3731074845244393 ) ) ;
#14139=ORIENTED_EDGE ( 'NONE', *, *, #3310, .T. ) ;
#14153=ADVANCED_FACE ( 'NONE', ( #91109 ), #35314, .T. ) ;
#14198=EDGE_CURVE ( 'NONE', #59994, #152240, #207223, .T. ) ;
#14210=AXIS2_PLACEMENT_3D ( 'NONE', #67291, #146812, #226342 ) ;
#14270=VERTEX_POINT ( 'NONE', #255261 ) ;
#14290=ORIENTED_EDGE ( 'NONE', *, *, #103134, .F. ) ;
#14296=ORIENTED_EDGE ( 'NONE', *, *, #192718, .T. ) ;
#14310=PLANE ( 'NONE',  #203705 ) ;
#14334=CARTESIAN_POINT ( 'NONE',  ( 18.57399277249656322, 65.66887361445387228, -164.4329845918269655 ) ) ;
#14366=VERTEX_POINT ( 'NONE', #20579 ) ;
#14372=FACE_OUTER_BOUND ( 'NONE', #159211, .T. ) ;
#14373=DIRECTION ( 'NONE',  ( 0.000000000000000000, -6.853228547068871147E-15, 1.000000000000000000 ) ) ;
#14398=AXIS2_PLACEMENT_3D ( 'NONE', #167204, #208865, #30244 ) ;
#14400=DIRECTION ( 'NONE',  ( -3.265361837132813093E-16, -1.000000000000000000, -6.982962677686266711E-15 ) ) ;
#14423=EDGE_LOOP ( 'NONE', ( #195186, #65745, #216533, #196968, #119983 ) ) ;
#14428=DIRECTION ( 'NONE',  ( 1.000000000000000000, 0.000000000000000000, 0.000000000000000000 ) ) ;
#14438=CARTESIAN_POINT ( 'NONE',  ( 21.05000000000000071, 76.00000000001267608, -203.5231074845243597 ) ) ;
#14441=CYLINDRICAL_SURFACE ( 'NONE', #160423, 0.09999999999999939493 ) ;
#14443=CARTESIAN_POINT ( 'NONE',  ( 18.49999999999998934, 65.75000000001251976, -178.8731074845244109 ) ) ;
#14490=CIRCLE ( 'NONE', #6062, 0.09999999999998898659 ) ;
#14492=ADVANCED_FACE ( 'NONE', ( #163925 ), #162646, .F. ) ;
#14527=CARTESIAN_POINT ( 'NONE',  ( 20.95512820512820440, 65.37615131630066401, -182.2731074845244450 ) ) ;
#14542=VERTEX_POINT ( 'NONE', #72540 ) ;
#14576=AXIS2_PLACEMENT_3D ( 'NONE', #100440, #2641, #41809 ) ;
#14579=AXIS2_PLACEMENT_3D ( 'NONE', #91079, #31150, #33721 ) ;
#14586=ORIENTED_EDGE ( 'NONE', *, *, #159863, .T. ) ;
#14597=ORIENTED_EDGE ( 'NONE', *, *, #35919, .T. ) ;
#14613=EDGE_CURVE ( 'NONE', #152534, #4741, #47901, .T. ) ;
#14634=CARTESIAN_POINT ( 'NONE',  ( 21.05000000000000071, 87.48912529308871910, -200.6231074845242688 ) ) ;
#14641=AXIS2_PLACEMENT_3D ( 'NONE', #255775, #167638, #247139 ) ;
#14678=CYLINDRICAL_SURFACE ( 'NONE', #19460, 0.09999999999998898659 ) ;
#14689=ORIENTED_EDGE ( 'NONE', *, *, #57593, .T. ) ;
#14694=SPHERICAL_SURFACE ( 'NONE', #98839, 0.1000000000000000056 ) ;
#14695=ORIENTED_EDGE ( 'NONE', *, *, #241057, .T. ) ;
#14728=CARTESIAN_POINT ( 'NONE',  ( 21.30000000000002558, 76.00000000001267608, -203.5231074845243597 ) ) ;
#14750=CARTESIAN_POINT ( 'NONE',  ( 20.95265033839679347, 65.48774916754547348, -195.9573437284944646 ) ) ;
#14767=CARTESIAN_POINT ( 'NONE',  ( 22.59999954896768770, 76.00882823225521179, -215.2736161585923469 ) ) ;
#14776=CARTESIAN_POINT ( 'NONE',  ( 20.94999999999999929, 71.00000000001253397, -182.4283735034374843 ) ) ;
#14779=AXIS2_PLACEMENT_3D ( 'NONE', #182193, #225131, #68658 ) ;
#14794=CARTESIAN_POINT ( 'NONE',  ( 20.94999999999999929, 85.40000000001252545, -179.9170766071767389 ) ) ;
#14800=CIRCLE ( 'NONE', #160539, 0.09999999999999939493 ) ;
#14812=ORIENTED_EDGE ( 'NONE', *, *, #53096, .T. ) ;
#14818=CARTESIAN_POINT ( 'NONE',  ( 21.05315837477245111, 64.25000000001249134, -176.8647514783818906 ) ) ;
#14834=DIRECTION ( 'NONE',  ( 0.000000000000000000, 0.000000000000000000, 1.000000000000000000 ) ) ;
#14847=TOROIDAL_SURFACE ( 'NONE', #160602, 4.099999999999999645, 0.1000000000000000056 ) ;
#14854=AXIS2_PLACEMENT_3D ( 'NONE', #49959, #227313, #188198 ) ;
#14884=DIRECTION ( 'NONE',  ( -2.840903330521632269E-16, -0.8700118002898356018, 0.4930308989875170078 ) ) ;
#14901=VERTEX_POINT ( 'NONE', #99138 ) ;
#14907=EDGE_LOOP ( 'NONE', ( #76843, #221871, #29608, #2864 ) ) ;
#14916=CARTESIAN_POINT ( 'NONE',  ( 21.14999999999999858, 69.45934304831143891, -203.5231074845243882 ) ) ;
#14924=DIRECTION ( 'NONE',  ( 0.000000000000000000, -8.267618268485201230E-15, 1.000000000000000000 ) ) ;
#14942=EDGE_LOOP ( 'NONE', ( #5541, #160162, #141582, #98498 ) ) ;
#14949=DIRECTION ( 'NONE',  ( -1.000000000000000000, 0.000000000000000000, 0.000000000000000000 ) ) ;
#14964=EDGE_CURVE ( 'NONE', #257328, #53042, #96566, .T. ) ;
#15003=EDGE_LOOP ( 'NONE', ( #204643, #13386, #175038, #139051 ) ) ;
#15010=ORIENTED_EDGE ( 'NONE', *, *, #55691, .F. ) ;
#15028=DIRECTION ( 'NONE',  ( 1.000000000000000000, -7.304098846218134667E-16, -5.100424963727255829E-30 ) ) ;
#15092=EDGE_CURVE ( 'NONE', #117519, #204559, #27374, .T. ) ;
#15094=DIRECTION ( 'NONE',  ( 0.000000000000000000, 7.056502275159890043E-15, -1.000000000000000000 ) ) ;
#15123=FACE_OUTER_BOUND ( 'NONE', #200358, .T. ) ;
#15131=AXIS2_PLACEMENT_3D ( 'NONE', #249822, #26950, #251083 ) ;
#15135=DIRECTION ( 'NONE',  ( 0.000000000000000000, -1.000000000000000000, 0.000000000000000000 ) ) ;
#15136=AXIS2_PLACEMENT_3D ( 'NONE', #157292, #119436, #178136 ) ;
#15157=DIRECTION ( 'NONE',  ( 1.000000000000000000, 0.000000000000000000, 0.000000000000000000 ) ) ;
#15181=PLANE ( 'NONE',  #160171 ) ;
#15186=ORIENTED_EDGE ( 'NONE', *, *, #59631, .F. ) ;
#15195=DIRECTION ( 'NONE',  ( 0.000000000000000000, 6.982962677686266711E-15, -1.000000000000000000 ) ) ;
#15196=CARTESIAN_POINT ( 'NONE',  ( -21.05000000000000071, 76.00000000001244871, -170.0231074845243597 ) ) ;
#15212=CIRCLE ( 'NONE', #52610, 11.75000000000001066 ) ;
#15214=AXIS2_PLACEMENT_3D ( 'NONE', #5796, #161054, #202732 ) ;
#15230=CARTESIAN_POINT ( 'NONE',  ( 18.59999999999998721, 56.14960075277911500, -201.2428044267231257 ) ) ;
#15235=DIRECTION ( 'NONE',  ( 1.000000000000000000, 7.304098846218134667E-16, 5.100424963727256530E-30 ) ) ;
#15281=AXIS2_PLACEMENT_3D ( 'NONE', #153177, #132280, #14924 ) ;
#15318=AXIS2_PLACEMENT_3D ( 'NONE', #239311, #63217, #41133 ) ;
#15334=CARTESIAN_POINT ( 'NONE',  ( 21.14999999999999503, 64.35000000001267040, -203.5231074845244166 ) ) ;
#15349=CARTESIAN_POINT ( 'NONE',  ( 18.49999999999998934, 64.35000000001251408, -178.7731074845244450 ) ) ;
#15351=ORIENTED_EDGE ( 'NONE', *, *, #35618, .T. ) ;
#15352=CARTESIAN_POINT ( 'NONE',  ( -18.50000000000000000, 66.75000000001253397, -182.2731074845244166 ) ) ;
#15365=CARTESIAN_POINT ( 'NONE',  ( -18.50000000000000711, 64.25000000001264766, -196.5083017138704236 ) ) ;
#15371=DIRECTION ( 'NONE',  ( 0.000000000000000000, -6.454785026890489601E-15, 1.000000000000000000 ) ) ;
#15400=DIRECTION ( 'NONE',  ( 4.408576920032446739E-17, 0.1350103645451945777, -0.9908441862701590219 ) ) ;
#15402=CYLINDRICAL_SURFACE ( 'NONE', #119849, 11.80000000000000426 ) ;
#15424=EDGE_CURVE ( 'NONE', #27358, #233060, #31764, .T. ) ;
#15440=VERTEX_POINT ( 'NONE', #246073 ) ;
#15451=CARTESIAN_POINT ( 'NONE',  ( -23.25000000000000000, 76.00000000001264766, -199.4731074845243484 ) ) ;
#15452=CARTESIAN_POINT ( 'NONE',  ( -23.25000000000000000, 76.00000000001244871, -170.0231074845243597 ) ) ;
#15467=VERTEX_POINT ( 'NONE', #45298 ) ;
#15471=VECTOR ( 'NONE', #79661, 1000.000000000000000 ) ;
#15473=CARTESIAN_POINT ( 'NONE',  ( -23.15000000000000213, 76.00000000001243450, -167.9231074845243938 ) ) ;
#15543=AXIS2_PLACEMENT_3D ( 'NONE', #47552, #51389, #90540 ) ;
#15553=CARTESIAN_POINT ( 'NONE',  ( 20.95262331984766391, 65.49584273722271632, -195.9622191549311481 ) ) ;
#15558=ORIENTED_EDGE ( 'NONE', *, *, #207947, .T. ) ;
#15566=EDGE_LOOP ( 'NONE', ( #62034, #90173, #240324, #214786 ) ) ;
#15578=ORIENTED_EDGE ( 'NONE', *, *, #128190, .T. ) ;
#15604=AXIS2_PLACEMENT_3D ( 'NONE', #187574, #168029, #169311 ) ;
#15608=EDGE_CURVE ( 'NONE', #85479, #48315, #89539, .T. ) ;
#15621=DIRECTION ( 'NONE',  ( 0.000000000000000000, 0.000000000000000000, -1.000000000000000000 ) ) ;
#15646=CARTESIAN_POINT ( 'NONE',  ( -21.14999999999999858, 87.75000000001267608, -203.5231074845243029 ) ) ;
#15686=CARTESIAN_POINT ( 'NONE',  ( 23.25000000000000000, 85.60000000001262777, -193.6291383618718385 ) ) ;
#15688=AXIS2_PLACEMENT_3D ( 'NONE', #78392, #220495, #120141 ) ;
#15690=ORIENTED_EDGE ( 'NONE', *, *, #105097, .T. ) ;
#15697=TOROIDAL_SURFACE ( 'NONE', #36548, 11.65000000000000036, 0.1000000000000000056 ) ;
#15708=TOROIDAL_SURFACE ( 'NONE', #153088, 4.099999999999999645, 0.1000000000000000056 ) ;
#15730=DIRECTION ( 'NONE',  ( -1.000000000000000000, -7.304098846218135653E-16, -4.639676173203994055E-30 ) ) ;
#15754=CARTESIAN_POINT ( 'NONE',  ( -23.25000000000000000, 76.00000000001270450, -207.5731074845243427 ) ) ;
#15758=CARTESIAN_POINT ( 'NONE',  ( 21.05000000000000071, 77.16270174995064224, -195.4231074845243370 ) ) ;
#15771=CIRCLE ( 'NONE', #215629, 0.5000000000000004441 ) ;
#15773=CARTESIAN_POINT ( 'NONE',  ( -18.59999999999999787, 66.65000000001259650, -191.2731074845244166 ) ) ;
#15781=CARTESIAN_POINT ( 'NONE',  ( 22.59999985501178799, 64.25013020700970401, -203.5887061543243419 ) ) ;
#15795=LINE ( 'NONE', #176142, #151037 ) ;
#15823=FACE_OUTER_BOUND ( 'NONE', #250485, .T. ) ;
#15848=ORIENTED_EDGE ( 'NONE', *, *, #25632, .T. ) ;
#15853=CARTESIAN_POINT ( 'NONE',  ( 20.85000000000000142, 75.83895117929372987, -170.3072973288845731 ) ) ;
#15858=ORIENTED_EDGE ( 'NONE', *, *, #203376, .F. ) ;
#15955=CARTESIAN_POINT ( 'NONE',  ( -20.94999999999999929, 68.87972903831482085, -166.3635444426850825 ) ) ;
#15990=DIRECTION ( 'NONE',  ( 0.000000000000000000, 0.000000000000000000, 1.000000000000000000 ) ) ;
#16003=CIRCLE ( 'NONE', #103250, 0.09999999999998898659 ) ;
#16004=CARTESIAN_POINT ( 'NONE',  ( -20.94999999999999929, 76.00000000001244871, -170.0231074845243597 ) ) ;
#16020=DIRECTION ( 'NONE',  ( 0.000000000000000000, -0.1350103645451945777, 0.9908441862701590219 ) ) ;
#16064=AXIS2_PLACEMENT_3D ( 'NONE', #132282, #110151, #28082 ) ;
#16099=CARTESIAN_POINT ( 'NONE',  ( 20.96428641294449235, 64.25000000001249134, -176.8482143065824062 ) ) ;
#16107=EDGE_CURVE ( 'NONE', #241382, #137660, #2850, .T. ) ;
#16114=DIRECTION ( 'NONE',  ( 1.000000000000000000, 0.000000000000000000, 0.000000000000000000 ) ) ;
#16138=AXIS2_PLACEMENT_3D ( 'NONE', #159087, #223718, #237321 ) ;
#16148=ORIENTED_EDGE ( 'NONE', *, *, #43437, .F. ) ;
#16151=ORIENTED_EDGE ( 'NONE', *, *, #248160, .T. ) ;
#16249=DIRECTION ( 'NONE',  ( -0.000000000000000000, -0.1350103645451718737, 0.9908441862701622416 ) ) ;
#16270=VERTEX_POINT ( 'NONE', #108507 ) ;
#16284=AXIS2_PLACEMENT_3D ( 'NONE', #132962, #33895, #192928 ) ;
#16285=ORIENTED_EDGE ( 'NONE', *, *, #81549, .T. ) ;
#16306=CARTESIAN_POINT ( 'NONE',  ( -22.57320508075687115, 64.25000000001269029, -203.5231074845244166 ) ) ;
#16335=FACE_OUTER_BOUND ( 'NONE', #19657, .T. ) ;
#16362=EDGE_LOOP ( 'NONE', ( #76648, #148320, #66267, #26139 ) ) ;
#16387=ORIENTED_EDGE ( 'NONE', *, *, #144772, .T. ) ;
#16414=CARTESIAN_POINT ( 'NONE',  ( 18.59999999999999076, 64.25000000001263345, -195.4231074845244223 ) ) ;
#16432=CARTESIAN_POINT ( 'NONE',  ( 23.14999999999999858, 69.35000000001259934, -191.1731074845243938 ) ) ;
#16450=CARTESIAN_POINT ( 'NONE',  ( 21.05000000000000071, 70.15000000001266756, -193.3906102602464330 ) ) ;
#16464=EDGE_LOOP ( 'NONE', ( #23261, #47620, #205130, #248786 ) ) ;
#16498=VERTEX_POINT ( 'NONE', #40233 ) ;
#16526=ORIENTED_EDGE ( 'NONE', *, *, #48219, .T. ) ;
#16531=DIRECTION ( 'NONE',  ( 1.000000000000000000, 0.000000000000000000, 0.000000000000000000 ) ) ;
#16554=DIRECTION ( 'NONE',  ( 0.000000000000000000, 6.982962677686267499E-15, -1.000000000000000000 ) ) ;
#16561=CARTESIAN_POINT ( 'NONE',  ( 18.39999999999999858, 85.50000000001242029, -163.1009576351939643 ) ) ;
#16579=CIRCLE ( 'NONE', #187269, 0.09999999999998898659 ) ;
#16615=ORIENTED_EDGE ( 'NONE', *, *, #78435, .F. ) ;
#16652=CARTESIAN_POINT ( 'NONE',  ( -21.05000000000000071, 69.74218538953657287, -203.6208977758331855 ) ) ;
#16656=EDGE_LOOP ( 'NONE', ( #197056, #93286, #230449, #44137 ) ) ;
#16682=CARTESIAN_POINT ( 'NONE',  ( 21.14999999999999858, 64.35000000001267040, -203.4231074845244507 ) ) ;
#16696=EDGE_LOOP ( 'NONE', ( #93953, #122212, #130847 ) ) ;
#16737=DIRECTION ( 'NONE',  ( 0.000000000000000000, -1.000000000000000000, 0.000000000000000000 ) ) ;
#16738=CARTESIAN_POINT ( 'NONE',  ( 23.14999999999999503, 69.55000000001260219, -191.1731074845243938 ) ) ;
#16748=ORIENTED_EDGE ( 'NONE', *, *, #226237, .F. ) ;
#16801=DIRECTION ( 'NONE',  ( 0.000000000000000000, -0.9915357197604982575, 0.1298341882519033486 ) ) ;
#16844=VECTOR ( 'NONE', #30224, 1000.000000000000114 ) ;
#16849=ORIENTED_EDGE ( 'NONE', *, *, #238717, .T. ) ;
#16888=AXIS2_PLACEMENT_3D ( 'NONE', #245303, #227009, #91369 ) ;
#16893=ORIENTED_EDGE ( 'NONE', *, *, #212430, .F. ) ;
#16948=CARTESIAN_POINT ( 'NONE',  ( 18.59999999999999076, 69.35000000001254250, -182.1731074845243938 ) ) ;
#16955=CARTESIAN_POINT ( 'NONE',  ( 18.49999999999999289, 65.75000000001253397, -182.1731074845244223 ) ) ;
#16999=CARTESIAN_POINT ( 'NONE',  ( 23.25000000000000000, 87.75000000001247713, -173.1231074845242688 ) ) ;
#17016=DIRECTION ( 'NONE',  ( 0.000000000000000000, 0.8700118002898393765, -0.4930308989875104575 ) ) ;
#17033=ORIENTED_EDGE ( 'NONE', *, *, #148849, .F. ) ;
#17038=VERTEX_POINT ( 'NONE', #26322 ) ;
#17052=CIRCLE ( 'NONE', #221019, 4.149999999999987033 ) ;
#17061=ORIENTED_EDGE ( 'NONE', *, *, #111400, .T. ) ;
#17066=EDGE_CURVE ( 'NONE', #70073, #14366, #188491, .T. ) ;
#17132=ORIENTED_EDGE ( 'NONE', *, *, #69419, .T. ) ;
#17143=DIRECTION ( 'NONE',  ( 0.000000000000000000, 6.982962677686266711E-15, -1.000000000000000000 ) ) ;
#17171=CARTESIAN_POINT ( 'NONE',  ( -22.49231231312463208, 64.35001509633539740, -203.5841603721258082 ) ) ;
#17226=CARTESIAN_POINT ( 'NONE',  ( 21.05000000000000071, 85.00000000001251976, -179.9170766071767389 ) ) ;
#17251=AXIS2_PLACEMENT_3D ( 'NONE', #196557, #62196, #158752 ) ;
#17262=DIRECTION ( 'NONE',  ( 0.000000000000000000, 6.982962677686266711E-15, -1.000000000000000000 ) ) ;
#17266=CARTESIAN_POINT ( 'NONE',  ( -18.59999999999999787, 77.85102823015347440, -191.8691942151018566 ) ) ;
#17269=AXIS2_PLACEMENT_3D ( 'NONE', #117967, #59228, #236618 ) ;
#17272=EDGE_CURVE ( 'NONE', #256678, #204385, #229806, .T. ) ;
#17285=CIRCLE ( 'NONE', #154669, 0.09999999999999939493 ) ;
#17291=CARTESIAN_POINT ( 'NONE',  ( 20.04142135623730070, 64.25000000001250555, -178.8731074845244393 ) ) ;
#17293=LINE ( 'NONE', #241467, #60853 ) ;
#17309=DIRECTION ( 'NONE',  ( -2.557131231893037478E-16, -0.8660254037844420383, 0.4999999999999941713 ) ) ;
#17330=DIRECTION ( 'NONE',  ( -1.000000000000000000, 0.000000000000000000, 0.000000000000000000 ) ) ;
#17349=AXIS2_PLACEMENT_3D ( 'NONE', #228809, #192255, #50144 ) ;
#17352=DIRECTION ( 'NONE',  ( 0.000000000000000000, 6.938893903907222067E-15, -1.000000000000000000 ) ) ;
#17412=FACE_OUTER_BOUND ( 'NONE', #209980, .T. ) ;
#17443=AXIS2_PLACEMENT_3D ( 'NONE', #205842, #227976, #27243 ) ;
#17449=CARTESIAN_POINT ( 'NONE',  ( -23.25000000000000000, 85.00000000001253397, -179.3170766071767446 ) ) ;
#17479=EDGE_CURVE ( 'NONE', #183861, #165380, #244356, .T. ) ;
#17505=CARTESIAN_POINT ( 'NONE',  ( -20.94999999999999929, 76.00000000001244871, -170.0231074845243597 ) ) ;
#17532=CARTESIAN_POINT ( 'NONE',  ( 21.00000000000000000, 66.25000000001253397, -182.3731074845244393 ) ) ;
#17575=EDGE_CURVE ( 'NONE', #166644, #152244, #46996, .T. ) ;
#17579=ADVANCED_FACE ( 'NONE', ( #208688 ), #189105, .T. ) ;
#17589=DIRECTION ( 'NONE',  ( 1.000000000000000000, 0.000000000000000000, 0.000000000000000000 ) ) ;
#17601=CARTESIAN_POINT ( 'NONE',  ( -21.05000000000000071, 74.16465844978819177, -191.9679561919613775 ) ) ;
#17603=CIRCLE ( 'NONE', #163381, 0.09999999999998898659 ) ;
#17620=AXIS2_PLACEMENT_3D ( 'NONE', #50901, #130465, #91357 ) ;
#17692=CARTESIAN_POINT ( 'NONE',  ( 18.59999999999999076, 74.16465844978819177, -191.8679561919614116 ) ) ;
#17699=CARTESIAN_POINT ( 'NONE',  ( 23.25000000000000000, 85.60000000001278408, -215.2731074845243029 ) ) ;
#17703=FACE_OUTER_BOUND ( 'NONE', #198077, .T. ) ;
#17720=VERTEX_POINT ( 'NONE', #112156 ) ;
#17736=ORIENTED_EDGE ( 'NONE', *, *, #122388, .T. ) ;
#17775=CIRCLE ( 'NONE', #46821, 11.89999999999999325 ) ;
#17784=ORIENTED_EDGE ( 'NONE', *, *, #168950, .T. ) ;
#17808=VECTOR ( 'NONE', #128399, 1000.000000000000000 ) ;
#17821=DIRECTION ( 'NONE',  ( 0.000000000000000000, 0.000000000000000000, 1.000000000000000000 ) ) ;
#17835=ADVANCED_FACE ( 'NONE', ( #215079 ), #255438, .T. ) ;
#17837=CARTESIAN_POINT ( 'NONE',  ( 22.44352723754029810, 75.99072290496948767, -215.1728288298730831 ) ) ;
#17868=DIRECTION ( 'NONE',  ( 0.000000000000000000, 0.000000000000000000, 1.000000000000000000 ) ) ;
#17887=CARTESIAN_POINT ( 'NONE',  ( 18.59999999999999432, 74.83729825007462466, -195.4231074845243654 ) ) ;
#17924=DIRECTION ( 'NONE',  ( 0.000000000000000000, 0.000000000000000000, -1.000000000000000000 ) ) ;
#17929=AXIS2_PLACEMENT_3D ( 'NONE', #188215, #248192, #65690 ) ;
#17933=AXIS2_PLACEMENT_3D ( 'NONE', #195347, #252707, #134049 ) ;
#17961=CARTESIAN_POINT ( 'NONE',  ( 23.14999999999999147, 76.00000000001267608, -203.5231074845243597 ) ) ;
#17965=DIRECTION ( 'NONE',  ( 0.000000000000000000, 1.000000000000000000, 1.387778780781444413E-14 ) ) ;
#17972=CYLINDRICAL_SURFACE ( 'NONE', #101184, 0.8750000000000007772 ) ;
#17977=ORIENTED_EDGE ( 'NONE', *, *, #200364, .F. ) ;
#17990=FACE_OUTER_BOUND ( 'NONE', #225529, .T. ) ;
#17992=DIRECTION ( 'NONE',  ( 1.000000000000000000, 0.000000000000000000, 0.000000000000000000 ) ) ;
#17994=AXIS2_PLACEMENT_3D ( 'NONE', #193765, #235439, #15135 ) ;
#18008=EDGE_CURVE ( 'NONE', #109246, #49859, #203115, .T. ) ;
#18021=CARTESIAN_POINT ( 'NONE',  ( -23.15000000000000213, 71.65000000001253966, -182.2731074845243882 ) ) ;
#18028=CARTESIAN_POINT ( 'NONE',  ( -22.50014994444006078, 64.25028026812042015, -203.6061876412429683 ) ) ;
#18069=CARTESIAN_POINT ( 'NONE',  ( 23.14999999999999858, 76.00000000001244871, -170.0231074845243597 ) ) ;
#18088=ORIENTED_EDGE ( 'NONE', *, *, #221686, .T. ) ;
#18092=AXIS2_PLACEMENT_3D ( 'NONE', #158078, #116348, #195888 ) ;
#18129=AXIS2_PLACEMENT_3D ( 'NONE', #58747, #60047, #79600 ) ;
#18166=CARTESIAN_POINT ( 'NONE',  ( 23.15000000000000213, 87.39257802171813694, -173.0970570643562212 ) ) ;
#18202=ADVANCED_FACE ( 'NONE', ( #81636 ), #97351, .T. ) ;
#18203=CYLINDRICAL_SURFACE ( 'NONE', #128939, 0.09999999999998898659 ) ;
#18204=CARTESIAN_POINT ( 'NONE',  ( 21.08198257630413508, 69.66340326599762989, -203.5957508083089920 ) ) ;
#18212=EDGE_CURVE ( 'NONE', #203961, #213320, #243683, .T. ) ;
#18277=EDGE_CURVE ( 'NONE', #188810, #212797, #82925, .T. ) ;
#18278=AXIS2_PLACEMENT_3D ( 'NONE', #15352, #75339, #32366 ) ;
#18294=DIRECTION ( 'NONE',  ( 0.000000000000000000, 0.000000000000000000, -1.000000000000000000 ) ) ;
#18329=EDGE_CURVE ( 'NONE', #210147, #6205, #199061, .T. ) ;
#18334=DIRECTION ( 'NONE',  ( 0.000000000000000000, 0.000000000000000000, 1.000000000000000000 ) ) ;
#18338=CIRCLE ( 'NONE', #64139, 0.09999999999999939493 ) ;
#18405=ORIENTED_EDGE ( 'NONE', *, *, #40577, .F. ) ;
#18425=VERTEX_POINT ( 'NONE', #111512 ) ;
#18449=ORIENTED_EDGE ( 'NONE', *, *, #188615, .T. ) ;
#18456=FACE_OUTER_BOUND ( 'NONE', #93697, .T. ) ;
#18459=DIRECTION ( 'NONE',  ( 0.000000000000000000, 1.429471705525953388E-14, -1.000000000000000000 ) ) ;
#18593=CARTESIAN_POINT ( 'NONE',  ( 20.94999999999999929, 70.10000000001251408, -180.2422072491807796 ) ) ;
#18597=AXIS2_PLACEMENT_3D ( 'NONE', #52424, #109832, #151574 ) ;
#18600=VECTOR ( 'NONE', #234737, 1000.000000000000114 ) ;
#18626=EDGE_CURVE ( 'NONE', #193318, #188520, #82645, .T. ) ;
#18630=ORIENTED_EDGE ( 'NONE', *, *, #67050, .T. ) ;
#18643=EDGE_CURVE ( 'NONE', #171376, #110731, #61844, .T. ) ;
#18647=FACE_BOUND ( 'NONE', #201737, .T. ) ;
#18660=CARTESIAN_POINT ( 'NONE',  ( -18.59999999999999787, 77.25000000001239187, -162.2226267301092548 ) ) ;
#18674=CARTESIAN_POINT ( 'NONE',  ( -18.51991288638512856, 85.39243678968547613, -196.3798410805651145 ) ) ;
#18697=ORIENTED_EDGE ( 'NONE', *, *, #151879, .F. ) ;
#18722=FACE_OUTER_BOUND ( 'NONE', #35097, .T. ) ;
#18724=VERTEX_POINT ( 'NONE', #11821 ) ;
#18733=CARTESIAN_POINT ( 'NONE',  ( -21.05000000000000071, 76.00000000001267608, -203.5231074845243597 ) ) ;
#18738=CARTESIAN_POINT ( 'NONE',  ( 22.57856590037849287, 76.00412833007710844, -215.2731659471998000 ) ) ;
#18743=TOROIDAL_SURFACE ( 'NONE', #139346, 11.89999999999999858, 0.1000000000000000056 ) ;
#18744=CARTESIAN_POINT ( 'NONE',  ( -20.94999999999999929, 76.00000000001263345, -195.6231074845243540 ) ) ;
#18751=DIRECTION ( 'NONE',  ( -1.000000000000000000, 0.000000000000000000, 0.000000000000000000 ) ) ;
#18765=SPHERICAL_SURFACE ( 'NONE', #198758, 0.1000000000000000056 ) ;
#18768=EDGE_CURVE ( 'NONE', #207133, #256678, #211878, .T. ) ;
#18774=DIRECTION ( 'NONE',  ( 0.5000000000001141309, -6.047423072554455661E-15, 0.8660254037843729824 ) ) ;
#18790=EDGE_CURVE ( 'NONE', #255597, #95948, #120144, .T. ) ;
#18794=CARTESIAN_POINT ( 'NONE',  ( -18.41809261886924887, 85.68240331476904714, -163.3662639344331922 ) ) ;
#18796=CARTESIAN_POINT ( 'NONE',  ( 20.94999999999999929, 74.16465844978819177, -191.9679561919613775 ) ) ;
#18813=EDGE_CURVE ( 'NONE', #57380, #174151, #57311, .T. ) ;
#18847=DIRECTION ( 'NONE',  ( -0.000000000000000000, 1.000000000000000000, 6.982962677686266711E-15 ) ) ;
#18883=ORIENTED_EDGE ( 'NONE', *, *, #178395, .T. ) ;
#18898=CYLINDRICAL_SURFACE ( 'NONE', #28998, 0.09999999999998898659 ) ;
#18922=CARTESIAN_POINT ( 'NONE',  ( 20.97224591636398472, 65.37484658384894942, -191.2731815798608466 ) ) ;
#18929=CARTESIAN_POINT ( 'NONE',  ( -23.25000000000000000, 87.65000000001246860, -173.1231074845242688 ) ) ;
#18966=CARTESIAN_POINT ( 'NONE',  ( 21.14999999999999858, 69.35000000001259934, -191.3731074845244109 ) ) ;
#18970=AXIS2_PLACEMENT_3D ( 'NONE', #101760, #243867, #62681 ) ;
#18976=AXIS2_PLACEMENT_3D ( 'NONE', #209885, #211157, #71664 ) ;
#19010=VECTOR ( 'NONE', #126521, 999.9999999999998863 ) ;
#19011=CARTESIAN_POINT ( 'NONE',  ( -20.85000000000000142, 87.75000000001246292, -170.0231074845242745 ) ) ;
#19023=CARTESIAN_POINT ( 'NONE',  ( -20.94999999999999929, 77.16412189325360771, -162.1082593989527254 ) ) ;
#19036=CARTESIAN_POINT ( 'NONE',  ( 18.49999999999998934, 69.45000000001260787, -193.5060803140843859 ) ) ;
#19065=TOROIDAL_SURFACE ( 'NONE', #164835, 0.2000000000000000111, 0.1000000000000000056 ) ;
#19071=VERTEX_POINT ( 'NONE', #96130 ) ;
#19073=AXIS2_PLACEMENT_3D ( 'NONE', #219213, #237515, #97962 ) ;
#19133=CARTESIAN_POINT ( 'NONE',  ( 22.49066049874202022, 75.94365674848053516, -215.1731197220414913 ) ) ;
#19137=CARTESIAN_POINT ( 'NONE',  ( 18.59999999999999787, 77.83534155023700407, -191.9679561919613491 ) ) ;
#19147=EDGE_LOOP ( 'NONE', ( #211263, #129109, #247784, #165265, #221423 ) ) ;
#19168=EDGE_CURVE ( 'NONE', #38969, #80372, #53171, .T. ) ;
#19203=CARTESIAN_POINT ( 'NONE',  ( -21.05000000000000071, 69.45934304831143891, -203.4231074845244223 ) ) ;
#19206=ORIENTED_EDGE ( 'NONE', *, *, #166921, .T. ) ;
#19209=AXIS2_PLACEMENT_3D ( 'NONE', #41240, #761, #182010 ) ;
#19212=DIRECTION ( 'NONE',  ( -1.000000000000000000, 0.000000000000000000, 0.000000000000000000 ) ) ;
#19243=DIRECTION ( 'NONE',  ( 0.000000000000000000, 0.8660254037844378194, 0.5000000000000016653 ) ) ;
#19259=CIRCLE ( 'NONE', #40140, 11.69999999999998863 ) ;
#19294=AXIS2_PLACEMENT_3D ( 'NONE', #94801, #239461, #99908 ) ;
#19301=CARTESIAN_POINT ( 'NONE',  ( 23.14999999999998437, 87.75000000001267608, -203.5231074845243029 ) ) ;
#19332=ORIENTED_EDGE ( 'NONE', *, *, #139135, .T. ) ;
#19333=CARTESIAN_POINT ( 'NONE',  ( 20.94999999999999574, 77.34908441863964867, -195.5366085209788594 ) ) ;
#19339=EDGE_CURVE ( 'NONE', #74995, #226175, #150184, .T. ) ;
#19340=CIRCLE ( 'NONE', #115017, 0.09999999999998898659 ) ;
#19354=CARTESIAN_POINT ( 'NONE',  ( -20.94999999999999929, 64.36312671090843196, -176.8448666978491701 ) ) ;
#19376=LINE ( 'NONE', #21948, #56587 ) ;
#19385=AXIS2_PLACEMENT_3D ( 'NONE', #133499, #155665, #77359 ) ;
#19398=TOROIDAL_SURFACE ( 'NONE', #227666, 0.2000000000000000111, 0.1000000000000000056 ) ;
#19454=VERTEX_POINT ( 'NONE', #85529 ) ;
#19459=LINE ( 'NONE', #36477, #174404 ) ;
#19460=AXIS2_PLACEMENT_3D ( 'NONE', #53771, #52466, #91615 ) ;
#19468=ORIENTED_EDGE ( 'NONE', *, *, #240402, .F. ) ;
#19479=ORIENTED_EDGE ( 'NONE', *, *, #230864, .T. ) ;
#19497=AXIS2_PLACEMENT_3D ( 'NONE', #236284, #194629, #15990 ) ;
#19519=CARTESIAN_POINT ( 'NONE',  ( 23.14999999999999503, 64.35000000001258513, -191.3731074845244393 ) ) ;
#19530=DIRECTION ( 'NONE',  ( 0.000000000000000000, 0.9999176327611370985, -0.01283462868041289687 ) ) ;
#19598=CARTESIAN_POINT ( 'NONE',  ( -22.39999999999999858, 64.35000000001268461, -203.6231074845244393 ) ) ;
#19620=ORIENTED_EDGE ( 'NONE', *, *, #232126, .F. ) ;
#19638=DIRECTION ( 'NONE',  ( 0.000000000000000000, 0.000000000000000000, 1.000000000000000000 ) ) ;
#19640=VERTEX_POINT ( 'NONE', #198779 ) ;
#19645=EDGE_CURVE ( 'NONE', #152549, #100865, #176679, .T. ) ;
#19651=EDGE_CURVE ( 'NONE', #37631, #244528, #13000, .T. ) ;
#19653=CARTESIAN_POINT ( 'NONE',  ( -22.50000000000000000, 64.25000000001269029, -203.5231074845244166 ) ) ;
#19657=EDGE_LOOP ( 'NONE', ( #105640, #9416, #4500, #203347 ) ) ;
#19679=AXIS2_PLACEMENT_3D ( 'NONE', #35236, #76881, #13090 ) ;
#19691=EDGE_CURVE ( 'NONE', #227674, #228133, #92068, .T. ) ;
#19708=DIRECTION ( 'NONE',  ( -1.000000000000000000, 0.000000000000000000, -0.000000000000000000 ) ) ;
#19719=CARTESIAN_POINT ( 'NONE',  ( 21.05000000000000071, 64.25000000001249134, -177.0379132551784096 ) ) ;
#19731=FACE_OUTER_BOUND ( 'NONE', #174934, .T. ) ;
#19746=DIRECTION ( 'NONE',  ( -0.000000000000000000, 6.982962677686266711E-15, -1.000000000000000000 ) ) ;
#19760=DIRECTION ( 'NONE',  ( 1.000000000000000000, 0.000000000000000000, 0.000000000000000000 ) ) ;
#19781=EDGE_LOOP ( 'NONE', ( #242329, #171297, #115439, #157132, #166602 ) ) ;
#19790=LINE ( 'NONE', #141017, #109715 ) ;
#19841=DIRECTION ( 'NONE',  ( -0.7071067811865127117, -0.7071067811865821007, 0.000000000000000000 ) ) ;
#19850=CARTESIAN_POINT ( 'NONE',  ( 20.94999999999999929, 87.29603075034795268, -200.4752083248604038 ) ) ;
#19860=SPHERICAL_SURFACE ( 'NONE', #11775, 0.1000000000000000056 ) ;
#19862=CIRCLE ( 'NONE', #157442, 0.09999999999998898659 ) ;
#19872=CARTESIAN_POINT ( 'NONE',  ( 23.14999999999999503, 64.35000000001254250, -182.1731074845244507 ) ) ;
#19876=ORIENTED_EDGE ( 'NONE', *, *, #30355, .T. ) ;
#19880=DIRECTION ( 'NONE',  ( 0.000000000000000000, -8.267618268485201230E-15, 1.000000000000000000 ) ) ;
#19884=ORIENTED_EDGE ( 'NONE', *, *, #223004, .T. ) ;
#19885=DIRECTION ( 'NONE',  ( 0.000000000000000000, -6.938893903907222067E-15, 1.000000000000000000 ) ) ;
#19922=EDGE_CURVE ( 'NONE', #209479, #226219, #221240, .T. ) ;
#19943=LINE ( 'NONE', #99437, #59433 ) ;
#19945=AXIS2_PLACEMENT_3D ( 'NONE', #135964, #158158, #215510 ) ;
#19974=ORIENTED_EDGE ( 'NONE', *, *, #73750, .T. ) ;
#19979=ORIENTED_EDGE ( 'NONE', *, *, #103594, .T. ) ;
#20009=ADVANCED_FACE ( 'NONE', ( #220626 ), #15708, .F. ) ;
#20020=ORIENTED_EDGE ( 'NONE', *, *, #248326, .F. ) ;
#20025=CIRCLE ( 'NONE', #194994, 0.09999999999998898659 ) ;
#20036=ORIENTED_EDGE ( 'NONE', *, *, #97676, .F. ) ;
#20038=DIRECTION ( 'NONE',  ( 0.000000000000000000, -6.938893903907222067E-15, 1.000000000000000000 ) ) ;
#20056=DIRECTION ( 'NONE',  ( 0.000000000000000000, 0.000000000000000000, 1.000000000000000000 ) ) ;
#20081=PLANE ( 'NONE',  #212990 ) ;
#20082=CARTESIAN_POINT ( 'NONE',  ( -18.50000000000000000, 64.35000000001276987, -215.2731074845244450 ) ) ;
#20085=ORIENTED_EDGE ( 'NONE', *, *, #174729, .T. ) ;
#20090=CARTESIAN_POINT ( 'NONE',  ( -21.64999999999999858, 68.75000000001254818, -182.3731074845244109 ) ) ;
#20109=VERTEX_POINT ( 'NONE', #117665 ) ;
#20112=DIRECTION ( 'NONE',  ( 0.000000000000000000, -6.467318590049456648E-15, 1.000000000000000000 ) ) ;
#20117=ADVANCED_FACE ( 'NONE', ( #21168 ), #119742, .F. ) ;
#20127=CARTESIAN_POINT ( 'NONE',  ( -23.25000000000000000, 64.35000000001254250, -182.2731074845244450 ) ) ;
#20194=DIRECTION ( 'NONE',  ( -1.000000000000000000, -0.000000000000000000, -0.000000000000000000 ) ) ;
#20231=CARTESIAN_POINT ( 'NONE',  ( -23.25000000000000000, 85.60000000001251408, -179.9170766071767389 ) ) ;
#20243=ORIENTED_EDGE ( 'NONE', *, *, #171564, .T. ) ;
#20294=CARTESIAN_POINT ( 'NONE',  ( -18.59999999999999787, 77.16270174995064224, -195.4231074845243370 ) ) ;
#20309=ORIENTED_EDGE ( 'NONE', *, *, #249303, .T. ) ;
#20310=AXIS2_PLACEMENT_3D ( 'NONE', #77156, #184, #156736 ) ;
#20354=CARTESIAN_POINT ( 'NONE',  ( 21.04999999999999716, 76.01681986839841443, -209.8305327040897055 ) ) ;
#20380=EDGE_LOOP ( 'NONE', ( #102293, #154345, #103467, #185918 ) ) ;
#20393=FACE_OUTER_BOUND ( 'NONE', #209526, .T. ) ;
#20407=VERTEX_POINT ( 'NONE', #246155 ) ;
#20414=CARTESIAN_POINT ( 'NONE',  ( 18.44206774312973707, 85.49102735755248261, -163.3968799798263092 ) ) ;
#20430=ORIENTED_EDGE ( 'NONE', *, *, #162699, .T. ) ;
#20433=ADVANCED_FACE ( 'NONE', ( #44103 ), #132627, .F. ) ;
#20440=CARTESIAN_POINT ( 'NONE',  ( -21.05000000000000071, 87.39257802171833589, -200.4491579046923277 ) ) ;
#20541=DIRECTION ( 'NONE',  ( 0.000000000000000000, 0.8068669527897506244, 0.5907332058516622242 ) ) ;
#20579=CARTESIAN_POINT ( 'NONE',  ( -22.39999999999999858, 76.00000000001276135, -215.1726782920691505 ) ) ;
#20610=ORIENTED_EDGE ( 'NONE', *, *, #209931, .F. ) ;
#20614=CARTESIAN_POINT ( 'NONE',  ( 21.05000000000000071, 77.16270174995064224, -195.6231074845243540 ) ) ;
#20631=LINE ( 'NONE', #243503, #55185 ) ;
#20641=TOROIDAL_SURFACE ( 'NONE', #220545, 0.4000000000000015210, 0.1000000000000000056 ) ;
#20653=CARTESIAN_POINT ( 'NONE',  ( -20.85000000106584750, 64.25000000001250555, -176.8676028280509911 ) ) ;
#20697=CARTESIAN_POINT ( 'NONE',  ( 21.14999999999999858, 67.21339244341248786, -191.2731074845244166 ) ) ;
#20705=ORIENTED_EDGE ( 'NONE', *, *, #73646, .T. ) ;
#20734=EDGE_LOOP ( 'NONE', ( #131252, #4945, #154119, #219070 ) ) ;
#20744=DIRECTION ( 'NONE',  ( 1.000000000000000000, 0.000000000000000000, 0.000000000000000000 ) ) ;
#20807=LINE ( 'NONE', #79454, #198024 ) ;
#20844=FACE_OUTER_BOUND ( 'NONE', #169277, .T. ) ;
#20862=CARTESIAN_POINT ( 'NONE',  ( 21.11747605621531321, 67.22129199451970294, -191.2785443147346598 ) ) ;
#20872=DIRECTION ( 'NONE',  ( 0.000000000000000000, -7.026728003956695223E-15, 1.000000000000000000 ) ) ;
#20912=CARTESIAN_POINT ( 'NONE',  ( -23.15000000000000213, 76.00000000001244871, -170.0231074845243597 ) ) ;
#20987=DIRECTION ( 'NONE',  ( -0.000000000000000000, -0.8660254037844468122, -0.4999999999999860112 ) ) ;
#20994=DIRECTION ( 'NONE',  ( 0.000000000000000000, 0.000000000000000000, 1.000000000000000000 ) ) ;
#21023=CARTESIAN_POINT ( 'NONE',  ( 18.39999999999999858, 85.50000000001240608, -163.4229180933022576 ) ) ;
#21035=ORIENTED_EDGE ( 'NONE', *, *, #202847, .T. ) ;
#21054=EDGE_CURVE ( 'NONE', #109083, #37631, #41185, .T. ) ;
#21060=DIRECTION ( 'NONE',  ( -0.000000000000000000, -6.982962677686266711E-15, 1.000000000000000000 ) ) ;
#21077=CARTESIAN_POINT ( 'NONE',  ( 23.14999999999999503, 64.35000000001249987, -177.0379132551783812 ) ) ;
#21084=ORIENTED_EDGE ( 'NONE', *, *, #134877, .F. ) ;
#21098=CARTESIAN_POINT ( 'NONE',  ( 20.94999999999999929, 71.00000000001260503, -191.1178414656112921 ) ) ;
#21108=ORIENTED_EDGE ( 'NONE', *, *, #67783, .T. ) ;
#21110=ORIENTED_EDGE ( 'NONE', *, *, #47339, .F. ) ;
#21141=DIRECTION ( 'NONE',  ( -1.000000000000000000, 1.836970198721029934E-16, 1.601412966608202925E-30 ) ) ;
#21144=DIRECTION ( 'NONE',  ( 0.000000000000000000, 0.000000000000000000, 1.000000000000000000 ) ) ;
#21156=AXIS2_PLACEMENT_3D ( 'NONE', #93873, #173477, #75624 ) ;
#21158=DIRECTION ( 'NONE',  ( 1.000000000000000000, -3.469446951953718318E-14, 2.003086131649645455E-14 ) ) ;
#21168=FACE_OUTER_BOUND ( 'NONE', #78656, .T. ) ;
#21181=FACE_OUTER_BOUND ( 'NONE', #64637, .T. ) ;
#21194=DIRECTION ( 'NONE',  ( 0.000000000000000000, 6.982962677686266711E-15, -1.000000000000000000 ) ) ;
#21195=( BOUNDED_SURFACE ( )  B_SPLINE_SURFACE ( 3, 2, ( 
 ( #178214, #16561, #199037 ),
 ( #238145, #257655, #158651 ),
 ( #218574, #96063, #99895 ),
 ( #39992, #119509, #175636 ),
 ( #20414, #179490, #796 ),
 ( #80332, #26842, #146729 ),
 ( #180760, #2096, #47633 ),
 ( #202874, #86761, #240734 ),
 ( #221146, #81609, #166360 ),
 ( #244564, #144167, #165037 ) ),
 .UNSPECIFIED., .F., .F., .F. ) 
 B_SPLINE_SURFACE_WITH_KNOTS ( ( 4, 2, 2, 2, 4 ),
 ( 3, 3 ),
 ( 0.0001701955120502350236, 0.0002247052511886079022, 0.0002792149903269808080, 0.0003882344686037266196, 0.0006062734251572181885 ),
 ( 0.000000000000000000, 1.000000000000000000 ),
 .UNSPECIFIED. ) 
 GEOMETRIC_REPRESENTATION_ITEM ( )  RATIONAL_B_SPLINE_SURFACE ( (
 ( 1.000000000000000000, 0.2966190024561151661, 1.000000000000000000),
 ( 1.000000000000000000, 0.2964522492711512691, 1.000000000000000000),
 ( 1.000000000000000000, 0.3059923531882601799, 1.000000000000000000),
 ( 1.000000000000000000, 0.3355751146946392427, 1.000000000000000000),
 ( 1.000000000000000000, 0.3550672384960338879, 1.000000000000000000),
 ( 1.000000000000000000, 0.4157034672187559510, 1.000000000000000000),
 ( 1.000000000000000000, 0.4588031877649293433, 1.000000000000000000),
 ( 1.000000000000000000, 0.5771441759671969152, 1.000000000000000000),
 ( 1.000000000000000000, 0.6469377121765136351, 1.000000000000000000),
 ( 1.000000000000000000, 0.7071067811865475727, 1.000000000000000000) ) ) 
 REPRESENTATION_ITEM ( '' )  SURFACE ( )  );
#21217=DIRECTION ( 'NONE',  ( 1.000000000000000000, 0.000000000000000000, 0.000000000000000000 ) ) ;
#21225=ADVANCED_FACE ( 'NONE', ( #245779 ), #45006, .T. ) ;
#21234=VERTEX_POINT ( 'NONE', #149266 ) ;
#21272=CARTESIAN_POINT ( 'NONE',  ( -18.43599941264928077, 85.51932742860661563, -196.5501306950018829 ) ) ;
#21281=CARTESIAN_POINT ( 'NONE',  ( -23.15000000000000213, 87.65000000001276703, -215.2731074845242745 ) ) ;
#21335=CARTESIAN_POINT ( 'NONE',  ( 22.60000000000000142, 75.89914163091405896, -215.2726746080137445 ) ) ;
#21345=CARTESIAN_POINT ( 'NONE',  ( 21.04999999999959570, 69.65564095796921151, -203.5379631194175261 ) ) ;
#21513=AXIS2_PLACEMENT_3D ( 'NONE', #57434, #194420, #79561 ) ;
#21546=EDGE_LOOP ( 'NONE', ( #239473, #102087, #127183 ) ) ;
#21547=CARTESIAN_POINT ( 'NONE',  ( 18.49999999999999289, 69.35000000001254250, -182.3731074845244109 ) ) ;
#21565=VECTOR ( 'NONE', #33446, 1000.000000000000000 ) ;
#21567=FACE_OUTER_BOUND ( 'NONE', #201873, .T. ) ;
#21584=ADVANCED_FACE ( 'NONE', ( #18722 ), #98215, .F. ) ;
#21588=CARTESIAN_POINT ( 'NONE',  ( -22.39999999999999858, 68.20922040163927136, -203.6231074845244109 ) ) ;
#21590=ORIENTED_EDGE ( 'NONE', *, *, #112158, .F. ) ;
#21612=CARTESIAN_POINT ( 'NONE',  ( -21.78635804494510708, 68.96433851485950584, -203.6221125500320852 ) ) ;
#21664=EDGE_CURVE ( 'NONE', #62333, #6765, #169819, .T. ) ;
#21669=LINE ( 'NONE', #27802, #149314 ) ;
#21677=CARTESIAN_POINT ( 'NONE',  ( -18.59999999999999787, 74.83729825007462466, -195.4231074845243654 ) ) ;
#21683=CARTESIAN_POINT ( 'NONE',  ( -20.85000000000000142, 77.13501884592258762, -162.3061306010920362 ) ) ;
#21690=CARTESIAN_POINT ( 'NONE',  ( 23.14999999999999858, 72.10000000001244302, -170.0231074845243882 ) ) ;
#21813=DIRECTION ( 'NONE',  ( 0.000000000000000000, 1.000000000000000000, 0.000000000000000000 ) ) ;
#21816=ORIENTED_EDGE ( 'NONE', *, *, #167862, .F. ) ;
#21838=DIRECTION ( 'NONE',  ( -4.448008912761042820E-16, -1.000000000000000000, -7.116814260417668513E-15 ) ) ;
#21877=ORIENTED_EDGE ( 'NONE', *, *, #40851, .T. ) ;
#21891=ORIENTED_EDGE ( 'NONE', *, *, #73264, .T. ) ;
#21909=ORIENTED_EDGE ( 'NONE', *, *, #6118, .F. ) ;
#21926=DIRECTION ( 'NONE',  ( 0.000000000000000000, 0.000000000000000000, 1.000000000000000000 ) ) ;
#21942=EDGE_LOOP ( 'NONE', ( #65869, #173096, #57823, #233654 ) ) ;
#21945=ORIENTED_EDGE ( 'NONE', *, *, #188834, .F. ) ;
#21948=CARTESIAN_POINT ( 'NONE',  ( -18.50000000000000000, 64.25000000001269029, -203.4231074845244507 ) ) ;
#21970=ADVANCED_FACE ( 'NONE', ( #33149 ), #70027, .T. ) ;
#22017=CARTESIAN_POINT ( 'NONE',  ( -21.05000000000000071, 64.40000000001249703, -176.9513107147999449 ) ) ;
#22030=AXIS2_PLACEMENT_3D ( 'NONE', #113754, #194616, #94187 ) ;
#22047=CARTESIAN_POINT ( 'NONE',  ( -21.11833042828101625, 75.99289949095337704, -209.9687521783793613 ) ) ;
#22055=CARTESIAN_POINT ( 'NONE',  ( 20.85000000000000142, 76.00000000001244871, -170.0231074845243597 ) ) ;
#22062=DIRECTION ( 'NONE',  ( 0.000000000000000000, 5.551115123126393596E-13, -1.000000000000000000 ) ) ;
#22065=AXIS2_PLACEMENT_3D ( 'NONE', #119380, #198903, #52333 ) ;
#22096=CIRCLE ( 'NONE', #35151, 0.1000000000000070832 ) ;
#22098=EDGE_CURVE ( 'NONE', #90063, #116223, #128682, .T. ) ;
#22105=ADVANCED_FACE ( 'NONE', ( #238900 ), #19860, .F. ) ;
#22109=AXIS2_PLACEMENT_3D ( 'NONE', #235229, #175292, #137399 ) ;
#22124=CARTESIAN_POINT ( 'NONE',  ( 22.49436431346199683, 64.35004905235922479, -203.5900110142466986 ) ) ;
#22132=CARTESIAN_POINT ( 'NONE',  ( 19.97071067811864609, 64.27928932189385591, -178.8731074845244393 ) ) ;
#22133=DIRECTION ( 'NONE',  ( -1.000000000000000000, -0.000000000000000000, -0.000000000000000000 ) ) ;
#22157=VECTOR ( 'NONE', #37669, 1000.000000000000000 ) ;
#22168=CYLINDRICAL_SURFACE ( 'NONE', #12494, 0.5000000000000004441 ) ;
#22258=EDGE_LOOP ( 'NONE', ( #214335, #13091, #110313, #177689 ) ) ;
#22282=ORIENTED_EDGE ( 'NONE', *, *, #48480, .T. ) ;
#22289=CIRCLE ( 'NONE', #5673, 0.5000000000000004441 ) ;
#22294=CARTESIAN_POINT ( 'NONE',  ( 20.84999999999999787, 64.25000000001249134, -176.9422547304831994 ) ) ;
#22300=EDGE_LOOP ( 'NONE', ( #10397, #5092, #33876, #157631 ) ) ;
#22316=CARTESIAN_POINT ( 'NONE',  ( -21.05000000000000426, 76.10000000001274145, -210.0001745056491131 ) ) ;
#22333=EDGE_CURVE ( 'NONE', #254122, #115263, #30138, .T. ) ;
#22338=DIRECTION ( 'NONE',  ( -1.000000000000000000, 0.000000000000000000, -0.000000000000000000 ) ) ;
#22352=DIRECTION ( 'NONE',  ( 0.000000000000000000, -1.000000000000000000, 0.000000000000000000 ) ) ;
#22374=FACE_OUTER_BOUND ( 'NONE', #185365, .T. ) ;
#22386=VECTOR ( 'NONE', #243940, 1000.000000000000000 ) ;
#22436=LINE ( 'NONE', #182786, #36698 ) ;
#22464=EDGE_LOOP ( 'NONE', ( #135728, #5547, #148841, #124685 ) ) ;
#22499=ORIENTED_EDGE ( 'NONE', *, *, #81204, .F. ) ;
#22503=CARTESIAN_POINT ( 'NONE',  ( -18.59999999999999787, 77.83585931145600512, -158.5186683157258187 ) ) ;
#22548=FACE_OUTER_BOUND ( 'NONE', #149635, .T. ) ;
#22571=CIRCLE ( 'NONE', #168356, 0.09999999999999939493 ) ;
#22604=DIRECTION ( 'NONE',  ( 1.000000000000000000, 0.000000000000000000, 0.000000000000000000 ) ) ;
#22633=LINE ( 'NONE', #102113, #90448 ) ;
#22651=CIRCLE ( 'NONE', #63755, 0.09999999999999939493 ) ;
#22661=ORIENTED_EDGE ( 'NONE', *, *, #43716, .T. ) ;
#22703=CIRCLE ( 'NONE', #18597, 0.09999999999999971412 ) ;
#22732=CARTESIAN_POINT ( 'NONE',  ( 20.94999999999999574, 77.25000000001263345, -195.5231074845243313 ) ) ;
#22744=VECTOR ( 'NONE', #159971, 1000.000000000000000 ) ;
#22754=CARTESIAN_POINT ( 'NONE',  ( -21.44999999999999929, 68.75000000001253397, -182.3731074845244109 ) ) ;
#22755=EDGE_CURVE ( 'NONE', #109096, #99184, #24609, .T. ) ;
#22760=DIRECTION ( 'NONE',  ( 0.000000000000000000, -1.000000000000000000, -6.982962677686265922E-15 ) ) ;
#22769=CIRCLE ( 'NONE', #14398, 0.1000000000000028644 ) ;
#22778=EDGE_LOOP ( 'NONE', ( #112292, #37221, #114318, #8487 ) ) ;
#22785=DIRECTION ( 'NONE',  ( 0.000000000000000000, 0.000000000000000000, 1.000000000000000000 ) ) ;
#22796=ORIENTED_EDGE ( 'NONE', *, *, #144346, .T. ) ;
#22801=DIRECTION ( 'NONE',  ( 0.000000000000000000, -0.9908441862701420355, -0.1350103645453197554 ) ) ;
#22807=CARTESIAN_POINT ( 'NONE',  ( -21.65000000000000213, 68.29142135624984178, -182.3731074845244109 ) ) ;
#22816=VERTEX_POINT ( 'NONE', #108068 ) ;
#22822=EDGE_CURVE ( 'NONE', #34176, #100484, #220412, .T. ) ;
#22826=ORIENTED_EDGE ( 'NONE', *, *, #124257, .F. ) ;
#22848=AXIS2_PLACEMENT_3D ( 'NONE', #209851, #108183, #231991 ) ;
#22850=ORIENTED_EDGE ( 'NONE', *, *, #53712, .T. ) ;
#22858=CARTESIAN_POINT ( 'NONE',  ( 20.13684514580103624, 66.50414460725998822, -195.3800757988351506 ) ) ;
#22860=FACE_OUTER_BOUND ( 'NONE', #198017, .T. ) ;
#22883=CARTESIAN_POINT ( 'NONE',  ( -22.50000000000088463, 75.95463834342507425, -215.1736163187297564 ) ) ;
#22905=ORIENTED_EDGE ( 'NONE', *, *, #131256, .F. ) ;
#22916=EDGE_LOOP ( 'NONE', ( #2600, #246476, #214072, #221351 ) ) ;
#22924=CARTESIAN_POINT ( 'NONE',  ( 21.05000000000000071, 76.10000000001272724, -210.0001538663142640 ) ) ;
#22931=AXIS2_PLACEMENT_3D ( 'NONE', #188489, #244609, #205477 ) ;
#22934=EDGE_CURVE ( 'NONE', #14366, #217036, #179607, .T. ) ;
#22981=AXIS2_PLACEMENT_3D ( 'NONE', #53671, #206333, #51060 ) ;
#22982=CARTESIAN_POINT ( 'NONE',  ( 20.94999999999999929, 84.73084112150785074, -179.6211822035086527 ) ) ;
#23000=EDGE_LOOP ( 'NONE', ( #140608, #219223, #246836, #216217 ) ) ;
#23009=FACE_OUTER_BOUND ( 'NONE', #213478, .T. ) ;
#23017=CARTESIAN_POINT ( 'NONE',  ( 22.39999999999999503, 76.00000000001276135, -215.1726782920691505 ) ) ;
#23104=CYLINDRICAL_SURFACE ( 'NONE', #77379, 0.1000000000000118433 ) ;
#23110=CARTESIAN_POINT ( 'NONE',  ( 18.39999999999999858, 85.68240343348880117, -163.3662641071115047 ) ) ;
#23156=AXIS2_PLACEMENT_3D ( 'NONE', #7142, #43717, #85370 ) ;
#23171=B_SPLINE_CURVE_WITH_KNOTS ( 'NONE', 3,
 ( #227611, #204194, #183371, #85501 ),
 .UNSPECIFIED., .F., .F.,
 ( 4, 4 ),
 ( 0.000000000000000000, 0.001767853679387121216 ),
 .UNSPECIFIED. ) ;
#23172=CARTESIAN_POINT ( 'NONE',  ( -18.50000000000000000, 68.97833521811233481, -166.1895420826271277 ) ) ;
#23205=AXIS2_PLACEMENT_3D ( 'NONE', #157007, #139962, #18751 ) ;
#23206=CARTESIAN_POINT ( 'NONE',  ( 20.85000000000000142, 68.92903212821357783, -166.2765432626560766 ) ) ;
#23219=DIRECTION ( 'NONE',  ( 1.000000000000000000, 0.000000000000000000, 0.000000000000000000 ) ) ;
#23222=FACE_OUTER_BOUND ( 'NONE', #33433, .T. ) ;
#23256=CIRCLE ( 'NONE', #106405, 0.09999999999998898659 ) ;
#23261=ORIENTED_EDGE ( 'NONE', *, *, #167173, .T. ) ;
#23292=ORIENTED_EDGE ( 'NONE', *, *, #141443, .F. ) ;
#23295=CARTESIAN_POINT ( 'NONE',  ( -22.59999999999999787, 75.90000000001276703, -215.1726782920691505 ) ) ;
#23327=CIRCLE ( 'NONE', #40077, 0.9750000000000036415 ) ;
#23352=ORIENTED_EDGE ( 'NONE', *, *, #204837, .T. ) ;
#23365=LINE ( 'NONE', #220264, #58615 ) ;
#23369=CARTESIAN_POINT ( 'NONE',  ( 18.49999999999999289, 65.76093837589102975, -178.7687100499267672 ) ) ;
#23436=CARTESIAN_POINT ( 'NONE',  ( 21.05543885634738643, 67.22422895316505276, -191.3387230138097266 ) ) ;
#23458=FACE_OUTER_BOUND ( 'NONE', #19781, .T. ) ;
#23459=LINE ( 'NONE', #125110, #7649 ) ;
#23463=EDGE_CURVE ( 'NONE', #654, #66129, #175024, .T. ) ;
#23468=CARTESIAN_POINT ( 'NONE',  ( 21.05563370358598263, 65.27576964416608973, -191.3400166685613328 ) ) ;
#23505=CARTESIAN_POINT ( 'NONE',  ( -20.64999999999999858, 68.85000000001259934, -191.1731074845243938 ) ) ;
#23568=ORIENTED_EDGE ( 'NONE', *, *, #23770, .T. ) ;
#23641=ADVANCED_FACE ( 'NONE', ( #219047 ), #22168, .F. ) ;
#23644=CIRCLE ( 'NONE', #215141, 0.2000000000000057288 ) ;
#23673=EDGE_CURVE ( 'NONE', #87546, #69800, #50062, .T. ) ;
#23684=CARTESIAN_POINT ( 'NONE',  ( -20.85000000000000142, 76.00000000001244871, -170.0231074845243597 ) ) ;
#23718=VECTOR ( 'NONE', #206841, 1000.000000000000000 ) ;
#23743=EDGE_CURVE ( 'NONE', #140330, #220964, #72133, .T. ) ;
#23770=EDGE_CURVE ( 'NONE', #221704, #239471, #229331, .T. ) ;
#23778=CARTESIAN_POINT ( 'NONE',  ( -22.50000000000000000, 75.90000000001276703, -215.1726782920691505 ) ) ;
#23785=DIRECTION ( 'NONE',  ( 2.879366945564059217E-14, 0.9875055080513762684, -0.1575844902526679081 ) ) ;
#23790=ORIENTED_EDGE ( 'NONE', *, *, #27924, .F. ) ;
#23814=CARTESIAN_POINT ( 'NONE',  ( -21.14999999999999858, 87.65000000001266756, -200.6231074845242688 ) ) ;
#23823=DIRECTION ( 'NONE',  ( -1.000000000000000000, 0.000000000000000000, 0.000000000000000000 ) ) ;
#23853=ORIENTED_EDGE ( 'NONE', *, *, #92770, .F. ) ;
#23872=EDGE_LOOP ( 'NONE', ( #158148, #106260, #33210, #29767 ) ) ;
#23926=DIRECTION ( 'NONE',  ( 0.000000000000000000, 6.982962677686266711E-15, -1.000000000000000000 ) ) ;
#23937=CYLINDRICAL_SURFACE ( 'NONE', #223559, 0.5000000000000004441 ) ;
#23945=DIRECTION ( 'NONE',  ( 0.000000000000000000, 0.000000000000000000, -1.000000000000000000 ) ) ;
#23953=DIRECTION ( 'NONE',  ( 8.673617379884087537E-15, 6.982962677686266711E-15, -1.000000000000000000 ) ) ;
#23955=ORIENTED_EDGE ( 'NONE', *, *, #15608, .F. ) ;
#23969=EDGE_LOOP ( 'NONE', ( #124859, #138386, #194941, #97185 ) ) ;
#23979=AXIS2_PLACEMENT_3D ( 'NONE', #216531, #2610, #82131 ) ;
#23985=CARTESIAN_POINT ( 'NONE',  ( 23.14999999999999858, 70.05000000001251692, -180.3288097895592159 ) ) ;
#24003=EDGE_LOOP ( 'NONE', ( #96415, #1704, #21909, #848 ) ) ;
#24028=CARTESIAN_POINT ( 'NONE',  ( 21.05000000000000071, 87.48912529308852015, -172.9231074845242802 ) ) ;
#24038=CARTESIAN_POINT ( 'NONE',  ( -18.51024323315077424, 65.68895814178293335, -164.5026557862138645 ) ) ;
#24045=CARTESIAN_POINT ( 'NONE',  ( 18.59999999999999432, 77.26178616857765746, -195.4366085209788935 ) ) ;
#24058=ORIENTED_EDGE ( 'NONE', *, *, #139310, .F. ) ;
#24072=ADVANCED_FACE ( 'NONE', ( #191878 ), #151455, .T. ) ;
#24095=EDGE_CURVE ( 'NONE', #95308, #165343, #150420, .T. ) ;
#24117=VERTEX_POINT ( 'NONE', #211412 ) ;
#24161=CARTESIAN_POINT ( 'NONE',  ( -22.45354308602447801, 75.99999978014568569, -215.2735403749861689 ) ) ;
#24166=ORIENTED_EDGE ( 'NONE', *, *, #209091, .T. ) ;
#24225=AXIS2_PLACEMENT_3D ( 'NONE', #1722, #39619, #20038 ) ;
#24236=DIRECTION ( 'NONE',  ( 0.000000000000000000, 0.9908441862701791170, -0.1350103645450472789 ) ) ;
#24264=CARTESIAN_POINT ( 'NONE',  ( -21.09610168723073187, 69.62104428478792784, -203.5566969914158904 ) ) ;
#24279=EDGE_CURVE ( 'NONE', #203821, #226489, #74512, .T. ) ;
#24281=VECTOR ( 'NONE', #31647, 1000.000000000000000 ) ;
#24286=DIRECTION ( 'NONE',  ( 1.000000000000000000, 0.000000000000000000, 0.000000000000000000 ) ) ;
#24288=AXIS2_PLACEMENT_3D ( 'NONE', #37677, #196718, #32560 ) ;
#24305=CARTESIAN_POINT ( 'NONE',  ( 21.30000000000002558, 76.00000000001264766, -199.4731074845243484 ) ) ;
#24313=CARTESIAN_POINT ( 'NONE',  ( 21.08134388332231879, 69.66531941949473605, -203.5989264020314238 ) ) ;
#24325=ORIENTED_EDGE ( 'NONE', *, *, #135882, .F. ) ;
#24346=DIRECTION ( 'NONE',  ( -0.000000000000000000, 1.000000000000000000, 6.982962677686266711E-15 ) ) ;
#24355=VERTEX_POINT ( 'NONE', #144694 ) ;
#24395=CIRCLE ( 'NONE', #195276, 11.70000000000001528 ) ;
#24400=ORIENTED_EDGE ( 'NONE', *, *, #231825, .F. ) ;
#24471=VECTOR ( 'NONE', #52851, 1000.000000000000000 ) ;
#24488=CARTESIAN_POINT ( 'NONE',  ( -18.50000000000000000, 76.00000000001267608, -203.5231074845243597 ) ) ;
#24544=ORIENTED_EDGE ( 'NONE', *, *, #249303, .F. ) ;
#24556=ORIENTED_EDGE ( 'NONE', *, *, #132492, .F. ) ;
#24579=AXIS2_PLACEMENT_3D ( 'NONE', #31216, #226795, #7305 ) ;
#24609=CIRCLE ( 'NONE', #241266, 0.09999999999998898659 ) ;
#24669=CARTESIAN_POINT ( 'NONE',  ( 20.94999999999999929, 87.48912529308852015, -172.9231074845242802 ) ) ;
#24671=DIRECTION ( 'NONE',  ( 0.000000000000000000, 6.982962677686266711E-15, -1.000000000000000000 ) ) ;
#24700=FACE_OUTER_BOUND ( 'NONE', #256720, .T. ) ;
#24701=DIRECTION ( 'NONE',  ( -1.000000000000000000, 0.000000000000000000, -0.000000000000000000 ) ) ;
#24732=DIRECTION ( 'NONE',  ( 2.915501640297156255E-16, 1.000000000000000000, 6.997203936713175802E-15 ) ) ;
#24745=DIRECTION ( 'NONE',  ( 0.000000000000000000, 1.000000000000000000, 6.982962677686266711E-15 ) ) ;
#24786=CIRCLE ( 'NONE', #257918, 0.8750000000000007772 ) ;
#24804=CIRCLE ( 'NONE', #41361, 0.09999999999998898659 ) ;
#24854=CARTESIAN_POINT ( 'NONE',  ( 20.95429402530550433, 67.12380584891043611, -195.0000207865866173 ) ) ;
#24876=CARTESIAN_POINT ( 'NONE',  ( 18.50000000000000000, 85.40000000001239755, -163.1410656363516125 ) ) ;
#24895=FACE_OUTER_BOUND ( 'NONE', #77151, .T. ) ;
#24904=DIRECTION ( 'NONE',  ( 0.000000000000000000, -1.000000000000000000, -6.982962677686265922E-15 ) ) ;
#24949=CARTESIAN_POINT ( 'NONE',  ( -18.58735405345342429, 85.56647862034900243, -163.2003928382583808 ) ) ;
#24962=CARTESIAN_POINT ( 'NONE',  ( 23.14999999999998437, 76.00000000001267608, -203.5231074845243597 ) ) ;
#24966=ORIENTED_EDGE ( 'NONE', *, *, #132005, .T. ) ;
#24984=ADVANCED_FACE ( 'NONE', ( #17703 ), #72581, .F. ) ;
#24990=DIRECTION ( 'NONE',  ( -2.940209281316621016E-16, -1.000000000000000000, -9.408669700213187250E-15 ) ) ;
#25001=CARTESIAN_POINT ( 'NONE',  ( -21.14999999999999858, 76.00000000001267608, -203.5231074845243597 ) ) ;
#25060=ORIENTED_EDGE ( 'NONE', *, *, #89287, .T. ) ;
#25064=LINE ( 'NONE', #220673, #242953 ) ;
#25074=VECTOR ( 'NONE', #164731, 1000.000000000000000 ) ;
#25100=CARTESIAN_POINT ( 'NONE',  ( -18.49513951962167368, 85.43772502669008873, -163.2450349094951321 ) ) ;
#25150=VECTOR ( 'NONE', #16020, 1000.000000000000114 ) ;
#25162=EDGE_CURVE ( 'NONE', #171376, #255434, #218106, .T. ) ;
#25175=ORIENTED_EDGE ( 'NONE', *, *, #10285, .F. ) ;
#25186=EDGE_LOOP ( 'NONE', ( #249833, #9952 ) ) ;
#25191=EDGE_LOOP ( 'NONE', ( #196562, #92235, #201866, #40888 ) ) ;
#25204=DIRECTION ( 'NONE',  ( 0.000000000000000000, 0.000000000000000000, -1.000000000000000000 ) ) ;
#25211=FACE_OUTER_BOUND ( 'NONE', #7152, .T. ) ;
#25217=VERTEX_POINT ( 'NONE', #29318 ) ;
#25219=EDGE_CURVE ( 'NONE', #37447, #75338, #46257, .T. ) ;
#25259=AXIS2_PLACEMENT_3D ( 'NONE', #95805, #178939, #185323 ) ;
#25265=DIRECTION ( 'NONE',  ( 0.000000000000000000, -7.086529944415886769E-15, 1.000000000000000000 ) ) ;
#25268=DIRECTION ( 'NONE',  ( 0.000000000000000000, 0.000000000000000000, 1.000000000000000000 ) ) ;
#25292=DIRECTION ( 'NONE',  ( 0.000000000000000000, -0.1350103645451807555, -0.9908441862701610203 ) ) ;
#25334=CARTESIAN_POINT ( 'NONE',  ( -18.59999999999999787, 77.83534155023700407, -191.8679561919613832 ) ) ;
#25339=EDGE_LOOP ( 'NONE', ( #208788, #184426, #19206, #199297 ) ) ;
#25370=VERTEX_POINT ( 'NONE', #100064 ) ;
#25373=ORIENTED_EDGE ( 'NONE', *, *, #48533, .F. ) ;
#25401=CARTESIAN_POINT ( 'NONE',  ( 23.14999999999999858, 69.35000000001259934, -191.1731074845243938 ) ) ;
#25437=CARTESIAN_POINT ( 'NONE',  ( -21.05000000000000071, 87.65000000001266756, -200.5231074845242745 ) ) ;
#25442=ADVANCED_FACE ( 'NONE', ( #6110 ), #80738, .T. ) ;
#25468=DIRECTION ( 'NONE',  ( -3.440080580676165868E-14, 0.1298341882520054891, 0.9915357197604850459 ) ) ;
#25473=CARTESIAN_POINT ( 'NONE',  ( -20.54999999999999716, 76.00000000001244871, -170.0231074845243597 ) ) ;
#25482=CIRCLE ( 'NONE', #166981, 4.099999999999992539 ) ;
#25518=ORIENTED_EDGE ( 'NONE', *, *, #139279, .F. ) ;
#25535=ADVANCED_FACE ( 'NONE', ( #68678 ), #64196, .F. ) ;
#25595=DIRECTION ( 'NONE',  ( -0.000000000000000000, 0.8660254037844424824, 0.4999999999999934497 ) ) ;
#25603=DIRECTION ( 'NONE',  ( 1.000000000000000000, 7.304098846218133681E-16, 4.639676173203992654E-30 ) ) ;
#25608=ORIENTED_EDGE ( 'NONE', *, *, #22822, .F. ) ;
#25618=DIRECTION ( 'NONE',  ( 0.000000000000000000, -0.01562499999996560217, -0.9998779222360102414 ) ) ;
#25632=EDGE_CURVE ( 'NONE', #106883, #113112, #209366, .T. ) ;
#25678=CIRCLE ( 'NONE', #88003, 0.09999999999999939493 ) ;
#25694=EDGE_LOOP ( 'NONE', ( #54353, #39795, #153817, #174846 ) ) ;
#25699=ORIENTED_EDGE ( 'NONE', *, *, #110298, .T. ) ;
#25702=FACE_OUTER_BOUND ( 'NONE', #251338, .T. ) ;
#25713=ORIENTED_EDGE ( 'NONE', *, *, #206290, .T. ) ;
#25724=DIRECTION ( 'NONE',  ( 0.000000000000000000, 7.056502275159890832E-15, -1.000000000000000000 ) ) ;
#25740=CYLINDRICAL_SURFACE ( 'NONE', #181221, 11.75000000000001066 ) ;
#25764=EDGE_LOOP ( 'NONE', ( #14597, #236378, #187817, #24058 ) ) ;
#25789=CARTESIAN_POINT ( 'NONE',  ( 23.14999999999999503, 69.45000000001252261, -182.2731074845244166 ) ) ;
#25801=EDGE_LOOP ( 'NONE', ( #210344, #19332, #213487 ) ) ;
#25829=CIRCLE ( 'NONE', #17443, 0.09999999999998898659 ) ;
#25840=CIRCLE ( 'NONE', #121538, 6.258578643762724880 ) ;
#25876=VECTOR ( 'NONE', #183150, 1000.000000000000000 ) ;
#25893=FACE_OUTER_BOUND ( 'NONE', #171226, .T. ) ;
#25993=AXIS2_PLACEMENT_3D ( 'NONE', #113394, #252893, #33905 ) ;
#25997=EDGE_CURVE ( 'NONE', #92780, #44979, #101172, .T. ) ;
#26057=ORIENTED_EDGE ( 'NONE', *, *, #700, .T. ) ;
#26069=ORIENTED_EDGE ( 'NONE', *, *, #210771, .T. ) ;
#26070=DIRECTION ( 'NONE',  ( 1.000000000000000000, -7.304098846218163263E-16, 4.217023435051626718E-16 ) ) ;
#26073=EDGE_CURVE ( 'NONE', #135203, #6205, #122256, .T. ) ;
#26080=AXIS2_PLACEMENT_3D ( 'NONE', #3380, #162493, #123358 ) ;
#26090=EDGE_CURVE ( 'NONE', #255448, #221704, #88912, .T. ) ;
#26108=ORIENTED_EDGE ( 'NONE', *, *, #200067, .T. ) ;
#26139=ORIENTED_EDGE ( 'NONE', *, *, #156993, .T. ) ;
#26145=CIRCLE ( 'NONE', #88455, 0.09999999999998898659 ) ;
#26146=LINE ( 'NONE', #66548, #71984 ) ;
#26152=CARTESIAN_POINT ( 'NONE',  ( 18.46947024752525479, 85.50929715716861779, -196.5364180358262161 ) ) ;
#26225=CARTESIAN_POINT ( 'NONE',  ( 20.12500000000000355, 65.75804927292995217, -195.6629037574383290 ) ) ;
#26236=DIRECTION ( 'NONE',  ( -1.000000000000000000, 2.952720810173289112E-16, 2.061873921506763405E-30 ) ) ;
#26239=CARTESIAN_POINT ( 'NONE',  ( -20.54999999999999716, 85.00000000001251976, -179.9170766071767389 ) ) ;
#26243=AXIS2_PLACEMENT_3D ( 'NONE', #11681, #129053, #54631 ) ;
#26308=EDGE_CURVE ( 'NONE', #232039, #142689, #220954, .T. ) ;
#26310=CARTESIAN_POINT ( 'NONE',  ( -23.25000000000000000, 87.65000000001246860, -173.0231074845243029 ) ) ;
#26322=CARTESIAN_POINT ( 'NONE',  ( -21.65000000000000213, 68.29142135624984178, -182.2731074845244166 ) ) ;
#26333=CARTESIAN_POINT ( 'NONE',  ( 23.14999999999998437, 76.00000000001264766, -199.4731074845243484 ) ) ;
#26341=ORIENTED_EDGE ( 'NONE', *, *, #240170, .T. ) ;
#26390=ADVANCED_FACE ( 'NONE', ( #125996 ), #162585, .T. ) ;
#26403=AXIS2_PLACEMENT_3D ( 'NONE', #58459, #78039, #63619 ) ;
#26471=CARTESIAN_POINT ( 'NONE',  ( 19.75857864376268935, 64.35000000001251408, -178.7731074845244450 ) ) ;
#26492=CARTESIAN_POINT ( 'NONE',  ( -20.94999999999999929, 87.39257802171813694, -173.0970570643562212 ) ) ;
#26494=FACE_OUTER_BOUND ( 'NONE', #182766, .T. ) ;
#26513=DIRECTION ( 'NONE',  ( 0.000000000000000000, -1.000000000000000000, -6.982962677686266711E-15 ) ) ;
#26530=ORIENTED_EDGE ( 'NONE', *, *, #38779, .F. ) ;
#26580=CIRCLE ( 'NONE', #184769, 0.1000000000000028644 ) ;
#26589=CARTESIAN_POINT ( 'NONE',  ( -18.59999999999999787, 66.65000000001253966, -182.3731074845244393 ) ) ;
#26596=ORIENTED_EDGE ( 'NONE', *, *, #134048, .T. ) ;
#26624=ADVANCED_BREP_SHAPE_REPRESENTATION ( '', ( #192084, #2425 ), #239393 ) ;
#26625=CYLINDRICAL_SURFACE ( 'NONE', #39259, 12.87499999999999822 ) ;
#26662=DIRECTION ( 'NONE',  ( 0.000000000000000000, -7.304098846218085561E-15, 1.000000000000000000 ) ) ;
#26667=CARTESIAN_POINT ( 'NONE',  ( -21.14999999999999858, 64.35000000001268461, -203.5231074845244166 ) ) ;
#26695=CYLINDRICAL_SURFACE ( 'NONE', #236356, 0.1000000000000028644 ) ;
#26698=AXIS2_PLACEMENT_3D ( 'NONE', #203369, #202087, #222914 ) ;
#26699=DIRECTION ( 'NONE',  ( 0.000000000000000000, -1.000000000000000000, 0.000000000000000000 ) ) ;
#26706=CARTESIAN_POINT ( 'NONE',  ( 20.84451136049616338, 65.37985808520433295, -196.0291829250029991 ) ) ;
#26742=CARTESIAN_POINT ( 'NONE',  ( -20.94999999999999929, 68.92903212821357783, -166.2765432626560766 ) ) ;
#26748=ADVANCED_FACE ( 'NONE', ( #121859 ), #26625, .T. ) ;
#26772=AXIS2_PLACEMENT_3D ( 'NONE', #86515, #166128, #183095 ) ;
#26791=ORIENTED_EDGE ( 'NONE', *, *, #135447, .F. ) ;
#26800=AXIS2_PLACEMENT_3D ( 'NONE', #154067, #75774, #151472 ) ;
#26809=FACE_OUTER_BOUND ( 'NONE', #116459, .T. ) ;
#26842=CARTESIAN_POINT ( 'NONE',  ( 18.33996824403475756, 85.56963985944447870, -163.2040418470076588 ) ) ;
#26846=EDGE_LOOP ( 'NONE', ( #81622, #45470, #84061, #223428 ) ) ;
#26851=DIRECTION ( 'NONE',  ( 0.000000000000000000, -0.9998779222360097974, 0.01562500000000363945 ) ) ;
#26854=ORIENTED_EDGE ( 'NONE', *, *, #215785, .T. ) ;
#26863=EDGE_LOOP ( 'NONE', ( #248958, #49567, #20085, #20430 ) ) ;
#26894=AXIS2_PLACEMENT_3D ( 'NONE', #19333, #96281, #237100 ) ;
#26909=DIRECTION ( 'NONE',  ( 0.000000000000000000, -1.000000000000000000, 0.000000000000000000 ) ) ;
#26910=ORIENTED_EDGE ( 'NONE', *, *, #174835, .T. ) ;
#26911=DIRECTION ( 'NONE',  ( 0.000000000000000000, -0.4999999999999088507, -0.8660254037844913322 ) ) ;
#26950=DIRECTION ( 'NONE',  ( 1.000000000000000000, 0.000000000000000000, 0.000000000000000000 ) ) ;
#26971=ORIENTED_EDGE ( 'NONE', *, *, #17066, .F. ) ;
#27031=CIRCLE ( 'NONE', #22931, 0.09999999999999939493 ) ;
#27036=EDGE_CURVE ( 'NONE', #6886, #186491, #114240, .T. ) ;
#27052=VERTEX_POINT ( 'NONE', #113836 ) ;
#27064=CIRCLE ( 'NONE', #47857, 0.09999999999998898659 ) ;
#27073=DIRECTION ( 'NONE',  ( 0.000000000000000000, 0.000000000000000000, 1.000000000000000000 ) ) ;
#27135=ORIENTED_EDGE ( 'NONE', *, *, #129702, .F. ) ;
#27146=EDGE_CURVE ( 'NONE', #227067, #48315, #76823, .T. ) ;
#27175=DIRECTION ( 'NONE',  ( 0.000000000000000000, -0.4999999999999088507, -0.8660254037844913322 ) ) ;
#27188=DIRECTION ( 'NONE',  ( 0.000000000000000000, 6.982962677686266711E-15, -1.000000000000000000 ) ) ;
#27202=CARTESIAN_POINT ( 'NONE',  ( -21.07954763557471267, 75.93412408139434433, -209.8523984745624205 ) ) ;
#27231=ADVANCED_FACE ( 'NONE', ( #139805 ), #242757, .T. ) ;
#27243=DIRECTION ( 'NONE',  ( 0.000000000000000000, 0.000000000000000000, -1.000000000000000000 ) ) ;
#27276=CARTESIAN_POINT ( 'NONE',  ( 21.05000000000000071, 64.35000000001267040, -203.4231074845244507 ) ) ;
#27289=CYLINDRICAL_SURFACE ( 'NONE', #103515, 0.09999999999998898659 ) ;
#27308=TOROIDAL_SURFACE ( 'NONE', #143778, 0.2000000000000000111, 0.1000000000000000056 ) ;
#27322=DIRECTION ( 'NONE',  ( 0.000000000000000000, 0.000000000000000000, -1.000000000000000000 ) ) ;
#27343=DIRECTION ( 'NONE',  ( 1.000000000000000000, -1.836970198721029934E-16, -1.282749433769087582E-30 ) ) ;
#27352=ADVANCED_FACE ( 'NONE', ( #88808 ), #18743, .T. ) ;
#27358=VERTEX_POINT ( 'NONE', #30167 ) ;
#27374=LINE ( 'NONE', #106848, #119212 ) ;
#27402=EDGE_CURVE ( 'NONE', #36482, #165694, #239326, .T. ) ;
#27407=EDGE_CURVE ( 'NONE', #256678, #11922, #156153, .T. ) ;
#27432=CIRCLE ( 'NONE', #39883, 0.09999999999998898659 ) ;
#27468=CARTESIAN_POINT ( 'NONE',  ( 21.14999999999999858, 64.35000000001258513, -191.3731074845244393 ) ) ;
#27470=CARTESIAN_POINT ( 'NONE',  ( 18.49713797159830264, 85.44648232759176665, -196.4516493629133720 ) ) ;
#27473=EDGE_CURVE ( 'NONE', #43445, #202942, #11230, .T. ) ;
#27475=DIRECTION ( 'NONE',  ( 0.000000000000000000, -0.1350103645451945777, 0.9908441862701590219 ) ) ;
#27483=CARTESIAN_POINT ( 'NONE',  ( -20.95613430942426092, 64.25000000001263345, -196.6659448363049876 ) ) ;
#27516=DIRECTION ( 'NONE',  ( 0.000000000000000000, 1.000000000000000000, 7.272083257015735086E-15 ) ) ;
#27525=AXIS2_PLACEMENT_3D ( 'NONE', #256637, #141876, #98871 ) ;
#27542=ORIENTED_EDGE ( 'NONE', *, *, #237786, .F. ) ;
#27609=B_SPLINE_CURVE_WITH_KNOTS ( 'NONE', 3,
 ( #42514, #184593, #85458, #24264, #202872, #105014, #103747, #125896 ),
 .UNSPECIFIED., .F., .F.,
 ( 4, 2, 2, 4 ),
 ( 0.000000000000000000, 6.534141206311939467E-05, 0.0001306828241262387893, 0.0002613656482524399569 ),
 .UNSPECIFIED. ) ;
#27644=DIRECTION ( 'NONE',  ( 0.000000000000000000, -7.086529944415886769E-15, 1.000000000000000000 ) ) ;
#27650=EDGE_LOOP ( 'NONE', ( #246902, #198179, #197361, #222431 ) ) ;
#27660=EDGE_LOOP ( 'NONE', ( #57433, #72036, #117493, #74443 ) ) ;
#27732=EDGE_CURVE ( 'NONE', #7443, #210483, #243789, .T. ) ;
#27739=CARTESIAN_POINT ( 'NONE',  ( -21.05000000000000071, 69.58633726514349860, -203.4375146211625065 ) ) ;
#27774=ORIENTED_EDGE ( 'NONE', *, *, #15092, .F. ) ;
#27776=CARTESIAN_POINT ( 'NONE',  ( 19.88284271247461987, 64.30857864377520627, -178.7731074845244450 ) ) ;
#27802=CARTESIAN_POINT ( 'NONE',  ( 19.97071067811864609, 64.27928932189385591, -178.7731074845244450 ) ) ;
#27809=DIRECTION ( 'NONE',  ( 0.000000000000000000, 0.000000000000000000, 1.000000000000000000 ) ) ;
#27811=CARTESIAN_POINT ( 'NONE',  ( 20.94999999999999929, 76.00000000001267608, -203.5231074845243597 ) ) ;
#27815=DIRECTION ( 'NONE',  ( 1.000000000000000000, 0.000000000000000000, 0.000000000000000000 ) ) ;
#27857=DIRECTION ( 'NONE',  ( -1.000000000000000000, -0.000000000000000000, -0.000000000000000000 ) ) ;
#27869=VECTOR ( 'NONE', #242297, 1000.000000000000000 ) ;
#27870=ORIENTED_EDGE ( 'NONE', *, *, #72921, .F. ) ;
#27883=EDGE_LOOP ( 'NONE', ( #111430, #37201, #14139, #178986 ) ) ;
#27904=CARTESIAN_POINT ( 'NONE',  ( -18.55121869061588669, 65.67252876774583115, -164.4457041994994881 ) ) ;
#27917=AXIS2_PLACEMENT_3D ( 'NONE', #158501, #80180, #140170 ) ;
#27924=EDGE_CURVE ( 'NONE', #64517, #69800, #33102, .T. ) ;
#27959=ORIENTED_EDGE ( 'NONE', *, *, #144710, .T. ) ;
#28006=CARTESIAN_POINT ( 'NONE',  ( 21.05000000000000071, 76.08559286337464300, -209.9367702193935372 ) ) ;
#28011=DIRECTION ( 'NONE',  ( 1.000000000000000000, 0.000000000000000000, 0.000000000000000000 ) ) ;
#28019=CIRCLE ( 'NONE', #73810, 0.09999999999998898659 ) ;
#28022=EDGE_LOOP ( 'NONE', ( #241689, #221485, #47257, #52793 ) ) ;
#28027=CARTESIAN_POINT ( 'NONE',  ( 21.04999999999999716, 67.12872031401695949, -191.3731074845244109 ) ) ;
#28037=LINE ( 'NONE', #150531, #56436 ) ;
#28045=ORIENTED_EDGE ( 'NONE', *, *, #171486, .T. ) ;
#28082=DIRECTION ( 'NONE',  ( 1.000000000000000000, 0.000000000000000000, 0.000000000000000000 ) ) ;
#28091=ORIENTED_EDGE ( 'NONE', *, *, #185825, .F. ) ;
#28122=CIRCLE ( 'NONE', #48759, 0.2000000000000057288 ) ;
#28141=CARTESIAN_POINT ( 'NONE',  ( -18.59999999999999787, 77.83585931145600512, -158.5186683157258187 ) ) ;
#28180=ORIENTED_EDGE ( 'NONE', *, *, #241854, .T. ) ;
#28187=EDGE_CURVE ( 'NONE', #75576, #16270, #231511, .T. ) ;
#28192=FACE_OUTER_BOUND ( 'NONE', #234320, .T. ) ;
#28265=ORIENTED_EDGE ( 'NONE', *, *, #147450, .F. ) ;
#28292=LINE ( 'NONE', #8694, #73519 ) ;
#28300=ORIENTED_EDGE ( 'NONE', *, *, #122048, .T. ) ;
#28341=ORIENTED_EDGE ( 'NONE', *, *, #34418, .T. ) ;
#28352=AXIS2_PLACEMENT_3D ( 'NONE', #39885, #119402, #198924 ) ;
#28360=VECTOR ( 'NONE', #57901, 1000.000000000000000 ) ;
#28376=CIRCLE ( 'NONE', #136459, 4.000000000000003553 ) ;
#28400=CARTESIAN_POINT ( 'NONE',  ( -18.59999999999999787, 77.26178616857765746, -195.4366085209788935 ) ) ;
#28423=CIRCLE ( 'NONE', #183175, 11.64999999999999325 ) ;
#28429=EDGE_LOOP ( 'NONE', ( #69999, #114677, #1810, #83793 ) ) ;
#28446=AXIS2_PLACEMENT_3D ( 'NONE', #34294, #113792, #155527 ) ;
#28447=CARTESIAN_POINT ( 'NONE',  ( -22.39999999999999503, 76.00000000001273293, -211.3138870828977645 ) ) ;
#28474=ORIENTED_EDGE ( 'NONE', *, *, #147968, .T. ) ;
#28510=TOROIDAL_SURFACE ( 'NONE', #49303, 2.100000000000002309, 0.1000000000000000056 ) ;
#28518=DIRECTION ( 'NONE',  ( 0.000000000000000000, 6.982962677686266711E-15, -1.000000000000000000 ) ) ;
#28524=ADVANCED_FACE ( 'NONE', ( #83390 ), #106772, .T. ) ;
#28544=CIRCLE ( 'NONE', #203465, 0.09999999999999939493 ) ;
#28569=VERTEX_POINT ( 'NONE', #243782 ) ;
#28578=CARTESIAN_POINT ( 'NONE',  ( 23.24999999999999645, 79.90000000001244018, -170.0231074845243313 ) ) ;
#28579=AXIS2_PLACEMENT_3D ( 'NONE', #38372, #132663, #257346 ) ;
#28612=ORIENTED_EDGE ( 'NONE', *, *, #99794, .F. ) ;
#28613=ORIENTED_EDGE ( 'NONE', *, *, #193143, .F. ) ;
#28614=DIRECTION ( 'NONE',  ( -1.000000000000000000, 0.000000000000000000, -0.000000000000000000 ) ) ;
#28624=DIRECTION ( 'NONE',  ( 1.000000000000000000, 0.000000000000000000, 0.000000000000000000 ) ) ;
#28626=VERTEX_POINT ( 'NONE', #128979 ) ;
#28717=DIRECTION ( 'NONE',  ( 0.000000000000000000, 0.4930308989874980785, 0.8700118002898462599 ) ) ;
#28719=CARTESIAN_POINT ( 'NONE',  ( 21.04999999999999716, 67.12872031401698791, -194.9644784893834810 ) ) ;
#28735=ORIENTED_EDGE ( 'NONE', *, *, #208449, .T. ) ;
#28739=ADVANCED_FACE ( 'NONE', ( #55482 ), #39839, .T. ) ;
#28744=EDGE_LOOP ( 'NONE', ( #173085, #208968, #240432, #4997 ) ) ;
#28752=DIRECTION ( 'NONE',  ( -0.000000000000000000, 1.000000000000000000, 8.717686153663073805E-15 ) ) ;
#28759=DIRECTION ( 'NONE',  ( 0.000000000000000000, -7.056502275159890832E-15, 1.000000000000000000 ) ) ;
#28767=EDGE_LOOP ( 'NONE', ( #231374, #213978, #82410, #227459 ) ) ;
#28787=AXIS2_PLACEMENT_3D ( 'NONE', #65530, #129366, #207639 ) ;
#28788=VERTEX_POINT ( 'NONE', #115488 ) ;
#28794=DIRECTION ( 'NONE',  ( 0.000000000000000000, -0.9915357197604982575, 0.1298341882519033486 ) ) ;
#28799=CARTESIAN_POINT ( 'NONE',  ( 20.94999999999999574, 62.00000000001264056, -198.0960149541419071 ) ) ;
#28803=DIRECTION ( 'NONE',  ( 1.000000000000000000, -0.000000000000000000, 0.000000000000000000 ) ) ;
#28845=DIRECTION ( 'NONE',  ( -1.000000000000000000, 0.000000000000000000, -0.000000000000000000 ) ) ;
#28849=AXIS2_PLACEMENT_3D ( 'NONE', #211560, #91605, #189429 ) ;
#28869=CIRCLE ( 'NONE', #103799, 0.09999999999999939493 ) ;
#28878=ADVANCED_FACE ( 'NONE', ( #144032 ), #1948, .T. ) ;
#28888=VECTOR ( 'NONE', #232795, 1000.000000000000000 ) ;
#28944=ORIENTED_EDGE ( 'NONE', *, *, #181862, .T. ) ;
#28955=CARTESIAN_POINT ( 'NONE',  ( -21.14999999999999858, 64.35000000001268461, -203.4231074845244507 ) ) ;
#28998=AXIS2_PLACEMENT_3D ( 'NONE', #17601, #56706, #22785 ) ;
#29012=EDGE_CURVE ( 'NONE', #144435, #235216, #98537, .T. ) ;
#29015=AXIS2_PLACEMENT_3D ( 'NONE', #110569, #130129, #233116 ) ;
#29025=AXIS2_PLACEMENT_3D ( 'NONE', #65972, #242035, #206768 ) ;
#29039=EDGE_LOOP ( 'NONE', ( #254555, #70789, #196064, #117543 ) ) ;
#29045=ORIENTED_EDGE ( 'NONE', *, *, #204191, .F. ) ;
#29099=( NAMED_UNIT ( * ) SI_UNIT ( $, .STERADIAN. ) SOLID_ANGLE_UNIT ( ) );
#29101=DIRECTION ( 'NONE',  ( 0.000000000000000000, 0.000000000000000000, 1.000000000000000000 ) ) ;
#29104=FACE_OUTER_BOUND ( 'NONE', #50059, .T. ) ;
#29133=AXIS2_PLACEMENT_3D ( 'NONE', #233419, #172190, #93880 ) ;
#29142=TOROIDAL_SURFACE ( 'NONE', #204045, 0.2000000000000000111, 0.1000000000000000056 ) ;
#29145=ORIENTED_EDGE ( 'NONE', *, *, #87534, .F. ) ;
#29147=AXIS2_PLACEMENT_3D ( 'NONE', #9787, #151897, #54047 ) ;
#29149=FACE_OUTER_BOUND ( 'NONE', #203469, .T. ) ;
#29154=FACE_OUTER_BOUND ( 'NONE', #115684, .T. ) ;
#29164=EDGE_LOOP ( 'NONE', ( #19876, #179780, #232334, #178753 ) ) ;
#29190=CARTESIAN_POINT ( 'NONE',  ( -23.25000000000000000, 64.25000000001277556, -215.2731074845244450 ) ) ;
#29207=FACE_OUTER_BOUND ( 'NONE', #186459, .T. ) ;
#29223=CARTESIAN_POINT ( 'NONE',  ( 18.59999999999999076, 70.05000000001267324, -193.2174051794895320 ) ) ;
#29257=ORIENTED_EDGE ( 'NONE', *, *, #254355, .F. ) ;
#29272=CARTESIAN_POINT ( 'NONE',  ( 22.14074124539698829, 68.60992214896893415, -203.6221603803684843 ) ) ;
#29275=CARTESIAN_POINT ( 'NONE',  ( -20.85000000000000142, 76.00000000001244871, -170.0231074845243597 ) ) ;
#29291=DIRECTION ( 'NONE',  ( -0.000000000000000000, 1.000000000000000000, 6.982962677686266711E-15 ) ) ;
#29318=CARTESIAN_POINT ( 'NONE',  ( -23.15000000000000213, 64.40000000001249703, -176.9513107147999449 ) ) ;
#29319=ORIENTED_EDGE ( 'NONE', *, *, #129543, .T. ) ;
#29342=DIRECTION ( 'NONE',  ( 0.000000000000000000, 0.000000000000000000, 1.000000000000000000 ) ) ;
#29359=EDGE_LOOP ( 'NONE', ( #51269, #32616, #45795, #197967 ) ) ;
#29360=AXIS2_PLACEMENT_3D ( 'NONE', #187971, #49732, #90123 ) ;
#29362=VECTOR ( 'NONE', #176311, 1000.000000000000000 ) ;
#29364=CIRCLE ( 'NONE', #87568, 7.899999999999990585 ) ;
#29403=AXIS2_PLACEMENT_3D ( 'NONE', #106680, #166711, #11470 ) ;
#29443=AXIS2_PLACEMENT_3D ( 'NONE', #87144, #28518, #71472 ) ;
#29447=CARTESIAN_POINT ( 'NONE',  ( -18.59999999999999787, 77.26327546522965406, -162.1212428177779543 ) ) ;
#29456=CARTESIAN_POINT ( 'NONE',  ( -23.25000000000000000, 76.00000000001267608, -203.5231074845243597 ) ) ;
#29504=CIRCLE ( 'NONE', #8626, 0.09999999999998898659 ) ;
#29542=CARTESIAN_POINT ( 'NONE',  ( 20.04142135623730070, 64.35000000001251408, -178.8731074845244393 ) ) ;
#29575=VERTEX_POINT ( 'NONE', #213999 ) ;
#29583=CARTESIAN_POINT ( 'NONE',  ( 21.05000000000000071, 64.40000000001248281, -176.9513107147999449 ) ) ;
#29593=CIRCLE ( 'NONE', #241937, 0.1000000000000000888 ) ;
#29608=ORIENTED_EDGE ( 'NONE', *, *, #42629, .F. ) ;
#29622=AXIS2_PLACEMENT_3D ( 'NONE', #150655, #230185, #191090 ) ;
#29628=CARTESIAN_POINT ( 'NONE',  ( 21.14999999999999503, 87.75000000001276135, -215.2731074845242745 ) ) ;
#29653=ORIENTED_EDGE ( 'NONE', *, *, #98256, .F. ) ;
#29666=ORIENTED_EDGE ( 'NONE', *, *, #18626, .F. ) ;
#29669=DIRECTION ( 'NONE',  ( -1.000000000000000000, -0.000000000000000000, 0.000000000000000000 ) ) ;
#29674=CARTESIAN_POINT ( 'NONE',  ( 21.14999999999999503, 87.65000000001266756, -200.6231074845242688 ) ) ;
#29718=DIRECTION ( 'NONE',  ( 0.000000000000000000, 0.000000000000000000, 1.000000000000000000 ) ) ;
#29723=CARTESIAN_POINT ( 'NONE',  ( -21.46681500597176395, 76.00000000001273293, -210.3806186439589396 ) ) ;
#29736=ORIENTED_EDGE ( 'NONE', *, *, #160351, .T. ) ;
#29743=B_SPLINE_CURVE_WITH_KNOTS ( 'NONE', 3,
 ( #107657, #68545, #131073, #187223, #146758, #226301, #227602, #48967 ),
 .UNSPECIFIED., .F., .F.,
 ( 4, 2, 2, 4 ),
 ( 0.000000000000000000, 0.0002114466876442231736, 0.0003171700314663234441, 0.0004228933752884237417 ),
 .UNSPECIFIED. ) ;
#29766=EDGE_LOOP ( 'NONE', ( #94971, #29736 ) ) ;
#29767=ORIENTED_EDGE ( 'NONE', *, *, #202522, .F. ) ;
#29777=VECTOR ( 'NONE', #238544, 1000.000000000000000 ) ;
#29800=AXIS2_PLACEMENT_3D ( 'NONE', #77544, #214507, #197509 ) ;
#29812=CARTESIAN_POINT ( 'NONE',  ( -23.25000000000000000, 76.00000000001244871, -170.0231074845243597 ) ) ;
#29872=CARTESIAN_POINT ( 'NONE',  ( -20.64999999999999858, 85.00000000001261924, -193.6291383618718385 ) ) ;
#29883=CARTESIAN_POINT ( 'NONE',  ( -18.59999999999999787, 85.32100840337392356, -196.2871692354464130 ) ) ;
#29945=CARTESIAN_POINT ( 'NONE',  ( 21.05000000000000071, 69.35000000001262777, -193.6792853948412869 ) ) ;
#29965=ORIENTED_EDGE ( 'NONE', *, *, #139310, .T. ) ;
#29999=CARTESIAN_POINT ( 'NONE',  ( 20.94999999999999574, 87.65000000001266756, -200.6231074845242688 ) ) ;
#30003=ADVANCED_FACE ( 'NONE', ( #113295 ), #103971, .T. ) ;
#30017=DIRECTION ( 'NONE',  ( 0.000000000000000000, -1.000000000000000000, 0.000000000000000000 ) ) ;
#30023=CARTESIAN_POINT ( 'NONE',  ( -21.05000000000000071, 74.25000000001259082, -191.8535959266227451 ) ) ;
#30050=EDGE_CURVE ( 'NONE', #88021, #72890, #89398, .T. ) ;
#30055=EDGE_LOOP ( 'NONE', ( #16151, #95392, #12236, #116090, #214159, #48471, #226920, #139009, #37460, #5865, #166546, #247419, #36431, #103301, #97150, #28474, #106950, #198827, #177757, #45654, #38819, #117522, #9921, #194567, #222507, #229855, #53271 ) ) ;
#30068=VECTOR ( 'NONE', #54328, 1000.000000000000000 ) ;
#30084=VERTEX_POINT ( 'NONE', #23206 ) ;
#30091=VECTOR ( 'NONE', #17309, 1000.000000000000000 ) ;
#30103=CIRCLE ( 'NONE', #184186, 0.09999999999999939493 ) ;
#30138=LINE ( 'NONE', #109638, #107772 ) ;
#30160=ADVANCED_FACE ( 'NONE', ( #247351 ), #172665, .T. ) ;
#30164=CIRCLE ( 'NONE', #92675, 0.1999999999999987899 ) ;
#30167=CARTESIAN_POINT ( 'NONE',  ( 20.94999999999999929, 76.00000000001246292, -171.9231074845243938 ) ) ;
#30196=CARTESIAN_POINT ( 'NONE',  ( 23.15000000000000213, 87.48912529308852015, -173.0231074845243029 ) ) ;
#30222=AXIS2_PLACEMENT_3D ( 'NONE', #165387, #124978, #201946 ) ;
#30224=DIRECTION ( 'NONE',  ( -0.000000000000000000, 0.1350103645451945777, -0.9908441862701590219 ) ) ;
#30237=ADVANCED_FACE ( 'NONE', ( #13889 ), #15181, .F. ) ;
#30244=DIRECTION ( 'NONE',  ( -3.469446951953515108E-14, 1.000000000000000000, 0.000000000000000000 ) ) ;
#30258=EDGE_CURVE ( 'NONE', #50587, #93986, #174296, .T. ) ;
#30263=CARTESIAN_POINT ( 'NONE',  ( 20.94999999999999929, 77.16270174995064224, -195.6231074845243540 ) ) ;
#30278=CIRCLE ( 'NONE', #192575, 0.1000000000000033362 ) ;
#30302=SPHERICAL_SURFACE ( 'NONE', #11770, 0.1000000000000000056 ) ;
#30324=CYLINDRICAL_SURFACE ( 'NONE', #221168, 7.899999999999990585 ) ;
#30332=DIRECTION ( 'NONE',  ( 2.659396599871503635E-15, -0.6132151058540604716, 0.7899159663865477077 ) ) ;
#30344=VERTEX_POINT ( 'NONE', #101063 ) ;
#30355=EDGE_CURVE ( 'NONE', #177267, #80905, #2083, .T. ) ;
#30433=CARTESIAN_POINT ( 'NONE',  ( 23.24999999999999289, 64.35000000001267040, -203.5231074845244166 ) ) ;
#30434=CARTESIAN_POINT ( 'NONE',  ( 20.85882249326303040, 65.66751761918722252, -164.4282609406112670 ) ) ;
#30464=TOROIDAL_SURFACE ( 'NONE', #239111, 1.900000000000002576, 0.1000000000000000056 ) ;
#30494=EDGE_CURVE ( 'NONE', #226290, #131204, #231086, .T. ) ;
#30509=EDGE_CURVE ( 'NONE', #235211, #182596, #6189, .T. ) ;
#30514=VECTOR ( 'NONE', #71622, 1000.000000000000000 ) ;
#30529=CARTESIAN_POINT ( 'NONE',  ( 21.13461538461538680, 65.38541703798705385, -191.1731074845244223 ) ) ;
#30546=DIRECTION ( 'NONE',  ( 0.000000000000000000, 0.000000000000000000, 1.000000000000000000 ) ) ;
#30550=ADVANCED_FACE ( 'NONE', ( #12000 ), #206124, .T. ) ;
#30594=DIRECTION ( 'NONE',  ( 0.000000000000000000, -6.982962677686266711E-15, 1.000000000000000000 ) ) ;
#30597=CARTESIAN_POINT ( 'NONE',  ( -20.64999999999999858, 74.00000000001259082, -190.7984855617622770 ) ) ;
#30606=CARTESIAN_POINT ( 'NONE',  ( 23.25000000000000000, 69.45000000001259366, -191.1731074845243938 ) ) ;
#30607=ORIENTED_EDGE ( 'NONE', *, *, #208223, .T. ) ;
#30613=CYLINDRICAL_SURFACE ( 'NONE', #193772, 2.000000000000001776 ) ;
#30623=CIRCLE ( 'NONE', #18129, 0.09999999999998898659 ) ;
#30681=AXIS2_PLACEMENT_3D ( 'NONE', #159044, #24671, #201995 ) ;
#30693=CARTESIAN_POINT ( 'NONE',  ( -18.49372193242259144, 85.44248452337019728, -163.2583262244892808 ) ) ;
#30749=CARTESIAN_POINT ( 'NONE',  ( 23.14999999999999858, 70.50000000001260503, -191.1178414656113205 ) ) ;
#30774=EDGE_CURVE ( 'NONE', #239471, #253555, #243712, .T. ) ;
#30798=ADVANCED_FACE ( 'NONE', ( #222997 ), #189729, .F. ) ;
#30819=DIRECTION ( 'NONE',  ( -1.000000000000000000, 2.775557561562908012E-13, 0.000000000000000000 ) ) ;
#30821=ORIENTED_EDGE ( 'NONE', *, *, #74480, .T. ) ;
#30828=CARTESIAN_POINT ( 'NONE',  ( -23.15000000000000213, 76.00000000001260503, -190.7481074845243256 ) ) ;
#30846=ADVANCED_FACE ( 'NONE', ( #103043 ), #59611, .F. ) ;
#30898=ADVANCED_FACE ( 'NONE', ( #94906 ), #140448, .T. ) ;
#30910=VERTEX_POINT ( 'NONE', #199155 ) ;
#30929=DIRECTION ( 'NONE',  ( 0.000000000000000000, -1.000000000000000000, -6.982962677686266711E-15 ) ) ;
#30936=CARTESIAN_POINT ( 'NONE',  ( 21.05000000000000071, 67.22371710472015138, -194.9644784893834810 ) ) ;
#30939=FACE_OUTER_BOUND ( 'NONE', #212190, .T. ) ;
#30965=LINE ( 'NONE', #93456, #30068 ) ;
#30992=DIRECTION ( 'NONE',  ( 0.000000000000000000, -6.982962677686266711E-15, 1.000000000000000000 ) ) ;
#31009=CARTESIAN_POINT ( 'NONE',  ( -22.39999999999999858, 64.35000000001268461, -203.4231074845244507 ) ) ;
#31056=CARTESIAN_POINT ( 'NONE',  ( -21.15000000000000213, 76.00000000001273293, -210.0637644362255969 ) ) ;
#31060=ORIENTED_EDGE ( 'NONE', *, *, #101714, .F. ) ;
#31063=ORIENTED_EDGE ( 'NONE', *, *, #87418, .T. ) ;
#31084=AXIS2_PLACEMENT_3D ( 'NONE', #84942, #238930, #241496 ) ;
#31095=DIRECTION ( 'NONE',  ( 0.000000000000000000, 1.000000000000000000, 6.938893903907222067E-15 ) ) ;
#31120=ORIENTED_EDGE ( 'NONE', *, *, #129702, .T. ) ;
#31123=ORIENTED_EDGE ( 'NONE', *, *, #18768, .F. ) ;
#31131=CARTESIAN_POINT ( 'NONE',  ( -20.85000000000000142, 77.16412189325360771, -162.3082593989527425 ) ) ;
#31133=DIRECTION ( 'NONE',  ( 0.000000000000000000, 0.4999999999999088507, -0.8660254037844913322 ) ) ;
#31148=EDGE_CURVE ( 'NONE', #210729, #219970, #14800, .T. ) ;
#31150=DIRECTION ( 'NONE',  ( 1.000000000000000000, 0.000000000000000000, 0.000000000000000000 ) ) ;
#31176=LINE ( 'NONE', #32452, #130081 ) ;
#31182=AXIS2_PLACEMENT_3D ( 'NONE', #251390, #151023, #88440 ) ;
#31187=DIRECTION ( 'NONE',  ( 0.000000000000000000, -7.147358527629766941E-15, 1.000000000000000000 ) ) ;
#31196=CARTESIAN_POINT ( 'NONE',  ( -20.64999999999999858, 76.00000000001253397, -182.8981074845243597 ) ) ;
#31200=CYLINDRICAL_SURFACE ( 'NONE', #126829, 0.09999999999998898659 ) ;
#31216=CARTESIAN_POINT ( 'NONE',  ( -18.39999999999999858, 85.60000000001241460, -163.4229180933022576 ) ) ;
#31269=DIRECTION ( 'NONE',  ( -0.000000000000000000, 0.1350103645451859180, 0.9908441862701603542 ) ) ;
#31294=CARTESIAN_POINT ( 'NONE',  ( 18.49999999999999289, 64.35000000001275566, -215.2731074845244450 ) ) ;
#31308=DIRECTION ( 'NONE',  ( -0.000000000000000000, 0.1298341882519668811, 0.9915357197604899309 ) ) ;
#31356=DIRECTION ( 'NONE',  ( 0.000000000000000000, -0.9915357197604982575, 0.1298341882519033486 ) ) ;
#31357=VERTEX_POINT ( 'NONE', #220335 ) ;
#31376=LINE ( 'NONE', #67892, #56692 ) ;
#31394=CARTESIAN_POINT ( 'NONE',  ( 21.14999999999999858, 76.00000000001260503, -191.3731074845243540 ) ) ;
#31421=AXIS2_PLACEMENT_3D ( 'NONE', #131427, #210974, #191444 ) ;
#31428=AXIS2_PLACEMENT_3D ( 'NONE', #188739, #33570, #113061 ) ;
#31432=LINE ( 'NONE', #91376, #221416 ) ;
#31439=CARTESIAN_POINT ( 'NONE',  ( 21.05000000000000071, 85.40000000001262492, -193.6291383618718385 ) ) ;
#31453=CARTESIAN_POINT ( 'NONE',  ( -20.94999999999999929, 87.48912529308852015, -173.1231074845242688 ) ) ;
#31489=EDGE_LOOP ( 'NONE', ( #11122, #167824, #195171, #134472, #74835 ) ) ;
#31491=CARTESIAN_POINT ( 'NONE',  ( 21.05000000000000071, 69.52293297888793688, -203.4231074845244223 ) ) ;
#31494=ORIENTED_EDGE ( 'NONE', *, *, #18813, .T. ) ;
#31502=CIRCLE ( 'NONE', #18976, 4.099999999999992539 ) ;
#31527=CARTESIAN_POINT ( 'NONE',  ( 23.24999999999999645, 76.00000000001244871, -170.0231074845243597 ) ) ;
#31552=VECTOR ( 'NONE', #72139, 1000.000000000000114 ) ;
#31577=EDGE_LOOP ( 'NONE', ( #10124, #54533, #177097, #236438 ) ) ;
#31587=ORIENTED_EDGE ( 'NONE', *, *, #79568, .T. ) ;
#31592=CARTESIAN_POINT ( 'NONE',  ( 23.24999999999999289, 80.15000000001268177, -203.5231074845243313 ) ) ;
#31599=LINE ( 'NONE', #108533, #84710 ) ;
#31647=DIRECTION ( 'NONE',  ( -1.000000000000000000, 0.000000000000000000, 0.000000000000000000 ) ) ;
#31657=LINE ( 'NONE', #53753, #62326 ) ;
#31680=DIRECTION ( 'NONE',  ( -0.7071067811865475727, 0.7071067811865475727, 4.937700262164531476E-15 ) ) ;
#31700=EDGE_CURVE ( 'NONE', #54936, #153680, #51947, .T. ) ;
#31738=CARTESIAN_POINT ( 'NONE',  ( 20.94788355080264353, 65.69792220476374212, -164.5335554128461979 ) ) ;
#31742=DIRECTION ( 'NONE',  ( 0.000000000000000000, 6.982962677686266711E-15, -1.000000000000000000 ) ) ;
#31764=CIRCLE ( 'NONE', #177504, 1.900000000000012790 ) ;
#31776=DIRECTION ( 'NONE',  ( 1.000000000000000000, 0.000000000000000000, 0.000000000000000000 ) ) ;
#31886=CIRCLE ( 'NONE', #148582, 0.09999999999998898659 ) ;
#31929=DIRECTION ( 'NONE',  ( -0.000000000000000000, 1.000000000000000000, 7.172728831056617961E-15 ) ) ;
#31972=DIRECTION ( 'NONE',  ( 1.000000000000000000, 0.000000000000000000, 0.000000000000000000 ) ) ;
#31987=CARTESIAN_POINT ( 'NONE',  ( -20.54999999999999716, 85.50000000001261924, -193.6291383618718385 ) ) ;
#32055=CARTESIAN_POINT ( 'NONE',  ( -18.59999999999999787, 74.65925378207906249, -213.7959699899455472 ) ) ;
#32063=AXIS2_PLACEMENT_3D ( 'NONE', #234218, #236783, #78972 ) ;
#32070=DIRECTION ( 'NONE',  ( -0.000000000000000000, 1.000000000000000000, 6.352154140967427193E-15 ) ) ;
#32083=CYLINDRICAL_SURFACE ( 'NONE', #103929, 4.000000000000003553 ) ;
#32107=CIRCLE ( 'NONE', #3024, 11.70000000000001528 ) ;
#32145=LINE ( 'NONE', #251142, #21565 ) ;
#32195=AXIS2_PLACEMENT_3D ( 'NONE', #104687, #66890, #147717 ) ;
#32197=CARTESIAN_POINT ( 'NONE',  ( -20.64999999999999858, 76.00000000001246292, -171.9231074845243938 ) ) ;
#32202=DIRECTION ( 'NONE',  ( 0.000000000000000000, 0.9908441862701420355, 0.1350103645453197554 ) ) ;
#32217=AXIS2_PLACEMENT_3D ( 'NONE', #45088, #224980, #46354 ) ;
#32250=DIRECTION ( 'NONE',  ( 0.000000000000000000, -0.1298341882519953860, -0.9915357197604862671 ) ) ;
#32259=AXIS2_PLACEMENT_3D ( 'NONE', #100634, #1556, #81089 ) ;
#32265=LINE ( 'NONE', #169220, #43869 ) ;
#32278=VECTOR ( 'NONE', #86113, 1000.000000000000000 ) ;
#32289=VERTEX_POINT ( 'NONE', #30196 ) ;
#32326=EDGE_CURVE ( 'NONE', #236840, #166875, #163707, .T. ) ;
#32354=CARTESIAN_POINT ( 'NONE',  ( -21.29999999999995808, 76.00000000001267608, -203.5231074845243597 ) ) ;
#32366=DIRECTION ( 'NONE',  ( 0.000000000000000000, -6.982962677686266711E-15, 1.000000000000000000 ) ) ;
#32371=DIRECTION ( 'NONE',  ( -2.915501640297152804E-16, -1.000000000000000000, -6.997203936713167125E-15 ) ) ;
#32372=CARTESIAN_POINT ( 'NONE',  ( -20.64999999999999858, 84.66355140188167638, -179.5472086025916099 ) ) ;
#32373=ADVANCED_FACE ( 'NONE', ( #173595 ), #198728, .T. ) ;
#32383=ORIENTED_EDGE ( 'NONE', *, *, #181833, .T. ) ;
#32390=ORIENTED_EDGE ( 'NONE', *, *, #158407, .T. ) ;
#32403=AXIS2_PLACEMENT_3D ( 'NONE', #167408, #147832, #9583 ) ;
#32411=DIRECTION ( 'NONE',  ( -0.000000000000000000, 1.000000000000000000, 6.982962677686267499E-15 ) ) ;
#32434=VERTEX_POINT ( 'NONE', #161698 ) ;
#32445=VECTOR ( 'NONE', #102358, 1000.000000000000000 ) ;
#32452=CARTESIAN_POINT ( 'NONE',  ( 20.94999999999999929, 85.50000000001251976, -179.9170766071767389 ) ) ;
#32476=AXIS2_PLACEMENT_3D ( 'NONE', #136807, #115986, #235904 ) ;
#32487=ADVANCED_FACE ( 'NONE', ( #139531 ), #182543, .F. ) ;
#32504=CARTESIAN_POINT ( 'NONE',  ( 20.94999999999999929, 76.00000000001242029, -166.0231074845243597 ) ) ;
#32519=DIRECTION ( 'NONE',  ( -1.000000000000000000, -0.000000000000000000, -0.000000000000000000 ) ) ;
#32532=CARTESIAN_POINT ( 'NONE',  ( 20.94999999999999929, 87.65000000001246860, -173.0231074845243029 ) ) ;
#32533=ORIENTED_EDGE ( 'NONE', *, *, #19645, .F. ) ;
#32552=VERTEX_POINT ( 'NONE', #62582 ) ;
#32560=DIRECTION ( 'NONE',  ( 0.000000000000000000, -0.1350103645451807555, -0.9908441862701610203 ) ) ;
#32565=ORIENTED_EDGE ( 'NONE', *, *, #12507, .T. ) ;
#32573=ORIENTED_EDGE ( 'NONE', *, *, #65028, .F. ) ;
#32590=EDGE_CURVE ( 'NONE', #207953, #225579, #205930, .T. ) ;
#32602=EDGE_LOOP ( 'NONE', ( #185301, #256011, #71061 ) ) ;
#32611=CIRCLE ( 'NONE', #65880, 0.1000000000000043771 ) ;
#32616=ORIENTED_EDGE ( 'NONE', *, *, #134121, .F. ) ;
#32630=CIRCLE ( 'NONE', #153435, 0.1000000000000011990 ) ;
#32686=DIRECTION ( 'NONE',  ( 0.7071067811865487940, 4.851104656540973741E-15, -0.7071067811865463515 ) ) ;
#32692=FACE_OUTER_BOUND ( 'NONE', #45627, .T. ) ;
#32713=DIRECTION ( 'NONE',  ( 0.000000000000000000, -6.982962677686266711E-15, 1.000000000000000000 ) ) ;
#32723=LINE ( 'NONE', #170960, #77503 ) ;
#32731=DIRECTION ( 'NONE',  ( 1.000000000000000000, 0.000000000000000000, 0.000000000000000000 ) ) ;
#32787=VECTOR ( 'NONE', #139576, 1000.000000000000000 ) ;
#32825=CARTESIAN_POINT ( 'NONE',  ( 20.95392731769792150, 67.11693852082386513, -195.0008795049531329 ) ) ;
#32857=ORIENTED_EDGE ( 'NONE', *, *, #251332, .T. ) ;
#32864=DIRECTION ( 'NONE',  ( 0.000000000000000000, 0.9999631594459055250, 0.008583690987131395445 ) ) ;
#32866=AXIS2_PLACEMENT_3D ( 'NONE', #249782, #234058, #248499 ) ;
#32914=ORIENTED_EDGE ( 'NONE', *, *, #152628, .T. ) ;
#32940=EDGE_LOOP ( 'NONE', ( #109812, #219955, #168064, #144695 ) ) ;
#32952=EDGE_CURVE ( 'NONE', #230341, #93986, #218747, .T. ) ;
#32956=VECTOR ( 'NONE', #209898, 1000.000000000000000 ) ;
#32978=DIRECTION ( 'NONE',  ( 1.000000000000000000, 0.000000000000000000, 0.000000000000000000 ) ) ;
#33043=SPHERICAL_SURFACE ( 'NONE', #227249, 0.1000000000000000056 ) ;
#33070=ADVANCED_FACE ( 'NONE', ( #11278 ), #19398, .T. ) ;
#33102=LINE ( 'NONE', #89164, #252146 ) ;
#33103=AXIS2_PLACEMENT_3D ( 'NONE', #124747, #107737, #225094 ) ;
#33109=CARTESIAN_POINT ( 'NONE',  ( 18.59999999999999076, 65.50857864377520912, -178.6731074845244223 ) ) ;
#33128=DIRECTION ( 'NONE',  ( -0.000000000000000000, -0.1350103645451807555, -0.9908441862701610203 ) ) ;
#33142=AXIS2_PLACEMENT_3D ( 'NONE', #164231, #28614, #123816 ) ;
#33143=CARTESIAN_POINT ( 'NONE',  ( -20.54999999999999716, 85.00000000001251976, -179.9170766071767389 ) ) ;
#33149=FACE_OUTER_BOUND ( 'NONE', #143166, .T. ) ;
#33183=DIRECTION ( 'NONE',  ( -1.000000000000000000, 0.000000000000000000, -0.000000000000000000 ) ) ;
#33197=LINE ( 'NONE', #90544, #134611 ) ;
#33210=ORIENTED_EDGE ( 'NONE', *, *, #222456, .F. ) ;
#33229=AXIS2_PLACEMENT_3D ( 'NONE', #49209, #85731, #166632 ) ;
#33252=EDGE_CURVE ( 'NONE', #257328, #111659, #11009, .T. ) ;
#33273=CARTESIAN_POINT ( 'NONE',  ( -18.46154800491006043, 85.48020627425442797, -163.3656566461428383 ) ) ;
#33308=DIRECTION ( 'NONE',  ( -1.000000000000000000, 0.000000000000000000, -0.000000000000000000 ) ) ;
#33340=DIRECTION ( 'NONE',  ( -3.265361837132813093E-16, -1.000000000000000000, 7.445645354460596589E-46 ) ) ;
#33341=CARTESIAN_POINT ( 'NONE',  ( -20.00857864376270001, 66.85000000001254250, -182.2731074845244166 ) ) ;
#33405=EDGE_CURVE ( 'NONE', #98885, #109697, #31886, .T. ) ;
#33433=EDGE_LOOP ( 'NONE', ( #154399, #93332, #201403, #78768 ) ) ;
#33434=AXIS2_PLACEMENT_3D ( 'NONE', #36104, #214718, #215989 ) ;
#33443=DIRECTION ( 'NONE',  ( -1.000000000000000000, 0.000000000000000000, 0.000000000000000000 ) ) ;
#33446=DIRECTION ( 'NONE',  ( 1.000000000000000000, -0.000000000000000000, 0.000000000000000000 ) ) ;
#33455=AXIS2_PLACEMENT_3D ( 'NONE', #78454, #138411, #158056 ) ;
#33463=( BOUNDED_SURFACE ( )  B_SPLINE_SURFACE ( 3, 2, ( 
 ( #217529, #38927, #80574 ),
 ( #19354, #118469, #20653 ),
 ( #79301, #59730, #160174 ),
 ( #139270, #239686, #220122 ),
 ( #41501, #121050, #200551 ),
 ( #22017, #101491, #41593 ) ),
 .UNSPECIFIED., .F., .F., .F. ) 
 B_SPLINE_SURFACE_WITH_KNOTS ( ( 4, 2, 4 ),
 ( 3, 3 ),
 ( 1.570796326794897668, 2.356194490192346169, 3.141592653589794448 ),
 ( 0.000000000000000000, 1.000000000000000000 ),
 .UNSPECIFIED. ) 
 GEOMETRIC_REPRESENTATION_ITEM ( )  RATIONAL_B_SPLINE_SURFACE ( (
 ( 1.000000000000000000, 0.7071067811865597852, 1.000000000000000000),
 ( 1.000000000000000000, 0.6611148371781052635, 1.000000000000000000),
 ( 1.000000000000000000, 0.6092287576693442563, 1.000000000000000000),
 ( 1.000000000000000000, 0.5278258667060597986, 1.000000000000000000),
 ( 1.000000000000000000, 0.4993418825334668965, 1.000000000000000000),
 ( 1.000000000000000000, 0.5000000000000456302, 1.000000000000000000) ) ) 
 REPRESENTATION_ITEM ( '' )  SURFACE ( )  );
#33468=DIRECTION ( 'NONE',  ( 0.000000000000000000, 0.000000000000000000, 1.000000000000000000 ) ) ;
#33492=CARTESIAN_POINT ( 'NONE',  ( -23.25000000000000000, 69.01799029515598249, -166.3269553662681233 ) ) ;
#33514=ORIENTED_EDGE ( 'NONE', *, *, #27407, .T. ) ;
#33526=ORIENTED_EDGE ( 'NONE', *, *, #54896, .T. ) ;
#33542=CYLINDRICAL_SURFACE ( 'NONE', #207637, 0.1000000000000106914 ) ;
#33555=EDGE_LOOP ( 'NONE', ( #2272, #233683, #44635, #34892, #150179, #120852, #193278, #174353, #4013, #136700, #90405 ) ) ;
#33557=LINE ( 'NONE', #10093, #201910 ) ;
#33564=VERTEX_POINT ( 'NONE', #198269 ) ;
#33570=DIRECTION ( 'NONE',  ( -0.000000000000000000, -6.982962677686266711E-15, 1.000000000000000000 ) ) ;
#33576=ORIENTED_EDGE ( 'NONE', *, *, #213842, .F. ) ;
#33582=ORIENTED_EDGE ( 'NONE', *, *, #111931, .T. ) ;
#33589=CARTESIAN_POINT ( 'NONE',  ( 20.94999999999999929, 87.48912529308852015, -173.1231074845242688 ) ) ;
#33617=AXIS2_PLACEMENT_3D ( 'NONE', #231720, #73947, #93463 ) ;
#33645=DIRECTION ( 'NONE',  ( 1.000000000000000000, 0.000000000000000000, 0.000000000000000000 ) ) ;
#33694=CARTESIAN_POINT ( 'NONE',  ( 21.05000000000000071, 70.50000000001253397, -182.4283735034374843 ) ) ;
#33721=DIRECTION ( 'NONE',  ( 0.000000000000000000, -7.124650136758317602E-15, 1.000000000000000000 ) ) ;
#33747=AXIS2_PLACEMENT_3D ( 'NONE', #248709, #32250, #34823 ) ;
#33761=EDGE_CURVE ( 'NONE', #178394, #94509, #156968, .T. ) ;
#33797=CARTESIAN_POINT ( 'NONE',  ( 18.49999999999999645, 74.36282728704222222, -191.9409541190523498 ) ) ;
#33798=CIRCLE ( 'NONE', #246135, 0.9750000000000036415 ) ;
#33817=CYLINDRICAL_SURFACE ( 'NONE', #130162, 0.09999999999998898659 ) ;
#33838=ORIENTED_EDGE ( 'NONE', *, *, #115932, .T. ) ;
#33876=ORIENTED_EDGE ( 'NONE', *, *, #141858, .T. ) ;
#33895=DIRECTION ( 'NONE',  ( 1.000000000000000000, 0.000000000000000000, 0.000000000000000000 ) ) ;
#33905=DIRECTION ( 'NONE',  ( -1.000000000000000000, 0.000000000000000000, 0.000000000000000000 ) ) ;
#33906=VERTEX_POINT ( 'NONE', #216227 ) ;
#33909=ADVANCED_FACE ( 'NONE', ( #177147 ), #15697, .T. ) ;
#33938=DIRECTION ( 'NONE',  ( 0.000000000000000000, 0.8660254037844377084, 0.5000000000000016653 ) ) ;
#33945=CARTESIAN_POINT ( 'NONE',  ( 22.47007471830798053, 76.00000000001274714, -211.2438181364508125 ) ) ;
#33978=VECTOR ( 'NONE', #227248, 1000.000000000000000 ) ;
#34005=CARTESIAN_POINT ( 'NONE',  ( -20.05000000000000426, 66.75000000001253397, -182.3731074845244393 ) ) ;
#34018=CARTESIAN_POINT ( 'NONE',  ( -18.59999999999999787, 64.35000000001276987, -215.2731074845244450 ) ) ;
#34022=ORIENTED_EDGE ( 'NONE', *, *, #87534, .T. ) ;
#34045=FACE_OUTER_BOUND ( 'NONE', #115222, .T. ) ;
#34054=DIRECTION ( 'NONE',  ( 0.000000000000000000, 1.000000000000000000, -1.387778780781444413E-14 ) ) ;
#34072=DIRECTION ( 'NONE',  ( 0.000000000000000000, -0.1495327102803283015, 0.9887567792719397231 ) ) ;
#34083=CARTESIAN_POINT ( 'NONE',  ( 21.93642651522410603, 68.67283376068688483, -203.5231074845243882 ) ) ;
#34160=CARTESIAN_POINT ( 'NONE',  ( 18.49999999999999645, 77.13501884592258762, -162.3061306010920362 ) ) ;
#34163=ADVANCED_FACE ( 'NONE', ( #148254 ), #67432, .T. ) ;
#34176=VERTEX_POINT ( 'NONE', #184810 ) ;
#34226=DIRECTION ( 'NONE',  ( 1.000000000000000000, 0.000000000000000000, 0.000000000000000000 ) ) ;
#34238=FACE_OUTER_BOUND ( 'NONE', #115216, .T. ) ;
#34247=CARTESIAN_POINT ( 'NONE',  ( 20.94999999999999929, 71.00000000001253397, -182.0283735034374786 ) ) ;
#34261=EDGE_LOOP ( 'NONE', ( #210170, #139281, #26530, #167511 ) ) ;
#34288=VERTEX_POINT ( 'NONE', #94689 ) ;
#34294=CARTESIAN_POINT ( 'NONE',  ( -18.59999999999999787, 77.83585931145600512, -158.5186683157258187 ) ) ;
#34300=CARTESIAN_POINT ( 'NONE',  ( 20.94999027547553894, 65.70673848567030007, -164.5638252334829588 ) ) ;
#34313=CARTESIAN_POINT ( 'NONE',  ( 20.95203847575071521, 65.49893946073862594, -195.9560361359008880 ) ) ;
#34326=EDGE_LOOP ( 'NONE', ( #78261, #161775, #98611, #172075 ) ) ;
#34330=CIRCLE ( 'NONE', #134236, 0.09999999999998898659 ) ;
#34368=AXIS2_PLACEMENT_3D ( 'NONE', #213962, #35364, #36641 ) ;
#34418=EDGE_CURVE ( 'NONE', #94115, #173853, #158546, .T. ) ;
#34420=DIRECTION ( 'NONE',  ( -1.000000000000000000, 2.952720810173289112E-16, 2.061873921506763405E-30 ) ) ;
#34449=EDGE_CURVE ( 'NONE', #256108, #138529, #249098, .T. ) ;
#34457=CARTESIAN_POINT ( 'NONE',  ( -23.25000000000000000, 76.00000000001242029, -166.1231074845243825 ) ) ;
#34471=VERTEX_POINT ( 'NONE', #137240 ) ;
#34479=EDGE_CURVE ( 'NONE', #105902, #91470, #203287, .T. ) ;
#34526=ORIENTED_EDGE ( 'NONE', *, *, #237213, .F. ) ;
#34607=DIRECTION ( 'NONE',  ( 0.000000000000000000, 6.982962677686267499E-15, -1.000000000000000000 ) ) ;
#34615=DIRECTION ( 'NONE',  ( 0.000000000000000000, -0.9908441862701791170, 0.1350103645450472789 ) ) ;
#34669=DIRECTION ( 'NONE',  ( 0.000000000000000000, 0.000000000000000000, 1.000000000000000000 ) ) ;
#34697=DIRECTION ( 'NONE',  ( 0.000000000000000000, 0.000000000000000000, 1.000000000000000000 ) ) ;
#34746=AXIS2_PLACEMENT_3D ( 'NONE', #203659, #122852, #5426 ) ;
#34758=LINE ( 'NONE', #217195, #47006 ) ;
#34770=DIRECTION ( 'NONE',  ( 6.938893903907991995E-14, 0.000000000000000000, -1.000000000000000000 ) ) ;
#34777=VERTEX_POINT ( 'NONE', #60737 ) ;
#34788=ADVANCED_FACE ( 'NONE', ( #89295 ), #50167, .F. ) ;
#34823=DIRECTION ( 'NONE',  ( 0.000000000000000000, 0.9915357197604982575, -0.1298341882519033486 ) ) ;
#34855=AXIS2_PLACEMENT_3D ( 'NONE', #209758, #165507, #67670 ) ;
#34859=VECTOR ( 'NONE', #202261, 999.9999999999998863 ) ;
#34871=ORIENTED_EDGE ( 'NONE', *, *, #198640, .T. ) ;
#34872=AXIS2_PLACEMENT_3D ( 'NONE', #238982, #236401, #95604 ) ;
#34892=ORIENTED_EDGE ( 'NONE', *, *, #93102, .T. ) ;
#34911=CIRCLE ( 'NONE', #47314, 0.4000000000000114575 ) ;
#34926=AXIS2_PLACEMENT_3D ( 'NONE', #1226, #58634, #258089 ) ;
#34935=CARTESIAN_POINT ( 'NONE',  ( 23.24999999999999289, 64.25000000001276135, -215.2731074845244450 ) ) ;
#34938=LINE ( 'NONE', #193994, #7220 ) ;
#34969=EDGE_CURVE ( 'NONE', #225579, #133625, #95326, .T. ) ;
#34989=CARTESIAN_POINT ( 'NONE',  ( -20.64999999999999858, 71.65000000001253966, -182.3731074845244109 ) ) ;
#35000=ORIENTED_EDGE ( 'NONE', *, *, #116149, .T. ) ;
#35020=DIRECTION ( 'NONE',  ( 0.000000000000000000, -6.982962677686266711E-15, 1.000000000000000000 ) ) ;
#35021=CARTESIAN_POINT ( 'NONE',  ( 23.14999999999999503, 69.55000000001253113, -182.3731074845244109 ) ) ;
#35023=CARTESIAN_POINT ( 'NONE',  ( -20.64999999999999858, 68.85000000001254250, -182.3731074845244109 ) ) ;
#35044=ORIENTED_EDGE ( 'NONE', *, *, #105332, .T. ) ;
#35048=CIRCLE ( 'NONE', #214071, 12.87499999999999822 ) ;
#35050=ORIENTED_EDGE ( 'NONE', *, *, #50551, .F. ) ;
#35097=EDGE_LOOP ( 'NONE', ( #238559, #201560, #187964, #154782 ) ) ;
#35110=LINE ( 'NONE', #1039, #176516 ) ;
#35137=AXIS2_PLACEMENT_3D ( 'NONE', #199046, #38692, #154812 ) ;
#35151=AXIS2_PLACEMENT_3D ( 'NONE', #51711, #210815, #32202 ) ;
#35163=PLANE ( 'NONE',  #94748 ) ;
#35165=PLANE ( 'NONE',  #157463 ) ;
#35169=ORIENTED_EDGE ( 'NONE', *, *, #146283, .F. ) ;
#35177=AXIS2_PLACEMENT_3D ( 'NONE', #36705, #32864, #254406 ) ;
#35182=ORIENTED_EDGE ( 'NONE', *, *, #73976, .T. ) ;
#35186=VERTEX_POINT ( 'NONE', #129415 ) ;
#35187=CARTESIAN_POINT ( 'NONE',  ( 21.14999999999999503, 76.10085836911147794, -215.2726746080137445 ) ) ;
#35193=EDGE_CURVE ( 'NONE', #20407, #254122, #211849, .T. ) ;
#35227=CARTESIAN_POINT ( 'NONE',  ( -20.85000000000000142, 76.00000000001244871, -170.0231074845243597 ) ) ;
#35236=CARTESIAN_POINT ( 'NONE',  ( -22.50000000000000000, 64.25000000001269029, -203.5231074845244166 ) ) ;
#35314=TOROIDAL_SURFACE ( 'NONE', #214330, 12.77499999999999858, 0.1000000000000000056 ) ;
#35318=LINE ( 'NONE', #198197, #72249 ) ;
#35324=DIRECTION ( 'NONE',  ( 1.000000000000000000, 0.000000000000000000, 0.000000000000000000 ) ) ;
#35342=ORIENTED_EDGE ( 'NONE', *, *, #220646, .T. ) ;
#35355=CARTESIAN_POINT ( 'NONE',  ( -20.94999999999999929, 77.36242903720570041, -162.1342262366031548 ) ) ;
#35364=DIRECTION ( 'NONE',  ( 1.000000000000000000, 0.000000000000000000, 0.000000000000000000 ) ) ;
#35391=DIRECTION ( 'NONE',  ( 0.000000000000000000, -1.000000000000000000, -8.717686153663073805E-15 ) ) ;
#35403=ORIENTED_EDGE ( 'NONE', *, *, #144346, .F. ) ;
#35422=FACE_OUTER_BOUND ( 'NONE', #115682, .T. ) ;
#35440=EDGE_CURVE ( 'NONE', #22816, #72890, #124732, .T. ) ;
#35448=TOROIDAL_SURFACE ( 'NONE', #135344, 0.2000000000000000111, 0.1000000000000000056 ) ;
#35451=CIRCLE ( 'NONE', #176898, 2.099999999999990763 ) ;
#35529=CARTESIAN_POINT ( 'NONE',  ( 23.14999999999999858, 70.50000000001253397, -182.4283735034374843 ) ) ;
#35550=ORIENTED_EDGE ( 'NONE', *, *, #6986, .F. ) ;
#35618=EDGE_CURVE ( 'NONE', #96501, #214102, #95497, .T. ) ;
#35635=CARTESIAN_POINT ( 'NONE',  ( 20.94999999999999929, 71.14953271029291670, -182.0573748935260880 ) ) ;
#35647=CARTESIAN_POINT ( 'NONE',  ( 18.39999999999999858, 85.50000000001263345, -196.4910380878246201 ) ) ;
#35669=CARTESIAN_POINT ( 'NONE',  ( 20.94999999999999929, 64.35000000001249987, -176.8069731475025321 ) ) ;
#35670=CARTESIAN_POINT ( 'NONE',  ( -23.25000000000000000, 77.14957036958807635, -162.2071950000224092 ) ) ;
#35690=CIRCLE ( 'NONE', #181426, 0.09999999999998898659 ) ;
#35694=ORIENTED_EDGE ( 'NONE', *, *, #48694, .F. ) ;
#35701=VERTEX_POINT ( 'NONE', #152233 ) ;
#35702=ADVANCED_FACE ( 'NONE', ( #231754 ), #209611, .T. ) ;
#35727=DIRECTION ( 'NONE',  ( -1.000000000000000000, 0.000000000000000000, 0.000000000000000000 ) ) ;
#35728=EDGE_CURVE ( 'NONE', #207133, #136223, #154003, .T. ) ;
#35732=ORIENTED_EDGE ( 'NONE', *, *, #189787, .F. ) ;
#35770=CARTESIAN_POINT ( 'NONE',  ( -20.94999999999999929, 69.15387683765983695, -166.2853812176745691 ) ) ;
#35782=CARTESIAN_POINT ( 'NONE',  ( 23.14999999999999147, 71.85000000001268461, -203.5231074845243597 ) ) ;
#35799=CIRCLE ( 'NONE', #181559, 0.09999999999998898659 ) ;
#35812=ORIENTED_EDGE ( 'NONE', *, *, #54698, .F. ) ;
#35816=DIRECTION ( 'NONE',  ( -1.000000000000000000, 2.952720810173289112E-16, 2.061873921506763405E-30 ) ) ;
#35855=AXIS2_PLACEMENT_3D ( 'NONE', #56280, #155442, #39330 ) ;
#35862=DIRECTION ( 'NONE',  ( 1.000000000000000000, -2.952720810173289112E-16, -2.061873921506763405E-30 ) ) ;
#35880=AXIS2_PLACEMENT_3D ( 'NONE', #244593, #215099, #116017 ) ;
#35919=EDGE_CURVE ( 'NONE', #122787, #28569, #27609, .T. ) ;
#35929=DIRECTION ( 'NONE',  ( 2.952720810173289112E-16, 1.000000000000000000, 6.938893903907229955E-15 ) ) ;
#35973=DIRECTION ( 'NONE',  ( 0.000000000000000000, 1.000000000000000000, 0.000000000000000000 ) ) ;
#35975=DIRECTION ( 'NONE',  ( 0.000000000000000000, -1.000000000000000000, -6.982962677686265922E-15 ) ) ;
#35987=DIRECTION ( 'NONE',  ( -1.000000000000000000, 2.952720810173289112E-16, 2.061873921506763405E-30 ) ) ;
#35993=ORIENTED_EDGE ( 'NONE', *, *, #244867, .T. ) ;
#36005=DIRECTION ( 'NONE',  ( -0.000000000000000000, 0.8660254037844377084, 0.5000000000000016653 ) ) ;
#36017=EDGE_CURVE ( 'NONE', #6205, #19640, #170759, .T. ) ;
#36025=ORIENTED_EDGE ( 'NONE', *, *, #212615, .T. ) ;
#36042=EDGE_LOOP ( 'NONE', ( #232531, #156046, #204730, #116255 ) ) ;
#36049=VERTEX_POINT ( 'NONE', #148047 ) ;
#36104=CARTESIAN_POINT ( 'NONE',  ( -21.14999999999999858, 64.25000000001269029, -203.4231074845244507 ) ) ;
#36110=ORIENTED_EDGE ( 'NONE', *, *, #102974, .F. ) ;
#36111=CARTESIAN_POINT ( 'NONE',  ( -20.64999999999999858, 74.00000000001259082, -190.2984855617622770 ) ) ;
#36188=EDGE_CURVE ( 'NONE', #92906, #170452, #77459, .T. ) ;
#36195=VERTEX_POINT ( 'NONE', #214420 ) ;
#36201=EDGE_CURVE ( 'NONE', #120584, #137554, #107762, .T. ) ;
#36204=FACE_OUTER_BOUND ( 'NONE', #221042, .T. ) ;
#36274=AXIS2_PLACEMENT_3D ( 'NONE', #193333, #72106, #113776 ) ;
#36278=ORIENTED_EDGE ( 'NONE', *, *, #208715, .T. ) ;
#36280=ORIENTED_EDGE ( 'NONE', *, *, #40743, .F. ) ;
#36329=CARTESIAN_POINT ( 'NONE',  ( -21.53551880898957904, 75.90103026544106513, -210.3079052459406739 ) ) ;
#36373=ADVANCED_FACE ( 'NONE', ( #190750 ), #9501, .F. ) ;
#36378=CARTESIAN_POINT ( 'NONE',  ( -21.05000000000000071, 87.39257802171813694, -173.0970570643562212 ) ) ;
#36422=ORIENTED_EDGE ( 'NONE', *, *, #96457, .T. ) ;
#36431=ORIENTED_EDGE ( 'NONE', *, *, #110004, .T. ) ;
#36436=CARTESIAN_POINT ( 'NONE',  ( -22.60000000000080789, 75.95218301954739104, -215.2731299156771172 ) ) ;
#36441=DIRECTION ( 'NONE',  ( 0.000000000000000000, 0.000000000000000000, 1.000000000000000000 ) ) ;
#36460=EDGE_CURVE ( 'NONE', #161032, #136223, #151623, .T. ) ;
#36477=CARTESIAN_POINT ( 'NONE',  ( -23.25000000000000000, 70.05000000001251692, -180.3288097895592159 ) ) ;
#36482=VERTEX_POINT ( 'NONE', #188155 ) ;
#36501=AXIS2_PLACEMENT_3D ( 'NONE', #183106, #224770, #163529 ) ;
#36507=CARTESIAN_POINT ( 'NONE',  ( -22.39999999999999858, 75.90000000001273861, -211.3138870828977645 ) ) ;
#36512=CARTESIAN_POINT ( 'NONE',  ( 21.09316766718127667, 69.62984668753827577, -203.5623708868390906 ) ) ;
#36524=ORIENTED_EDGE ( 'NONE', *, *, #83752, .T. ) ;
#36535=ADVANCED_FACE ( 'NONE', ( #94172 ), #12124, .F. ) ;
#36548=AXIS2_PLACEMENT_3D ( 'NONE', #136693, #76721, #251512 ) ;
#36568=CARTESIAN_POINT ( 'NONE',  ( -21.05000000000000071, 76.00000000001264766, -199.2231074845243768 ) ) ;
#36569=FACE_OUTER_BOUND ( 'NONE', #237870, .T. ) ;
#36572=CIRCLE ( 'NONE', #182289, 11.64999999999999325 ) ;
#36583=DIRECTION ( 'NONE',  ( 1.000000000000000000, -3.265361837132813093E-16, -2.280189983783949500E-30 ) ) ;
#36629=CARTESIAN_POINT ( 'NONE',  ( -21.06715728752538652, 64.25000000001264766, -196.5083017138704236 ) ) ;
#36641=DIRECTION ( 'NONE',  ( 0.000000000000000000, -6.454785026890489601E-15, 1.000000000000000000 ) ) ;
#36649=CYLINDRICAL_SURFACE ( 'NONE', #137875, 0.09999999999999939493 ) ;
#36658=ORIENTED_EDGE ( 'NONE', *, *, #92096, .T. ) ;
#36665=CARTESIAN_POINT ( 'NONE',  ( 20.94999999999999574, 77.73625713161000306, -191.9544551555068495 ) ) ;
#36667=FACE_OUTER_BOUND ( 'NONE', #54574, .T. ) ;
#36672=FACE_OUTER_BOUND ( 'NONE', #137804, .T. ) ;
#36698=VECTOR ( 'NONE', #61541, 1000.000000000000000 ) ;
#36702=DIRECTION ( 'NONE',  ( 0.000000000000000000, 0.8700118002898357128, -0.4930308989875170633 ) ) ;
#36705=CARTESIAN_POINT ( 'NONE',  ( -21.14999999999999858, 76.10000000001276987, -215.1726782920691505 ) ) ;
#36711=CARTESIAN_POINT ( 'NONE',  ( 20.85000000000000142, 69.15387683765983695, -166.2853812176745691 ) ) ;
#36714=ADVANCED_FACE ( 'NONE', ( #142294 ), #143586, .T. ) ;
#36750=LINE ( 'NONE', #139639, #81656 ) ;
#36771=ORIENTED_EDGE ( 'NONE', *, *, #54896, .F. ) ;
#36815=DIRECTION ( 'NONE',  ( 0.000000000000000000, 0.000000000000000000, 1.000000000000000000 ) ) ;
#36852=DIRECTION ( 'NONE',  ( 1.000000000000000000, 0.000000000000000000, 0.000000000000000000 ) ) ;
#36853=ORIENTED_EDGE ( 'NONE', *, *, #146853, .F. ) ;
#36857=ORIENTED_EDGE ( 'NONE', *, *, #252022, .F. ) ;
#36859=DIRECTION ( 'NONE',  ( 0.000000000000000000, 7.116814260417676401E-15, -1.000000000000000000 ) ) ;
#36930=CARTESIAN_POINT ( 'NONE',  ( -1.820710678118658388, 85.92928932189384739, -178.8731074845242972 ) ) ;
#36965=PLANE ( 'NONE',  #194570 ) ;
#36987=EDGE_CURVE ( 'NONE', #138354, #110167, #166434, .T. ) ;
#36996=ORIENTED_EDGE ( 'NONE', *, *, #53096, .F. ) ;
#37002=DIRECTION ( 'NONE',  ( -1.000000000000000000, 0.000000000000000000, 0.000000000000000000 ) ) ;
#37011=DIRECTION ( 'NONE',  ( 0.000000000000000000, -1.000000000000000000, -8.717686153663073805E-15 ) ) ;
#37019=DIRECTION ( 'NONE',  ( 0.000000000000000000, 0.1568667991644355497, 0.9876197685951332295 ) ) ;
#37025=ORIENTED_EDGE ( 'NONE', *, *, #38621, .T. ) ;
#37036=EDGE_CURVE ( 'NONE', #611, #203688, #56007, .T. ) ;
#37088=DIRECTION ( 'NONE',  ( 0.000000000000000000, -1.000000000000000000, -6.982962677686265922E-15 ) ) ;
#37105=CARTESIAN_POINT ( 'NONE',  ( 20.94999999999999929, 64.35000000001245724, -170.0231074845244166 ) ) ;
#37110=CARTESIAN_POINT ( 'NONE',  ( -18.46919391072059113, 85.67072438829022474, -163.3493039527248811 ) ) ;
#37113=AXIS2_PLACEMENT_3D ( 'NONE', #240421, #177891, #117892 ) ;
#37153=DIRECTION ( 'NONE',  ( 1.000000000000000000, 0.000000000000000000, 0.000000000000000000 ) ) ;
#37172=DIRECTION ( 'NONE',  ( -1.000000000000000000, 7.304098846218134667E-16, 5.100424963727256530E-30 ) ) ;
#37197=ADVANCED_FACE ( 'NONE', ( #149726 ), #227953, .T. ) ;
#37201=ORIENTED_EDGE ( 'NONE', *, *, #250051, .T. ) ;
#37205=CIRCLE ( 'NONE', #182955, 0.09999999999998898659 ) ;
#37212=PLANE ( 'NONE',  #228864 ) ;
#37214=VERTEX_POINT ( 'NONE', #66316 ) ;
#37215=CARTESIAN_POINT ( 'NONE',  ( 18.59999999999999432, 74.73821383144760944, -195.4366085209788935 ) ) ;
#37221=ORIENTED_EDGE ( 'NONE', *, *, #150995, .T. ) ;
#37240=ADVANCED_FACE ( 'NONE', ( #229248 ), #127571, .F. ) ;
#37259=CARTESIAN_POINT ( 'NONE',  ( 20.85000000000000142, 76.00000000001244871, -170.0231074845243597 ) ) ;
#37265=ORIENTED_EDGE ( 'NONE', *, *, #150565, .T. ) ;
#37313=FACE_OUTER_BOUND ( 'NONE', #42554, .T. ) ;
#37318=CARTESIAN_POINT ( 'NONE',  ( -20.54999999999999716, 74.00000000001259082, -190.2984855617622770 ) ) ;
#37346=CIRCLE ( 'NONE', #183089, 0.1000000000000028644 ) ;
#37374=EDGE_LOOP ( 'NONE', ( #15558, #149906, #150509, #127558 ) ) ;
#37385=ORIENTED_EDGE ( 'NONE', *, *, #207847, .F. ) ;
#37429=ORIENTED_EDGE ( 'NONE', *, *, #88801, .F. ) ;
#37432=VECTOR ( 'NONE', #105713, 1000.000000000000000 ) ;
#37447=VERTEX_POINT ( 'NONE', #136188 ) ;
#37460=ORIENTED_EDGE ( 'NONE', *, *, #180929, .F. ) ;
#37473=CARTESIAN_POINT ( 'NONE',  ( -21.05000000000000071, 61.95000000001265050, -198.0094124137634708 ) ) ;
#37507=CARTESIAN_POINT ( 'NONE',  ( 23.15000000000000213, 85.60000000001251408, -179.9170766071767389 ) ) ;
#37521=CARTESIAN_POINT ( 'NONE',  ( -20.94999999999999929, 77.73625713161000306, -191.9544551555068495 ) ) ;
#37528=DIRECTION ( 'NONE',  ( 0.000000000000000000, -1.000000000000000000, -6.982962677686265922E-15 ) ) ;
#37577=DIRECTION ( 'NONE',  ( 1.000000000000000000, 0.000000000000000000, 0.000000000000000000 ) ) ;
#37611=PLANE ( 'NONE',  #229852 ) ;
#37617=CARTESIAN_POINT ( 'NONE',  ( -22.49544290803757107, 64.25012976215539595, -203.5884194437828114 ) ) ;
#37631=VERTEX_POINT ( 'NONE', #108652 ) ;
#37654=CIRCLE ( 'NONE', #245929, 4.000000000000003553 ) ;
#37669=DIRECTION ( 'NONE',  ( 0.000000000000000000, 6.982962677686266711E-15, -1.000000000000000000 ) ) ;
#37677=CARTESIAN_POINT ( 'NONE',  ( -21.05000000000000071, 77.25000000001263345, -195.5231074845243313 ) ) ;
#37679=CIRCLE ( 'NONE', #125156, 0.09999999999998898659 ) ;
#37699=ORIENTED_EDGE ( 'NONE', *, *, #209753, .F. ) ;
#37719=VERTEX_POINT ( 'NONE', #113783 ) ;
#37765=AXIS2_PLACEMENT_3D ( 'NONE', #59548, #4725, #127267 ) ;
#37768=CARTESIAN_POINT ( 'NONE',  ( 22.39999999999999503, 76.00000000001273293, -211.3138870828977360 ) ) ;
#37782=CARTESIAN_POINT ( 'NONE',  ( -18.50000000000000000, 74.83729825007462466, -195.4231074845243654 ) ) ;
#37787=CARTESIAN_POINT ( 'NONE',  ( 21.30000000000002558, 76.00000000001264766, -199.4731074845243484 ) ) ;
#37788=CARTESIAN_POINT ( 'NONE',  ( 21.09813707148777340, 69.61493789427618140, -203.5544589840539231 ) ) ;
#37820=CARTESIAN_POINT ( 'NONE',  ( 21.30000000000002558, 76.00000000001270450, -207.5731074845243427 ) ) ;
#37842=DIRECTION ( 'NONE',  ( 0.000000000000000000, -1.000000000000000000, -7.272083257015735086E-15 ) ) ;
#37846=CARTESIAN_POINT ( 'NONE',  ( -18.59999999999999787, 69.01799029515598249, -166.3269553662681233 ) ) ;
#37901=CARTESIAN_POINT ( 'NONE',  ( 22.48660254037844197, 64.35000000001267040, -203.5731074845244564 ) ) ;
#37919=CARTESIAN_POINT ( 'NONE',  ( 21.14999999999999858, 69.45934304831143891, -203.5231074845243882 ) ) ;
#37923=ADVANCED_FACE ( 'NONE', ( #105749 ), #202312, .F. ) ;
#37941=CARTESIAN_POINT ( 'NONE',  ( 20.95159278453404283, 67.09210366206356468, -195.0383872994151773 ) ) ;
#37954=AXIS2_PLACEMENT_3D ( 'NONE', #194633, #175088, #250715 ) ;
#37958=FACE_OUTER_BOUND ( 'NONE', #105282, .T. ) ;
#37969=EDGE_CURVE ( 'NONE', #101145, #70073, #100287, .T. ) ;
#38027=ORIENTED_EDGE ( 'NONE', *, *, #215351, .T. ) ;
#38032=( BOUNDED_SURFACE ( )  B_SPLINE_SURFACE ( 3, 2, ( 
 ( #183224, #123241, #202776 ),
 ( #4560, #244465, #86650 ),
 ( #64546, #102354, #8439 ),
 ( #141514, #7132, #124537 ),
 ( #125798, #146633, #205323 ),
 ( #3272, #28027, #67119 ) ),
 .UNSPECIFIED., .F., .F., .F. ) 
 B_SPLINE_SURFACE_WITH_KNOTS ( ( 4, 2, 4 ),
 ( 3, 3 ),
 ( 0.0001381104793128061785, 0.0002947094729387477754, 0.0004513084665646893722 ),
 ( 0.000000000000000000, 1.000000000000000000 ),
 .UNSPECIFIED. ) 
 GEOMETRIC_REPRESENTATION_ITEM ( )  RATIONAL_B_SPLINE_SURFACE ( (
 ( 1.000000000000000000, 0.7071067811865494601, 1.000000000000000000),
 ( 1.000000000000000000, 0.6919563088098275028, 1.000000000000000000),
 ( 1.000000000000000000, 0.6959445945718949478, 1.000000000000000000),
 ( 1.000000000000000000, 0.7137882985310208817, 1.000000000000000000),
 ( 1.000000000000000000, 0.7257496306098795147, 1.000000000000000000),
 ( 1.000000000000000000, 0.7250110520819876836, 1.000000000000000000) ) ) 
 REPRESENTATION_ITEM ( '' )  SURFACE ( )  );
#38035=ORIENTED_EDGE ( 'NONE', *, *, #255479, .T. ) ;
#38042=EDGE_LOOP ( 'NONE', ( #218798, #109738, #20020, #94722 ) ) ;
#38047=SPHERICAL_SURFACE ( 'NONE', #19073, 0.1000000000000000056 ) ;
#38059=ORIENTED_EDGE ( 'NONE', *, *, #75288, .T. ) ;
#38124=AXIS2_PLACEMENT_3D ( 'NONE', #181925, #82774, #162375 ) ;
#38130=FACE_OUTER_BOUND ( 'NONE', #175475, .T. ) ;
#38136=CARTESIAN_POINT ( 'NONE',  ( -23.25000000000000000, 76.10085836911147794, -215.2726746080137445 ) ) ;
#38172=ORIENTED_EDGE ( 'NONE', *, *, #198815, .T. ) ;
#38223=AXIS2_PLACEMENT_3D ( 'NONE', #6917, #8223, #23945 ) ;
#38245=CARTESIAN_POINT ( 'NONE',  ( -18.47079683080343315, 85.47166410525755964, -196.4142469435320777 ) ) ;
#38294=EDGE_CURVE ( 'NONE', #47404, #228403, #130171, .T. ) ;
#38356=FACE_OUTER_BOUND ( 'NONE', #73640, .T. ) ;
#38372=CARTESIAN_POINT ( 'NONE',  ( -23.15000000000000213, 84.59626168225550202, -179.4732350016745954 ) ) ;
#38375=FACE_OUTER_BOUND ( 'NONE', #193715, .T. ) ;
#38395=DIRECTION ( 'NONE',  ( -1.000000000000000000, -7.304098846218135653E-16, -5.100424963727256530E-30 ) ) ;
#38411=VECTOR ( 'NONE', #41807, 1000.000000000000000 ) ;
#38429=CARTESIAN_POINT ( 'NONE',  ( -21.05000000000000071, 70.10000000001251408, -180.2422072491807796 ) ) ;
#38448=EDGE_CURVE ( 'NONE', #3727, #110167, #134446, .T. ) ;
#38460=CARTESIAN_POINT ( 'NONE',  ( 23.15000000000000213, 85.60000000001261355, -193.6291383618718385 ) ) ;
#38466=LINE ( 'NONE', #100950, #225669 ) ;
#38505=CARTESIAN_POINT ( 'NONE',  ( 21.08489834409762054, 65.37767610527707518, -191.1731074845243370 ) ) ;
#38551=SPHERICAL_SURFACE ( 'NONE', #176842, 0.1000000000000000056 ) ;
#38553=EDGE_LOOP ( 'NONE', ( #164370, #12184, #54406, #175239 ) ) ;
#38577=EDGE_CURVE ( 'NONE', #31357, #222338, #205179, .T. ) ;
#38607=AXIS2_PLACEMENT_3D ( 'NONE', #115590, #215961, #137703 ) ;
#38621=EDGE_CURVE ( 'NONE', #103860, #181359, #192741, .T. ) ;
#38634=CIRCLE ( 'NONE', #234250, 0.1000000000000028644 ) ;
#38643=EDGE_CURVE ( 'NONE', #216335, #239176, #213565, .T. ) ;
#38649=ORIENTED_EDGE ( 'NONE', *, *, #509, .T. ) ;
#38656=ORIENTED_EDGE ( 'NONE', *, *, #60262, .F. ) ;
#38666=ORIENTED_EDGE ( 'NONE', *, *, #198572, .T. ) ;
#38668=VECTOR ( 'NONE', #95775, 1000.000000000000000 ) ;
#38670=ORIENTED_EDGE ( 'NONE', *, *, #139697, .T. ) ;
#38671=DIRECTION ( 'NONE',  ( 1.000000000000000000, 0.000000000000000000, 0.000000000000000000 ) ) ;
#38692=DIRECTION ( 'NONE',  ( 1.000000000000000000, 0.000000000000000000, 0.000000000000000000 ) ) ;
#38708=DIRECTION ( 'NONE',  ( -0.000000000000000000, 1.000000000000000000, 6.982962677686266711E-15 ) ) ;
#38709=CARTESIAN_POINT ( 'NONE',  ( -21.05000000000000071, 77.16270174995064224, -195.5231074845243313 ) ) ;
#38714=( BOUNDED_SURFACE ( )  B_SPLINE_SURFACE ( 3, 2, ( 
 ( #196659, #242204, #995 ),
 ( #119713, #18028, #197942 ),
 ( #42726, #37617, #102674 ),
 ( #157592, #40196, #216220 ) ),
 .UNSPECIFIED., .F., .F., .F. ) 
 B_SPLINE_SURFACE_WITH_KNOTS ( ( 4, 4 ),
 ( 3, 3 ),
 ( 0.0006461284895273765793, 0.0007503702773986202284 ),
 ( 0.000000000000000000, 1.000000000000000000 ),
 .UNSPECIFIED. ) 
 GEOMETRIC_REPRESENTATION_ITEM ( )  RATIONAL_B_SPLINE_SURFACE ( (
 ( 1.000000000000000000, 0.7071067811865483499, 1.000000000000000000),
 ( 1.000000000000000000, 0.7076476444648377440, 1.000000000000000000),
 ( 1.000000000000000000, 0.7075727925192694112, 1.000000000000000000),
 ( 1.000000000000000000, 0.7071067811865581199, 1.000000000000000000) ) ) 
 REPRESENTATION_ITEM ( '' )  SURFACE ( )  );
#38716=DIRECTION ( 'NONE',  ( 0.000000000000000000, 0.000000000000000000, -1.000000000000000000 ) ) ;
#38732=ORIENTED_EDGE ( 'NONE', *, *, #165971, .F. ) ;
#38741=LINE ( 'NONE', #136524, #248818 ) ;
#38748=PLANE ( 'NONE',  #169928 ) ;
#38767=CIRCLE ( 'NONE', #101054, 0.09999999999999939493 ) ;
#38772=DIRECTION ( 'NONE',  ( 0.000000000000000000, -6.853228547068871147E-15, 1.000000000000000000 ) ) ;
#38779=EDGE_CURVE ( 'NONE', #162952, #135929, #126271, .T. ) ;
#38817=ADVANCED_FACE ( 'NONE', ( #164803 ), #101270, .T. ) ;
#38819=ORIENTED_EDGE ( 'NONE', *, *, #221686, .F. ) ;
#38825=VERTEX_POINT ( 'NONE', #68271 ) ;
#38830=ORIENTED_EDGE ( 'NONE', *, *, #97948, .F. ) ;
#38839=CARTESIAN_POINT ( 'NONE',  ( -20.85000000000000142, 68.97833521811233481, -166.2895420826271220 ) ) ;
#38858=CARTESIAN_POINT ( 'NONE',  ( 20.04142135623730070, 64.35000000001254250, -182.1731074845244507 ) ) ;
#38921=CARTESIAN_POINT ( 'NONE',  ( 18.59999999999999076, 65.79142135624982757, -178.7731074845244450 ) ) ;
#38927=CARTESIAN_POINT ( 'NONE',  ( -20.94999999999999929, 64.25000000001250555, -176.8069731475025890 ) ) ;
#38939=VERTEX_POINT ( 'NONE', #172558 ) ;
#38957=DIRECTION ( 'NONE',  ( 0.000000000000000000, 0.000000000000000000, 1.000000000000000000 ) ) ;
#38960=ORIENTED_EDGE ( 'NONE', *, *, #141279, .F. ) ;
#38961=AXIS2_PLACEMENT_3D ( 'NONE', #41499, #157618, #21926 ) ;
#38969=VERTEX_POINT ( 'NONE', #171273 ) ;
#38985=FACE_OUTER_BOUND ( 'NONE', #170860, .T. ) ;
#39000=ORIENTED_EDGE ( 'NONE', *, *, #214254, .T. ) ;
#39004=DIRECTION ( 'NONE',  ( -1.000000000000000000, -0.000000000000000000, -0.000000000000000000 ) ) ;
#39017=CARTESIAN_POINT ( 'NONE',  ( 18.53317502108576775, 65.67736539654997330, -164.4625116876572406 ) ) ;
#39023=CARTESIAN_POINT ( 'NONE',  ( 23.14999999999999858, 78.10000000001245724, -170.0231074845243313 ) ) ;
#39028=CARTESIAN_POINT ( 'NONE',  ( 23.24999999999999645, 76.00000000001267608, -203.5231074845243597 ) ) ;
#39029=DIRECTION ( 'NONE',  ( 0.000000000000000000, -6.982962677686266711E-15, 1.000000000000000000 ) ) ;
#39038=ORIENTED_EDGE ( 'NONE', *, *, #3115, .F. ) ;
#39039=CIRCLE ( 'NONE', #122220, 0.1000000000000072220 ) ;
#39051=CYLINDRICAL_SURFACE ( 'NONE', #146637, 0.1000000000000028644 ) ;
#39062=CIRCLE ( 'NONE', #68448, 0.09999999999998898659 ) ;
#39071=DIRECTION ( 'NONE',  ( 1.000000000000000000, 0.000000000000000000, 0.000000000000000000 ) ) ;
#39076=EDGE_LOOP ( 'NONE', ( #124924, #239437, #142218, #21110 ) ) ;
#39084=ORIENTED_EDGE ( 'NONE', *, *, #129279, .F. ) ;
#39107=PRODUCT_CONTEXT ( 'NONE', #140721, 'mechanical' ) ;
#39160=DIRECTION ( 'NONE',  ( 0.000000000000000000, -0.8660254037844343777, 0.5000000000000074385 ) ) ;
#39166=CARTESIAN_POINT ( 'NONE',  ( -18.59999999999999787, 66.65000000001253966, -182.1731074845244223 ) ) ;
#39191=AXIS2_PLACEMENT_3D ( 'NONE', #189265, #148859, #34072 ) ;
#39224=AXIS2_PLACEMENT_3D ( 'NONE', #185116, #3913, #142132 ) ;
#39229=DIRECTION ( 'NONE',  ( 1.000000000000000000, 0.000000000000000000, 0.000000000000000000 ) ) ;
#39255=CARTESIAN_POINT ( 'NONE',  ( -20.00857864376270001, 66.85000000001259934, -191.1731074845244223 ) ) ;
#39256=VECTOR ( 'NONE', #137397, 1000.000000000000000 ) ;
#39259=AXIS2_PLACEMENT_3D ( 'NONE', #201379, #106108, #7033 ) ;
#39267=EDGE_CURVE ( 'NONE', #256994, #233248, #184705, .T. ) ;
#39270=ORIENTED_EDGE ( 'NONE', *, *, #165971, .T. ) ;
#39299=DIRECTION ( 'NONE',  ( -0.000000000000000000, 1.000000000000000000, 6.982962677686266711E-15 ) ) ;
#39330=DIRECTION ( 'NONE',  ( 0.000000000000000000, -1.000000000000000000, 0.000000000000000000 ) ) ;
#39334=CIRCLE ( 'NONE', #176696, 0.09999999999999939493 ) ;
#39340=AXIS2_PLACEMENT_3D ( 'NONE', #229062, #129929, #209484 ) ;
#39360=DIRECTION ( 'NONE',  ( 1.000000000000000000, 0.000000000000000000, 0.000000000000000000 ) ) ;
#39397=VECTOR ( 'NONE', #170701, 1000.000000000000000 ) ;
#39404=CARTESIAN_POINT ( 'NONE',  ( 20.95512820512820440, 67.12384868372450342, -194.9644784893834810 ) ) ;
#39406=AXIS2_PLACEMENT_3D ( 'NONE', #108151, #9044, #69040 ) ;
#39477=EDGE_LOOP ( 'NONE', ( #27870, #90152, #82934, #50124, #198239 ) ) ;
#39486=DIRECTION ( 'NONE',  ( 0.000000000000000000, -6.982962677686266711E-15, 1.000000000000000000 ) ) ;
#39499=DIRECTION ( 'NONE',  ( 0.000000000000000000, -6.938893903907222067E-15, 1.000000000000000000 ) ) ;
#39503=CARTESIAN_POINT ( 'NONE',  ( -23.25000000000000000, 76.00000000001244871, -170.0231074845243597 ) ) ;
#39508=ORIENTED_EDGE ( 'NONE', *, *, #214019, .T. ) ;
#39567=DIRECTION ( 'NONE',  ( -1.000000000000000000, 0.000000000000000000, 0.000000000000000000 ) ) ;
#39581=CARTESIAN_POINT ( 'NONE',  ( -22.39999999999999858, 75.90000000001273861, -211.3138870828977645 ) ) ;
#39594=EDGE_CURVE ( 'NONE', #16498, #201210, #105459, .T. ) ;
#39614=ORIENTED_EDGE ( 'NONE', *, *, #243178, .F. ) ;
#39619=DIRECTION ( 'NONE',  ( 1.000000000000000000, 0.000000000000000000, 0.000000000000000000 ) ) ;
#39621=ORIENTED_EDGE ( 'NONE', *, *, #165027, .F. ) ;
#39633=CARTESIAN_POINT ( 'NONE',  ( 21.07928932188134397, 69.67148334361937145, -203.6220026301788266 ) ) ;
#39656=ADVANCED_FACE ( 'NONE', ( #74109 ), #15402, .F. ) ;
#39667=DIRECTION ( 'NONE',  ( 0.000000000000000000, -1.000000000000000000, -6.982962677686266711E-15 ) ) ;
#39738=CYLINDRICAL_SURFACE ( 'NONE', #250523, 0.09999999999998898659 ) ;
#39773=ORIENTED_EDGE ( 'NONE', *, *, #124362, .F. ) ;
#39795=ORIENTED_EDGE ( 'NONE', *, *, #10929, .F. ) ;
#39803=ORIENTED_EDGE ( 'NONE', *, *, #15424, .F. ) ;
#39810=AXIS2_PLACEMENT_3D ( 'NONE', #202231, #11756, #112138 ) ;
#39825=CIRCLE ( 'NONE', #81454, 0.09999999999999938105 ) ;
#39837=DIRECTION ( 'NONE',  ( -1.000000000000000000, -0.000000000000000000, -0.000000000000000000 ) ) ;
#39839=SPHERICAL_SURFACE ( 'NONE', #90189, 0.1000000000000000056 ) ;
#39883=AXIS2_PLACEMENT_3D ( 'NONE', #12918, #92412, #110704 ) ;
#39885=CARTESIAN_POINT ( 'NONE',  ( -18.59999999999999787, 85.40000000001258229, -196.2258477248610120 ) ) ;
#39890=CARTESIAN_POINT ( 'NONE',  ( 19.94784844284962233, 64.28691006698339550, -178.8209087672258022 ) ) ;
#39911=DIRECTION ( 'NONE',  ( 0.000000000000000000, -0.9915357197604982575, 0.1298341882519033486 ) ) ;
#39921=ORIENTED_EDGE ( 'NONE', *, *, #5548, .F. ) ;
#39940=AXIS2_PLACEMENT_3D ( 'NONE', #93391, #15157, #58098 ) ;
#39973=CARTESIAN_POINT ( 'NONE',  ( -18.59999999999999787, 64.35000000001254250, -182.1731074845244507 ) ) ;
#39992=CARTESIAN_POINT ( 'NONE',  ( 18.43466021071417060, 85.49419069046894037, -163.4060459243964374 ) ) ;
#39999=ORIENTED_EDGE ( 'NONE', *, *, #190365, .T. ) ;
#40025=CARTESIAN_POINT ( 'NONE',  ( 23.24999999999999645, 70.40000000001261071, -191.1178414656113205 ) ) ;
#40062=ORIENTED_EDGE ( 'NONE', *, *, #157953, .T. ) ;
#40077=AXIS2_PLACEMENT_3D ( 'NONE', #225176, #106511, #186081 ) ;
#40140=AXIS2_PLACEMENT_3D ( 'NONE', #192308, #214418, #13663 ) ;
#40147=CARTESIAN_POINT ( 'NONE',  ( 21.07928932188134397, 69.67148334361938566, -203.6220026301787982 ) ) ;
#40149=FACE_OUTER_BOUND ( 'NONE', #68552, .T. ) ;
#40196=CARTESIAN_POINT ( 'NONE',  ( -22.48660254037843131, 64.25000000001267608, -203.5731074845243995 ) ) ;
#40206=DIRECTION ( 'NONE',  ( 0.000000000000000000, 6.997203936713175802E-15, -1.000000000000000000 ) ) ;
#40227=ORIENTED_EDGE ( 'NONE', *, *, #255749, .T. ) ;
#40233=CARTESIAN_POINT ( 'NONE',  ( 20.94999999999999574, 70.10000000001267040, -193.3040077198679967 ) ) ;
#40238=ORIENTED_EDGE ( 'NONE', *, *, #47457, .T. ) ;
#40243=ORIENTED_EDGE ( 'NONE', *, *, #46101, .F. ) ;
#40251=CARTESIAN_POINT ( 'NONE',  ( 20.94999999999999929, 65.52661458509973613, -195.9444530202758870 ) ) ;
#40255=AXIS2_PLACEMENT_3D ( 'NONE', #10983, #28011, #86634 ) ;
#40270=DIRECTION ( 'NONE',  ( 0.000000000000000000, 0.9893560106964510714, -0.1455152366551481502 ) ) ;
#40294=DIRECTION ( 'NONE',  ( -1.000000000000000000, 0.000000000000000000, 0.000000000000000000 ) ) ;
#40299=CYLINDRICAL_SURFACE ( 'NONE', #178993, 0.1000000000000028644 ) ;
#40319=DIRECTION ( 'NONE',  ( 1.000000000000000000, -1.875376730785737719E-16, -1.309568571767809260E-30 ) ) ;
#40330=EDGE_LOOP ( 'NONE', ( #117826, #68214, #101998, #21945 ) ) ;
#40355=CARTESIAN_POINT ( 'NONE',  ( 20.94999999999999929, 69.45000000001260787, -193.5060803140843859 ) ) ;
#40359=ORIENTED_EDGE ( 'NONE', *, *, #135608, .F. ) ;
#40375=CARTESIAN_POINT ( 'NONE',  ( -23.25000000000000000, 87.75000000001276135, -215.2731074845242745 ) ) ;
#40401=LINE ( 'NONE', #37820, #75893 ) ;
#40410=LINE ( 'NONE', #199467, #54917 ) ;
#40434=CARTESIAN_POINT ( 'NONE',  ( -18.59999999999999787, 64.35000000001264198, -196.5083017138704236 ) ) ;
#40435=FACE_OUTER_BOUND ( 'NONE', #160182, .T. ) ;
#40443=EDGE_LOOP ( 'NONE', ( #55341, #175644, #35403, #40602 ) ) ;
#40452=VECTOR ( 'NONE', #141208, 1000.000000000000114 ) ;
#40453=DIRECTION ( 'NONE',  ( 0.7071067811865475727, 0.7071067811865475727, 4.937700262164531476E-15 ) ) ;
#40470=CARTESIAN_POINT ( 'NONE',  ( 21.13507111622889667, 65.28231661301421695, -191.2739388981636353 ) ) ;
#40472=CARTESIAN_POINT ( 'NONE',  ( 20.94999999999999929, 65.61821452928846554, -164.5152621206402728 ) ) ;
#40486=DIRECTION ( 'NONE',  ( 0.000000000000000000, -6.982962677686266711E-15, 1.000000000000000000 ) ) ;
#40543=ORIENTED_EDGE ( 'NONE', *, *, #210585, .T. ) ;
#40577=EDGE_CURVE ( 'NONE', #144435, #135406, #139517, .T. ) ;
#40601=CARTESIAN_POINT ( 'NONE',  ( 18.42636655943174162, 85.49694431578303977, -163.4140269133687866 ) ) ;
#40602=ORIENTED_EDGE ( 'NONE', *, *, #169333, .F. ) ;
#40712=DIRECTION ( 'NONE',  ( 0.000000000000000000, -6.982962677686266711E-15, 1.000000000000000000 ) ) ;
#40732=CARTESIAN_POINT ( 'NONE',  ( -18.39999999999999858, 85.50000000001263345, -196.5238218066854472 ) ) ;
#40736=DIRECTION ( 'NONE',  ( 0.000000000000000000, -6.982962677686266711E-15, 1.000000000000000000 ) ) ;
#40739=CARTESIAN_POINT ( 'NONE',  ( 20.95556889135987788, 65.37805641227753028, -195.8807132626668874 ) ) ;
#40743=EDGE_CURVE ( 'NONE', #43270, #256108, #168348, .T. ) ;
#40803=CARTESIAN_POINT ( 'NONE',  ( 20.85000000106584750, 64.25000000001249134, -176.8676028280509911 ) ) ;
#40851=EDGE_CURVE ( 'NONE', #25217, #231047, #130221, .T. ) ;
#40859=FACE_OUTER_BOUND ( 'NONE', #22464, .T. ) ;
#40870=FACE_OUTER_BOUND ( 'NONE', #141950, .T. ) ;
#40888=ORIENTED_EDGE ( 'NONE', *, *, #76086, .F. ) ;
#40899=DIRECTION ( 'NONE',  ( -1.836970198721029934E-16, -1.000000000000000000, -6.982962677686266711E-15 ) ) ;
#40902=CARTESIAN_POINT ( 'NONE',  ( -23.15000000000000213, 87.75000000001267608, -203.5231074845243029 ) ) ;
#40914=CARTESIAN_POINT ( 'NONE',  ( 18.59999999999999787, 85.32100840337393777, -196.2871692354464130 ) ) ;
#40947=DIRECTION ( 'NONE',  ( 1.000000000000000000, 0.000000000000000000, 0.000000000000000000 ) ) ;
#40964=CARTESIAN_POINT ( 'NONE',  ( 20.94999999999999929, 76.00000000001244871, -170.0231074845243597 ) ) ;
#40980=AXIS2_PLACEMENT_3D ( 'NONE', #243753, #144641, #139506 ) ;
#41017=FACE_OUTER_BOUND ( 'NONE', #171781, .T. ) ;
#41037=DIRECTION ( 'NONE',  ( 0.000000000000000000, -1.000000000000000000, 0.000000000000000000 ) ) ;
#41038=EDGE_CURVE ( 'NONE', #69740, #236913, #141772, .T. ) ;
#41077=DIRECTION ( 'NONE',  ( 0.000000000000000000, -0.1350103645451974088, 0.9908441862701587999 ) ) ;
#41082=CARTESIAN_POINT ( 'NONE',  ( -20.54999999999999716, 68.85000000001257092, -186.7731074845244166 ) ) ;
#41094=AXIS2_PLACEMENT_3D ( 'NONE', #89065, #227298, #168670 ) ;
#41133=DIRECTION ( 'NONE',  ( 0.000000000000000000, -1.000000000000000000, 0.000000000000000000 ) ) ;
#41137=CARTESIAN_POINT ( 'NONE',  ( 18.59999999999999076, 69.45000000001252261, -182.3731074845244109 ) ) ;
#41142=VERTEX_POINT ( 'NONE', #143051 ) ;
#41144=CIRCLE ( 'NONE', #24579, 0.09999999999998898659 ) ;
#41155=VERTEX_POINT ( 'NONE', #114213 ) ;
#41185=CIRCLE ( 'NONE', #49540, 0.09999999999998898659 ) ;
#41231=ADVANCED_FACE ( 'NONE', ( #15123 ), #253709, .T. ) ;
#41233=ORIENTED_EDGE ( 'NONE', *, *, #38294, .T. ) ;
#41240=CARTESIAN_POINT ( 'NONE',  ( 20.02499999999999858, 66.25000000001253397, -182.3731074845244393 ) ) ;
#41259=VERTEX_POINT ( 'NONE', #119359 ) ;
#41281=ORIENTED_EDGE ( 'NONE', *, *, #4078, .F. ) ;
#41295=AXIS2_PLACEMENT_3D ( 'NONE', #74939, #55306, #76178 ) ;
#41317=CIRCLE ( 'NONE', #208084, 0.1000000000000072220 ) ;
#41322=ORIENTED_EDGE ( 'NONE', *, *, #161012, .T. ) ;
#41334=CIRCLE ( 'NONE', #132895, 0.09999999999998898659 ) ;
#41336=ORIENTED_EDGE ( 'NONE', *, *, #117088, .F. ) ;
#41352=DIRECTION ( 'NONE',  ( 1.000000000000000000, 0.000000000000000000, 0.000000000000000000 ) ) ;
#41357=AXIS2_PLACEMENT_3D ( 'NONE', #152914, #52473, #151626 ) ;
#41361=AXIS2_PLACEMENT_3D ( 'NONE', #126205, #105327, #66249 ) ;
#41374=AXIS2_PLACEMENT_3D ( 'NONE', #170320, #134962, #231540 ) ;
#41392=VECTOR ( 'NONE', #219260, 1000.000000000000000 ) ;
#41396=VERTEX_POINT ( 'NONE', #97167 ) ;
#41407=EDGE_CURVE ( 'NONE', #216782, #183838, #241195, .T. ) ;
#41418=DIRECTION ( 'NONE',  ( 0.000000000000000000, -0.1350103645451807555, -0.9908441862701609093 ) ) ;
#41441=CARTESIAN_POINT ( 'NONE',  ( -20.54999999999999716, 76.00000000001243450, -168.1231074845243540 ) ) ;
#41466=CARTESIAN_POINT ( 'NONE',  ( -22.42357213249529480, 75.90091303601117545, -211.1960398708842774 ) ) ;
#41470=CARTESIAN_POINT ( 'NONE',  ( 20.94999999999999929, 76.00000000001244871, -170.0231074845243597 ) ) ;
#41499=CARTESIAN_POINT ( 'NONE',  ( -20.64999999999999858, 85.00000000001251976, -179.9170766071767389 ) ) ;
#41501=CARTESIAN_POINT ( 'NONE',  ( -21.02374657821590631, 64.39999999919233176, -176.9513107143264108 ) ) ;
#41529=CARTESIAN_POINT ( 'NONE',  ( 20.95595012432474391, 65.39582078693628375, -195.9273381543061987 ) ) ;
#41530=AXIS2_PLACEMENT_3D ( 'NONE', #111517, #68544, #9844 ) ;
#41547=CARTESIAN_POINT ( 'NONE',  ( 23.14999999999999503, 69.35000000001254250, -182.3731074845244109 ) ) ;
#41563=LINE ( 'NONE', #160231, #103299 ) ;
#41582=CARTESIAN_POINT ( 'NONE',  ( -23.25000000000000000, 65.66751761918722252, -164.4282609406112670 ) ) ;
#41593=CARTESIAN_POINT ( 'NONE',  ( -21.05000000000000071, 64.25000000001250555, -177.0379132551784096 ) ) ;
#41597=EDGE_CURVE ( 'NONE', #186763, #6765, #193138, .T. ) ;
#41607=CARTESIAN_POINT ( 'NONE',  ( -20.94999999999999929, 76.00000000001242029, -166.0231074845243597 ) ) ;
#41633=DIRECTION ( 'NONE',  ( -2.952720810173289112E-16, -1.000000000000000000, -6.982962677686266711E-15 ) ) ;
#41636=CARTESIAN_POINT ( 'NONE',  ( 18.49999999999999289, 65.65621891165940838, -178.6946622066474504 ) ) ;
#41661=ORIENTED_EDGE ( 'NONE', *, *, #105039, .F. ) ;
#41679=ORIENTED_EDGE ( 'NONE', *, *, #158432, .T. ) ;
#41680=DIRECTION ( 'NONE',  ( 1.000000000000000000, 0.000000000000000000, 0.000000000000000000 ) ) ;
#41698=CARTESIAN_POINT ( 'NONE',  ( -22.39999999999999858, 76.00000000001273293, -211.3138870828977645 ) ) ;
#41722=ORIENTED_EDGE ( 'NONE', *, *, #123801, .F. ) ;
#41776=CIRCLE ( 'NONE', #187521, 0.09999999999998898659 ) ;
#41778=DIRECTION ( 'NONE',  ( 1.000000000000000000, 0.000000000000000000, 0.000000000000000000 ) ) ;
#41800=DIRECTION ( 'NONE',  ( 0.000000000000000000, 0.000000000000000000, 1.000000000000000000 ) ) ;
#41803=TOROIDAL_SURFACE ( 'NONE', #108416, 11.65000000000000036, 0.1000000000000000056 ) ;
#41807=DIRECTION ( 'NONE',  ( 0.000000000000000000, -6.982962677686266711E-15, 1.000000000000000000 ) ) ;
#41809=DIRECTION ( 'NONE',  ( 1.000000000000000000, 0.000000000000000000, 0.000000000000000000 ) ) ;
#41811=( BOUNDED_SURFACE ( )  B_SPLINE_SURFACE ( 3, 2, ( 
 ( #236429, #98171, #56491 ),
 ( #156927, #158226, #21272 ),
 ( #175228, #78628, #100733 ),
 ( #138582, #59045, #61651 ),
 ( #38245, #180320, #139883 ),
 ( #115203, #18674, #1660 ),
 ( #136020, #177772, #57778 ),
 ( #81191, #239009, #95629 ) ),
 .UNSPECIFIED., .F., .F., .F. ) 
 B_SPLINE_SURFACE_WITH_KNOTS ( ( 4, 2, 2, 4 ),
 ( 3, 3 ),
 ( 0.0001723339234021429623, 0.0002782939632049932365, 0.0003842540030078435377, 0.0005961740826135441401 ),
 ( 0.000000000000000000, 1.000000000000000000 ),
 .UNSPECIFIED. ) 
 GEOMETRIC_REPRESENTATION_ITEM ( )  RATIONAL_B_SPLINE_SURFACE ( (
 ( 1.000000000000000000, 0.9504532311154358926, 1.000000000000000000),
 ( 1.000000000000000000, 0.9506023220705802634, 1.000000000000000000),
 ( 1.000000000000000000, 0.9395774818187462296, 1.000000000000000000),
 ( 1.000000000000000000, 0.9079328464641803764, 1.000000000000000000),
 ( 1.000000000000000000, 0.8875702416206912027, 1.000000000000000000),
 ( 1.000000000000000000, 0.8205919608037689494, 1.000000000000000000),
 ( 1.000000000000000000, 0.7666842783600247291, 1.000000000000000000),
 ( 1.000000000000000000, 0.7071067811865302533, 1.000000000000000000) ) ) 
 REPRESENTATION_ITEM ( '' )  SURFACE ( )  );
#41821=DIRECTION ( 'NONE',  ( 0.000000000000000000, -1.000000000000000000, 0.000000000000000000 ) ) ;
#41837=DIRECTION ( 'NONE',  ( 1.000000000000000000, 0.000000000000000000, 0.000000000000000000 ) ) ;
#41860=CARTESIAN_POINT ( 'NONE',  ( -21.44999999999999929, 68.65000000001261071, -191.1731074845243938 ) ) ;
#41881=ORIENTED_EDGE ( 'NONE', *, *, #36017, .T. ) ;
#41906=ORIENTED_EDGE ( 'NONE', *, *, #241721, .T. ) ;
#41917=DIRECTION ( 'NONE',  ( 0.000000000000000000, -0.1298341882519953583, -0.9915357197604862671 ) ) ;
#41929=CARTESIAN_POINT ( 'NONE',  ( 20.85000000000000142, 76.00000000001244871, -170.0231074845243597 ) ) ;
#41961=LINE ( 'NONE', #120234, #209538 ) ;
#41970=EDGE_CURVE ( 'NONE', #46643, #227800, #237446, .T. ) ;
#41982=DIRECTION ( 'NONE',  ( 0.000000000000000000, -0.2605042016806740079, 0.9654727137038698892 ) ) ;
#41989=CARTESIAN_POINT ( 'NONE',  ( 23.24999999999999289, 69.55000000001277272, -215.2731074845244166 ) ) ;
#42007=DIRECTION ( 'NONE',  ( 1.000000000000000000, 0.000000000000000000, 0.000000000000000000 ) ) ;
#42009=DIRECTION ( 'NONE',  ( 1.000000000000000000, 0.000000000000000000, 0.000000000000000000 ) ) ;
#42060=EDGE_CURVE ( 'NONE', #209479, #100484, #154787, .T. ) ;
#42104=CIRCLE ( 'NONE', #254429, 0.5000000000000004441 ) ;
#42136=ORIENTED_EDGE ( 'NONE', *, *, #49743, .T. ) ;
#42165=ORIENTED_EDGE ( 'NONE', *, *, #111288, .T. ) ;
#42189=CARTESIAN_POINT ( 'NONE',  ( -23.25000000000000000, 77.85161776048127535, -158.4199177649206831 ) ) ;
#42200=DIRECTION ( 'NONE',  ( 0.000000000000000000, -1.000000000000000000, -6.982962677686265922E-15 ) ) ;
#42211=B_SPLINE_CURVE_WITH_KNOTS ( 'NONE', 3,
 ( #248041, #22924, #123288, #239381, #20354, #161132, #202813, #62037 ),
 .UNSPECIFIED., .F., .F.,
 ( 4, 2, 2, 4 ),
 ( 0.000000000000000000, 0.0001881495939909316674, 0.0002822243909863870115, 0.0003762991879818423013 ),
 .UNSPECIFIED. ) ;
#42216=CARTESIAN_POINT ( 'NONE',  ( 23.15000000000000213, 85.50000000001251976, -179.9170766071767389 ) ) ;
#42242=ORIENTED_EDGE ( 'NONE', *, *, #124785, .F. ) ;
#42244=ADVANCED_FACE ( 'NONE', ( #149339 ), #182908, .T. ) ;
#42245=AXIS2_PLACEMENT_3D ( 'NONE', #114179, #253678, #15094 ) ;
#42261=CARTESIAN_POINT ( 'NONE',  ( 21.14999999999999858, 69.45000000001259366, -191.1731074845243938 ) ) ;
#42309=AXIS2_PLACEMENT_3D ( 'NONE', #66897, #164719, #27809 ) ;
#42316=DIRECTION ( 'NONE',  ( -0.000000000000000000, 6.982962677686266711E-15, -1.000000000000000000 ) ) ;
#42350=EDGE_CURVE ( 'NONE', #77018, #207338, #253607, .T. ) ;
#42362=EDGE_CURVE ( 'NONE', #242182, #202321, #220538, .T. ) ;
#42382=ORIENTED_EDGE ( 'NONE', *, *, #56948, .F. ) ;
#42402=AXIS2_PLACEMENT_3D ( 'NONE', #86953, #143087, #222616 ) ;
#42412=CARTESIAN_POINT ( 'NONE',  ( -21.55000000000000426, 68.29142135624984178, -182.2731074845244166 ) ) ;
#42440=VERTEX_POINT ( 'NONE', #82266 ) ;
#42514=CARTESIAN_POINT ( 'NONE',  ( -21.07928932188134041, 69.67148334361938566, -203.6220026301787982 ) ) ;
#42524=ORIENTED_EDGE ( 'NONE', *, *, #22333, .T. ) ;
#42539=DIRECTION ( 'NONE',  ( 0.000000000000000000, 0.000000000000000000, -1.000000000000000000 ) ) ;
#42550=CARTESIAN_POINT ( 'NONE',  ( 20.94999999999999929, 74.16465844978819177, -191.9679561919613775 ) ) ;
#42552=DIRECTION ( 'NONE',  ( -0.7071067811865389130, -5.024295867788141276E-15, 0.7071067811865561215 ) ) ;
#42554=EDGE_LOOP ( 'NONE', ( #107758, #228460, #141001, #160453 ) ) ;
#42626=AXIS2_PLACEMENT_3D ( 'NONE', #45440, #8883, #128839 ) ;
#42629=EDGE_CURVE ( 'NONE', #185777, #54825, #116458, .T. ) ;
#42664=EDGE_LOOP ( 'NONE', ( #13856, #88405, #42242, #255574 ) ) ;
#42673=CARTESIAN_POINT ( 'NONE',  ( -20.64999999999999858, 76.00000000001243450, -168.0231074845243597 ) ) ;
#42674=DIRECTION ( 'NONE',  ( -1.000000000000000000, 3.265361837132813093E-16, 2.280189983783949500E-30 ) ) ;
#42701=DIRECTION ( 'NONE',  ( -0.000000000000000000, -0.01283462868040327436, 0.9999176327611370985 ) ) ;
#42702=AXIS2_PLACEMENT_3D ( 'NONE', #135487, #54680, #252879 ) ;
#42708=DIRECTION ( 'NONE',  ( 1.000000000000000000, -0.000000000000000000, 0.000000000000000000 ) ) ;
#42712=EDGE_CURVE ( 'NONE', #68808, #207338, #37346, .T. ) ;
#42714=CARTESIAN_POINT ( 'NONE',  ( -21.07971444708686093, 75.91217656369489930, -209.8528995661509100 ) ) ;
#42726=CARTESIAN_POINT ( 'NONE',  ( -22.49533356619858893, 64.34999999370857893, -203.5882300648471244 ) ) ;
#42759=ORIENTED_EDGE ( 'NONE', *, *, #10597, .T. ) ;
#42797=ORIENTED_EDGE ( 'NONE', *, *, #75007, .F. ) ;
#42806=DIRECTION ( 'NONE',  ( 0.000000000000000000, 0.1455152366551700771, 0.9893560106964479628 ) ) ;
#42819=VERTEX_POINT ( 'NONE', #140682 ) ;
#42872=EDGE_LOOP ( 'NONE', ( #33514, #212962, #80916, #208042 ) ) ;
#42888=ORIENTED_EDGE ( 'NONE', *, *, #139178, .F. ) ;
#42927=CYLINDRICAL_SURFACE ( 'NONE', #66567, 0.09999999999998898659 ) ;
#42935=VERTEX_POINT ( 'NONE', #70164 ) ;
#42971=CARTESIAN_POINT ( 'NONE',  ( 21.05281448260627641, 67.22398984147497458, -191.3495495727129878 ) ) ;
#42986=VECTOR ( 'NONE', #26070, 1000.000000000000000 ) ;
#43028=ORIENTED_EDGE ( 'NONE', *, *, #201011, .T. ) ;
#43044=AXIS2_PLACEMENT_3D ( 'NONE', #121572, #237639, #19885 ) ;
#43050=EDGE_LOOP ( 'NONE', ( #33838, #2426, #106209, #178799 ) ) ;
#43067=AXIS2_PLACEMENT_3D ( 'NONE', #115151, #113864, #117711 ) ;
#43071=DIRECTION ( 'NONE',  ( 0.000000000000000000, 0.000000000000000000, -1.000000000000000000 ) ) ;
#43097=CARTESIAN_POINT ( 'NONE',  ( -23.25000000000000000, 85.00000000001251976, -179.9170766071767389 ) ) ;
#43105=CARTESIAN_POINT ( 'NONE',  ( 21.05000000000000071, 67.18479819544567988, -195.1025699878404112 ) ) ;
#43137=CARTESIAN_POINT ( 'NONE',  ( 18.47688499308726051, 85.46485595029653837, -163.3217597313869192 ) ) ;
#43159=CARTESIAN_POINT ( 'NONE',  ( -18.59999999999999787, 77.16412189325360771, -162.1082593989527254 ) ) ;
#43166=FACE_OUTER_BOUND ( 'NONE', #244326, .T. ) ;
#43173=EDGE_CURVE ( 'NONE', #246161, #78303, #176969, .T. ) ;
#43186=DIRECTION ( 'NONE',  ( 1.000000000000000000, 0.000000000000000000, 0.000000000000000000 ) ) ;
#43213=EDGE_CURVE ( 'NONE', #183861, #83659, #208216, .T. ) ;
#43227=TOROIDAL_SURFACE ( 'NONE', #188974, 11.90000000000000213, 0.1000000000000000056 ) ;
#43243=AXIS2_PLACEMENT_3D ( 'NONE', #121082, #78057, #38957 ) ;
#43253=VERTEX_POINT ( 'NONE', #107662 ) ;
#43267=EDGE_CURVE ( 'NONE', #8263, #156110, #200017, .T. ) ;
#43270=VERTEX_POINT ( 'NONE', #146763 ) ;
#43275=DIRECTION ( 'NONE',  ( 0.000000000000000000, 0.000000000000000000, 1.000000000000000000 ) ) ;
#43287=ORIENTED_EDGE ( 'NONE', *, *, #19168, .T. ) ;
#43325=DIRECTION ( 'NONE',  ( 1.000000000000000000, 0.000000000000000000, 0.000000000000000000 ) ) ;
#43392=EDGE_CURVE ( 'NONE', #99184, #257935, #75138, .T. ) ;
#43422=TOROIDAL_SURFACE ( 'NONE', #189175, 7.800000000000000711, 0.1000000000000000056 ) ;
#43437=EDGE_CURVE ( 'NONE', #16270, #28626, #29364, .T. ) ;
#43441=AXIS2_PLACEMENT_3D ( 'NONE', #80552, #160151, #100119 ) ;
#43445=VERTEX_POINT ( 'NONE', #153252 ) ;
#43461=DIRECTION ( 'NONE',  ( 0.000000000000000000, 0.000000000000000000, -1.000000000000000000 ) ) ;
#43465=AXIS2_PLACEMENT_3D ( 'NONE', #105168, #51629, #86913 ) ;
#43479=B_SPLINE_CURVE_WITH_KNOTS ( 'NONE', 3,
 ( #213786, #97663, #132985, #254179, #54709, #153870, #232089, #75589, #114687, #53431, #39017, #194255, #95124, #252906, #195537, #14334, #233381, #93834, #237210 ),
 .UNSPECIFIED., .F., .F.,
 ( 4, 3, 3, 3, 3, 3, 4 ),
 ( -2.000416914662652606E-06, 0.000000000000000000, 4.714008503744773841E-05, 9.979203887777149504E-05, 0.0001372215519229469133, 0.0001635031576220970250, 0.0001900083748504064938 ),
 .UNSPECIFIED. ) ;
#43544=DIRECTION ( 'NONE',  ( -1.000000000000000000, -0.000000000000000000, -0.000000000000000000 ) ) ;
#43609=CIRCLE ( 'NONE', #197708, 11.75000000000001066 ) ;
#43634=VERTEX_POINT ( 'NONE', #42261 ) ;
#43669=CIRCLE ( 'NONE', #88862, 0.09999999999999344136 ) ;
#43682=CARTESIAN_POINT ( 'NONE',  ( 20.53930447208010790, 67.02285131248760308, -195.0806003429519535 ) ) ;
#43687=ORIENTED_EDGE ( 'NONE', *, *, #124429, .T. ) ;
#43707=CARTESIAN_POINT ( 'NONE',  ( -22.50875500270927532, 76.10085791378739373, -215.2726746119222696 ) ) ;
#43716=EDGE_CURVE ( 'NONE', #124908, #98885, #225987, .T. ) ;
#43717=DIRECTION ( 'NONE',  ( 1.000000000000000000, 0.000000000000000000, 0.000000000000000000 ) ) ;
#43741=LINE ( 'NONE', #185815, #231251 ) ;
#43744=ORIENTED_EDGE ( 'NONE', *, *, #68585, .F. ) ;
#43761=DIRECTION ( 'NONE',  ( 0.7071067811865127117, 0.7071067811865821007, 0.000000000000000000 ) ) ;
#43810=CARTESIAN_POINT ( 'NONE',  ( -18.50000000000000000, 77.16412189325360771, -162.3082593989527425 ) ) ;
#43829=ADVANCED_FACE ( 'NONE', ( #13410 ), #172527, .T. ) ;
#43851=DIRECTION ( 'NONE',  ( -0.000000000000000000, 6.982962677686266711E-15, -1.000000000000000000 ) ) ;
#43861=CARTESIAN_POINT ( 'NONE',  ( 21.08376601933332495, 69.65805272873703302, -203.5868834954544013 ) ) ;
#43869=VECTOR ( 'NONE', #30992, 1000.000000000000000 ) ;
#43877=CIRCLE ( 'NONE', #39810, 0.4000000000000114575 ) ;
#43917=LINE ( 'NONE', #219984, #145132 ) ;
#43919=CARTESIAN_POINT ( 'NONE',  ( 23.14999999999999503, 69.45000000001252261, -182.3731074845244109 ) ) ;
#44046=EDGE_CURVE ( 'NONE', #209410, #69800, #179555, .T. ) ;
#44048=EDGE_CURVE ( 'NONE', #35701, #92871, #237796, .T. ) ;
#44103=FACE_OUTER_BOUND ( 'NONE', #16362, .T. ) ;
#44110=CARTESIAN_POINT ( 'NONE',  ( 20.85000000000000142, 77.83585931145600512, -158.5186683157258187 ) ) ;
#44137=ORIENTED_EDGE ( 'NONE', *, *, #220646, .F. ) ;
#44148=EDGE_CURVE ( 'NONE', #221522, #64517, #154621, .T. ) ;
#44151=ORIENTED_EDGE ( 'NONE', *, *, #187693, .F. ) ;
#44172=ORIENTED_EDGE ( 'NONE', *, *, #146107, .T. ) ;
#44182=AXIS2_PLACEMENT_3D ( 'NONE', #144913, #47090, #242733 ) ;
#44196=CARTESIAN_POINT ( 'NONE',  ( 18.52928932304156717, 65.72071067697093838, -178.8468540517211807 ) ) ;
#44207=CARTESIAN_POINT ( 'NONE',  ( -20.54999999999999716, 84.73084112150795022, -193.9250327655399531 ) ) ;
#44214=DIRECTION ( 'NONE',  ( 0.000000000000000000, -1.000000000000000000, 0.000000000000000000 ) ) ;
#44293=CARTESIAN_POINT ( 'NONE',  ( 21.05933563467872105, 65.27547528793127185, -191.3294597355684630 ) ) ;
#44331=FACE_OUTER_BOUND ( 'NONE', #115367, .T. ) ;
#44343=DIRECTION ( 'NONE',  ( 0.000000000000000000, 6.982962677686266711E-15, -1.000000000000000000 ) ) ;
#44346=CYLINDRICAL_SURFACE ( 'NONE', #50133, 0.09999999999999939493 ) ;
#44349=AXIS2_PLACEMENT_3D ( 'NONE', #165530, #243770, #148527 ) ;
#44367=ORIENTED_EDGE ( 'NONE', *, *, #162221, .T. ) ;
#44374=ORIENTED_EDGE ( 'NONE', *, *, #81196, .F. ) ;
#44377=DIRECTION ( 'NONE',  ( 1.000000000000000000, 0.000000000000000000, 0.000000000000000000 ) ) ;
#44411=AXIS2_PLACEMENT_3D ( 'NONE', #219007, #156517, #121246 ) ;
#44435=DIRECTION ( 'NONE',  ( 0.000000000000000000, 0.000000000000000000, 1.000000000000000000 ) ) ;
#44508=ORIENTED_EDGE ( 'NONE', *, *, #165027, .T. ) ;
#44517=DIRECTION ( 'NONE',  ( 1.000000000000000000, -0.000000000000000000, 0.000000000000000000 ) ) ;
#44548=LINE ( 'NONE', #41989, #144425 ) ;
#44561=CARTESIAN_POINT ( 'NONE',  ( 20.95496329884391784, 65.43256679391959096, -195.9487975522395971 ) ) ;
#44591=AXIS2_PLACEMENT_3D ( 'NONE', #96478, #37842, #157808 ) ;
#44600=ORIENTED_EDGE ( 'NONE', *, *, #89681, .F. ) ;
#44635=ORIENTED_EDGE ( 'NONE', *, *, #30774, .T. ) ;
#44665=TOROIDAL_SURFACE ( 'NONE', #73911, 11.65000000000000036, 0.1000000000000000056 ) ;
#44671=VERTEX_POINT ( 'NONE', #201364 ) ;
#44675=AXIS2_PLACEMENT_3D ( 'NONE', #70129, #49246, #128800 ) ;
#44692=CARTESIAN_POINT ( 'NONE',  ( -20.64999999999999858, 74.00000000001254818, -183.2477294072864709 ) ) ;
#44726=CARTESIAN_POINT ( 'NONE',  ( 18.59999999999999076, 64.35000000001251408, -178.6731074845244507 ) ) ;
#44751=CARTESIAN_POINT ( 'NONE',  ( -18.44362607810620247, 85.49049615809748559, -196.4651536176772311 ) ) ;
#44772=AXIS2_PLACEMENT_3D ( 'NONE', #164557, #208809, #168452 ) ;
#44781=CARTESIAN_POINT ( 'NONE',  ( 18.59999999999999076, 69.55000000001261640, -193.5060803140843859 ) ) ;
#44783=ORIENTED_EDGE ( 'NONE', *, *, #18277, .F. ) ;
#44797=ORIENTED_EDGE ( 'NONE', *, *, #226161, .T. ) ;
#44819=DIRECTION ( 'NONE',  ( -1.000000000000000000, 2.952720810173289112E-16, 2.061873921506763405E-30 ) ) ;
#44848=VECTOR ( 'NONE', #243155, 1000.000000000000000 ) ;
#44849=AXIS2_PLACEMENT_3D ( 'NONE', #17505, #136143, #97010 ) ;
#44853=DIRECTION ( 'NONE',  ( 1.000000000000000000, 0.000000000000000000, 0.000000000000000000 ) ) ;
#44880=AXIS2_PLACEMENT_3D ( 'NONE', #114957, #251894, #75833 ) ;
#44937=CARTESIAN_POINT ( 'NONE',  ( 21.06089410995835109, 65.27470446788900915, -191.3207267534812104 ) ) ;
#44962=EDGE_CURVE ( 'NONE', #110731, #77018, #116405, .T. ) ;
#44966=CARTESIAN_POINT ( 'NONE',  ( 20.58091095332318332, 66.98152984665888710, -195.1044573023666544 ) ) ;
#44979=VERTEX_POINT ( 'NONE', #176391 ) ;
#45003=ORIENTED_EDGE ( 'NONE', *, *, #40851, .F. ) ;
#45006=CYLINDRICAL_SURFACE ( 'NONE', #174497, 7.899999999999990585 ) ;
#45015=AXIS2_PLACEMENT_3D ( 'NONE', #88461, #115756, #216126 ) ;
#45026=ORIENTED_EDGE ( 'NONE', *, *, #66632, .F. ) ;
#45058=ORIENTED_EDGE ( 'NONE', *, *, #57682, .T. ) ;
#45069=DIRECTION ( 'NONE',  ( 0.000000000000000000, -6.997203936713175802E-15, 1.000000000000000000 ) ) ;
#45080=DIRECTION ( 'NONE',  ( 0.000000000000000000, -0.01562499999999307672, 0.9998779222360100194 ) ) ;
#45081=ORIENTED_EDGE ( 'NONE', *, *, #157731, .T. ) ;
#45088=CARTESIAN_POINT ( 'NONE',  ( -20.85000000000000142, 68.97833521811233481, -166.1895420826271277 ) ) ;
#45095=ORIENTED_EDGE ( 'NONE', *, *, #77527, .T. ) ;
#45098=ORIENTED_EDGE ( 'NONE', *, *, #146597, .T. ) ;
#45145=DIRECTION ( 'NONE',  ( 0.000000000000000000, 0.4999999999999088507, -0.8660254037844913322 ) ) ;
#45152=CARTESIAN_POINT ( 'NONE',  ( -18.50000000000000000, 64.35000000001268461, -203.4231074845244507 ) ) ;
#45156=ORIENTED_EDGE ( 'NONE', *, *, #30494, .T. ) ;
#45169=CIRCLE ( 'NONE', #82546, 0.6000000000000033085 ) ;
#45193=EDGE_CURVE ( 'NONE', #3812, #74995, #155181, .T. ) ;
#45244=EDGE_CURVE ( 'NONE', #248091, #256994, #55319, .T. ) ;
#45245=CARTESIAN_POINT ( 'NONE',  ( -21.46681500593004444, 69.14248884062553202, -203.5231074845244166 ) ) ;
#45255=DIRECTION ( 'NONE',  ( -1.000000000000000000, 0.000000000000000000, -0.000000000000000000 ) ) ;
#45264=CARTESIAN_POINT ( 'NONE',  ( 18.59999999999999076, 77.16412189325360771, -162.1082593989527254 ) ) ;
#45266=CARTESIAN_POINT ( 'NONE',  ( -20.00857864376270001, 66.85000000001259934, -191.2731074845244166 ) ) ;
#45286=CYLINDRICAL_SURFACE ( 'NONE', #250478, 11.80000000000000426 ) ;
#45298=CARTESIAN_POINT ( 'NONE',  ( -23.25000000000000000, 70.05000000001251692, -180.3288097895592159 ) ) ;
#45307=DIRECTION ( 'NONE',  ( 1.000000000000000000, -0.000000000000000000, 0.000000000000000000 ) ) ;
#45351=VECTOR ( 'NONE', #226430, 1000.000000000000000 ) ;
#45352=CARTESIAN_POINT ( 'NONE',  ( -20.85000000000000142, 76.00000000001239187, -162.1231074845243825 ) ) ;
#45372=VECTOR ( 'NONE', #55913, 1000.000000000000000 ) ;
#45376=EDGE_LOOP ( 'NONE', ( #173675, #60955, #130873, #47105 ) ) ;
#45401=DIRECTION ( 'NONE',  ( 2.952720810173289112E-16, 1.000000000000000000, 6.982962677686266711E-15 ) ) ;
#45407=DIRECTION ( 'NONE',  ( 1.000000000000000000, -2.952720810173289112E-16, -2.061873921506763405E-30 ) ) ;
#45435=CARTESIAN_POINT ( 'NONE',  ( 23.24999999999999289, 69.55000000001253113, -182.3731074845244109 ) ) ;
#45440=CARTESIAN_POINT ( 'NONE',  ( -23.15000000000000213, 76.00000000001244871, -170.0231074845243597 ) ) ;
#45457=DIRECTION ( 'NONE',  ( 1.000000000000000000, 0.000000000000000000, 0.000000000000000000 ) ) ;
#45461=DIRECTION ( 'NONE',  ( 1.000000000000000000, 0.000000000000000000, 0.000000000000000000 ) ) ;
#45465=CYLINDRICAL_SURFACE ( 'NONE', #258062, 0.09999999999998898659 ) ;
#45470=ORIENTED_EDGE ( 'NONE', *, *, #50223, .F. ) ;
#45489=VERTEX_POINT ( 'NONE', #71394 ) ;
#45490=DIRECTION ( 'NONE',  ( 1.000000000000000000, -2.952720810173289112E-16, -2.061873921506763405E-30 ) ) ;
#45546=AXIS2_PLACEMENT_3D ( 'NONE', #21547, #101016, #26699 ) ;
#45558=EDGE_CURVE ( 'NONE', #46643, #137948, #11412, .T. ) ;
#45579=CARTESIAN_POINT ( 'NONE',  ( -20.85000000000000142, 87.65000000001246860, -172.9231074845242802 ) ) ;
#45627=EDGE_LOOP ( 'NONE', ( #53257, #61398, #98764, #249649, #159832, #103194, #27542, #128745, #87260, #203777, #255056, #181368, #223270, #61473, #14296, #86027, #1330, #253553 ) ) ;
#45639=DIRECTION ( 'NONE',  ( 0.000000000000000000, -6.982962677686266711E-15, 1.000000000000000000 ) ) ;
#45654=ORIENTED_EDGE ( 'NONE', *, *, #2280, .T. ) ;
#45668=AXIS2_PLACEMENT_3D ( 'NONE', #237826, #37088, #257325 ) ;
#45669=CARTESIAN_POINT ( 'NONE',  ( 21.04999999999999716, 67.10527618163501984, -195.0360231613764199 ) ) ;
#45700=DIRECTION ( 'NONE',  ( -0.000000000000000000, 0.9908441862701591329, 0.1350103645451946055 ) ) ;
#45731=AXIS2_PLACEMENT_3D ( 'NONE', #139049, #80366, #219909 ) ;
#45743=PLANE ( 'NONE',  #58473 ) ;
#45795=ORIENTED_EDGE ( 'NONE', *, *, #67783, .F. ) ;
#45842=DIRECTION ( 'NONE',  ( -1.000000000000000000, 2.952720810173289112E-16, 2.061873921506763405E-30 ) ) ;
#45888=AXIS2_PLACEMENT_3D ( 'NONE', #212967, #171329, #172608 ) ;
#45919=CARTESIAN_POINT ( 'NONE',  ( -22.50000000000000000, 76.00000000001267608, -203.5231074845243597 ) ) ;
#45920=ORIENTED_EDGE ( 'NONE', *, *, #177417, .T. ) ;
#46000=ORIENTED_EDGE ( 'NONE', *, *, #55409, .T. ) ;
#46010=CARTESIAN_POINT ( 'NONE',  ( 19.97071067811865319, 64.27928932189384170, -178.8145288407617670 ) ) ;
#46018=CARTESIAN_POINT ( 'NONE',  ( 21.14999999999999858, 87.65000000001268177, -203.5231074845243029 ) ) ;
#46042=FACE_OUTER_BOUND ( 'NONE', #130943, .T. ) ;
#46048=VERTEX_POINT ( 'NONE', #78210 ) ;
#46049=CARTESIAN_POINT ( 'NONE',  ( -22.50000000000000000, 76.00000000001267608, -203.6231074845243540 ) ) ;
#46051=DIRECTION ( 'NONE',  ( -1.000000000000000000, 0.000000000000000000, -0.000000000000000000 ) ) ;
#46053=EDGE_LOOP ( 'NONE', ( #132084, #214058, #179526, #196938, #192010 ) ) ;
#46055=FACE_OUTER_BOUND ( 'NONE', #149182, .T. ) ;
#46086=CARTESIAN_POINT ( 'NONE',  ( 21.05000000000000071, 76.00000000001260503, -190.6481074845243597 ) ) ;
#46097=CARTESIAN_POINT ( 'NONE',  ( -20.85000000000000142, 87.75000000001246292, -170.0231074845242745 ) ) ;
#46101=EDGE_CURVE ( 'NONE', #223699, #227067, #184711, .T. ) ;
#46110=ADVANCED_FACE ( 'NONE', ( #101592 ), #220311, .T. ) ;
#46119=FACE_OUTER_BOUND ( 'NONE', #162485, .T. ) ;
#46130=DIRECTION ( 'NONE',  ( 0.000000000000000000, 0.000000000000000000, 1.000000000000000000 ) ) ;
#46135=DIRECTION ( 'NONE',  ( 0.000000000000000000, 1.000000000000000000, 6.982962677686266711E-15 ) ) ;
#46140=CARTESIAN_POINT ( 'NONE',  ( -18.50596464788227635, 65.69367753730709580, -164.5189238066348594 ) ) ;
#46178=CARTESIAN_POINT ( 'NONE',  ( -20.94999999999999929, 74.63912941282058000, -195.4501095574334215 ) ) ;
#46187=DIRECTION ( 'NONE',  ( -1.000000000000000000, 0.000000000000000000, -0.000000000000000000 ) ) ;
#46191=ORIENTED_EDGE ( 'NONE', *, *, #35440, .T. ) ;
#46242=FACE_OUTER_BOUND ( 'NONE', #66979, .T. ) ;
#46257=LINE ( 'NONE', #25437, #59887 ) ;
#46259=CARTESIAN_POINT ( 'NONE',  ( -22.50000000000094147, 75.90000000001286651, -215.1726782920691790 ) ) ;
#46261=( BOUNDED_SURFACE ( )  B_SPLINE_SURFACE ( 3, 2, ( 
 ( #130827, #171296, #151714 ),
 ( #58962, #176400, #14767 ),
 ( #117684, #77263, #296 ),
 ( #98086, #235079, #55110 ) ),
 .UNSPECIFIED., .F., .F., .F. ) 
 B_SPLINE_SURFACE_WITH_KNOTS ( ( 4, 4 ),
 ( 3, 3 ),
 ( -1.044899843732904898E-17, 0.0003124336600439518762 ),
 ( 0.000000000000000000, 1.000000000000000000 ),
 .UNSPECIFIED. ) 
 GEOMETRIC_REPRESENTATION_ITEM ( )  RATIONAL_B_SPLINE_SURFACE ( (
 ( 1.000000000000000000, 0.7071067811864494290, 1.000000000000000000),
 ( 1.000000000000000000, 0.7089187706050879001, 1.000000000000000000),
 ( 1.000000000000000000, 0.7039288185050927016, 1.000000000000000000),
 ( 1.000000000000000000, 0.7040654476015839602, 1.000000000000000000) ) ) 
 REPRESENTATION_ITEM ( '' )  SURFACE ( )  );
#46265=DIRECTION ( 'NONE',  ( 0.000000000000000000, -7.272083257015735086E-15, 1.000000000000000000 ) ) ;
#46269=VECTOR ( 'NONE', #82657, 1000.000000000000000 ) ;
#46295=CARTESIAN_POINT ( 'NONE',  ( -21.55000000000000071, 68.65000000001261071, -191.1731074845243938 ) ) ;
#46315=CARTESIAN_POINT ( 'NONE',  ( -20.94999999999999929, 65.70711192142420032, -164.5651054685122574 ) ) ;
#46329=ORIENTED_EDGE ( 'NONE', *, *, #6699, .F. ) ;
#46354=DIRECTION ( 'NONE',  ( 0.000000000000000000, 0.000000000000000000, -1.000000000000000000 ) ) ;
#46361=( BOUNDED_SURFACE ( )  B_SPLINE_SURFACE ( 3, 2, ( 
 ( #162385, #247026, #222307 ),
 ( #164934, #24161, #43707 ),
 ( #22883, #103651, #5839 ),
 ( #46259, #184485, #144066 ) ),
 .UNSPECIFIED., .F., .F., .F. ) 
 B_SPLINE_SURFACE_WITH_KNOTS ( ( 4, 4 ),
 ( 3, 3 ),
 ( -5.692061405548898279E-19, 0.0003124336117481333599 ),
 ( 0.000000000000000000, 1.000000000000000000 ),
 .UNSPECIFIED. ) 
 GEOMETRIC_REPRESENTATION_ITEM ( )  RATIONAL_B_SPLINE_SURFACE ( (
 ( 1.000000000000000000, 0.7040654476014845953, 1.000000000000000000),
 ( 1.000000000000000000, 0.7039193538783811155, 1.000000000000000000),
 ( 1.000000000000000000, 0.7089171279145194404, 1.000000000000000000),
 ( 1.000000000000000000, 0.7071067811865509034, 1.000000000000000000) ) ) 
 REPRESENTATION_ITEM ( '' )  SURFACE ( )  );
#46372=SPHERICAL_SURFACE ( 'NONE', #256939, 0.1000000000000000056 ) ;
#46393=DIRECTION ( 'NONE',  ( -1.040834085586090694E-13, 0.1568667991644355497, 0.9876197685951332295 ) ) ;
#46420=EDGE_CURVE ( 'NONE', #227800, #127123, #58317, .T. ) ;
#46431=EDGE_CURVE ( 'NONE', #121283, #191888, #118280, .T. ) ;
#46449=ORIENTED_EDGE ( 'NONE', *, *, #50583, .T. ) ;
#46482=CARTESIAN_POINT ( 'NONE',  ( 21.05000000000000071, 64.40000000001248281, -176.9513107147999449 ) ) ;
#46498=ORIENTED_EDGE ( 'NONE', *, *, #255873, .T. ) ;
#46503=EDGE_CURVE ( 'NONE', #231047, #200485, #255783, .T. ) ;
#46509=DIRECTION ( 'NONE',  ( -1.000000000000000000, 0.000000000000000000, 0.000000000000000000 ) ) ;
#46518=VERTEX_POINT ( 'NONE', #201703 ) ;
#46529=DIRECTION ( 'NONE',  ( 0.000000000000000000, -1.000000000000000000, -6.982962677686266711E-15 ) ) ;
#46549=DIRECTION ( 'NONE',  ( -1.000000000000000000, 0.000000000000000000, 0.000000000000000000 ) ) ;
#46553=CARTESIAN_POINT ( 'NONE',  ( -21.05000000000000071, 76.00000000001244871, -170.0231074845243597 ) ) ;
#46603=AXIS2_PLACEMENT_3D ( 'NONE', #213236, #52882, #132435 ) ;
#46606=VERTEX_POINT ( 'NONE', #127305 ) ;
#46637=ORIENTED_EDGE ( 'NONE', *, *, #208165, .T. ) ;
#46643=VERTEX_POINT ( 'NONE', #90729 ) ;
#46669=FACE_OUTER_BOUND ( 'NONE', #99026, .T. ) ;
#46728=CARTESIAN_POINT ( 'NONE',  ( 23.14999999999999503, 69.35000000001254250, -182.3731074845244109 ) ) ;
#46733=DIRECTION ( 'NONE',  ( -0.000000000000000000, 1.000000000000000000, 6.982962677686266711E-15 ) ) ;
#46736=DIRECTION ( 'NONE',  ( -1.000000000000000000, -0.000000000000000000, -0.000000000000000000 ) ) ;
#46781=CARTESIAN_POINT ( 'NONE',  ( -18.50000000000000000, 74.13328508995527955, -191.7704322382423641 ) ) ;
#46795=CARTESIAN_POINT ( 'NONE',  ( 18.49999999999999645, 76.00000000001244871, -170.0231074845243597 ) ) ;
#46808=CIRCLE ( 'NONE', #25993, 0.09999999999999939493 ) ;
#46820=CARTESIAN_POINT ( 'NONE',  ( -20.94999999999999929, 77.83534155023700407, -191.8679561919613832 ) ) ;
#46821=AXIS2_PLACEMENT_3D ( 'NONE', #24488, #124852, #40206 ) ;
#46825=CARTESIAN_POINT ( 'NONE',  ( -18.50000000000000000, 68.97833521811233481, -166.1895420826271277 ) ) ;
#46831=EDGE_LOOP ( 'NONE', ( #249236, #151512, #151586, #100784 ) ) ;
#46843=CIRCLE ( 'NONE', #17620, 0.5000000000000004441 ) ;
#46877=CIRCLE ( 'NONE', #134356, 0.5000000000000004441 ) ;
#46945=ORIENTED_EDGE ( 'NONE', *, *, #223149, .T. ) ;
#46963=CARTESIAN_POINT ( 'NONE',  ( 18.54147908293604985, 85.46326165794067720, -196.4741585877683860 ) ) ;
#46967=AXIS2_PLACEMENT_3D ( 'NONE', #181530, #204907, #241491 ) ;
#46975=CARTESIAN_POINT ( 'NONE',  ( -21.05000000000000071, 64.25000000001264766, -196.7392418215463010 ) ) ;
#46984=CARTESIAN_POINT ( 'NONE',  ( 23.24999999999999289, 70.05000000001251692, -180.3288097895592159 ) ) ;
#46996=LINE ( 'NONE', #228240, #32278 ) ;
#47006=VECTOR ( 'NONE', #136358, 1000.000000000000000 ) ;
#47017=VERTEX_POINT ( 'NONE', #111304 ) ;
#47082=DIRECTION ( 'NONE',  ( 0.000000000000000000, -6.454785026890406770E-15, 1.000000000000000000 ) ) ;
#47090=DIRECTION ( 'NONE',  ( -1.000000000000000000, 2.952720810173289112E-16, 2.061873921506763405E-30 ) ) ;
#47101=CARTESIAN_POINT ( 'NONE',  ( -20.54999999999999716, 71.65000000001259650, -191.1731074845243654 ) ) ;
#47105=ORIENTED_EDGE ( 'NONE', *, *, #45558, .F. ) ;
#47118=DIRECTION ( 'NONE',  ( 0.000000000000000000, 0.000000000000000000, 1.000000000000000000 ) ) ;
#47163=CARTESIAN_POINT ( 'NONE',  ( 18.59999999999999432, 77.86671491006991630, -191.7704322382423356 ) ) ;
#47165=AXIS2_PLACEMENT_3D ( 'NONE', #56311, #249405, #13359 ) ;
#47167=DIRECTION ( 'NONE',  ( 1.000000000000000000, 0.000000000000000000, 0.000000000000000000 ) ) ;
#47173=EDGE_LOOP ( 'NONE', ( #63670, #217434, #99283, #227176 ) ) ;
#47193=PRODUCT_DEFINITION_SHAPE ( 'NONE', 'NONE',  #168000 ) ;
#47224=EDGE_CURVE ( 'NONE', #239420, #202942, #222083, .T. ) ;
#47228=ORIENTED_EDGE ( 'NONE', *, *, #58117, .F. ) ;
#47240=EDGE_CURVE ( 'NONE', #164247, #167877, #5606, .T. ) ;
#47257=ORIENTED_EDGE ( 'NONE', *, *, #181829, .F. ) ;
#47261=ORIENTED_EDGE ( 'NONE', *, *, #144846, .F. ) ;
#47276=CYLINDRICAL_SURFACE ( 'NONE', #229577, 11.80000000000000426 ) ;
#47281=CARTESIAN_POINT ( 'NONE',  ( -18.45068461519106151, 85.48650652910174585, -196.4543303156196146 ) ) ;
#47284=CARTESIAN_POINT ( 'NONE',  ( -18.59999999999999787, 76.00000000001267608, -203.5231074845243597 ) ) ;
#47303=( LENGTH_UNIT ( ) NAMED_UNIT ( * ) SI_UNIT ( .MILLI., .METRE. ) );
#47314=AXIS2_PLACEMENT_3D ( 'NONE', #63361, #124643, #85467 ) ;
#47318=ORIENTED_EDGE ( 'NONE', *, *, #61373, .F. ) ;
#47322=EDGE_CURVE ( 'NONE', #236908, #3727, #25064, .T. ) ;
#47339=EDGE_CURVE ( 'NONE', #29575, #180641, #226368, .T. ) ;
#47352=EDGE_CURVE ( 'NONE', #228403, #46643, #68183, .T. ) ;
#47364=CARTESIAN_POINT ( 'NONE',  ( -20.07928932188135107, 66.77928932189394118, -191.1731074845244223 ) ) ;
#47367=CARTESIAN_POINT ( 'NONE',  ( -23.25000000000000000, 77.83585931145600512, -158.4186683157258244 ) ) ;
#47393=CARTESIAN_POINT ( 'NONE',  ( 18.59999999999999076, 64.35000000001251408, -178.6731074845244507 ) ) ;
#47403=CARTESIAN_POINT ( 'NONE',  ( -20.85000000000000142, 87.65000000001245439, -170.0231074845242745 ) ) ;
#47404=VERTEX_POINT ( 'NONE', #168454 ) ;
#47411=DIRECTION ( 'NONE',  ( 0.000000000000000000, 0.000000000000000000, 1.000000000000000000 ) ) ;
#47416=FACE_OUTER_BOUND ( 'NONE', #199726, .T. ) ;
#47442=ORIENTED_EDGE ( 'NONE', *, *, #107138, .T. ) ;
#47457=EDGE_CURVE ( 'NONE', #177284, #100958, #172465, .T. ) ;
#47481=EDGE_LOOP ( 'NONE', ( #150356, #249660, #8212, #180630 ) ) ;
#47502=ORIENTED_EDGE ( 'NONE', *, *, #71685, .F. ) ;
#47504=DIRECTION ( 'NONE',  ( 1.000000000000000000, 0.000000000000000000, 0.000000000000000000 ) ) ;
#47521=ORIENTED_EDGE ( 'NONE', *, *, #43267, .T. ) ;
#47523=ORIENTED_EDGE ( 'NONE', *, *, #254209, .T. ) ;
#47552=CARTESIAN_POINT ( 'NONE',  ( -20.94999999999999929, 74.83729825007462466, -195.4231074845243654 ) ) ;
#47565=EDGE_CURVE ( 'NONE', #182093, #200908, #218181, .T. ) ;
#47570=CYLINDRICAL_SURFACE ( 'NONE', #17349, 0.09999999999998898659 ) ;
#47596=CARTESIAN_POINT ( 'NONE',  ( -20.94999675878240808, 65.70692517833285251, -164.5644653378304270 ) ) ;
#47620=ORIENTED_EDGE ( 'NONE', *, *, #14613, .T. ) ;
#47621=DIRECTION ( 'NONE',  ( 0.000000000000000000, 0.000000000000000000, 1.000000000000000000 ) ) ;
#47633=CARTESIAN_POINT ( 'NONE',  ( 18.54271179734073982, 85.62408429011104261, -163.2821426318238593 ) ) ;
#47635=CYLINDRICAL_SURFACE ( 'NONE', #184873, 12.87499999999999822 ) ;
#47657=EDGE_CURVE ( 'NONE', #165694, #59994, #184877, .T. ) ;
#47726=DIRECTION ( 'NONE',  ( 0.000000000000000000, -7.086529944415886769E-15, 1.000000000000000000 ) ) ;
#47780=( BOUNDED_SURFACE ( )  B_SPLINE_SURFACE ( 3, 2, ( 
 ( #108908, #248430, #69810 ),
 ( #209294, #51477, #52776 ),
 ( #30693, #110188, #189741 ),
 ( #111485, #191050, #12410 ),
 ( #33273, #112773, #192313 ),
 ( #93196, #133608, #97014 ),
 ( #176616, #74958, #37110 ),
 ( #157047, #114037, #138710 ),
 ( #196155, #99593, #18794 ),
 ( #505, #257347, #216986 ) ),
 .UNSPECIFIED., .F., .F., .F. ) 
 B_SPLINE_SURFACE_WITH_KNOTS ( ( 4, 2, 2, 2, 4 ),
 ( 3, 3 ),
 ( 0.0001836757140119112878, 0.0004000170051583610588, 0.0005081876507315859172, 0.0005622729735181982921, 0.0006163582963048107755 ),
 ( 0.000000000000000000, 1.000000000000000000 ),
 .UNSPECIFIED. ) 
 GEOMETRIC_REPRESENTATION_ITEM ( )  RATIONAL_B_SPLINE_SURFACE ( (
 ( 1.000000000000000000, 0.7071067811865475727, 1.000000000000000000),
 ( 1.000000000000000000, 0.6461995200012254914, 1.000000000000000000),
 ( 1.000000000000000000, 0.5776453529573883916, 1.000000000000000000),
 ( 1.000000000000000000, 0.4585233068339760187, 1.000000000000000000),
 ( 1.000000000000000000, 0.4154092989943317660, 1.000000000000000000),
 ( 1.000000000000000000, 0.3550093145834672392, 1.000000000000000000),
 ( 1.000000000000000000, 0.3354498651689156175, 1.000000000000000000),
 ( 1.000000000000000000, 0.3060347992252056004, 1.000000000000000000),
 ( 1.000000000000000000, 0.2963555829629416771, 1.000000000000000000),
 ( 1.000000000000000000, 0.2966190024560776406, 1.000000000000000000) ) ) 
 REPRESENTATION_ITEM ( '' )  SURFACE ( )  );
#47785=DIRECTION ( 'NONE',  ( 1.000000000000000000, -0.000000000000000000, 0.000000000000000000 ) ) ;
#47823=AXIS2_PLACEMENT_3D ( 'NONE', #163590, #183158, #82720 ) ;
#47857=AXIS2_PLACEMENT_3D ( 'NONE', #244107, #2923, #82444 ) ;
#47901=CIRCLE ( 'NONE', #193676, 0.09999999999998898659 ) ;
#47903=FACE_BOUND ( 'NONE', #97171, .T. ) ;
#47960=DIRECTION ( 'NONE',  ( 1.000000000000000000, -3.265361837132813093E-16, -2.280189983783949500E-30 ) ) ;
#48000=DIRECTION ( 'NONE',  ( -1.000000000000000000, 0.000000000000000000, -0.000000000000000000 ) ) ;
#48024=DIRECTION ( 'NONE',  ( 1.000000000000000000, 0.000000000000000000, 0.000000000000000000 ) ) ;
#48034=ORIENTED_EDGE ( 'NONE', *, *, #215391, .F. ) ;
#48108=VECTOR ( 'NONE', #217839, 1000.000000000000000 ) ;
#48121=DIRECTION ( 'NONE',  ( 1.000000000000000000, 0.000000000000000000, 0.000000000000000000 ) ) ;
#48136=DIRECTION ( 'NONE',  ( 0.000000000000000000, 0.000000000000000000, 1.000000000000000000 ) ) ;
#48139=CARTESIAN_POINT ( 'NONE',  ( -20.54999999999999716, 71.75000000001259082, -191.1731074845243654 ) ) ;
#48171=ORIENTED_EDGE ( 'NONE', *, *, #141247, .F. ) ;
#48211=ORIENTED_EDGE ( 'NONE', *, *, #247706, .F. ) ;
#48219=EDGE_CURVE ( 'NONE', #227674, #179110, #43609, .T. ) ;
#48255=VERTEX_POINT ( 'NONE', #94323 ) ;
#48270=DIRECTION ( 'NONE',  ( -0.000000000000000000, -6.982962677686266711E-15, 1.000000000000000000 ) ) ;
#48276=ORIENTED_EDGE ( 'NONE', *, *, #135447, .T. ) ;
#48288=DIRECTION ( 'NONE',  ( 0.000000000000000000, -6.982962677686266711E-15, 1.000000000000000000 ) ) ;
#48306=AXIS2_PLACEMENT_3D ( 'NONE', #103108, #22338, #206088 ) ;
#48315=VERTEX_POINT ( 'NONE', #214289 ) ;
#48319=EDGE_LOOP ( 'NONE', ( #96769, #249618, #117830, #29257 ) ) ;
#48322=CARTESIAN_POINT ( 'NONE',  ( 20.95512820512820440, 67.12384868372441815, -182.2731074845244166 ) ) ;
#48348=DIRECTION ( 'NONE',  ( 0.000000000000000000, 6.938893903907222067E-15, -1.000000000000000000 ) ) ;
#48442=EDGE_CURVE ( 'NONE', #60192, #105425, #27064, .T. ) ;
#48471=ORIENTED_EDGE ( 'NONE', *, *, #215022, .T. ) ;
#48480=EDGE_CURVE ( 'NONE', #63948, #257629, #119246, .T. ) ;
#48501=ORIENTED_EDGE ( 'NONE', *, *, #237600, .F. ) ;
#48502=CIRCLE ( 'NONE', #81784, 0.4000000000000114575 ) ;
#48522=DIRECTION ( 'NONE',  ( 1.000000000000000000, 0.000000000000000000, 0.000000000000000000 ) ) ;
#48533=EDGE_CURVE ( 'NONE', #105425, #172898, #35451, .T. ) ;
#48562=CARTESIAN_POINT ( 'NONE',  ( -18.59999999999999787, 69.15387683765983695, -166.2853812176745691 ) ) ;
#48579=DIRECTION ( 'NONE',  ( 1.000000000000000000, 0.000000000000000000, 0.000000000000000000 ) ) ;
#48589=DIRECTION ( 'NONE',  ( 0.000000000000000000, 0.000000000000000000, 1.000000000000000000 ) ) ;
#48591=AXIS2_PLACEMENT_3D ( 'NONE', #150377, #9561, #111238 ) ;
#48611=CYLINDRICAL_SURFACE ( 'NONE', #42309, 0.09999999999998898659 ) ;
#48627=CARTESIAN_POINT ( 'NONE',  ( -20.94999999999999929, 87.41227409416215721, -172.9231074845242802 ) ) ;
#48646=VECTOR ( 'NONE', #91608, 1000.000000000000114 ) ;
#48674=ORIENTED_EDGE ( 'NONE', *, *, #132492, .T. ) ;
#48694=EDGE_CURVE ( 'NONE', #139578, #239511, #229701, .T. ) ;
#48699=DIRECTION ( 'NONE',  ( -0.000000000000000000, -6.982962677686266711E-15, 1.000000000000000000 ) ) ;
#48704=CARTESIAN_POINT ( 'NONE',  ( -18.50000000000000000, 65.70729864261058140, -164.5657455973725121 ) ) ;
#48725=CARTESIAN_POINT ( 'NONE',  ( 20.84999999999999432, 77.16412189325360771, -162.1082593989527254 ) ) ;
#48733=AXIS2_PLACEMENT_3D ( 'NONE', #94149, #133291, #9478 ) ;
#48759=AXIS2_PLACEMENT_3D ( 'NONE', #45266, #240906, #62263 ) ;
#48769=ADVANCED_FACE ( 'NONE', ( #134419 ), #94318, .F. ) ;
#48881=DIRECTION ( 'NONE',  ( 0.000000000000000000, -0.1350103645451945777, 0.9908441862701590219 ) ) ;
#48909=AXIS2_PLACEMENT_3D ( 'NONE', #180131, #96688, #215386 ) ;
#48967=CARTESIAN_POINT ( 'NONE',  ( 18.39999999999999858, 85.51932773110506503, -196.5501311079649724 ) ) ;
#48991=CARTESIAN_POINT ( 'NONE',  ( 18.59999999999999787, 77.73670573947995877, -158.5056848969006182 ) ) ;
#49015=DIRECTION ( 'NONE',  ( 2.952720810173289112E-16, 1.000000000000000000, 7.086529944415894657E-15 ) ) ;
#49082=EDGE_LOOP ( 'NONE', ( #34022, #236839, #16387, #219436, #126342, #7928, #132008, #42759, #165319, #47442 ) ) ;
#49120=CARTESIAN_POINT ( 'NONE',  ( 22.39999999999999503, 76.10085836911147794, -215.2726746080137445 ) ) ;
#49160=ADVANCED_FACE ( 'NONE', ( #6996 ), #206489, .F. ) ;
#49162=EDGE_LOOP ( 'NONE', ( #97576, #221972, #47261, #21108 ) ) ;
#49189=ADVANCED_FACE ( 'NONE', ( #46119 ), #210350, .F. ) ;
#49209=CARTESIAN_POINT ( 'NONE',  ( -18.50000000000000000, 77.16412189325360771, -162.1082593989527254 ) ) ;
#49217=ORIENTED_EDGE ( 'NONE', *, *, #96471, .T. ) ;
#49244=AXIS2_PLACEMENT_3D ( 'NONE', #92967, #120282, #142362 ) ;
#49246=DIRECTION ( 'NONE',  ( 1.000000000000000000, 0.000000000000000000, 0.000000000000000000 ) ) ;
#49253=ORIENTED_EDGE ( 'NONE', *, *, #114664, .T. ) ;
#49303=AXIS2_PLACEMENT_3D ( 'NONE', #61563, #100648, #257136 ) ;
#49331=DIRECTION ( 'NONE',  ( -1.000000000000000000, 3.265361837132813093E-16, 2.280189983783949500E-30 ) ) ;
#49378=FACE_OUTER_BOUND ( 'NONE', #126303, .T. ) ;
#49379=VECTOR ( 'NONE', #157822, 1000.000000000000000 ) ;
#49388=FACE_OUTER_BOUND ( 'NONE', #112711, .T. ) ;
#49454=AXIS2_PLACEMENT_3D ( 'NONE', #240348, #61697, #222024 ) ;
#49512=VECTOR ( 'NONE', #193592, 1000.000000000000000 ) ;
#49513=CIRCLE ( 'NONE', #141109, 0.09999999999998898659 ) ;
#49522=CIRCLE ( 'NONE', #195297, 0.09999999999998898659 ) ;
#49540=AXIS2_PLACEMENT_3D ( 'NONE', #192535, #170449, #34770 ) ;
#49567=ORIENTED_EDGE ( 'NONE', *, *, #209613, .T. ) ;
#49601=DIRECTION ( 'NONE',  ( 0.000000000000000000, 0.000000000000000000, -1.000000000000000000 ) ) ;
#49607=EDGE_CURVE ( 'NONE', #183161, #44671, #220010, .T. ) ;
#49621=EDGE_CURVE ( 'NONE', #154576, #36482, #84913, .T. ) ;
#49634=FACE_OUTER_BOUND ( 'NONE', #182064, .T. ) ;
#49660=CARTESIAN_POINT ( 'NONE',  ( 23.14999999999999858, 76.00000000001244871, -170.0231074845243597 ) ) ;
#49662=CIRCLE ( 'NONE', #62142, 11.64999999999999325 ) ;
#49672=DIRECTION ( 'NONE',  ( 1.000000000000000000, 0.000000000000000000, 0.000000000000000000 ) ) ;
#49732=DIRECTION ( 'NONE',  ( 0.000000000000000000, -7.272083257015735086E-15, 1.000000000000000000 ) ) ;
#49743=EDGE_CURVE ( 'NONE', #226489, #254689, #133072, .T. ) ;
#49787=CARTESIAN_POINT ( 'NONE',  ( 22.50000000000000000, 75.90000000001276703, -215.1726782920691505 ) ) ;
#49824=CARTESIAN_POINT ( 'NONE',  ( -21.04999999999999716, 69.70076908992041353, -203.6215449845247178 ) ) ;
#49835=ORIENTED_EDGE ( 'NONE', *, *, #227825, .T. ) ;
#49841=VERTEX_POINT ( 'NONE', #1232 ) ;
#49859=VERTEX_POINT ( 'NONE', #46781 ) ;
#49889=DIRECTION ( 'NONE',  ( -0.9880948137434723000, -0.1538461538461483591, -1.074301950413233512E-15 ) ) ;
#49905=ADVANCED_FACE ( 'NONE', ( #24700 ), #124528, .T. ) ;
#49923=DIRECTION ( 'NONE',  ( -1.000000000000000000, -0.000000000000000000, -0.000000000000000000 ) ) ;
#49959=CARTESIAN_POINT ( 'NONE',  ( -18.59999999999999787, 85.50000000001263345, -195.4231074845242802 ) ) ;
#49974=FACE_OUTER_BOUND ( 'NONE', #98947, .T. ) ;
#49980=CARTESIAN_POINT ( 'NONE',  ( -21.05000000000000071, 75.74389420792046224, -203.5580039261966760 ) ) ;
#49997=DIRECTION ( 'NONE',  ( 0.000000000000000000, -6.982962677686266711E-15, 1.000000000000000000 ) ) ;
#50019=EDGE_CURVE ( 'NONE', #75576, #222999, #49513, .T. ) ;
#50045=EDGE_CURVE ( 'NONE', #81897, #51105, #220215, .T. ) ;
#50057=AXIS2_PLACEMENT_3D ( 'NONE', #10203, #144547, #45461 ) ;
#50059=EDGE_LOOP ( 'NONE', ( #226317, #84254, #31123, #118779 ) ) ;
#50062=CIRCLE ( 'NONE', #116703, 0.1000000000000070832 ) ;
#50068=ORIENTED_EDGE ( 'NONE', *, *, #127798, .T. ) ;
#50072=ORIENTED_EDGE ( 'NONE', *, *, #214933, .F. ) ;
#50073=CARTESIAN_POINT ( 'NONE',  ( -22.47071067811865319, 68.27992525551462677, -203.6221999392270448 ) ) ;
#50089=ADVANCED_FACE ( 'NONE', ( #54495 ), #190175, .T. ) ;
#50124=ORIENTED_EDGE ( 'NONE', *, *, #6521, .T. ) ;
#50133=AXIS2_PLACEMENT_3D ( 'NONE', #82145, #203416, #85992 ) ;
#50144=DIRECTION ( 'NONE',  ( 0.000000000000000000, 0.000000000000000000, 1.000000000000000000 ) ) ;
#50167=PLANE ( 'NONE',  #16064 ) ;
#50180=ORIENTED_EDGE ( 'NONE', *, *, #43267, .F. ) ;
#50193=LINE ( 'NONE', #111471, #157838 ) ;
#50200=EDGE_LOOP ( 'NONE', ( #104220, #50981, #97996, #175103 ) ) ;
#50205=DIRECTION ( 'NONE',  ( 1.000000000000000000, 0.000000000000000000, 0.000000000000000000 ) ) ;
#50223=EDGE_CURVE ( 'NONE', #185777, #228133, #3908, .T. ) ;
#50255=VERTEX_POINT ( 'NONE', #37521 ) ;
#50257=EDGE_CURVE ( 'NONE', #122787, #232039, #112260, .T. ) ;
#50288=EDGE_CURVE ( 'NONE', #248274, #25370, #89045, .T. ) ;
#50295=ORIENTED_EDGE ( 'NONE', *, *, #4902, .T. ) ;
#50315=DIRECTION ( 'NONE',  ( -1.000000000000000000, 2.952720810173289112E-16, 2.061873921506763405E-30 ) ) ;
#50330=DIRECTION ( 'NONE',  ( -1.000000000000000000, -0.000000000000000000, -0.000000000000000000 ) ) ;
#50338=CARTESIAN_POINT ( 'NONE',  ( 21.05000000000000071, 69.35000000001262777, -193.5060803140843859 ) ) ;
#50356=DIRECTION ( 'NONE',  ( 0.000000000000000000, -6.982962677686266711E-15, 1.000000000000000000 ) ) ;
#50415=EDGE_CURVE ( 'NONE', #196072, #182596, #24786, .T. ) ;
#50416=CARTESIAN_POINT ( 'NONE',  ( -18.59999999999999787, 74.83729825007462466, -195.4231074845243654 ) ) ;
#50422=CYLINDRICAL_SURFACE ( 'NONE', #102794, 0.09999999999999939493 ) ;
#50463=CARTESIAN_POINT ( 'NONE',  ( -21.05000000000000071, 76.00000000001247713, -174.0231074845243882 ) ) ;
#50481=EDGE_LOOP ( 'NONE', ( #142133, #61938, #124676, #89845, #144966, #72186, #200143, #232018, #180418 ) ) ;
#50507=CARTESIAN_POINT ( 'NONE',  ( -21.53752568622148900, 75.90102553874208979, -210.3099153590730168 ) ) ;
#50524=AXIS2_PLACEMENT_3D ( 'NONE', #37507, #239548, #19212 ) ;
#50551=EDGE_CURVE ( 'NONE', #238502, #187182, #223206, .T. ) ;
#50583=EDGE_CURVE ( 'NONE', #177267, #166644, #16579, .T. ) ;
#50587=VERTEX_POINT ( 'NONE', #186676 ) ;
#50590=DIRECTION ( 'NONE',  ( 1.000000000000000000, -7.304098846218134667E-16, -5.100424963727256530E-30 ) ) ;
#50596=CARTESIAN_POINT ( 'NONE',  ( 23.14999999999999858, 76.00000000001244871, -170.0231074845243597 ) ) ;
#50656=CIRCLE ( 'NONE', #142259, 4.150000000000001243 ) ;
#50673=CARTESIAN_POINT ( 'NONE',  ( -23.25000000000000000, 69.06610602788607878, -166.2374616501508342 ) ) ;
#50688=ORIENTED_EDGE ( 'NONE', *, *, #61213, .F. ) ;
#50737=VECTOR ( 'NONE', #190475, 1000.000000000000000 ) ;
#50804=ORIENTED_EDGE ( 'NONE', *, *, #161872, .T. ) ;
#50810=ORIENTED_EDGE ( 'NONE', *, *, #256161, .T. ) ;
#50838=DIRECTION ( 'NONE',  ( 1.000000000000000000, 0.000000000000000000, 0.000000000000000000 ) ) ;
#50901=CARTESIAN_POINT ( 'NONE',  ( 23.14999999999999858, 71.00000000001253397, -182.4283735034374843 ) ) ;
#50910=EDGE_CURVE ( 'NONE', #46606, #82861, #104210, .T. ) ;
#50962=CIRCLE ( 'NONE', #205085, 0.09999999999999939493 ) ;
#50967=EDGE_LOOP ( 'NONE', ( #219448, #128214, #44600, #195415 ) ) ;
#50969=CARTESIAN_POINT ( 'NONE',  ( 18.59999999999999787, 76.00000000001267608, -203.5231074845243597 ) ) ;
#50981=ORIENTED_EDGE ( 'NONE', *, *, #119195, .F. ) ;
#51004=DIRECTION ( 'NONE',  ( 0.000000000000000000, -0.4999999999999943379, -0.8660254037844420383 ) ) ;
#51049=ORIENTED_EDGE ( 'NONE', *, *, #213842, .T. ) ;
#51059=ORIENTED_EDGE ( 'NONE', *, *, #30774, .F. ) ;
#51060=DIRECTION ( 'NONE',  ( -1.000000000000000000, 0.000000000000000000, 0.000000000000000000 ) ) ;
#51099=ORIENTED_EDGE ( 'NONE', *, *, #210839, .F. ) ;
#51100=VERTEX_POINT ( 'NONE', #156239 ) ;
#51105=VERTEX_POINT ( 'NONE', #196609 ) ;
#51110=EDGE_LOOP ( 'NONE', ( #97248, #213765, #104614, #148656, #77567 ) ) ;
#51121=ADVANCED_FACE ( 'NONE', ( #93667 ), #151082, .T. ) ;
#51122=AXIS2_PLACEMENT_3D ( 'NONE', #231608, #254944, #75120 ) ;
#51151=FILL_AREA_STYLE_COLOUR ( '', #135321 ) ;
#51190=AXIS2_PLACEMENT_3D ( 'NONE', #90706, #127279, #206815 ) ;
#51233=CARTESIAN_POINT ( 'NONE',  ( 20.91682497891422798, 65.67736539654997330, -164.4625116876572406 ) ) ;
#51237=EDGE_CURVE ( 'NONE', #96257, #183594, #108696, .T. ) ;
#51269=ORIENTED_EDGE ( 'NONE', *, *, #97676, .T. ) ;
#51270=AXIS2_PLACEMENT_3D ( 'NONE', #3808, #221540, #159057 ) ;
#51273=AXIS2_PLACEMENT_3D ( 'NONE', #175260, #33183, #13588 ) ;
#51274=CARTESIAN_POINT ( 'NONE',  ( 20.94999999999999574, 67.07338541492552508, -195.0514244653012952 ) ) ;
#51279=ORIENTED_EDGE ( 'NONE', *, *, #35728, .T. ) ;
#51286=CARTESIAN_POINT ( 'NONE',  ( 18.45068634130097607, 85.48650607335541451, -196.4543290533561901 ) ) ;
#51297=CIRCLE ( 'NONE', #251214, 0.1000000000000028644 ) ;
#51328=CARTESIAN_POINT ( 'NONE',  ( -23.25000000000000000, 77.83585931145600512, -158.5186683157258187 ) ) ;
#51335=VERTEX_POINT ( 'NONE', #238301 ) ;
#51336=FACE_OUTER_BOUND ( 'NONE', #130559, .T. ) ;
#51353=ORIENTED_EDGE ( 'NONE', *, *, #23463, .T. ) ;
#51360=ADVANCED_FACE ( 'NONE', ( #182199 ), #142364, .F. ) ;
#51364=ORIENTED_EDGE ( 'NONE', *, *, #66953, .F. ) ;
#51389=DIRECTION ( 'NONE',  ( 1.000000000000000000, 0.000000000000000000, 0.000000000000000000 ) ) ;
#51426=CARTESIAN_POINT ( 'NONE',  ( 20.94999999999999929, 69.35000000001254250, -182.2731074845244166 ) ) ;
#51477=CARTESIAN_POINT ( 'NONE',  ( -18.48179518609409655, 85.51832530050660353, -163.1334019077635276 ) ) ;
#51487=FACE_OUTER_BOUND ( 'NONE', #91891, .T. ) ;
#51512=DIRECTION ( 'NONE',  ( 1.713247197920696616E-14, -0.9876197685951263461, 0.1568667991644794590 ) ) ;
#51521=VERTEX_POINT ( 'NONE', #212040 ) ;
#51522=ORIENTED_EDGE ( 'NONE', *, *, #60833, .F. ) ;
#51550=DIRECTION ( 'NONE',  ( 0.000000000000000000, 0.000000000000000000, 1.000000000000000000 ) ) ;
#51553=FACE_OUTER_BOUND ( 'NONE', #254407, .T. ) ;
#51629=DIRECTION ( 'NONE',  ( 0.000000000000000000, -6.982962677686266711E-15, 1.000000000000000000 ) ) ;
#51659=ORIENTED_EDGE ( 'NONE', *, *, #226672, .F. ) ;
#51678=EDGE_LOOP ( 'NONE', ( #191704, #18630, #32914, #212625 ) ) ;
#51694=LINE ( 'NONE', #29628, #134312 ) ;
#51711=CARTESIAN_POINT ( 'NONE',  ( -18.59999999999999787, 74.83729825007462466, -195.4231074845243654 ) ) ;
#51732=DIRECTION ( 'NONE',  ( -1.000000000000000000, -0.000000000000000000, -0.000000000000000000 ) ) ;
#51734=LINE ( 'NONE', #90885, #242889 ) ;
#51787=AXIS2_PLACEMENT_3D ( 'NONE', #186107, #110409, #189960 ) ;
#51796=CARTESIAN_POINT ( 'NONE',  ( -18.59999999999999787, 65.66751761918722252, -164.4282609406112670 ) ) ;
#51837=DIRECTION ( 'NONE',  ( 0.000000000000000000, -1.000000000000000000, -6.982962677686265922E-15 ) ) ;
#51838=CARTESIAN_POINT ( 'NONE',  ( -21.05000000000000071, 76.09999996531227850, -210.0006596670181409 ) ) ;
#51846=CARTESIAN_POINT ( 'NONE',  ( 23.14999999999999503, 69.35000000001254250, -182.2731074845244166 ) ) ;
#51851=VECTOR ( 'NONE', #250450, 1000.000000000000000 ) ;
#51862=AXIS2_PLACEMENT_3D ( 'NONE', #143186, #84460, #139327 ) ;
#51870=PLANE ( 'NONE',  #96020 ) ;
#51874=LINE ( 'NONE', #70206, #175710 ) ;
#51899=EDGE_LOOP ( 'NONE', ( #229769, #229779, #253223, #47502 ) ) ;
#51934=DIRECTION ( 'NONE',  ( -0.000000000000000000, -1.000000000000000000, -6.982962677686266711E-15 ) ) ;
#51947=CIRCLE ( 'NONE', #206104, 0.09999999999998898659 ) ;
#51950=DIRECTION ( 'NONE',  ( -1.000000000000000000, 0.000000000000000000, 0.000000000000000000 ) ) ;
#51964=ORIENTED_EDGE ( 'NONE', *, *, #73005, .T. ) ;
#52001=LINE ( 'NONE', #32504, #224040 ) ;
#52003=AXIS2_PLACEMENT_3D ( 'NONE', #25401, #243137, #166213 ) ;
#52060=FACE_OUTER_BOUND ( 'NONE', #51678, .T. ) ;
#52065=CARTESIAN_POINT ( 'NONE',  ( -18.59999999999999787, 64.25000000001253397, -182.2731074845244450 ) ) ;
#52075=CARTESIAN_POINT ( 'NONE',  ( 18.49999999999999645, 70.05000000001267324, -193.2174051794895320 ) ) ;
#52088=ORIENTED_EDGE ( 'NONE', *, *, #128282, .F. ) ;
#52093=CARTESIAN_POINT ( 'NONE',  ( -22.39999999999999858, 64.25000000001269029, -203.4231074845244507 ) ) ;
#52106=DIRECTION ( 'NONE',  ( -0.000000000000000000, -1.000000000000000000, -6.982962677686266711E-15 ) ) ;
#52196=EDGE_CURVE ( 'NONE', #105902, #248551, #142371, .T. ) ;
#52269=B_SPLINE_CURVE_WITH_KNOTS ( 'NONE', 3,
 ( #24876, #164368, #121419, #43137, #243886, #219181, #144769, #40601, #199657, #21023 ),
 .UNSPECIFIED., .F., .F.,
 ( 4, 2, 2, 2, 4 ),
 ( 0.000000000000000000, 0.0001660831991681966670, 0.0002491247987522938892, 0.0002906455985443780351, 0.0003321663983364622351 ),
 .UNSPECIFIED. ) ;
#52275=VECTOR ( 'NONE', #125027, 1000.000000000000000 ) ;
#52286=ORIENTED_EDGE ( 'NONE', *, *, #77080, .F. ) ;
#52313=ORIENTED_EDGE ( 'NONE', *, *, #168303, .F. ) ;
#52333=DIRECTION ( 'NONE',  ( 0.000000000000000000, 1.000000000000000000, 6.938893903907222067E-15 ) ) ;
#52395=EDGE_LOOP ( 'NONE', ( #39803, #96764, #116547, #197676 ) ) ;
#52424=CARTESIAN_POINT ( 'NONE',  ( 23.15000000000000213, 87.48912529308852015, -173.1231074845242688 ) ) ;
#52447=SHAPE_REPRESENTATION_RELATIONSHIP ( 'NONE' , 'NONE' ,  #213520, #26624 ) ;
#52466=DIRECTION ( 'NONE',  ( 1.000000000000000000, 0.000000000000000000, 0.000000000000000000 ) ) ;
#52468=DIRECTION ( 'NONE',  ( -0.000000000000000000, -1.000000000000000000, -6.982962677686266711E-15 ) ) ;
#52469=DIRECTION ( 'NONE',  ( 0.000000000000000000, -1.000000000000000000, 0.000000000000000000 ) ) ;
#52471=CARTESIAN_POINT ( 'NONE',  ( 20.94999999999999929, 76.00000000001267608, -203.5231074845243597 ) ) ;
#52473=DIRECTION ( 'NONE',  ( 0.000000000000000000, -1.000000000000000000, -6.982962677686266711E-15 ) ) ;
#52502=CARTESIAN_POINT ( 'NONE',  ( 22.39999999999999503, 76.00000000001276135, -215.1726782920691505 ) ) ;
#52503=AXIS2_PLACEMENT_3D ( 'NONE', #19598, #178697, #97806 ) ;
#52545=ORIENTED_EDGE ( 'NONE', *, *, #232400, .F. ) ;
#52610=AXIS2_PLACEMENT_3D ( 'NONE', #229876, #145182, #125633 ) ;
#52628=CARTESIAN_POINT ( 'NONE',  ( 21.76363531954645936, 68.98706345214095847, -203.6221093588238489 ) ) ;
#52637=CARTESIAN_POINT ( 'NONE',  ( 21.05000000000000071, 76.00000000001260503, -191.3731074845243540 ) ) ;
#52658=CIRCLE ( 'NONE', #65141, 0.1000000000000026007 ) ;
#52688=CARTESIAN_POINT ( 'NONE',  ( 18.59999999999999076, 69.01799029515596828, -166.3269553662681233 ) ) ;
#52715=VERTEX_POINT ( 'NONE', #193891 ) ;
#52730=ORIENTED_EDGE ( 'NONE', *, *, #1459, .T. ) ;
#52745=AXIS2_PLACEMENT_3D ( 'NONE', #41860, #2692, #1406 ) ;
#52762=LINE ( 'NONE', #74940, #105991 ) ;
#52771=CARTESIAN_POINT ( 'NONE',  ( -20.94999999999999929, 76.00000000001244871, -170.0231074845243597 ) ) ;
#52776=CARTESIAN_POINT ( 'NONE',  ( -18.59999994787167310, 85.52363768977448899, -163.1406579497524376 ) ) ;
#52791=ADVANCED_FACE ( 'NONE', ( #20393 ), #192075, .T. ) ;
#52793=ORIENTED_EDGE ( 'NONE', *, *, #34418, .F. ) ;
#52799=EDGE_LOOP ( 'NONE', ( #54818, #119761, #19620, #89501 ) ) ;
#52822=AXIS2_PLACEMENT_3D ( 'NONE', #156386, #54677, #238455 ) ;
#52851=DIRECTION ( 'NONE',  ( -1.000000000000000000, -7.304098846218134667E-16, -5.311601492717084346E-30 ) ) ;
#52859=CYLINDRICAL_SURFACE ( 'NONE', #157291, 0.1000000000000033362 ) ;
#52882=DIRECTION ( 'NONE',  ( 1.000000000000000000, 0.000000000000000000, 0.000000000000000000 ) ) ;
#52889=EDGE_CURVE ( 'NONE', #206261, #250604, #9455, .T. ) ;
#52895=CARTESIAN_POINT ( 'NONE',  ( 20.94999999999999929, 76.00000000001244871, -170.0231074845243597 ) ) ;
#52906=DIRECTION ( 'NONE',  ( 0.000000000000000000, -0.1568667991644355497, -0.9876197685951332295 ) ) ;
#52936=DIRECTION ( 'NONE',  ( -1.000000000000000000, 1.875376730785737719E-16, 1.309568571767809260E-30 ) ) ;
#52942=CARTESIAN_POINT ( 'NONE',  ( -21.14999999999999858, 76.00000000001271871, -209.7816861282870775 ) ) ;
#52944=ORIENTED_EDGE ( 'NONE', *, *, #8709, .T. ) ;
#52949=VERTEX_POINT ( 'NONE', #71075 ) ;
#52963=AXIS2_PLACEMENT_3D ( 'NONE', #59891, #140733, #238549 ) ;
#52994=ORIENTED_EDGE ( 'NONE', *, *, #197086, .T. ) ;
#52997=DIRECTION ( 'NONE',  ( 0.000000000000000000, 6.938893903907222067E-15, -1.000000000000000000 ) ) ;
#53035=CARTESIAN_POINT ( 'NONE',  ( 20.12500000000000000, 66.25000000001263345, -195.4113362024101548 ) ) ;
#53042=VERTEX_POINT ( 'NONE', #228852 ) ;
#53055=ORIENTED_EDGE ( 'NONE', *, *, #191610, .F. ) ;
#53056=CIRCLE ( 'NONE', #15688, 0.09999999999999939493 ) ;
#53058=FACE_OUTER_BOUND ( 'NONE', #96372, .T. ) ;
#53079=CYLINDRICAL_SURFACE ( 'NONE', #33434, 0.09999999999998898659 ) ;
#53086=EDGE_LOOP ( 'NONE', ( #209388, #127436, #106935, #108697 ) ) ;
#53094=CARTESIAN_POINT ( 'NONE',  ( -22.47071067811865319, 75.90090754531013317, -211.2431822290224375 ) ) ;
#53096=EDGE_CURVE ( 'NONE', #41155, #257555, #59306, .T. ) ;
#53115=EDGE_CURVE ( 'NONE', #253585, #204559, #17285, .T. ) ;
#53171=LINE ( 'NONE', #15349, #74547 ) ;
#53204=CARTESIAN_POINT ( 'NONE',  ( -20.94999999999999929, 76.00000000001253397, -181.7231074845243484 ) ) ;
#53224=DIRECTION ( 'NONE',  ( 0.000000000000000000, 0.000000000000000000, 1.000000000000000000 ) ) ;
#53248=CARTESIAN_POINT ( 'NONE',  ( -23.25000000000000000, 87.75000000001266187, -200.4231074845242802 ) ) ;
#53250=VECTOR ( 'NONE', #165835, 1000.000000000000000 ) ;
#53257=ORIENTED_EDGE ( 'NONE', *, *, #59620, .T. ) ;
#53266=DIRECTION ( 'NONE',  ( -0.000000000000000000, 6.982962677686266711E-15, -1.000000000000000000 ) ) ;
#53271=ORIENTED_EDGE ( 'NONE', *, *, #201124, .T. ) ;
#53281=AXIS2_PLACEMENT_3D ( 'NONE', #217034, #556, #81360 ) ;
#53294=ORIENTED_EDGE ( 'NONE', *, *, #76527, .F. ) ;
#53298=CIRCLE ( 'NONE', #161656, 11.64999999999999325 ) ;
#53358=DIRECTION ( 'NONE',  ( 0.000000000000000000, 0.8777080977375655291, -0.4791956752370622463 ) ) ;
#53365=EDGE_CURVE ( 'NONE', #38939, #146901, #244233, .T. ) ;
#53398=DIRECTION ( 'NONE',  ( 1.000000000000000000, 0.000000000000000000, 0.000000000000000000 ) ) ;
#53401=FACE_OUTER_BOUND ( 'NONE', #8630, .T. ) ;
#53431=CARTESIAN_POINT ( 'NONE',  ( 18.52643265882457868, 65.68026841930954163, -164.4725740131889893 ) ) ;
#53457=DIRECTION ( 'NONE',  ( 1.000000000000000000, -0.000000000000000000, 0.000000000000000000 ) ) ;
#53461=DIRECTION ( 'NONE',  ( 0.000000000000000000, 0.6728971962617102953, -0.7397360091702507301 ) ) ;
#53498=CIRCLE ( 'NONE', #82499, 4.049999999999998046 ) ;
#53500=LINE ( 'NONE', #16955, #111427 ) ;
#53522=ORIENTED_EDGE ( 'NONE', *, *, #158411, .F. ) ;
#53577=ORIENTED_EDGE ( 'NONE', *, *, #13517, .F. ) ;
#53598=VECTOR ( 'NONE', #58115, 1000.000000000000000 ) ;
#53601=CARTESIAN_POINT ( 'NONE',  ( 23.14999999999999858, 76.00000000001246292, -172.0231074845243597 ) ) ;
#53652=ADVANCED_FACE ( 'NONE', ( #181111 ), #214124, .F. ) ;
#53671=CARTESIAN_POINT ( 'NONE',  ( -23.15000000000000213, 87.48912529308852015, -173.1231074845242688 ) ) ;
#53687=CARTESIAN_POINT ( 'NONE',  ( 20.94999999999999574, 87.65000000001266756, -200.5231074845242745 ) ) ;
#53690=VERTEX_POINT ( 'NONE', #166695 ) ;
#53712=EDGE_CURVE ( 'NONE', #175328, #69740, #192425, .T. ) ;
#53714=CARTESIAN_POINT ( 'NONE',  ( -23.15000000000000213, 64.35000000001268461, -203.5231074845244166 ) ) ;
#53728=TOROIDAL_SURFACE ( 'NONE', #199502, 0.2000000000000000111, 0.1000000000000000056 ) ;
#53743=CARTESIAN_POINT ( 'NONE',  ( 21.08479644141222664, 75.94144555744861691, -209.8681461422562506 ) ) ;
#53745=DIRECTION ( 'NONE',  ( 1.000000000000000000, 0.000000000000000000, 0.000000000000000000 ) ) ;
#53753=CARTESIAN_POINT ( 'NONE',  ( 20.94999999999999929, 85.50000000001261924, -193.6291383618718385 ) ) ;
#53761=DIRECTION ( 'NONE',  ( 0.000000000000000000, 0.1455152366551700771, 0.9893560106964479628 ) ) ;
#53771=CARTESIAN_POINT ( 'NONE',  ( -21.05000000000000071, 77.83534155023700407, -191.9679561919613491 ) ) ;
#53780=EDGE_LOOP ( 'NONE', ( #87284, #86024, #44508, #101748 ) ) ;
#53793=ORIENTED_EDGE ( 'NONE', *, *, #231711, .F. ) ;
#53808=CARTESIAN_POINT ( 'NONE',  ( -20.85000000000000142, 64.35000000001245724, -170.0231074845244166 ) ) ;
#53827=ORIENTED_EDGE ( 'NONE', *, *, #168303, .T. ) ;
#53845=AXIS2_PLACEMENT_3D ( 'NONE', #146146, #144857, #206133 ) ;
#53846=EDGE_CURVE ( 'NONE', #229015, #58850, #25840, .T. ) ;
#53865=ORIENTED_EDGE ( 'NONE', *, *, #47657, .F. ) ;
#53953=ORIENTED_EDGE ( 'NONE', *, *, #170422, .F. ) ;
#54032=CARTESIAN_POINT ( 'NONE',  ( 18.49999999999999645, 77.86671491006991630, -191.7704322382423356 ) ) ;
#54038=DIRECTION ( 'NONE',  ( -0.000000000000000000, 6.982962677686266711E-15, -1.000000000000000000 ) ) ;
#54047=DIRECTION ( 'NONE',  ( 0.000000000000000000, -7.056502275159890832E-15, 1.000000000000000000 ) ) ;
#54052=FACE_OUTER_BOUND ( 'NONE', #188605, .T. ) ;
#54072=CARTESIAN_POINT ( 'NONE',  ( -21.44999999999999929, 68.75000000001260503, -191.1731074845243938 ) ) ;
#54080=ORIENTED_EDGE ( 'NONE', *, *, #115647, .T. ) ;
#54106=ORIENTED_EDGE ( 'NONE', *, *, #104389, .F. ) ;
#54166=CARTESIAN_POINT ( 'NONE',  ( 21.05000000000000071, 85.50000000001261924, -193.6291383618718385 ) ) ;
#54177=CARTESIAN_POINT ( 'NONE',  ( 18.49999999999999645, 70.30054753569118020, -216.0653814410942175 ) ) ;
#54208=ORIENTED_EDGE ( 'NONE', *, *, #2906, .T. ) ;
#54231=ORIENTED_EDGE ( 'NONE', *, *, #164632, .F. ) ;
#54237=CARTESIAN_POINT ( 'NONE',  ( 18.59999999999999432, 85.48068669529136798, -163.0819923157664562 ) ) ;
#54328=DIRECTION ( 'NONE',  ( -1.000000000000000000, -0.000000000000000000, -0.000000000000000000 ) ) ;
#54330=AXIS2_PLACEMENT_3D ( 'NONE', #171872, #210963, #133976 ) ;
#54337=EDGE_CURVE ( 'NONE', #250604, #79652, #67895, .T. ) ;
#54353=ORIENTED_EDGE ( 'NONE', *, *, #86238, .T. ) ;
#54367=EDGE_LOOP ( 'NONE', ( #6855, #189756, #119064, #91199 ) ) ;
#54389=EDGE_CURVE ( 'NONE', #105519, #162952, #115355, .T. ) ;
#54402=AXIS2_PLACEMENT_3D ( 'NONE', #164117, #59842, #243639 ) ;
#54406=ORIENTED_EDGE ( 'NONE', *, *, #238717, .F. ) ;
#54423=CARTESIAN_POINT ( 'NONE',  ( -18.59999999999999787, 64.35000000001254250, -182.1731074845244507 ) ) ;
#54462=CARTESIAN_POINT ( 'NONE',  ( 20.94999999999999929, 64.35000000001249987, -176.8647081744214802 ) ) ;
#54488=ORIENTED_EDGE ( 'NONE', *, *, #134463, .F. ) ;
#54495=FACE_OUTER_BOUND ( 'NONE', #66810, .T. ) ;
#54529=CIRCLE ( 'NONE', #158609, 6.258578643762696458 ) ;
#54533=ORIENTED_EDGE ( 'NONE', *, *, #53365, .F. ) ;
#54540=DIRECTION ( 'NONE',  ( 0.000000000000000000, 0.000000000000000000, 1.000000000000000000 ) ) ;
#54574=EDGE_LOOP ( 'NONE', ( #188102, #80707, #201791, #150583 ) ) ;
#54602=ORIENTED_EDGE ( 'NONE', *, *, #162807, .T. ) ;
#54631=DIRECTION ( 'NONE',  ( 0.000000000000000000, -8.987377189994711700E-15, 1.000000000000000000 ) ) ;
#54664=ORIENTED_EDGE ( 'NONE', *, *, #78839, .F. ) ;
#54674=DIRECTION ( 'NONE',  ( -1.000000000000000000, -0.000000000000000000, -0.000000000000000000 ) ) ;
#54677=DIRECTION ( 'NONE',  ( 1.000000000000000000, 0.000000000000000000, 0.000000000000000000 ) ) ;
#54680=DIRECTION ( 'NONE',  ( -1.000000000000000000, -0.000000000000000000, -0.000000000000000000 ) ) ;
#54698=EDGE_CURVE ( 'NONE', #107411, #97198, #6016, .T. ) ;
#54704=CARTESIAN_POINT ( 'NONE',  ( -21.59142135623730852, 68.15000000001253966, -182.2731074845244166 ) ) ;
#54709=CARTESIAN_POINT ( 'NONE',  ( 18.50016250449482413, 65.70233904877169095, -164.5487410911965469 ) ) ;
#54713=CARTESIAN_POINT ( 'NONE',  ( -21.05000000000000071, 74.16465844978819177, -191.8679561919614116 ) ) ;
#54729=ORIENTED_EDGE ( 'NONE', *, *, #52196, .F. ) ;
#54733=CARTESIAN_POINT ( 'NONE',  ( 21.07094088545369814, 75.90110629746051529, -209.8432747064415196 ) ) ;
#54772=DIRECTION ( 'NONE',  ( 1.000000000000000000, 0.000000000000000000, 0.000000000000000000 ) ) ;
#54818=ORIENTED_EDGE ( 'NONE', *, *, #166415, .T. ) ;
#54823=DIRECTION ( 'NONE',  ( 0.000000000000000000, 0.4930308989874980785, 0.8700118002898462599 ) ) ;
#54825=VERTEX_POINT ( 'NONE', #203580 ) ;
#54827=EDGE_CURVE ( 'NONE', #53690, #139621, #41961, .T. ) ;
#54833=CARTESIAN_POINT ( 'NONE',  ( 20.04142135623730070, 64.25000000001250555, -178.8731074845244393 ) ) ;
#54872=CARTESIAN_POINT ( 'NONE',  ( 20.94999999999999929, 61.95000000001248708, -175.5368025552853624 ) ) ;
#54879=EDGE_LOOP ( 'NONE', ( #76243, #101058, #22826, #233965 ) ) ;
#54894=DIRECTION ( 'NONE',  ( 0.000000000000000000, -8.717686153663073805E-15, 1.000000000000000000 ) ) ;
#54896=EDGE_CURVE ( 'NONE', #59470, #42819, #121504, .T. ) ;
#54905=CARTESIAN_POINT ( 'NONE',  ( -20.94999999999999929, 76.00000000001267608, -203.5231074845243597 ) ) ;
#54911=EDGE_CURVE ( 'NONE', #41259, #226219, #126328, .T. ) ;
#54917=VECTOR ( 'NONE', #142031, 1000.000000000000000 ) ;
#54932=AXIS2_PLACEMENT_3D ( 'NONE', #191752, #13097, #234698 ) ;
#54936=VERTEX_POINT ( 'NONE', #5350 ) ;
#54943=B_SPLINE_CURVE_WITH_KNOTS ( 'NONE', 3,
 ( #209813, #74184, #109406, #108143, #188962, #153740, #131551, #248946, #72895, #233247 ),
 .UNSPECIFIED., .F., .F.,
 ( 4, 3, 3, 4 ),
 ( 3.103167691559091397E-17, 0.0002000000000008536833, 0.001000000000082982687, 0.001967863649483335420 ),
 .UNSPECIFIED. ) ;
#54955=ORIENTED_EDGE ( 'NONE', *, *, #200067, .F. ) ;
#55005=PLANE ( 'NONE',  #48733 ) ;
#55010=SURFACE_SIDE_STYLE ('',( #113724 ) ) ;
#55026=DIRECTION ( 'NONE',  ( 1.000000000000000000, 7.304098846218134667E-16, 5.100424963727256530E-30 ) ) ;
#55027=CARTESIAN_POINT ( 'NONE',  ( 21.14999999999999858, 69.35000000001259934, -191.3731074845244109 ) ) ;
#55041=ORIENTED_EDGE ( 'NONE', *, *, #8912, .T. ) ;
#55056=VECTOR ( 'NONE', #84523, 1000.000000000000000 ) ;
#55058=CARTESIAN_POINT ( 'NONE',  ( 20.84999999999998721, 64.25000000001244871, -170.0231074845244166 ) ) ;
#55110=CARTESIAN_POINT ( 'NONE',  ( 22.40000000000020819, 76.10085836911243007, -215.2726746080140572 ) ) ;
#55154=VERTEX_POINT ( 'NONE', #113463 ) ;
#55179=EDGE_CURVE ( 'NONE', #246415, #79128, #26580, .T. ) ;
#55185=VECTOR ( 'NONE', #184811, 1000.000000000000000 ) ;
#55257=CARTESIAN_POINT ( 'NONE',  ( 23.24999999999997513, 64.25000000001249134, -177.0379132551784096 ) ) ;
#55264=ADVANCED_FACE ( 'NONE', ( #63760 ), #222823, .T. ) ;
#55290=EDGE_CURVE ( 'NONE', #181442, #153430, #39062, .T. ) ;
#55294=DIRECTION ( 'NONE',  ( 1.000000000000000000, 0.000000000000000000, 0.000000000000000000 ) ) ;
#55302=PLANE ( 'NONE',  #242207 ) ;
#55306=DIRECTION ( 'NONE',  ( 0.000000000000000000, 0.9887567792719329507, 0.1495327102803732933 ) ) ;
#55319=CIRCLE ( 'NONE', #96846, 0.5000000000000004441 ) ;
#55328=DIRECTION ( 'NONE',  ( 0.000000000000000000, 0.000000000000000000, 1.000000000000000000 ) ) ;
#55331=ADVANCED_FACE ( 'NONE', ( #106724 ), #222341, .T. ) ;
#55341=ORIENTED_EDGE ( 'NONE', *, *, #230952, .T. ) ;
#55347=AXIS2_PLACEMENT_3D ( 'NONE', #254459, #134525, #73324 ) ;
#55397=ORIENTED_EDGE ( 'NONE', *, *, #128614, .F. ) ;
#55409=EDGE_CURVE ( 'NONE', #139907, #13339, #12472, .T. ) ;
#55436=CARTESIAN_POINT ( 'NONE',  ( -21.45000000000000284, 68.29142135624991283, -191.1731074845243938 ) ) ;
#55449=ORIENTED_EDGE ( 'NONE', *, *, #17575, .T. ) ;
#55478=DIRECTION ( 'NONE',  ( 0.000000000000000000, -6.982962677686267499E-15, 1.000000000000000000 ) ) ;
#55481=EDGE_LOOP ( 'NONE', ( #156384, #70580, #71028 ) ) ;
#55482=FACE_OUTER_BOUND ( 'NONE', #116381, .T. ) ;
#55500=ORIENTED_EDGE ( 'NONE', *, *, #161650, .F. ) ;
#55593=ORIENTED_EDGE ( 'NONE', *, *, #203975, .T. ) ;
#55605=EDGE_LOOP ( 'NONE', ( #175834, #200025, #25518, #193792 ) ) ;
#55615=EDGE_CURVE ( 'NONE', #211067, #184002, #143269, .T. ) ;
#55682=CYLINDRICAL_SURFACE ( 'NONE', #111612, 0.5000000000000004441 ) ;
#55691=EDGE_CURVE ( 'NONE', #30344, #75338, #139134, .T. ) ;
#55693=EDGE_LOOP ( 'NONE', ( #205940, #165329, #77022, #225266 ) ) ;
#55713=ORIENTED_EDGE ( 'NONE', *, *, #169386, .F. ) ;
#55714=CARTESIAN_POINT ( 'NONE',  ( -21.05000000000000071, 76.00000000001267608, -203.5231074845243597 ) ) ;
#55739=ORIENTED_EDGE ( 'NONE', *, *, #251038, .F. ) ;
#55777=EDGE_LOOP ( 'NONE', ( #136040, #25175, #157484, #161412 ) ) ;
#55787=EDGE_CURVE ( 'NONE', #225819, #217036, #14490, .T. ) ;
#55797=EDGE_CURVE ( 'NONE', #161777, #76140, #59300, .T. ) ;
#55818=VERTEX_POINT ( 'NONE', #155549 ) ;
#55826=DIRECTION ( 'NONE',  ( -0.000000000000000000, 1.000000000000000000, 6.982962677686267499E-15 ) ) ;
#55892=ORIENTED_EDGE ( 'NONE', *, *, #253272, .F. ) ;
#55894=LINE ( 'NONE', #214992, #22157 ) ;
#55913=DIRECTION ( 'NONE',  ( -1.000000000000000000, 0.000000000000000000, 0.000000000000000000 ) ) ;
#55922=ADVANCED_FACE ( 'NONE', ( #158129 ), #198486, .T. ) ;
#55927=EDGE_CURVE ( 'NONE', #133309, #139578, #240816, .T. ) ;
#55972=LINE ( 'NONE', #177262, #157912 ) ;
#56007=LINE ( 'NONE', #176015, #257917 ) ;
#56008=DIRECTION ( 'NONE',  ( 0.7071359030028113724, 0.000000000000000000, -0.7070776581708677622 ) ) ;
#56018=DIRECTION ( 'NONE',  ( -1.000000000000000000, -0.000000000000000000, 0.000000000000000000 ) ) ;
#56042=EDGE_CURVE ( 'NONE', #210729, #133901, #202341, .T. ) ;
#56064=VECTOR ( 'NONE', #253760, 1000.000000000000000 ) ;
#56076=DIRECTION ( 'NONE',  ( 0.000000000000000000, -6.467318590049456648E-15, 1.000000000000000000 ) ) ;
#56125=ADVANCED_FACE ( 'NONE', ( #189206 ), #11872, .T. ) ;
#56136=ORIENTED_EDGE ( 'NONE', *, *, #149542, .F. ) ;
#56143=EDGE_CURVE ( 'NONE', #13712, #87244, #81251, .T. ) ;
#56144=ADVANCED_FACE ( 'NONE', ( #113512 ), #14441, .T. ) ;
#56165=ORIENTED_EDGE ( 'NONE', *, *, #209196, .T. ) ;
#56183=VERTEX_POINT ( 'NONE', #173542 ) ;
#56197=CIRCLE ( 'NONE', #89519, 0.1000000000000046685 ) ;
#56219=DIRECTION ( 'NONE',  ( -0.000000000000000000, 0.4791956752371485107, 0.8777080977375185666 ) ) ;
#56254=AXIS2_PLACEMENT_3D ( 'NONE', #91519, #68098, #171100 ) ;
#56276=EDGE_CURVE ( 'NONE', #70073, #192399, #32265, .T. ) ;
#56280=CARTESIAN_POINT ( 'NONE',  ( -21.44999999999999929, 68.65000000001261071, -191.2731074845244166 ) ) ;
#56311=CARTESIAN_POINT ( 'NONE',  ( 20.94999999999999574, 77.16270174995064224, -195.4231074845243370 ) ) ;
#56329=AXIS2_PLACEMENT_3D ( 'NONE', #67191, #175010, #254462 ) ;
#56331=EDGE_CURVE ( 'NONE', #204733, #230108, #176991, .T. ) ;
#56365=ORIENTED_EDGE ( 'NONE', *, *, #132859, .F. ) ;
#56366=AXIS2_PLACEMENT_3D ( 'NONE', #224926, #87974, #223640 ) ;
#56376=LINE ( 'NONE', #38136, #56935 ) ;
#56381=CIRCLE ( 'NONE', #243835, 0.09999999999998898659 ) ;
#56403=LINE ( 'NONE', #135940, #215868 ) ;
#56409=DIRECTION ( 'NONE',  ( -0.000000000000000000, 1.000000000000000000, 6.982962677686266711E-15 ) ) ;
#56410=ORIENTED_EDGE ( 'NONE', *, *, #114639, .F. ) ;
#56436=VECTOR ( 'NONE', #248337, 1000.000000000000000 ) ;
#56445=AXIS2_PLACEMENT_3D ( 'NONE', #257787, #196577, #178334 ) ;
#56448=CIRCLE ( 'NONE', #10677, 0.09999999999999080458 ) ;
#56469=ORIENTED_EDGE ( 'NONE', *, *, #116428, .F. ) ;
#56476=CARTESIAN_POINT ( 'NONE',  ( 21.13461538461538325, 67.11458296203814200, -191.1731074845244223 ) ) ;
#56486=VERTEX_POINT ( 'NONE', #138629 ) ;
#56491=CARTESIAN_POINT ( 'NONE',  ( -18.40000000000000213, 85.51932773110506503, -196.5501311079650009 ) ) ;
#56538=CIRCLE ( 'NONE', #160657, 0.1000000000000028644 ) ;
#56543=ORIENTED_EDGE ( 'NONE', *, *, #87986, .T. ) ;
#56544=ORIENTED_EDGE ( 'NONE', *, *, #199176, .F. ) ;
#56587=VECTOR ( 'NONE', #97587, 1000.000000000000000 ) ;
#56638=ORIENTED_EDGE ( 'NONE', *, *, #168909, .T. ) ;
#56646=ADVANCED_FACE ( 'NONE', ( #5220 ), #14847, .F. ) ;
#56649=CARTESIAN_POINT ( 'NONE',  ( -20.64999999999999858, 71.65000000001253966, -182.3731074845244109 ) ) ;
#56656=CARTESIAN_POINT ( 'NONE',  ( -20.64999999999999858, 76.00000000001259082, -190.5481074845243654 ) ) ;
#56664=DIRECTION ( 'NONE',  ( -7.304098846217948299E-16, -1.000000000000000000, 0.000000000000000000 ) ) ;
#56672=ORIENTED_EDGE ( 'NONE', *, *, #231325, .T. ) ;
#56692=VECTOR ( 'NONE', #131719, 1000.000000000000000 ) ;
#56706=DIRECTION ( 'NONE',  ( 1.000000000000000000, 0.000000000000000000, 0.000000000000000000 ) ) ;
#56743=ORIENTED_EDGE ( 'NONE', *, *, #183288, .F. ) ;
#56798=EDGE_CURVE ( 'NONE', #218130, #225579, #173087, .T. ) ;
#56800=ORIENTED_EDGE ( 'NONE', *, *, #1645, .T. ) ;
#56814=FACE_OUTER_BOUND ( 'NONE', #248820, .T. ) ;
#56823=LINE ( 'NONE', #136359, #53598 ) ;
#56924=CARTESIAN_POINT ( 'NONE',  ( -23.15000000000000213, 64.35000000001254250, -182.2731074845244450 ) ) ;
#56934=ADVANCED_FACE ( 'NONE', ( #101420 ), #222683, .F. ) ;
#56935=VECTOR ( 'NONE', #113801, 1000.000000000000000 ) ;
#56947=( BOUNDED_CURVE ( )  B_SPLINE_CURVE ( 3, ( #248071, #46010, #27776, #26471 ),
 .UNSPECIFIED., .F., .F. ) 
 B_SPLINE_CURVE_WITH_KNOTS ( ( 4, 4 ),
 ( 4.937700262164173333E-15, 1.570796326794912323 ),
 .UNSPECIFIED. ) 
 CURVE ( )  GEOMETRIC_REPRESENTATION_ITEM ( )  RATIONAL_B_SPLINE_CURVE ( ( 1.000000000000000000, 0.8047378541243623840, 0.8047378541243623840, 1.000000000000000000 ) ) 
 REPRESENTATION_ITEM ( '' )  );
#56948=EDGE_CURVE ( 'NONE', #95948, #131701, #98168, .T. ) ;
#56986=FACE_OUTER_BOUND ( 'NONE', #110739, .T. ) ;
#56995=CARTESIAN_POINT ( 'NONE',  ( 21.13461538461538325, 67.11458296203814200, -191.1731074845244223 ) ) ;
#57090=CARTESIAN_POINT ( 'NONE',  ( 23.24999999999999289, 69.55000000001260219, -191.1731074845243938 ) ) ;
#57147=DIRECTION ( 'NONE',  ( 3.469446951953635015E-14, 6.982962677686266711E-15, -1.000000000000000000 ) ) ;
#57219=EDGE_LOOP ( 'NONE', ( #161484, #158274, #60469, #74424 ) ) ;
#57233=DIRECTION ( 'NONE',  ( 0.000000000000000000, 1.000000000000000000, 6.982962677686266711E-15 ) ) ;
#57236=CIRCLE ( 'NONE', #52963, 0.2000000000000057288 ) ;
#57256=AXIS2_PLACEMENT_3D ( 'NONE', #108150, #67733, #243801 ) ;
#57265=CARTESIAN_POINT ( 'NONE',  ( -20.54999999999999716, 68.75000000001260503, -191.2731074845244166 ) ) ;
#57311=LINE ( 'NONE', #78165, #3767 ) ;
#57363=CARTESIAN_POINT ( 'NONE',  ( 20.94999999999999929, 77.83534155023701828, -191.9679561919613491 ) ) ;
#57380=VERTEX_POINT ( 'NONE', #137701 ) ;
#57392=CARTESIAN_POINT ( 'NONE',  ( -20.54999999999999716, 68.85000000001254250, -182.3731074845244109 ) ) ;
#57433=ORIENTED_EDGE ( 'NONE', *, *, #96116, .F. ) ;
#57434=CARTESIAN_POINT ( 'NONE',  ( 21.14999999999999858, 64.35000000001258513, -191.3731074845244393 ) ) ;
#57444=DIRECTION ( 'NONE',  ( -1.000000000000000000, 0.000000000000000000, 0.000000000000000000 ) ) ;
#57462=CARTESIAN_POINT ( 'NONE',  ( 20.95224633520496127, 67.09947783345539563, -195.0298310366031558 ) ) ;
#57467=VERTEX_POINT ( 'NONE', #185834 ) ;
#57482=AXIS2_PLACEMENT_3D ( 'NONE', #203731, #244126, #204987 ) ;
#57484=LINE ( 'NONE', #99173, #48108 ) ;
#57579=CARTESIAN_POINT ( 'NONE',  ( 21.10257677756356998, 75.97504925044474078, -209.9214892270570942 ) ) ;
#57593=EDGE_CURVE ( 'NONE', #99483, #198203, #48502, .T. ) ;
#57633=CARTESIAN_POINT ( 'NONE',  ( 20.12500000000000000, 66.25000000001263345, -195.4113362024101548 ) ) ;
#57644=FACE_OUTER_BOUND ( 'NONE', #202084, .T. ) ;
#57655=DIRECTION ( 'NONE',  ( 7.304098846218134667E-16, -1.000000000000000000, -6.982962677686267499E-15 ) ) ;
#57664=DIRECTION ( 'NONE',  ( -3.469446951953515108E-14, -1.000000000000000000, 0.000000000000000000 ) ) ;
#57682=EDGE_CURVE ( 'NONE', #222338, #251965, #210456, .T. ) ;
#57704=AXIS2_PLACEMENT_3D ( 'NONE', #29190, #44853, #10871 ) ;
#57716=EDGE_CURVE ( 'NONE', #123921, #199924, #135593, .T. ) ;
#57721=CYLINDRICAL_SURFACE ( 'NONE', #77271, 0.1000000000000038219 ) ;
#57723=ORIENTED_EDGE ( 'NONE', *, *, #71685, .T. ) ;
#57739=CIRCLE ( 'NONE', #220063, 11.64999999999999325 ) ;
#57778=CARTESIAN_POINT ( 'NONE',  ( -18.59999996769639097, 85.36327376984304749, -196.3416135690586088 ) ) ;
#57785=AXIS2_PLACEMENT_3D ( 'NONE', #109944, #128242, #129522 ) ;
#57802=TOROIDAL_SURFACE ( 'NONE', #70335, 0.2000000000000000111, 0.1000000000000000056 ) ;
#57823=ORIENTED_EDGE ( 'NONE', *, *, #241839, .F. ) ;
#57832=DIRECTION ( 'NONE',  ( 1.000000000000000000, -0.000000000000000000, 0.000000000000000000 ) ) ;
#57861=EDGE_CURVE ( 'NONE', #654, #135929, #82544, .T. ) ;
#57901=DIRECTION ( 'NONE',  ( -1.000000000000000000, 0.000000000000000000, -0.000000000000000000 ) ) ;
#57912=EDGE_CURVE ( 'NONE', #48255, #138529, #202699, .T. ) ;
#57913=EDGE_CURVE ( 'NONE', #223699, #45489, #243752, .T. ) ;
#57964=DIRECTION ( 'NONE',  ( 0.000000000000000000, -6.982962677686266711E-15, 1.000000000000000000 ) ) ;
#57989=AXIS2_PLACEMENT_3D ( 'NONE', #65330, #234684, #131729 ) ;
#58014=FACE_OUTER_BOUND ( 'NONE', #212031, .T. ) ;
#58031=ORIENTED_EDGE ( 'NONE', *, *, #219934, .T. ) ;
#58076=DIRECTION ( 'NONE',  ( 0.000000000000000000, 1.000000000000000000, 0.000000000000000000 ) ) ;
#58086=CARTESIAN_POINT ( 'NONE',  ( -23.25000000000000000, 69.01799029515598249, -166.3269553662681233 ) ) ;
#58098=DIRECTION ( 'NONE',  ( 0.000000000000000000, 0.000000000000000000, 1.000000000000000000 ) ) ;
#58112=ADVANCED_FACE ( 'NONE', ( #78418 ), #236213, .T. ) ;
#58115=DIRECTION ( 'NONE',  ( 0.000000000000000000, -6.982962677686266711E-15, 1.000000000000000000 ) ) ;
#58117=EDGE_CURVE ( 'NONE', #182617, #132760, #148257, .T. ) ;
#58129=DIRECTION ( 'NONE',  ( 0.000000000000000000, 0.8777080977375655291, -0.4791956752370622463 ) ) ;
#58130=LINE ( 'NONE', #173022, #189502 ) ;
#58137=ADVANCED_FACE ( 'NONE', ( #160562 ), #73285, .T. ) ;
#58161=ADVANCED_FACE ( 'NONE', ( #194557 ), #38047, .T. ) ;
#58176=ADVANCED_FACE ( 'NONE', ( #177572 ), #235547, .T. ) ;
#58201=DIRECTION ( 'NONE',  ( 0.000000000000000000, 0.000000000000000000, 1.000000000000000000 ) ) ;
#58214=ADVANCED_FACE ( 'NONE', ( #255736 ), #98154, .F. ) ;
#58277=AXIS2_PLACEMENT_3D ( 'NONE', #235164, #34420, #113918 ) ;
#58304=FACE_OUTER_BOUND ( 'NONE', #135195, .T. ) ;
#58311=ORIENTED_EDGE ( 'NONE', *, *, #94519, .T. ) ;
#58317=LINE ( 'NONE', #139131, #189195 ) ;
#58335=CIRCLE ( 'NONE', #154090, 4.299999999999970512 ) ;
#58412=ORIENTED_EDGE ( 'NONE', *, *, #240140, .F. ) ;
#58438=DIRECTION ( 'NONE',  ( 0.000000000000000000, 0.000000000000000000, -1.000000000000000000 ) ) ;
#58459=CARTESIAN_POINT ( 'NONE',  ( 20.84999999999999432, 68.97833521811233481, -166.1895420826271277 ) ) ;
#58473=AXIS2_PLACEMENT_3D ( 'NONE', #104409, #160592, #79714 ) ;
#58474=CARTESIAN_POINT ( 'NONE',  ( 21.05000000000000071, 65.52661458509972192, -195.9444530202758870 ) ) ;
#58479=ORIENTED_EDGE ( 'NONE', *, *, #215022, .F. ) ;
#58530=EDGE_CURVE ( 'NONE', #66231, #19454, #148461, .T. ) ;
#58582=FACE_OUTER_BOUND ( 'NONE', #217248, .T. ) ;
#58615=VECTOR ( 'NONE', #41633, 1000.000000000000000 ) ;
#58634=DIRECTION ( 'NONE',  ( -1.000000000000000000, -0.000000000000000000, -0.000000000000000000 ) ) ;
#58637=CARTESIAN_POINT ( 'NONE',  ( 22.48660254037844197, 64.35000000001267040, -203.5731074845244564 ) ) ;
#58652=DIRECTION ( 'NONE',  ( 0.000000000000000000, -1.000000000000000000, -6.982962677686265922E-15 ) ) ;
#58661=VERTEX_POINT ( 'NONE', #88033 ) ;
#58673=EDGE_CURVE ( 'NONE', #94393, #55154, #256523, .T. ) ;
#58721=CARTESIAN_POINT ( 'NONE',  ( -21.55000000000000426, 68.25000000001260503, -191.1731074845243938 ) ) ;
#58744=AXIS2_PLACEMENT_3D ( 'NONE', #45919, #23823, #145003 ) ;
#58747=CARTESIAN_POINT ( 'NONE',  ( 21.05000000000000071, 76.00000000001246292, -171.9231074845243938 ) ) ;
#58761=DIRECTION ( 'NONE',  ( -0.000000000000000000, 7.272083257015735086E-15, -1.000000000000000000 ) ) ;
#58772=EDGE_CURVE ( 'NONE', #11922, #247736, #19259, .T. ) ;
#58790=FACE_OUTER_BOUND ( 'NONE', #97730, .T. ) ;
#58809=VERTEX_POINT ( 'NONE', #37105 ) ;
#58849=AXIS2_PLACEMENT_3D ( 'NONE', #40434, #104203, #142054 ) ;
#58850=VERTEX_POINT ( 'NONE', #59165 ) ;
#58863=CARTESIAN_POINT ( 'NONE',  ( 20.85000000000000142, 77.83585931145600512, -158.5186683157258187 ) ) ;
#58962=CARTESIAN_POINT ( 'NONE',  ( 22.50000000000000000, 75.95437663941648054, -215.1736118230719512 ) ) ;
#59003=EDGE_CURVE ( 'NONE', #65541, #210276, #69541, .T. ) ;
#59011=CARTESIAN_POINT ( 'NONE',  ( 20.87155475150661132, 64.25000000001249134, -176.9275209553668162 ) ) ;
#59031=CARTESIAN_POINT ( 'NONE',  ( 20.94999999999999929, 71.14953271029297355, -191.4888400755227167 ) ) ;
#59039=ADVANCED_FACE ( 'NONE', ( #46055 ), #14678, .F. ) ;
#59045=CARTESIAN_POINT ( 'NONE',  ( -18.48550754432078236, 85.46339977857238068, -196.4743177321096823 ) ) ;
#59053=VERTEX_POINT ( 'NONE', #232434 ) ;
#59105=LINE ( 'NONE', #55257, #158447 ) ;
#59165=CARTESIAN_POINT ( 'NONE',  ( 21.05000000000000071, 69.74218538953655866, -203.6208977758331855 ) ) ;
#59176=VECTOR ( 'NONE', #104176, 1000.000000000000000 ) ;
#59193=DIRECTION ( 'NONE',  ( 1.000000000000000000, 0.000000000000000000, 0.000000000000000000 ) ) ;
#59228=DIRECTION ( 'NONE',  ( -1.000000000000000000, -9.012599976027990443E-15, -6.882867235861669241E-14 ) ) ;
#59270=ORIENTED_EDGE ( 'NONE', *, *, #159405, .F. ) ;
#59293=ADVANCED_FACE ( 'NONE', ( #22374 ), #199729, .F. ) ;
#59300=( BOUNDED_CURVE ( )  B_SPLINE_CURVE ( 3, ( #188220, #228653, #109958, #169988 ),
 .UNSPECIFIED., .F., .F. ) 
 B_SPLINE_CURVE_WITH_KNOTS ( ( 4, 4 ),
 ( 1.570796326794901665, 3.141592653589802886 ),
 .UNSPECIFIED. ) 
 CURVE ( )  GEOMETRIC_REPRESENTATION_ITEM ( )  RATIONAL_B_SPLINE_CURVE ( ( 1.000000000000000000, 0.8047378541243639383, 0.8047378541243639383, 1.000000000000000000 ) ) 
 REPRESENTATION_ITEM ( '' )  );
#59306=CIRCLE ( 'NONE', #105098, 0.1000000000000060701 ) ;
#59348=FACE_OUTER_BOUND ( 'NONE', #240364, .T. ) ;
#59353=ORIENTED_EDGE ( 'NONE', *, *, #54827, .T. ) ;
#59433=VECTOR ( 'NONE', #176454, 1000.000000000000114 ) ;
#59462=CARTESIAN_POINT ( 'NONE',  ( -20.94999999999999929, 61.95000000001265050, -198.0094124137634708 ) ) ;
#59470=VERTEX_POINT ( 'NONE', #233417 ) ;
#59499=EDGE_CURVE ( 'NONE', #158664, #241281, #229141, .T. ) ;
#59510=CARTESIAN_POINT ( 'NONE',  ( 22.49436431346199683, 75.93309647029050780, -215.1730584321778110 ) ) ;
#59513=DIRECTION ( 'NONE',  ( -3.265361837132813093E-16, -1.000000000000000000, 7.445645354460596589E-46 ) ) ;
#59516=DIRECTION ( 'NONE',  ( 1.000000000000000000, -0.000000000000000000, 0.000000000000000000 ) ) ;
#59548=CARTESIAN_POINT ( 'NONE',  ( -23.25000000000000000, 74.00000000001254818, -183.2477294072864709 ) ) ;
#59611=SPHERICAL_SURFACE ( 'NONE', #114729, 0.1000000000000000056 ) ;
#59620=EDGE_CURVE ( 'NONE', #232039, #217568, #54529, .T. ) ;
#59631=EDGE_CURVE ( 'NONE', #213320, #132574, #121023, .T. ) ;
#59641=CIRCLE ( 'NONE', #51273, 11.75000000000001066 ) ;
#59656=ORIENTED_EDGE ( 'NONE', *, *, #67871, .F. ) ;
#59657=CARTESIAN_POINT ( 'NONE',  ( -21.05000000000000071, 61.95000000001265050, -198.0094124137634708 ) ) ;
#59686=DIRECTION ( 'NONE',  ( 0.000000000000000000, -6.982962677686266711E-15, 1.000000000000000000 ) ) ;
#59694=DIRECTION ( 'NONE',  ( 0.000000000000000000, 0.000000000000000000, -1.000000000000000000 ) ) ;
#59698=CIRCLE ( 'NONE', #84622, 0.09999999999998898659 ) ;
#59702=EDGE_LOOP ( 'NONE', ( #157992, #135144, #142034, #220456 ) ) ;
#59717=DIRECTION ( 'NONE',  ( 1.000000000000000000, 0.000000000000000000, 0.000000000000000000 ) ) ;
#59722=ORIENTED_EDGE ( 'NONE', *, *, #88836, .T. ) ;
#59730=CARTESIAN_POINT ( 'NONE',  ( -20.99551997958407412, 64.25000000001251976, -176.8714483468355922 ) ) ;
#59752=EDGE_CURVE ( 'NONE', #4179, #153430, #23365, .T. ) ;
#59793=CIRCLE ( 'NONE', #97180, 11.80000000000000426 ) ;
#59842=DIRECTION ( 'NONE',  ( -0.000000000000000000, -6.982962677686266711E-15, 1.000000000000000000 ) ) ;
#59887=VECTOR ( 'NONE', #228774, 1000.000000000000000 ) ;
#59891=CARTESIAN_POINT ( 'NONE',  ( 21.05000000000000071, 74.83729825007462466, -195.4231074845243654 ) ) ;
#59893=CARTESIAN_POINT ( 'NONE',  ( 23.24999999999999645, 76.00000000001267608, -203.5231074845243597 ) ) ;
#59897=EDGE_CURVE ( 'NONE', #252148, #97927, #96025, .T. ) ;
#59921=CARTESIAN_POINT ( 'NONE',  ( 21.14999999999999858, 64.35000000001267040, -203.4231074845244507 ) ) ;
#59961=DIRECTION ( 'NONE',  ( 0.000000000000000000, 0.000000000000000000, 1.000000000000000000 ) ) ;
#59972=EDGE_LOOP ( 'NONE', ( #50804, #191607, #60375 ) ) ;
#59989=CIRCLE ( 'NONE', #239078, 0.1000000000000046685 ) ;
#59992=LINE ( 'NONE', #253065, #168577 ) ;
#59994=VERTEX_POINT ( 'NONE', #144079 ) ;
#60002=DIRECTION ( 'NONE',  ( -1.000000000000000000, 0.000000000000000000, -0.000000000000000000 ) ) ;
#60024=DIRECTION ( 'NONE',  ( 0.000000000000000000, 6.938893903907222067E-15, -1.000000000000000000 ) ) ;
#60041=AXIS2_PLACEMENT_3D ( 'NONE', #62540, #202049, #20872 ) ;
#60047=DIRECTION ( 'NONE',  ( 0.000000000000000000, -1.000000000000000000, -6.860497997771531562E-15 ) ) ;
#60084=VERTEX_POINT ( 'NONE', #11547 ) ;
#60141=AXIS2_PLACEMENT_3D ( 'NONE', #255404, #57233, #75567 ) ;
#60152=ADVANCED_FACE ( 'NONE', ( #49378 ), #72819, .T. ) ;
#60192=VERTEX_POINT ( 'NONE', #190180 ) ;
#60234=AXIS2_PLACEMENT_3D ( 'NONE', #169682, #249185, #66689 ) ;
#60238=TOROIDAL_SURFACE ( 'NONE', #147168, 0.2000000000000000111, 0.1000000000000000056 ) ;
#60242=CARTESIAN_POINT ( 'NONE',  ( 19.75857864376268935, 64.25000000001250555, -178.6731074845244507 ) ) ;
#60262=EDGE_CURVE ( 'NONE', #8118, #220769, #79636, .T. ) ;
#60275=CARTESIAN_POINT ( 'NONE',  ( 20.85000000000000142, 87.65000000001244018, -170.0231074845242745 ) ) ;
#60276=AXIS2_PLACEMENT_3D ( 'NONE', #31439, #88781, #107076 ) ;
#60298=DIRECTION ( 'NONE',  ( 1.000000000000000000, 0.000000000000000000, 0.000000000000000000 ) ) ;
#60375=ORIENTED_EDGE ( 'NONE', *, *, #868, .F. ) ;
#60394=DIRECTION ( 'NONE',  ( 1.000000000000000000, 0.000000000000000000, 0.000000000000000000 ) ) ;
#60404=CARTESIAN_POINT ( 'NONE',  ( 21.05000000000000071, 76.00000000001246292, -172.0231074845243597 ) ) ;
#60415=FACE_OUTER_BOUND ( 'NONE', #227442, .T. ) ;
#60428=CARTESIAN_POINT ( 'NONE',  ( 21.13422380239045850, 69.50667348520697431, -203.5231074845243882 ) ) ;
#60451=CARTESIAN_POINT ( 'NONE',  ( -21.52071067811865746, 68.22071067813118361, -182.3731074845244109 ) ) ;
#60454=VERTEX_POINT ( 'NONE', #188568 ) ;
#60469=ORIENTED_EDGE ( 'NONE', *, *, #140315, .F. ) ;
#60494=CIRCLE ( 'NONE', #156423, 0.5999999999999894307 ) ;
#60504=DIRECTION ( 'NONE',  ( 0.000000000000000000, -6.938893903907222067E-15, 1.000000000000000000 ) ) ;
#60569=CARTESIAN_POINT ( 'NONE',  ( 20.94999999999999574, 76.00000000001267608, -203.5231074845243597 ) ) ;
#60576=DIRECTION ( 'NONE',  ( -0.000000000000000000, 1.000000000000000000, 6.982962677686266711E-15 ) ) ;
#60600=DIRECTION ( 'NONE',  ( -1.000000000000000000, -0.000000000000000000, -0.000000000000000000 ) ) ;
#60608=VERTEX_POINT ( 'NONE', #196270 ) ;
#60640=EDGE_LOOP ( 'NONE', ( #91527, #214672, #69975, #256077 ) ) ;
#60652=DIRECTION ( 'NONE',  ( 0.000000000000000000, -0.1495327102803283015, -0.9887567792719397231 ) ) ;
#60662=CIRCLE ( 'NONE', #143882, 0.1000000000000118433 ) ;
#60666=DIRECTION ( 'NONE',  ( 0.000000000000000000, 0.000000000000000000, 1.000000000000000000 ) ) ;
#60667=ORIENTED_EDGE ( 'NONE', *, *, #194691, .T. ) ;
#60687=CARTESIAN_POINT ( 'NONE',  ( 19.83283456528358002, 64.25000000001250555, -178.6731074851066694 ) ) ;
#60703=AXIS2_PLACEMENT_3D ( 'NONE', #231065, #131939, #206353 ) ;
#60705=CARTESIAN_POINT ( 'NONE',  ( -21.22070241538126112, 69.53005372714306986, -203.6220265150594173 ) ) ;
#60737=CARTESIAN_POINT ( 'NONE',  ( -23.15000000000000213, 76.00000000001243450, -168.0231074845243597 ) ) ;
#60739=AXIS2_PLACEMENT_3D ( 'NONE', #44110, #141914, #3688 ) ;
#60764=DIRECTION ( 'NONE',  ( -1.000000000000000000, 3.265361837132813093E-16, 2.280189983783949500E-30 ) ) ;
#60765=CARTESIAN_POINT ( 'NONE',  ( -18.50000000000000000, 66.65000000001259650, -191.1731074845244223 ) ) ;
#60809=ORIENTED_EDGE ( 'NONE', *, *, #115866, .F. ) ;
#60814=EDGE_CURVE ( 'NONE', #70041, #136156, #201405, .T. ) ;
#60833=EDGE_CURVE ( 'NONE', #17038, #109261, #171638, .T. ) ;
#60853=VECTOR ( 'NONE', #271, 1000.000000000000000 ) ;
#60870=LINE ( 'NONE', #101236, #161376 ) ;
#60891=AXIS2_PLACEMENT_3D ( 'NONE', #1417, #80951, #61407 ) ;
#60955=ORIENTED_EDGE ( 'NONE', *, *, #46420, .T. ) ;
#60959=ORIENTED_EDGE ( 'NONE', *, *, #104389, .T. ) ;
#60963=CARTESIAN_POINT ( 'NONE',  ( -21.44999999999999929, 68.65000000001253966, -182.2731074845244166 ) ) ;
#61028=CIRCLE ( 'NONE', #74120, 11.70000000000001528 ) ;
#61036=AXIS2_PLACEMENT_3D ( 'NONE', #30023, #45700, #27475 ) ;
#61052=EDGE_CURVE ( 'NONE', #85479, #37719, #88569, .T. ) ;
#61074=ORIENTED_EDGE ( 'NONE', *, *, #6699, .T. ) ;
#61117=DIRECTION ( 'NONE',  ( 0.000000000000000000, -1.000000000000000000, -6.982962677686265922E-15 ) ) ;
#61119=CARTESIAN_POINT ( 'NONE',  ( 21.30000000000002558, 76.00000000001267608, -203.5231074845243597 ) ) ;
#61124=DIRECTION ( 'NONE',  ( 1.000000000000000000, 0.000000000000000000, -0.000000000000000000 ) ) ;
#61159=EDGE_CURVE ( 'NONE', #144129, #234461, #50962, .T. ) ;
#61168=DIRECTION ( 'NONE',  ( 1.000000000000000000, 0.000000000000000000, 0.000000000000000000 ) ) ;
#61213=EDGE_CURVE ( 'NONE', #49841, #6886, #31176, .T. ) ;
#61214=SHAPE_DEFINITION_REPRESENTATION ( #47193, #213520 ) ;
#61245=DIRECTION ( 'NONE',  ( 0.000000000000000000, -6.853228547068871147E-15, 1.000000000000000000 ) ) ;
#61257=EDGE_CURVE ( 'NONE', #257053, #255448, #46877, .T. ) ;
#61271=DIRECTION ( 'NONE',  ( 1.000000000000000000, 0.000000000000000000, 0.000000000000000000 ) ) ;
#61345=ORIENTED_EDGE ( 'NONE', *, *, #83341, .F. ) ;
#61373=EDGE_CURVE ( 'NONE', #136156, #3432, #146827, .T. ) ;
#61387=EDGE_LOOP ( 'NONE', ( #66542, #218154, #176934, #240701 ) ) ;
#61398=ORIENTED_EDGE ( 'NONE', *, *, #211975, .T. ) ;
#61407=DIRECTION ( 'NONE',  ( 0.000000000000000000, 0.000000000000000000, -1.000000000000000000 ) ) ;
#61413=ORIENTED_EDGE ( 'NONE', *, *, #161407, .F. ) ;
#61432=DIRECTION ( 'NONE',  ( 0.000000000000000000, -6.417474130781257643E-15, 1.000000000000000000 ) ) ;
#61473=ORIENTED_EDGE ( 'NONE', *, *, #186905, .T. ) ;
#61478=ADVANCED_FACE ( 'NONE', ( #40149 ), #17972, .T. ) ;
#61531=CIRCLE ( 'NONE', #7349, 2.000000000000001776 ) ;
#61541=DIRECTION ( 'NONE',  ( -1.000000000000000000, 0.000000000000000000, -0.000000000000000000 ) ) ;
#61562=DIRECTION ( 'NONE',  ( 2.952720810173289112E-16, 1.000000000000000000, 6.530723674265620862E-15 ) ) ;
#61563=CARTESIAN_POINT ( 'NONE',  ( -23.15000000000000213, 76.00000000001244871, -170.0231074845243597 ) ) ;
#61575=DIRECTION ( 'NONE',  ( 1.000000000000000000, 0.000000000000000000, 0.000000000000000000 ) ) ;
#61579=DIRECTION ( 'NONE',  ( 4.239556034732057360E-17, 0.1298341882519953860, 0.9915357197604862671 ) ) ;
#61604=CIRCLE ( 'NONE', #228011, 0.09999999999998898659 ) ;
#61625=ORIENTED_EDGE ( 'NONE', *, *, #203519, .T. ) ;
#61627=AXIS2_PLACEMENT_3D ( 'NONE', #139330, #119813, #199341 ) ;
#61634=EDGE_LOOP ( 'NONE', ( #206164, #222653, #169851, #16748 ) ) ;
#61651=CARTESIAN_POINT ( 'NONE',  ( -18.52186455169011481, 85.48101848145532244, -196.4980910066099966 ) ) ;
#61661=AXIS2_PLACEMENT_3D ( 'NONE', #208953, #30332, #112437 ) ;
#61666=CARTESIAN_POINT ( 'NONE',  ( -18.50000000000000000, 72.08710075277916474, -192.0412845115134246 ) ) ;
#61686=B_SPLINE_CURVE_WITH_KNOTS ( 'NONE', 3,
 ( #138127, #4705, #216396, #155185, #202923, #242047, #163814, #37788, #36512, #117307, #215117, #43861, #18204, #24313, #123396, #201641, #243329, #78159, #176021 ),
 .UNSPECIFIED., .F., .F.,
 ( 4, 3, 3, 3, 3, 3, 4 ),
 ( 0.000000000000000000, 7.110282409889155599E-05, 0.0001508797727291355647, 0.0002027344179858367663, 0.0002343294522348933582, 0.0002454816334821332082, 0.0002619873080085637876 ),
 .UNSPECIFIED. ) ;
#61697=DIRECTION ( 'NONE',  ( 1.000000000000000000, 0.000000000000000000, 0.000000000000000000 ) ) ;
#61723=AXIS2_PLACEMENT_3D ( 'NONE', #141097, #83639, #42009 ) ;
#61743=FACE_OUTER_BOUND ( 'NONE', #106342, .T. ) ;
#61752=ORIENTED_EDGE ( 'NONE', *, *, #76889, .T. ) ;
#61759=ORIENTED_EDGE ( 'NONE', *, *, #236295, .T. ) ;
#61765=LINE ( 'NONE', #205106, #241199 ) ;
#61766=DIRECTION ( 'NONE',  ( 0.000000000000000000, -7.056502275159890832E-15, 1.000000000000000000 ) ) ;
#61844=CIRCLE ( 'NONE', #103510, 0.1000000000000072220 ) ;
#61845=CIRCLE ( 'NONE', #28579, 0.09999999999998712696 ) ;
#61879=ORIENTED_EDGE ( 'NONE', *, *, #124257, .T. ) ;
#61882=CARTESIAN_POINT ( 'NONE',  ( -22.39999999999999858, 76.00000000001271871, -209.7731074845243597 ) ) ;
#61924=ADVANCED_FACE ( 'NONE', ( #172944 ), #133764, .T. ) ;
#61930=AXIS2_PLACEMENT_3D ( 'NONE', #134851, #39667, #216968 ) ;
#61938=ORIENTED_EDGE ( 'NONE', *, *, #182288, .T. ) ;
#61966=DIRECTION ( 'NONE',  ( 0.000000000000000000, 6.982962677686267499E-15, -1.000000000000000000 ) ) ;
#61991=DIRECTION ( 'NONE',  ( 1.000000000000000000, -2.952720810173289112E-16, -2.061873921506763405E-30 ) ) ;
#62004=CARTESIAN_POINT ( 'NONE',  ( 19.97071067811865674, 64.27928932189384170, -178.8731074845244393 ) ) ;
#62026=VERTEX_POINT ( 'NONE', #219717 ) ;
#62034=ORIENTED_EDGE ( 'NONE', *, *, #6136, .T. ) ;
#62037=CARTESIAN_POINT ( 'NONE',  ( 21.05000000000000071, 75.90220970870393558, -209.7809220950004772 ) ) ;
#62051=DIRECTION ( 'NONE',  ( 0.000000000000000000, 0.000000000000000000, -1.000000000000000000 ) ) ;
#62054=CIRCLE ( 'NONE', #28787, 0.09999999999998898659 ) ;
#62055=DIRECTION ( 'NONE',  ( 1.000000000000000000, 0.000000000000000000, 0.000000000000000000 ) ) ;
#62061=ORIENTED_EDGE ( 'NONE', *, *, #231595, .T. ) ;
#62103=DIRECTION ( 'NONE',  ( 2.694716079187273439E-16, 1.000000000000000000, 6.467318590049456648E-15 ) ) ;
#62123=CARTESIAN_POINT ( 'NONE',  ( 22.47809213839789066, 75.96246293238424130, -215.1730808193121618 ) ) ;
#62126=CYLINDRICAL_SURFACE ( 'NONE', #35880, 0.1000000000000026007 ) ;
#62129=CARTESIAN_POINT ( 'NONE',  ( -20.54999999999999716, 76.00000000001244871, -170.0231074845243597 ) ) ;
#62130=DIRECTION ( 'NONE',  ( 0.000000000000000000, 0.1350103645451945777, -0.9908441862701589109 ) ) ;
#62131=DIRECTION ( 'NONE',  ( 0.000000000000000000, -6.938893903907222067E-15, 1.000000000000000000 ) ) ;
#62142=AXIS2_PLACEMENT_3D ( 'NONE', #143671, #163259, #165833 ) ;
#62154=ORIENTED_EDGE ( 'NONE', *, *, #73750, .F. ) ;
#62161=VECTOR ( 'NONE', #70882, 1000.000000000000000 ) ;
#62196=DIRECTION ( 'NONE',  ( 1.000000000000000000, 0.000000000000000000, 0.000000000000000000 ) ) ;
#62220=AXIS2_PLACEMENT_3D ( 'NONE', #133320, #193301, #52469 ) ;
#62231=ORIENTED_EDGE ( 'NONE', *, *, #182163, .T. ) ;
#62244=CARTESIAN_POINT ( 'NONE',  ( 18.49999999999999645, 76.00000000001244871, -170.0231074845243597 ) ) ;
#62263=DIRECTION ( 'NONE',  ( 0.000000000000000000, -1.000000000000000000, 0.000000000000000000 ) ) ;
#62326=VECTOR ( 'NONE', #147725, 1000.000000000000000 ) ;
#62333=VERTEX_POINT ( 'NONE', #240289 ) ;
#62366=COLOUR_RGB ( '', 0.66274510, 0.83137255, 0.94901961) ;
#62451=CARTESIAN_POINT ( 'NONE',  ( 21.05000000000000426, 65.27628289530510131, -195.9286900929113244 ) ) ;
#62513=TOROIDAL_SURFACE ( 'NONE', #129157, 11.65000000000000036, 0.1000000000000000056 ) ;
#62540=CARTESIAN_POINT ( 'NONE',  ( -23.25000000000000000, 76.00000000001244871, -170.0231074845243597 ) ) ;
#62542=ORIENTED_EDGE ( 'NONE', *, *, #23673, .T. ) ;
#62581=CARTESIAN_POINT ( 'NONE',  ( -20.54999999999999716, 76.00000000001253397, -182.8981074845243597 ) ) ;
#62582=CARTESIAN_POINT ( 'NONE',  ( 21.05000000000000071, 76.10000000001276987, -215.1726782920691505 ) ) ;
#62609=EDGE_LOOP ( 'NONE', ( #74643, #252735, #23568, #24325 ) ) ;
#62639=EDGE_CURVE ( 'NONE', #180867, #90288, #105273, .T. ) ;
#62658=ORIENTED_EDGE ( 'NONE', *, *, #169463, .T. ) ;
#62668=DIRECTION ( 'NONE',  ( 0.000000000000000000, 0.000000000000000000, 1.000000000000000000 ) ) ;
#62670=ORIENTED_EDGE ( 'NONE', *, *, #30050, .T. ) ;
#62681=DIRECTION ( 'NONE',  ( -1.000000000000000000, 1.387778780781454006E-13, 0.000000000000000000 ) ) ;
#62683=ADVANCED_FACE ( 'NONE', ( #15823 ), #95327, .T. ) ;
#62725=DIRECTION ( 'NONE',  ( 0.000000000000000000, -1.000000000000000000, -6.982962677686265922E-15 ) ) ;
#62778=AXIS2_PLACEMENT_3D ( 'NONE', #204485, #88377, #205778 ) ;
#62786=VECTOR ( 'NONE', #27516, 1000.000000000000000 ) ;
#62804=TOROIDAL_SURFACE ( 'NONE', #162771, 12.97499999999999787, 0.1000000000000000056 ) ;
#62819=DIRECTION ( 'NONE',  ( 0.000000000000000000, 0.1298341882519953583, 0.9915357197604862671 ) ) ;
#62869=ORIENTED_EDGE ( 'NONE', *, *, #1998, .T. ) ;
#62877=DIRECTION ( 'NONE',  ( 0.000000000000000000, -0.008583690987135041833, 0.9999631594459055250 ) ) ;
#62971=CARTESIAN_POINT ( 'NONE',  ( 21.05000000000000071, 76.00000000001243450, -168.0231074845243597 ) ) ;
#63031=ORIENTED_EDGE ( 'NONE', *, *, #73539, .F. ) ;
#63068=EDGE_CURVE ( 'NONE', #81897, #66231, #209552, .T. ) ;
#63070=EDGE_CURVE ( 'NONE', #162124, #94393, #98487, .T. ) ;
#63094=ORIENTED_EDGE ( 'NONE', *, *, #243411, .T. ) ;
#63125=FACE_OUTER_BOUND ( 'NONE', #67152, .T. ) ;
#63142=CARTESIAN_POINT ( 'NONE',  ( 20.94999999999999929, 85.00000000001251976, -179.9170766071767389 ) ) ;
#63191=ORIENTED_EDGE ( 'NONE', *, *, #210771, .F. ) ;
#63196=ORIENTED_EDGE ( 'NONE', *, *, #12581, .F. ) ;
#63217=DIRECTION ( 'NONE',  ( -0.000000000000000000, 7.272083257015735086E-15, -1.000000000000000000 ) ) ;
#63242=VERTEX_POINT ( 'NONE', #149241 ) ;
#63301=AXIS2_PLACEMENT_3D ( 'NONE', #124354, #203875, #25265 ) ;
#63319=ORIENTED_EDGE ( 'NONE', *, *, #216551, .T. ) ;
#63330=ORIENTED_EDGE ( 'NONE', *, *, #59752, .T. ) ;
#63347=CIRCLE ( 'NONE', #209116, 0.4000000000000114575 ) ;
#63361=CARTESIAN_POINT ( 'NONE',  ( -20.54999999999999716, 85.00000000001251976, -179.9170766071767389 ) ) ;
#63377=ADVANCED_FACE ( 'NONE', ( #17412 ), #118153, .T. ) ;
#63397=CARTESIAN_POINT ( 'NONE',  ( 18.49999999999999289, 64.25000000001263345, -195.4231074845244223 ) ) ;
#63410=ORIENTED_EDGE ( 'NONE', *, *, #65028, .T. ) ;
#63454=EDGE_CURVE ( 'NONE', #195444, #192399, #193184, .T. ) ;
#63514=CIRCLE ( 'NONE', #167602, 0.2000000000000057288 ) ;
#63551=CARTESIAN_POINT ( 'NONE',  ( -21.14250536705909411, 76.00000000001271871, -210.0412796614051274 ) ) ;
#63600=EDGE_CURVE ( 'NONE', #181442, #10156, #99486, .T. ) ;
#63619=DIRECTION ( 'NONE',  ( 0.000000000000000000, 0.000000000000000000, 1.000000000000000000 ) ) ;
#63620=ORIENTED_EDGE ( 'NONE', *, *, #100048, .T. ) ;
#63657=PLANE ( 'NONE',  #51862 ) ;
#63670=ORIENTED_EDGE ( 'NONE', *, *, #134213, .T. ) ;
#63717=CARTESIAN_POINT ( 'NONE',  ( -18.59999999999999787, 66.65000000001259650, -191.1731074845244223 ) ) ;
#63734=DIRECTION ( 'NONE',  ( 0.000000000000000000, -1.000000000000000000, -6.982962677686266711E-15 ) ) ;
#63755=AXIS2_PLACEMENT_3D ( 'NONE', #38460, #157149, #236651 ) ;
#63760=FACE_OUTER_BOUND ( 'NONE', #192422, .T. ) ;
#63768=VECTOR ( 'NONE', #215203, 999.9999999999998863 ) ;
#63795=AXIS2_PLACEMENT_3D ( 'NONE', #2791, #44517, #221828 ) ;
#63809=EDGE_CURVE ( 'NONE', #203688, #225819, #139153, .T. ) ;
#63845=CARTESIAN_POINT ( 'NONE',  ( 21.07888907270776002, 65.27493078649737868, -191.3019138976912359 ) ) ;
#63856=ORIENTED_EDGE ( 'NONE', *, *, #41038, .T. ) ;
#63910=EDGE_LOOP ( 'NONE', ( #23352, #118870, #159912, #192665 ) ) ;
#63935=DIRECTION ( 'NONE',  ( 0.000000000000000000, -0.4999999999999088507, 0.8660254037844913322 ) ) ;
#63948=VERTEX_POINT ( 'NONE', #178490 ) ;
#63974=CARTESIAN_POINT ( 'NONE',  ( -20.54999999999999716, 68.75000000001253397, -182.3731074845244109 ) ) ;
#63979=ORIENTED_EDGE ( 'NONE', *, *, #252204, .F. ) ;
#64030=ORIENTED_EDGE ( 'NONE', *, *, #196, .T. ) ;
#64048=DIRECTION ( 'NONE',  ( 1.000000000000000000, 0.000000000000000000, 0.000000000000000000 ) ) ;
#64073=CARTESIAN_POINT ( 'NONE',  ( -23.15000000000000213, 74.00000000001254818, -183.2477294072864709 ) ) ;
#64084=CARTESIAN_POINT ( 'NONE',  ( -20.54999999999999716, 87.75000000001256240, -186.7731074845242745 ) ) ;
#64098=ADVANCED_FACE ( 'NONE', ( #64919 ), #189268, .T. ) ;
#64105=FACE_OUTER_BOUND ( 'NONE', #207927, .T. ) ;
#64122=EDGE_CURVE ( 'NONE', #223652, #82861, #33557, .T. ) ;
#64133=CIRCLE ( 'NONE', #89052, 0.1000000000000072220 ) ;
#64139=AXIS2_PLACEMENT_3D ( 'NONE', #35021, #53266, #256530 ) ;
#64148=CARTESIAN_POINT ( 'NONE',  ( -23.25000000000000000, 64.35000000001268461, -203.5231074845244166 ) ) ;
#64153=CYLINDRICAL_SURFACE ( 'NONE', #34746, 0.09999999999999939493 ) ;
#64174=CARTESIAN_POINT ( 'NONE',  ( -18.59999999999999787, 76.00000000001244871, -170.0231074845243597 ) ) ;
#64196=TOROIDAL_SURFACE ( 'NONE', #234893, 0.4000000000000010214, 0.1000000000000000056 ) ;
#64203=CARTESIAN_POINT ( 'NONE',  ( -18.46907102845854709, 85.47372736477650790, -163.3470727457878411 ) ) ;
#64209=CARTESIAN_POINT ( 'NONE',  ( 21.05000000000000071, 71.14953271029291670, -182.0573748935260880 ) ) ;
#64233=ORIENTED_EDGE ( 'NONE', *, *, #236960, .T. ) ;
#64303=CARTESIAN_POINT ( 'NONE',  ( -18.39999999999999858, 85.50000000001263345, -196.4910380878246201 ) ) ;
#64316=CIRCLE ( 'NONE', #210081, 0.09999999999999971412 ) ;
#64378=CARTESIAN_POINT ( 'NONE',  ( -21.05000000000000071, 76.00000000001267608, -203.5231074845243597 ) ) ;
#64388=EDGE_LOOP ( 'NONE', ( #52944, #187766, #88600, #63196 ) ) ;
#64447=ORIENTED_EDGE ( 'NONE', *, *, #246771, .F. ) ;
#64451=DIRECTION ( 'NONE',  ( 1.000000000000000000, 0.000000000000000000, 0.000000000000000000 ) ) ;
#64489=CARTESIAN_POINT ( 'NONE',  ( -23.15000000000000213, 71.85000000001259934, -191.1731074845243654 ) ) ;
#64498=ORIENTED_EDGE ( 'NONE', *, *, #120936, .F. ) ;
#64499=CARTESIAN_POINT ( 'NONE',  ( 20.97468175916167255, 65.37473483564157561, -191.2683460491116421 ) ) ;
#64510=CIRCLE ( 'NONE', #160397, 11.80000000000000426 ) ;
#64517=VERTEX_POINT ( 'NONE', #102423 ) ;
#64518=DIRECTION ( 'NONE',  ( -2.602085213965226419E-14, -6.982962677686266711E-15, 1.000000000000000000 ) ) ;
#64531=CYLINDRICAL_SURFACE ( 'NONE', #209528, 0.1000000000000118433 ) ;
#64546=CARTESIAN_POINT ( 'NONE',  ( 21.04105312098497649, 67.12466737696898633, -191.1946007373123564 ) ) ;
#64559=CARTESIAN_POINT ( 'NONE',  ( 22.57320508075687115, 64.25000000001269029, -203.5231074845244166 ) ) ;
#64598=CARTESIAN_POINT ( 'NONE',  ( -20.93975676684922504, 65.68895814178293335, -164.5026557862138645 ) ) ;
#64631=ADVANCED_FACE ( 'NONE', ( #26809 ), #95421, .F. ) ;
#64637=EDGE_LOOP ( 'NONE', ( #124445, #170817, #13273, #25373 ) ) ;
#64679=CARTESIAN_POINT ( 'NONE',  ( 21.00000000000000000, 66.25000000001253397, -182.3731074845244393 ) ) ;
#64702=EDGE_CURVE ( 'NONE', #173853, #186763, #2723, .T. ) ;
#64708=CARTESIAN_POINT ( 'NONE',  ( 20.94999999999999929, 76.00000000001244871, -170.0231074845243597 ) ) ;
#64730=DIRECTION ( 'NONE',  ( 0.000000000000000000, 0.000000000000000000, 1.000000000000000000 ) ) ;
#64810=DIRECTION ( 'NONE',  ( -1.000000000000000000, 0.000000000000000000, -0.000000000000000000 ) ) ;
#64815=CYLINDRICAL_SURFACE ( 'NONE', #121964, 0.09999999999999939493 ) ;
#64834=CARTESIAN_POINT ( 'NONE',  ( -21.08621493067320429, 75.94380516053668373, -209.8724017756962894 ) ) ;
#64844=DIRECTION ( 'NONE',  ( 0.000000000000000000, 0.000000000000000000, 1.000000000000000000 ) ) ;
#64882=EDGE_CURVE ( 'NONE', #145935, #143032, #43877, .T. ) ;
#64919=FACE_OUTER_BOUND ( 'NONE', #228745, .T. ) ;
#64951=VERTEX_POINT ( 'NONE', #54704 ) ;
#65003=TOROIDAL_SURFACE ( 'NONE', #231614, 0.2000000000000000111, 0.1000000000000000056 ) ;
#65014=DIRECTION ( 'NONE',  ( 1.000000000000000000, 0.000000000000000000, 0.000000000000000000 ) ) ;
#65021=FACE_OUTER_BOUND ( 'NONE', #42664, .T. ) ;
#65028=EDGE_CURVE ( 'NONE', #246982, #246161, #197982, .T. ) ;
#65041=AXIS2_PLACEMENT_3D ( 'NONE', #70139, #45407, #207056 ) ;
#65051=CARTESIAN_POINT ( 'NONE',  ( -20.54999999999999716, 84.66355140188177586, -193.9990063664569959 ) ) ;
#65054=CARTESIAN_POINT ( 'NONE',  ( -23.25000000000000000, 71.65000000001259650, -191.2731074845243882 ) ) ;
#65060=CIRCLE ( 'NONE', #210802, 0.09999999999999939493 ) ;
#65063=TOROIDAL_SURFACE ( 'NONE', #210804, 4.149999999999999467, 0.1000000000000000056 ) ;
#65070=EDGE_CURVE ( 'NONE', #133285, #47404, #110502, .T. ) ;
#65087=CIRCLE ( 'NONE', #19294, 0.4000000000000114575 ) ;
#65121=CARTESIAN_POINT ( 'NONE',  ( -18.43569575749026512, 85.51932773110507924, -196.5501311079650293 ) ) ;
#65131=CARTESIAN_POINT ( 'NONE',  ( 18.49999999999998934, 69.45000000001252261, -182.2731074845244166 ) ) ;
#65141=AXIS2_PLACEMENT_3D ( 'NONE', #142829, #201542, #43761 ) ;
#65208=CARTESIAN_POINT ( 'NONE',  ( 18.49999999999999645, 77.16412189325360771, -162.1082593989527254 ) ) ;
#65221=CARTESIAN_POINT ( 'NONE',  ( 18.49999999999999289, 69.35000000001254250, -182.1731074845243938 ) ) ;
#65263=FACE_OUTER_BOUND ( 'NONE', #192137, .T. ) ;
#65283=DIRECTION ( 'NONE',  ( 0.000000000000000000, 1.000000000000000000, 6.982962677686266711E-15 ) ) ;
#65312=VERTEX_POINT ( 'NONE', #210906 ) ;
#65330=CARTESIAN_POINT ( 'NONE',  ( 20.94999999999999929, 76.00000000001244871, -170.0231074845243597 ) ) ;
#65332=CARTESIAN_POINT ( 'NONE',  ( -21.05000000000000071, 70.10000000001267040, -193.3040077198679967 ) ) ;
#65343=FACE_OUTER_BOUND ( 'NONE', #211892, .T. ) ;
#65357=DIRECTION ( 'NONE',  ( 0.000000000000000000, -1.000000000000000000, 0.000000000000000000 ) ) ;
#65382=DIRECTION ( 'NONE',  ( 0.000000000000000000, -1.000000000000000000, -6.982962677686265922E-15 ) ) ;
#65395=CARTESIAN_POINT ( 'NONE',  ( 20.95520789717937404, 65.42306940062766785, -195.9428745106495739 ) ) ;
#65411=CYLINDRICAL_SURFACE ( 'NONE', #46967, 0.09999999999999939493 ) ;
#65436=ORIENTED_EDGE ( 'NONE', *, *, #67944, .T. ) ;
#65463=CIRCLE ( 'NONE', #73877, 0.1000000000000011990 ) ;
#65465=AXIS2_PLACEMENT_3D ( 'NONE', #87796, #186954, #229904 ) ;
#65473=CARTESIAN_POINT ( 'NONE',  ( -18.50000000000000355, 85.41908450282569731, -163.1931996774988818 ) ) ;
#65525=EDGE_CURVE ( 'NONE', #114775, #225348, #65087, .T. ) ;
#65528=VERTEX_POINT ( 'NONE', #213468 ) ;
#65530=CARTESIAN_POINT ( 'NONE',  ( -21.05000000000000071, 76.00000000001253397, -181.7231074845243484 ) ) ;
#65541=VERTEX_POINT ( 'NONE', #182056 ) ;
#65567=EDGE_LOOP ( 'NONE', ( #153863, #256972, #76863, #67519 ) ) ;
#65588=AXIS2_PLACEMENT_3D ( 'NONE', #22055, #224074, #2458 ) ;
#65675=CARTESIAN_POINT ( 'NONE',  ( -18.59999999999999787, 77.83585931145600512, -158.5186683157258187 ) ) ;
#65690=DIRECTION ( 'NONE',  ( -1.000000000000000000, 0.000000000000000000, 0.000000000000000000 ) ) ;
#65693=FACE_OUTER_BOUND ( 'NONE', #37374, .T. ) ;
#65732=AXIS2_PLACEMENT_3D ( 'NONE', #167850, #126107, #229087 ) ;
#65745=ORIENTED_EDGE ( 'NONE', *, *, #142683, .T. ) ;
#65775=CIRCLE ( 'NONE', #215784, 0.09999999999998898659 ) ;
#65778=CARTESIAN_POINT ( 'NONE',  ( 21.08804281139604342, 65.37816569817142920, -191.1731075171456098 ) ) ;
#65803=CARTESIAN_POINT ( 'NONE',  ( 20.72390388899090041, 65.41003688158858154, -196.0117591887780861 ) ) ;
#65806=LINE ( 'NONE', #206604, #106494 ) ;
#65823=CIRCLE ( 'NONE', #90957, 0.09999999999998898659 ) ;
#65844=CARTESIAN_POINT ( 'NONE',  ( 22.59080734064468388, 64.25000000001269029, -203.5538571926215070 ) ) ;
#65863=FACE_OUTER_BOUND ( 'NONE', #22778, .T. ) ;
#65869=ORIENTED_EDGE ( 'NONE', *, *, #43213, .T. ) ;
#65880=AXIS2_PLACEMENT_3D ( 'NONE', #110932, #170964, #70558 ) ;
#65887=CARTESIAN_POINT ( 'NONE',  ( 23.14999999999999858, 76.00000000001244871, -170.0231074845243597 ) ) ;
#65896=CIRCLE ( 'NONE', #19945, 11.75000000000001066 ) ;
#65963=VERTEX_POINT ( 'NONE', #123061 ) ;
#65967=CARTESIAN_POINT ( 'NONE',  ( -21.05000000000000071, 76.00000000001267608, -203.5231074845243597 ) ) ;
#65970=FACE_OUTER_BOUND ( 'NONE', #73545, .T. ) ;
#65972=CARTESIAN_POINT ( 'NONE',  ( -23.15000000000000213, 74.00000000001259082, -190.2984855617622770 ) ) ;
#65985=FACE_OUTER_BOUND ( 'NONE', #226113, .T. ) ;
#66018=DIRECTION ( 'NONE',  ( 0.000000000000000000, -1.000000000000000000, -6.982962677686266711E-15 ) ) ;
#66025=ORIENTED_EDGE ( 'NONE', *, *, #103594, .F. ) ;
#66026=ORIENTED_EDGE ( 'NONE', *, *, #240596, .T. ) ;
#66037=ORIENTED_EDGE ( 'NONE', *, *, #114851, .T. ) ;
#66039=ORIENTED_EDGE ( 'NONE', *, *, #58530, .T. ) ;
#66089=CARTESIAN_POINT ( 'NONE',  ( -22.47071067811865319, 68.27992525551461256, -203.6221999392270448 ) ) ;
#66100=ORIENTED_EDGE ( 'NONE', *, *, #173563, .F. ) ;
#66117=ORIENTED_EDGE ( 'NONE', *, *, #36017, .F. ) ;
#66129=VERTEX_POINT ( 'NONE', #133330 ) ;
#66154=( BOUNDED_CURVE ( )  B_SPLINE_CURVE ( 3, ( #198336, #22294, #157978, #19719 ),
 .UNSPECIFIED., .F., .F. ) 
 B_SPLINE_CURVE_WITH_KNOTS ( ( 4, 4 ),
 ( 4.712388980384690562, 6.283185307179586232 ),
 .UNSPECIFIED. ) 
 CURVE ( )  GEOMETRIC_REPRESENTATION_ITEM ( )  RATIONAL_B_SPLINE_CURVE ( ( 1.000000000000000000, 0.8047378541243652705, 0.8047378541243652705, 1.000000000000000000 ) ) 
 REPRESENTATION_ITEM ( '' )  );
#66217=CARTESIAN_POINT ( 'NONE',  ( -20.54999999999999716, 68.85000000001259934, -191.1731074845243938 ) ) ;
#66223=EDGE_CURVE ( 'NONE', #133612, #164331, #190376, .T. ) ;
#66231=VERTEX_POINT ( 'NONE', #232449 ) ;
#66233=ORIENTED_EDGE ( 'NONE', *, *, #191498, .T. ) ;
#66249=DIRECTION ( 'NONE',  ( 0.000000000000000000, 0.000000000000000000, 1.000000000000000000 ) ) ;
#66259=ORIENTED_EDGE ( 'NONE', *, *, #29012, .F. ) ;
#66265=ORIENTED_EDGE ( 'NONE', *, *, #19168, .F. ) ;
#66267=ORIENTED_EDGE ( 'NONE', *, *, #98909, .T. ) ;
#66270=AXIS2_PLACEMENT_3D ( 'NONE', #108065, #205867, #145887 ) ;
#66275=EDGE_CURVE ( 'NONE', #49841, #67817, #177738, .T. ) ;
#66314=DIRECTION ( 'NONE',  ( 0.000000000000000000, -0.9999631594459057471, 0.008583690987121077309 ) ) ;
#66316=CARTESIAN_POINT ( 'NONE',  ( 21.05000000000000071, 70.50000000001260503, -191.1178414656113205 ) ) ;
#66334=EDGE_LOOP ( 'NONE', ( #36658, #101386, #3583, #170008 ) ) ;
#66359=ORIENTED_EDGE ( 'NONE', *, *, #27036, .F. ) ;
#66374=CARTESIAN_POINT ( 'NONE',  ( -20.94999999999999929, 76.00000000001267608, -203.5231074845243597 ) ) ;
#66382=CARTESIAN_POINT ( 'NONE',  ( -21.56666275994540172, 76.00000000001271871, -210.4804758914176830 ) ) ;
#66441=ORIENTED_EDGE ( 'NONE', *, *, #56798, .T. ) ;
#66481=DIRECTION ( 'NONE',  ( -0.000000000000000000, 1.000000000000000000, 6.982962677686266711E-15 ) ) ;
#66539=CIRCLE ( 'NONE', #8285, 0.09999999999999080458 ) ;
#66542=ORIENTED_EDGE ( 'NONE', *, *, #191902, .T. ) ;
#66548=CARTESIAN_POINT ( 'NONE',  ( 21.05000000000000071, 87.75000000001264766, -200.6231074845242688 ) ) ;
#66555=CARTESIAN_POINT ( 'NONE',  ( 18.51997666896902928, 85.39233213153144675, -196.3797012970422031 ) ) ;
#66567=AXIS2_PLACEMENT_3D ( 'NONE', #224117, #200719, #199452 ) ;
#66623=DIRECTION ( 'NONE',  ( 1.000000000000000000, 0.000000000000000000, 0.000000000000000000 ) ) ;
#66632=EDGE_CURVE ( 'NONE', #176065, #133309, #38741, .T. ) ;
#66647=AXIS2_PLACEMENT_3D ( 'NONE', #132502, #110360, #89504 ) ;
#66664=ADVANCED_FACE ( 'NONE', ( #234353 ), #55682, .F. ) ;
#66689=DIRECTION ( 'NONE',  ( 1.000000000000000000, 0.000000000000000000, 0.000000000000000000 ) ) ;
#66699=DIRECTION ( 'NONE',  ( 0.000000000000000000, -6.982962677686266711E-15, 1.000000000000000000 ) ) ;
#66720=DIRECTION ( 'NONE',  ( -1.000000000000000000, -0.000000000000000000, -0.000000000000000000 ) ) ;
#66763=CIRCLE ( 'NONE', #4200, 0.09999999999998898659 ) ;
#66765=DIRECTION ( 'NONE',  ( 0.000000000000000000, 0.000000000000000000, 1.000000000000000000 ) ) ;
#66773=CARTESIAN_POINT ( 'NONE',  ( -18.42637059832564717, 85.49694546190212918, -163.4140301747244450 ) ) ;
#66810=EDGE_LOOP ( 'NONE', ( #124262, #181246, #3848, #114468 ) ) ;
#66854=CARTESIAN_POINT ( 'NONE',  ( 22.39999999999999503, 64.25000000001269029, -203.4231074845244507 ) ) ;
#66867=DIRECTION ( 'NONE',  ( -1.000000000000000000, 0.000000000000000000, 0.000000000000000000 ) ) ;
#66890=DIRECTION ( 'NONE',  ( 1.000000000000000000, 0.000000000000000000, 0.000000000000000000 ) ) ;
#66897=CARTESIAN_POINT ( 'NONE',  ( -20.54999999999999716, 66.65000000001253966, -182.3731074845244393 ) ) ;
#66904=DIRECTION ( 'NONE',  ( 0.000000000000000000, 0.000000000000000000, -1.000000000000000000 ) ) ;
#66907=DIRECTION ( 'NONE',  ( -2.952720810173289605E-16, -1.000000000000000000, -7.086529944415894657E-15 ) ) ;
#66911=VECTOR ( 'NONE', #242365, 1000.000000000000000 ) ;
#66912=DIRECTION ( 'NONE',  ( 1.000000000000000000, 0.000000000000000000, 0.000000000000000000 ) ) ;
#66953=EDGE_CURVE ( 'NONE', #133285, #247461, #19862, .T. ) ;
#66963=DIRECTION ( 'NONE',  ( 0.000000000000000000, 0.9893560106964510714, -0.1455152366551481502 ) ) ;
#66979=EDGE_LOOP ( 'NONE', ( #172360, #205390, #176161, #74464 ) ) ;
#67050=EDGE_CURVE ( 'NONE', #83828, #155749, #183076, .T. ) ;
#67102=CARTESIAN_POINT ( 'NONE',  ( 21.04999999999999716, 75.98528214348870335, -209.8678308886149750 ) ) ;
#67119=CARTESIAN_POINT ( 'NONE',  ( 21.05000000000000071, 67.22371710472012296, -191.3731074845244109 ) ) ;
#67152=EDGE_LOOP ( 'NONE', ( #13459, #61345, #210632, #158074 ) ) ;
#67179=DIRECTION ( 'NONE',  ( 0.000000000000000000, -7.172728831056617961E-15, 1.000000000000000000 ) ) ;
#67181=CARTESIAN_POINT ( 'NONE',  ( -20.94999027547553894, 65.70673848567030007, -164.5638252334829588 ) ) ;
#67191=CARTESIAN_POINT ( 'NONE',  ( -21.05000000000000071, 61.95000000001265050, -198.0094124137634708 ) ) ;
#67201=CARTESIAN_POINT ( 'NONE',  ( -23.25000000000000000, 76.00000000001244871, -170.0231074845243597 ) ) ;
#67227=EDGE_LOOP ( 'NONE', ( #225168, #38059, #88864, #112582 ) ) ;
#67233=ADVANCED_FACE ( 'NONE', ( #38130 ), #194652, .F. ) ;
#67234=EDGE_CURVE ( 'NONE', #92906, #257555, #203381, .T. ) ;
#67242=CIRCLE ( 'NONE', #58849, 0.09999999999998898659 ) ;
#67289=ORIENTED_EDGE ( 'NONE', *, *, #202759, .T. ) ;
#67291=CARTESIAN_POINT ( 'NONE',  ( 23.14999999999999858, 71.00000000001253397, -182.4283735034374843 ) ) ;
#67299=ADVANCED_FACE ( 'NONE', ( #254558 ), #255826, .T. ) ;
#67325=CARTESIAN_POINT ( 'NONE',  ( -20.94999999999999929, 74.83729825007462466, -195.5231074845243597 ) ) ;
#67335=CARTESIAN_POINT ( 'NONE',  ( 18.55857864376268296, 65.63284271248713253, -178.7731074845244450 ) ) ;
#67339=AXIS2_PLACEMENT_3D ( 'NONE', #17532, #97039, #155806 ) ;
#67384=ORIENTED_EDGE ( 'NONE', *, *, #132859, .T. ) ;
#67411=CARTESIAN_POINT ( 'NONE',  ( -21.07933241753356413, 75.90662040959345802, -209.8517534329041041 ) ) ;
#67413=CARTESIAN_POINT ( 'NONE',  ( -18.50000000000000000, 66.85000000001254250, -182.3731074845244393 ) ) ;
#67425=ORIENTED_EDGE ( 'NONE', *, *, #230864, .F. ) ;
#67432=CYLINDRICAL_SURFACE ( 'NONE', #65732, 0.09999999999998898659 ) ;
#67458=CARTESIAN_POINT ( 'NONE',  ( 21.53752568617687402, 69.21319212550885425, -203.6220819458088158 ) ) ;
#67460=ORIENTED_EDGE ( 'NONE', *, *, #252819, .T. ) ;
#67468=ADVANCED_FACE ( 'NONE', ( #4473 ), #141422, .T. ) ;
#67494=CIRCLE ( 'NONE', #134129, 0.09999999999998898659 ) ;
#67498=CARTESIAN_POINT ( 'NONE',  ( 20.94999999999999929, 71.00000000001253397, -181.9283735034374843 ) ) ;
#67501=ORIENTED_EDGE ( 'NONE', *, *, #169333, .T. ) ;
#67516=VERTEX_POINT ( 'NONE', #119303 ) ;
#67519=ORIENTED_EDGE ( 'NONE', *, *, #237452, .F. ) ;
#67593=DIRECTION ( 'NONE',  ( 0.000000000000000000, 0.000000000000000000, 1.000000000000000000 ) ) ;
#67594=FACE_OUTER_BOUND ( 'NONE', #51899, .T. ) ;
#67604=ORIENTED_EDGE ( 'NONE', *, *, #177886, .F. ) ;
#67618=CIRCLE ( 'NONE', #30222, 0.2000000000000057288 ) ;
#67666=ORIENTED_EDGE ( 'NONE', *, *, #168950, .F. ) ;
#67670=DIRECTION ( 'NONE',  ( 0.000000000000000000, 0.000000000000000000, 1.000000000000000000 ) ) ;
#67715=EDGE_LOOP ( 'NONE', ( #88375, #26971, #219399, #11338 ) ) ;
#67733=DIRECTION ( 'NONE',  ( 0.000000000000000000, -1.000000000000000000, -6.982962677686265922E-15 ) ) ;
#67761=DIRECTION ( 'NONE',  ( 0.000000000000000000, 6.982962677686266711E-15, -1.000000000000000000 ) ) ;
#67774=DIRECTION ( 'NONE',  ( 0.000000000000000000, 6.982962677686266711E-15, -1.000000000000000000 ) ) ;
#67783=EDGE_CURVE ( 'NONE', #88021, #54936, #120494, .T. ) ;
#67793=CARTESIAN_POINT ( 'NONE',  ( 21.05000000000000071, 67.22371710472015138, -194.9644784893834810 ) ) ;
#67796=ORIENTED_EDGE ( 'NONE', *, *, #221550, .F. ) ;
#67798=VECTOR ( 'NONE', #219906, 1000.000000000000000 ) ;
#67817=VERTEX_POINT ( 'NONE', #14794 ) ;
#67841=CARTESIAN_POINT ( 'NONE',  ( -21.14999999893415250, 64.25000000001264766, -196.6786121409979273 ) ) ;
#67871=EDGE_CURVE ( 'NONE', #192399, #151179, #90547, .T. ) ;
#67880=ORIENTED_EDGE ( 'NONE', *, *, #133221, .F. ) ;
#67892=CARTESIAN_POINT ( 'NONE',  ( -21.55000000000000426, 68.25000000001253397, -182.3731074845244109 ) ) ;
#67895=CIRCLE ( 'NONE', #192800, 0.09999999999999939493 ) ;
#67904=LINE ( 'NONE', #65332, #214943 ) ;
#67942=EDGE_CURVE ( 'NONE', #223851, #71853, #61531, .T. ) ;
#67944=EDGE_CURVE ( 'NONE', #95308, #143032, #194824, .T. ) ;
#67947=ORIENTED_EDGE ( 'NONE', *, *, #131979, .F. ) ;
#67990=EDGE_CURVE ( 'NONE', #233373, #244528, #128163, .T. ) ;
#68003=CARTESIAN_POINT ( 'NONE',  ( -22.43310005002225438, 75.99436305787187962, -215.1727696116587651 ) ) ;
#68004=EDGE_LOOP ( 'NONE', ( #17784, #194640, #143524, #117166, #244123 ) ) ;
#68050=CIRCLE ( 'NONE', #143031, 0.09999999999998898659 ) ;
#68076=EDGE_CURVE ( 'NONE', #116470, #37214, #15771, .T. ) ;
#68082=AXIS2_PLACEMENT_3D ( 'NONE', #124114, #45842, #61562 ) ;
#68092=ORIENTED_EDGE ( 'NONE', *, *, #161650, .T. ) ;
#68098=DIRECTION ( 'NONE',  ( -1.000000000000000000, 2.952720810173289112E-16, 2.061873921506763405E-30 ) ) ;
#68105=ADVANCED_FACE ( 'NONE', ( #88830 ), #228379, .T. ) ;
#68163=CIRCLE ( 'NONE', #213909, 4.000000000000003553 ) ;
#68183=CIRCLE ( 'NONE', #176355, 0.09999999999999939493 ) ;
#68199=DIRECTION ( 'NONE',  ( 0.000000000000000000, -0.1298341882519953860, -0.9915357197604862671 ) ) ;
#68214=ORIENTED_EDGE ( 'NONE', *, *, #58772, .F. ) ;
#68218=ORIENTED_EDGE ( 'NONE', *, *, #203182, .F. ) ;
#68223=CIRCLE ( 'NONE', #226606, 0.09999999999999939493 ) ;
#68241=VERTEX_POINT ( 'NONE', #15773 ) ;
#68271=CARTESIAN_POINT ( 'NONE',  ( 22.47071067811865319, 68.27992525551464098, -203.6221999392270448 ) ) ;
#68284=CARTESIAN_POINT ( 'NONE',  ( -20.64999999999999858, 71.65000000001253966, -182.2731074845243882 ) ) ;
#68287=ORIENTED_EDGE ( 'NONE', *, *, #183782, .F. ) ;
#68289=CARTESIAN_POINT ( 'NONE',  ( -18.50016250449483479, 65.70233904877069619, -164.5487410911968595 ) ) ;
#68291=CYLINDRICAL_SURFACE ( 'NONE', #36501, 0.5000000000000004441 ) ;
#68340=VECTOR ( 'NONE', #194470, 1000.000000000000000 ) ;
#68342=VERTEX_POINT ( 'NONE', #159129 ) ;
#68380=AXIS2_PLACEMENT_3D ( 'NONE', #11318, #242545, #52997 ) ;
#68385=CIRCLE ( 'NONE', #39191, 0.09999999999999080458 ) ;
#68421=DIRECTION ( 'NONE',  ( -1.000000000000000000, -0.000000000000000000, -0.000000000000000000 ) ) ;
#68448=AXIS2_PLACEMENT_3D ( 'NONE', #19519, #80740, #82007 ) ;
#68455=CIRCLE ( 'NONE', #93381, 0.1000000000000046685 ) ;
#68471=CARTESIAN_POINT ( 'NONE',  ( -20.91682497891422798, 65.67736539654997330, -164.4625116876572406 ) ) ;
#68488=CARTESIAN_POINT ( 'NONE',  ( 23.24999999999997513, 64.35000000001249987, -177.0379132551783812 ) ) ;
#68496=EDGE_CURVE ( 'NONE', #29575, #196694, #144894, .T. ) ;
#68514=DIRECTION ( 'NONE',  ( 0.000000000000000000, 0.000000000000000000, 1.000000000000000000 ) ) ;
#68516=DIRECTION ( 'NONE',  ( 0.000000000000000000, 6.467318590049456648E-15, -1.000000000000000000 ) ) ;
#68544=DIRECTION ( 'NONE',  ( 0.000000000000000000, -1.000000000000000000, -7.109473446599835262E-15 ) ) ;
#68545=CARTESIAN_POINT ( 'NONE',  ( 18.60000000000000853, 85.36423601037941467, -196.3428530837996959 ) ) ;
#68547=CARTESIAN_POINT ( 'NONE',  ( 23.24999999999999289, 69.35000000001259934, -191.3731074845244109 ) ) ;
#68552=EDGE_LOOP ( 'NONE', ( #93677, #70720, #40227, #120780, #170086, #40062, #86975 ) ) ;
#68559=ORIENTED_EDGE ( 'NONE', *, *, #77297, .F. ) ;
#68569=DIRECTION ( 'NONE',  ( 1.000000000000000000, 0.000000000000000000, 0.000000000000000000 ) ) ;
#68576=DIRECTION ( 'NONE',  ( 0.000000000000000000, 0.000000000000000000, 1.000000000000000000 ) ) ;
#68585=EDGE_CURVE ( 'NONE', #203688, #37447, #28423, .T. ) ;
#68606=FACE_OUTER_BOUND ( 'NONE', #191311, .T. ) ;
#68636=DIRECTION ( 'NONE',  ( -1.000000000000000000, 0.000000000000000000, 0.000000000000000000 ) ) ;
#68642=AXIS2_PLACEMENT_3D ( 'NONE', #174840, #114814, #251756 ) ;
#68658=DIRECTION ( 'NONE',  ( 0.000000000000000000, 0.000000000000000000, -1.000000000000000000 ) ) ;
#68668=CARTESIAN_POINT ( 'NONE',  ( -21.93340585972069334, 68.67585297715930892, -203.5231074845244166 ) ) ;
#68670=DIRECTION ( 'NONE',  ( 1.000000000000000000, 0.000000000000000000, 0.000000000000000000 ) ) ;
#68678=FACE_OUTER_BOUND ( 'NONE', #233939, .T. ) ;
#68763=CYLINDRICAL_SURFACE ( 'NONE', #197062, 0.1000000000000028644 ) ;
#68797=ADVANCED_FACE ( 'NONE', ( #179654 ), #158819, .F. ) ;
#68800=AXIS2_PLACEMENT_3D ( 'NONE', #157558, #197911, #16737 ) ;
#68808=VERTEX_POINT ( 'NONE', #182213 ) ;
#68819=DIRECTION ( 'NONE',  ( 0.000000000000000000, 0.000000000000000000, -1.000000000000000000 ) ) ;
#68853=ORIENTED_EDGE ( 'NONE', *, *, #107267, .F. ) ;
#68916=CARTESIAN_POINT ( 'NONE',  ( 18.49999999999999645, 76.00000000001267608, -203.5231074845243597 ) ) ;
#68953=EDGE_CURVE ( 'NONE', #226290, #204385, #79083, .T. ) ;
#68968=CARTESIAN_POINT ( 'NONE',  ( -21.14999999999999858, 64.25000000001269029, -203.5231074845244166 ) ) ;
#68995=AXIS2_PLACEMENT_3D ( 'NONE', #161234, #4692, #62131 ) ;
#69007=SPHERICAL_SURFACE ( 'NONE', #44349, 0.1000000000000000056 ) ;
#69008=ORIENTED_EDGE ( 'NONE', *, *, #123801, .T. ) ;
#69040=DIRECTION ( 'NONE',  ( 0.000000000000000000, -0.6728971962617102953, -0.7397360091702507301 ) ) ;
#69054=AXIS2_PLACEMENT_3D ( 'NONE', #69935, #167755, #68636 ) ;
#69122=ORIENTED_EDGE ( 'NONE', *, *, #154228, .T. ) ;
#69166=EDGE_CURVE ( 'NONE', #18425, #105519, #68223, .T. ) ;
#69180=VERTEX_POINT ( 'NONE', #201450 ) ;
#69199=ORIENTED_EDGE ( 'NONE', *, *, #30258, .F. ) ;
#69340=TOROIDAL_SURFACE ( 'NONE', #240022, 0.4000000000000009104, 0.1000000000000000056 ) ;
#69353=ORIENTED_EDGE ( 'NONE', *, *, #198549, .T. ) ;
#69391=DIRECTION ( 'NONE',  ( 0.000000000000000000, -1.000000000000000000, -6.982962677686266711E-15 ) ) ;
#69399=DIRECTION ( 'NONE',  ( -0.000000000000000000, 1.000000000000000000, 6.982962677686266711E-15 ) ) ;
#69411=EDGE_CURVE ( 'NONE', #89282, #65312, #235007, .T. ) ;
#69412=CARTESIAN_POINT ( 'NONE',  ( -21.07954640115405454, 69.67071230398777004, -203.5891151916643480 ) ) ;
#69419=EDGE_CURVE ( 'NONE', #121003, #6765, #176750, .T. ) ;
#69471=CIRCLE ( 'NONE', #190276, 11.74999999999999645 ) ;
#69480=CARTESIAN_POINT ( 'NONE',  ( 21.14999999999999858, 65.28660755661270798, -191.1731074845244223 ) ) ;
#69529=ORIENTED_EDGE ( 'NONE', *, *, #174506, .F. ) ;
#69530=VECTOR ( 'NONE', #113362, 1000.000000000000000 ) ;
#69541=CIRCLE ( 'NONE', #161106, 0.09999999999999230338 ) ;
#69546=ORIENTED_EDGE ( 'NONE', *, *, #21054, .F. ) ;
#69552=DIRECTION ( 'NONE',  ( 0.000000000000000000, -0.1575844902526687130, -0.9875055080513762684 ) ) ;
#69566=CARTESIAN_POINT ( 'NONE',  ( 20.94999999999999929, 74.16465844978819177, -191.9679561919613775 ) ) ;
#69582=CARTESIAN_POINT ( 'NONE',  ( -18.50000000000000000, 65.70711192142420032, -164.5651054685122574 ) ) ;
#69590=AXIS2_PLACEMENT_3D ( 'NONE', #211610, #92922, #9538 ) ;
#69650=ORIENTED_EDGE ( 'NONE', *, *, #224111, .T. ) ;
#69651=CARTESIAN_POINT ( 'NONE',  ( 21.53551880898956838, 69.21520223859636189, -203.6220772190960702 ) ) ;
#69696=EDGE_CURVE ( 'NONE', #150814, #180782, #147703, .T. ) ;
#69716=DIRECTION ( 'NONE',  ( -1.000000000000000000, 0.000000000000000000, 0.000000000000000000 ) ) ;
#69721=ORIENTED_EDGE ( 'NONE', *, *, #158679, .T. ) ;
#69740=VERTEX_POINT ( 'NONE', #11644 ) ;
#69800=VERTEX_POINT ( 'NONE', #33797 ) ;
#69801=PRESENTATION_STYLE_ASSIGNMENT (( #151912 ) ) ;
#69803=CARTESIAN_POINT ( 'NONE',  ( 18.59999999999999076, 64.25000000001250555, -178.6731074845244507 ) ) ;
#69810=CARTESIAN_POINT ( 'NONE',  ( -18.59999999999999787, 85.48068669529138219, -163.0819923157664562 ) ) ;
#69818=LINE ( 'NONE', #91917, #163871 ) ;
#69849=DIRECTION ( 'NONE',  ( 0.000000000000000000, -6.688090509790120484E-15, 1.000000000000000000 ) ) ;
#69856=ORIENTED_EDGE ( 'NONE', *, *, #46431, .T. ) ;
#69875=CARTESIAN_POINT ( 'NONE',  ( -18.59999999999999787, 74.75000000001261924, -195.5231074845243597 ) ) ;
#69877=TOROIDAL_SURFACE ( 'NONE', #253008, 0.2000000000000000111, 0.1000000000000000056 ) ;
#69890=SPHERICAL_SURFACE ( 'NONE', #80149, 0.1000000000000000056 ) ;
#69935=CARTESIAN_POINT ( 'NONE',  ( 18.59999999999999787, 87.75000000001250555, -178.6731074845242802 ) ) ;
#69975=ORIENTED_EDGE ( 'NONE', *, *, #74158, .F. ) ;
#69999=ORIENTED_EDGE ( 'NONE', *, *, #170157, .F. ) ;
#70001=FACE_OUTER_BOUND ( 'NONE', #140337, .T. ) ;
#70007=ADVANCED_FACE ( 'NONE', ( #162689 ), #25740, .T. ) ;
#70014=CARTESIAN_POINT ( 'NONE',  ( -20.85000000000000142, 77.83585931145600512, -158.5186683157258187 ) ) ;
#70027=TOROIDAL_SURFACE ( 'NONE', #128279, 12.77500000000000036, 0.1000000000000000056 ) ;
#70041=VERTEX_POINT ( 'NONE', #8743 ) ;
#70053=VECTOR ( 'NONE', #197768, 1000.000000000000000 ) ;
#70062=EDGE_LOOP ( 'NONE', ( #168485, #83130, #103917, #133232 ) ) ;
#70073=VERTEX_POINT ( 'NONE', #144368 ) ;
#70098=AXIS2_PLACEMENT_3D ( 'NONE', #15758, #129585, #209109 ) ;
#70117=DIRECTION ( 'NONE',  ( -1.000000000000000000, 0.000000000000000000, -0.000000000000000000 ) ) ;
#70129=CARTESIAN_POINT ( 'NONE',  ( 21.05000000000000071, 76.00000000001267608, -203.5231074845243597 ) ) ;
#70130=DIRECTION ( 'NONE',  ( 1.000000000000000000, 0.000000000000000000, 0.000000000000000000 ) ) ;
#70135=CARTESIAN_POINT ( 'NONE',  ( 20.94999999999999929, 74.63912941282058000, -195.4501095574334215 ) ) ;
#70139=CARTESIAN_POINT ( 'NONE',  ( 23.14999999999998437, 76.00000000001267608, -203.5231074845243597 ) ) ;
#70157=DIRECTION ( 'NONE',  ( 0.000000000000000000, -6.652207440891554563E-15, 1.000000000000000000 ) ) ;
#70164=CARTESIAN_POINT ( 'NONE',  ( -20.94999999999999929, 76.00000000001247713, -174.1231074845243540 ) ) ;
#70174=VECTOR ( 'NONE', #246443, 1000.000000000000000 ) ;
#70206=CARTESIAN_POINT ( 'NONE',  ( 22.39999999999999503, 64.25000000001269029, -203.5231074845244166 ) ) ;
#70231=CARTESIAN_POINT ( 'NONE',  ( 20.94999999999999929, 67.12338541492553645, -195.1380270056797599 ) ) ;
#70235=CARTESIAN_POINT ( 'NONE',  ( -20.64999999999999858, 76.00000000001259082, -190.6481074845243597 ) ) ;
#70241=ORIENTED_EDGE ( 'NONE', *, *, #158202, .F. ) ;
#70283=ADVANCED_FACE ( 'NONE', ( #56814 ), #257554, .T. ) ;
#70333=EDGE_CURVE ( 'NONE', #170452, #87006, #227162, .T. ) ;
#70335=AXIS2_PLACEMENT_3D ( 'NONE', #82262, #125285, #5294 ) ;
#70360=DIRECTION ( 'NONE',  ( -0.000000000000000000, 6.982962677686266711E-15, -1.000000000000000000 ) ) ;
#70380=ORIENTED_EDGE ( 'NONE', *, *, #245879, .F. ) ;
#70391=AXIS2_PLACEMENT_3D ( 'NONE', #31131, #174514, #251419 ) ;
#70396=AXIS2_PLACEMENT_3D ( 'NONE', #237030, #153701, #17965 ) ;
#70401=ADVANCED_FACE ( 'NONE', ( #241895 ), #46361, .T. ) ;
#70402=CIRCLE ( 'NONE', #20310, 12.87499999999999822 ) ;
#70410=EDGE_LOOP ( 'NONE', ( #212076, #1396, #161691, #174411 ) ) ;
#70414=CARTESIAN_POINT ( 'NONE',  ( 21.14999999999999858, 76.00000000001271871, -210.0637644362255969 ) ) ;
#70420=ADVANCED_FACE ( 'NONE', ( #87939 ), #38032, .F. ) ;
#70435=LINE ( 'NONE', #151231, #77437 ) ;
#70453=CARTESIAN_POINT ( 'NONE',  ( -20.94999999999999929, 64.25000000001263345, -196.5083017138704236 ) ) ;
#70479=DIRECTION ( 'NONE',  ( 0.000000000000000000, 0.1298341882519953583, 0.9915357197604861561 ) ) ;
#70488=CARTESIAN_POINT ( 'NONE',  ( -18.59999999999999787, 74.16465844978819177, -191.9679561919613775 ) ) ;
#70512=DIRECTION ( 'NONE',  ( 0.000000000000000000, 0.000000000000000000, 1.000000000000000000 ) ) ;
#70540=CARTESIAN_POINT ( 'NONE',  ( -21.51976009735018991, 69.08954155835347422, -203.5231074845243882 ) ) ;
#70558=DIRECTION ( 'NONE',  ( 0.000000000000000000, -0.9999631594459053030, -0.008583690987162452199 ) ) ;
#70570=LINE ( 'NONE', #170973, #49379 ) ;
#70578=ORIENTED_EDGE ( 'NONE', *, *, #94539, .F. ) ;
#70580=ORIENTED_EDGE ( 'NONE', *, *, #70333, .T. ) ;
#70653=DIRECTION ( 'NONE',  ( -1.000000000000000000, -0.000000000000000000, -0.000000000000000000 ) ) ;
#70659=ADVANCED_FACE ( 'NONE', ( #40870 ), #120413, .F. ) ;
#70669=ORIENTED_EDGE ( 'NONE', *, *, #147323, .F. ) ;
#70678=AXIS2_PLACEMENT_3D ( 'NONE', #86549, #166159, #245658 ) ;
#70692=ORIENTED_EDGE ( 'NONE', *, *, #254286, .T. ) ;
#70707=CARTESIAN_POINT ( 'NONE',  ( -21.04999999999960281, 69.65527659592207499, -203.5378253410476077 ) ) ;
#70720=ORIENTED_EDGE ( 'NONE', *, *, #207778, .T. ) ;
#70726=FACE_OUTER_BOUND ( 'NONE', #197287, .T. ) ;
#70739=VECTOR ( 'NONE', #6712, 1000.000000000000000 ) ;
#70789=ORIENTED_EDGE ( 'NONE', *, *, #206023, .F. ) ;
#70801=CIRCLE ( 'NONE', #179133, 0.1000000000000072220 ) ;
#70807=AXIS2_PLACEMENT_3D ( 'NONE', #36507, #174753, #56008 ) ;
#70816=ADVANCED_FACE ( 'NONE', ( #180350 ), #81219, .T. ) ;
#70857=FACE_OUTER_BOUND ( 'NONE', #201891, .T. ) ;
#70882=DIRECTION ( 'NONE',  ( -0.000000000000000000, 6.982962677686266711E-15, -1.000000000000000000 ) ) ;
#70891=DIRECTION ( 'NONE',  ( 1.000000000000000000, 0.000000000000000000, 0.000000000000000000 ) ) ;
#70921=VECTOR ( 'NONE', #230833, 1000.000000000000000 ) ;
#70935=EDGE_LOOP ( 'NONE', ( #236222, #49253, #214010, #10371 ) ) ;
#70936=DIRECTION ( 'NONE',  ( 0.000000000000000000, 1.000000000000000000, 6.982962677686266711E-15 ) ) ;
#70957=ORIENTED_EDGE ( 'NONE', *, *, #82411, .T. ) ;
#70961=ORIENTED_EDGE ( 'NONE', *, *, #27146, .F. ) ;
#71028=ORIENTED_EDGE ( 'NONE', *, *, #78606, .F. ) ;
#71061=ORIENTED_EDGE ( 'NONE', *, *, #42350, .F. ) ;
#71075=CARTESIAN_POINT ( 'NONE',  ( -20.64999999999999858, 85.00000000001253397, -179.4170766071767389 ) ) ;
#71100=CYLINDRICAL_SURFACE ( 'NONE', #226373, 0.09999999999998898659 ) ;
#71103=CYLINDRICAL_SURFACE ( 'NONE', #14641, 0.09999999999998898659 ) ;
#71116=AXIS2_PLACEMENT_3D ( 'NONE', #32354, #253918, #115708 ) ;
#71118=TOROIDAL_SURFACE ( 'NONE', #216835, 0.2000000000000000111, 0.1000000000000000056 ) ;
#71149=CARTESIAN_POINT ( 'NONE',  ( -21.55000000000000426, 68.29142135624984178, -182.3731074845244109 ) ) ;
#71248=CARTESIAN_POINT ( 'NONE',  ( 18.50000000000000000, 85.50000000001240608, -163.4229180933022576 ) ) ;
#71275=ADVANCED_FACE ( 'NONE', ( #109121 ), #89560, .T. ) ;
#71288=ADVANCED_FACE ( 'NONE', ( #10034 ), #50422, .F. ) ;
#71315=DIRECTION ( 'NONE',  ( -0.000000000000000000, 1.000000000000000000, 6.982962677686266711E-15 ) ) ;
#71338=CARTESIAN_POINT ( 'NONE',  ( 21.53699400380723361, 69.21228820682206617, -203.5231074845244166 ) ) ;
#71362=DIRECTION ( 'NONE',  ( 0.000000000000000000, 0.9876197685951241256, 0.1568667991644932258 ) ) ;
#71364=ORIENTED_EDGE ( 'NONE', *, *, #181960, .T. ) ;
#71381=VERTEX_POINT ( 'NONE', #97228 ) ;
#71394=CARTESIAN_POINT ( 'NONE',  ( -23.15000000000000213, 76.00000000001242029, -166.0231074845243597 ) ) ;
#71402=CIRCLE ( 'NONE', #204638, 0.09999999999998898659 ) ;
#71405=CARTESIAN_POINT ( 'NONE',  ( -21.93340585900940454, 76.00000000001273293, -210.8472545066297812 ) ) ;
#71406=DIRECTION ( 'NONE',  ( 0.000000000000000000, 0.000000000000000000, 1.000000000000000000 ) ) ;
#71421=CYLINDRICAL_SURFACE ( 'NONE', #174131, 0.1000000000000072220 ) ;
#71451=FACE_OUTER_BOUND ( 'NONE', #250924, .T. ) ;
#71452=AXIS2_PLACEMENT_3D ( 'NONE', #114246, #174268, #33468 ) ;
#71458=AXIS2_PLACEMENT_3D ( 'NONE', #222821, #204551, #181159 ) ;
#71472=DIRECTION ( 'NONE',  ( 1.000000000000000000, 0.000000000000000000, 0.000000000000000000 ) ) ;
#71511=CARTESIAN_POINT ( 'NONE',  ( -20.64999999999999858, 76.00000000001267608, -203.5231074845243597 ) ) ;
#71516=VERTEX_POINT ( 'NONE', #162401 ) ;
#71539=EDGE_CURVE ( 'NONE', #196694, #20109, #236722, .T. ) ;
#71540=CIRCLE ( 'NONE', #167218, 4.299999999999970512 ) ;
#71543=DIRECTION ( 'NONE',  ( 1.000000000000000000, 0.000000000000000000, 0.000000000000000000 ) ) ;
#71574=CARTESIAN_POINT ( 'NONE',  ( -20.94999999999999929, 64.40000000001249703, -176.9513107147999449 ) ) ;
#71622=DIRECTION ( 'NONE',  ( 5.603264701231745086E-32, 7.172728831056619538E-15, -1.000000000000000000 ) ) ;
#71664=DIRECTION ( 'NONE',  ( 0.000000000000000000, -6.769652589177795712E-15, 1.000000000000000000 ) ) ;
#71669=DIRECTION ( 'NONE',  ( 1.000000000000000000, 0.000000000000000000, 0.000000000000000000 ) ) ;
#71685=EDGE_CURVE ( 'NONE', #162952, #151569, #250896, .T. ) ;
#71703=DIRECTION ( 'NONE',  ( 1.000000000000000000, 0.000000000000000000, 0.000000000000000000 ) ) ;
#71707=ADVANCED_FACE ( 'NONE', ( #168851 ), #173797, .F. ) ;
#71716=ORIENTED_EDGE ( 'NONE', *, *, #184909, .F. ) ;
#71729=CARTESIAN_POINT ( 'NONE',  ( -20.54999999999999716, 74.00000000001254818, -183.2477294072864709 ) ) ;
#71744=CARTESIAN_POINT ( 'NONE',  ( -23.25000000000000000, 76.00000000001267608, -203.5231074845243597 ) ) ;
#71777=VECTOR ( 'NONE', #158147, 1000.000000000000000 ) ;
#71782=DIRECTION ( 'NONE',  ( -0.000000000000000000, 1.000000000000000000, 6.982962677686266711E-15 ) ) ;
#71791=CYLINDRICAL_SURFACE ( 'NONE', #11633, 0.09999999999998898659 ) ;
#71793=FACE_OUTER_BOUND ( 'NONE', #49162, .T. ) ;
#71798=EDGE_LOOP ( 'NONE', ( #149770, #203282, #199894, #187733 ) ) ;
#71823=DIRECTION ( 'NONE',  ( 0.000000000000000000, -6.530723674265620862E-15, 1.000000000000000000 ) ) ;
#71824=EDGE_CURVE ( 'NONE', #161922, #99797, #32107, .T. ) ;
#71845=EDGE_CURVE ( 'NONE', #43634, #204747, #207066, .T. ) ;
#71851=DIRECTION ( 'NONE',  ( -1.000000000000000000, 0.000000000000000000, 0.000000000000000000 ) ) ;
#71853=VERTEX_POINT ( 'NONE', #60404 ) ;
#71903=DIRECTION ( 'NONE',  ( 1.000000000000000000, 0.000000000000000000, 0.000000000000000000 ) ) ;
#71919=CARTESIAN_POINT ( 'NONE',  ( -23.25000000000000000, 76.00000000001244871, -170.0231074845243597 ) ) ;
#71921=ORIENTED_EDGE ( 'NONE', *, *, #143997, .T. ) ;
#71923=ORIENTED_EDGE ( 'NONE', *, *, #47240, .T. ) ;
#71930=ORIENTED_EDGE ( 'NONE', *, *, #77455, .T. ) ;
#71984=VECTOR ( 'NONE', #28752, 1000.000000000000000 ) ;
#72009=AXIS2_PLACEMENT_3D ( 'NONE', #92471, #255346, #172056 ) ;
#72036=ORIENTED_EDGE ( 'NONE', *, *, #254524, .F. ) ;
#72074=CARTESIAN_POINT ( 'NONE',  ( 18.43709777086140278, 85.68240343348880117, -163.3662641071115615 ) ) ;
#72106=DIRECTION ( 'NONE',  ( 0.000000000000000000, -6.982962677686266711E-15, 1.000000000000000000 ) ) ;
#72123=AXIS2_PLACEMENT_3D ( 'NONE', #26589, #7002, #185648 ) ;
#72130=CARTESIAN_POINT ( 'NONE',  ( 20.92356734117541706, 65.68026841930954163, -164.4725740131889893 ) ) ;
#72133=LINE ( 'NONE', #49980, #25150 ) ;
#72139=DIRECTION ( 'NONE',  ( 0.000000000000000000, -0.1350103645451945777, 0.9908441862701590219 ) ) ;
#72143=DIRECTION ( 'NONE',  ( -0.7071067811865475727, 0.7071067811865475727, 4.937700262164531476E-15 ) ) ;
#72156=VERTEX_POINT ( 'NONE', #53687 ) ;
#72158=VERTEX_POINT ( 'NONE', #215325 ) ;
#72179=ADVANCED_FACE ( 'NONE', ( #126157 ), #85722, .F. ) ;
#72183=CARTESIAN_POINT ( 'NONE',  ( -18.59999999999999787, 77.83534155023700407, -191.9679561919613491 ) ) ;
#72186=ORIENTED_EDGE ( 'NONE', *, *, #217958, .T. ) ;
#72195=AXIS2_PLACEMENT_3D ( 'NONE', #217151, #82758, #183197 ) ;
#72212=FACE_OUTER_BOUND ( 'NONE', #53086, .T. ) ;
#72249=VECTOR ( 'NONE', #153990, 1000.000000000000000 ) ;
#72316=VERTEX_POINT ( 'NONE', #93453 ) ;
#72378=CARTESIAN_POINT ( 'NONE',  ( 23.25000000000000000, 84.59626168225550202, -179.4732350016745954 ) ) ;
#72451=ORIENTED_EDGE ( 'NONE', *, *, #63068, .F. ) ;
#72456=CARTESIAN_POINT ( 'NONE',  ( -23.15000000000000213, 64.35000000001275566, -215.2731074845244450 ) ) ;
#72475=FACE_OUTER_BOUND ( 'NONE', #251593, .T. ) ;
#72540=CARTESIAN_POINT ( 'NONE',  ( 23.14999999999998437, 80.05000000001268745, -203.5231074845243313 ) ) ;
#72581=SPHERICAL_SURFACE ( 'NONE', #122092, 0.1000000000000000056 ) ;
#72595=DIRECTION ( 'NONE',  ( -0.000000000000000000, 0.1350103645451807555, 0.9908441862701610203 ) ) ;
#72643=FACE_OUTER_BOUND ( 'NONE', #186946, .T. ) ;
#72656=EDGE_LOOP ( 'NONE', ( #247641, #233122, #95763 ) ) ;
#72684=ORIENTED_EDGE ( 'NONE', *, *, #214145, .F. ) ;
#72686=ORIENTED_EDGE ( 'NONE', *, *, #16107, .F. ) ;
#72695=DIRECTION ( 'NONE',  ( 0.000000000000000000, -1.000000000000000000, -6.352154140967427193E-15 ) ) ;
#72711=DIRECTION ( 'NONE',  ( 1.000000000000000000, 0.000000000000000000, 0.000000000000000000 ) ) ;
#72763=VERTEX_POINT ( 'NONE', #128439 ) ;
#72764=CARTESIAN_POINT ( 'NONE',  ( 23.14999999999999858, 71.22429906543317202, -191.6743393804784148 ) ) ;
#72789=CYLINDRICAL_SURFACE ( 'NONE', #244682, 0.8750000000000007772 ) ;
#72814=DIRECTION ( 'NONE',  ( -1.000000000000000000, 0.000000000000000000, -0.000000000000000000 ) ) ;
#72819=CYLINDRICAL_SURFACE ( 'NONE', #154524, 0.1000000000000070832 ) ;
#72827=DIRECTION ( 'NONE',  ( 0.000000000000000000, -1.000000000000000000, -6.352154140967427193E-15 ) ) ;
#72843=CIRCLE ( 'NONE', #97721, 0.09999999999998898659 ) ;
#72845=TOROIDAL_SURFACE ( 'NONE', #101823, 11.90000000000000391, 0.1000000000000000056 ) ;
#72847=EDGE_LOOP ( 'NONE', ( #67425, #173209, #162790, #112674 ) ) ;
#72848=DIRECTION ( 'NONE',  ( -0.000000000000000000, -6.982962677686266711E-15, 1.000000000000000000 ) ) ;
#72890=VERTEX_POINT ( 'NONE', #54032 ) ;
#72895=CARTESIAN_POINT ( 'NONE',  ( 22.24259225415828922, 75.90093411655990963, -211.0150453550897680 ) ) ;
#72921=EDGE_CURVE ( 'NONE', #165093, #151955, #240369, .T. ) ;
#72949=VECTOR ( 'NONE', #208160, 1000.000000000000114 ) ;
#72951=CARTESIAN_POINT ( 'NONE',  ( -21.45000000000000284, 68.29142135624984178, -182.2731074845244166 ) ) ;
#72987=B_SPLINE_CURVE_WITH_KNOTS ( 'NONE', 3,
 ( #236949, #115722, #183083, #235653, #197813, #56995 ),
 .UNSPECIFIED., .F., .F.,
 ( 4, 2, 4 ),
 ( 0.000000000000000000, 0.0001496588209255806561, 0.0002993176418511613122 ),
 .UNSPECIFIED. ) ;
#73005=EDGE_CURVE ( 'NONE', #244528, #177284, #5587, .T. ) ;
#73049=CYLINDRICAL_SURFACE ( 'NONE', #157278, 0.1000000000000106914 ) ;
#73108=AXIS2_PLACEMENT_3D ( 'NONE', #248383, #96965, #20056 ) ;
#73116=ORIENTED_EDGE ( 'NONE', *, *, #255004, .F. ) ;
#73117=CARTESIAN_POINT ( 'NONE',  ( 21.05000000000000071, 64.35000000001249987, -177.0379132551784096 ) ) ;
#73127=ADVANCED_FACE ( 'NONE', ( #210255 ), #13332, .F. ) ;
#73152=ORIENTED_EDGE ( 'NONE', *, *, #240170, .F. ) ;
#73163=CARTESIAN_POINT ( 'NONE',  ( 21.05000000000000071, 85.00000000001251976, -179.9170766071767389 ) ) ;
#73201=DIRECTION ( 'NONE',  ( -1.000000000000000000, -0.000000000000000000, -0.000000000000000000 ) ) ;
#73207=DIRECTION ( 'NONE',  ( -1.000000000000000000, -7.304098846218105085E-16, -4.217023435051676515E-16 ) ) ;
#73217=DIRECTION ( 'NONE',  ( 1.000000000000000000, -2.952720810173289112E-16, -2.061873921506763405E-30 ) ) ;
#73219=CARTESIAN_POINT ( 'NONE',  ( -21.05000000000000071, 74.14897176987174987, -191.8691942151018850 ) ) ;
#73223=DIRECTION ( 'NONE',  ( 1.000000000000000000, 0.000000000000000000, 0.000000000000000000 ) ) ;
#73264=EDGE_CURVE ( 'NONE', #215277, #187182, #244627, .T. ) ;
#73285=TOROIDAL_SURFACE ( 'NONE', #210620, 0.2000000000000000111, 0.1000000000000000056 ) ;
#73324=DIRECTION ( 'NONE',  ( 2.952720810173289112E-16, 1.000000000000000000, 1.261617073437673512E-14 ) ) ;
#73366=DIRECTION ( 'NONE',  ( 1.000000000000000000, 0.000000000000000000, 0.000000000000000000 ) ) ;
#73378=CARTESIAN_POINT ( 'NONE',  ( 18.59999999999999432, 74.26374286841520700, -191.9544551555068779 ) ) ;
#73389=ORIENTED_EDGE ( 'NONE', *, *, #44048, .T. ) ;
#73403=ORIENTED_EDGE ( 'NONE', *, *, #139381, .F. ) ;
#73411=VECTOR ( 'NONE', #54674, 1000.000000000000000 ) ;
#73423=ORIENTED_EDGE ( 'NONE', *, *, #162823, .T. ) ;
#73439=DIRECTION ( 'NONE',  ( -1.000000000000000000, 0.000000000000000000, -0.000000000000000000 ) ) ;
#73481=DIRECTION ( 'NONE',  ( 1.000000000000000000, -0.000000000000000000, 0.000000000000000000 ) ) ;
#73504=AXIS2_PLACEMENT_3D ( 'NONE', #39023, #76839, #140667 ) ;
#73511=DIRECTION ( 'NONE',  ( -1.000000000000000000, -0.000000000000000000, -0.000000000000000000 ) ) ;
#73519=VECTOR ( 'NONE', #124796, 1000.000000000000000 ) ;
#73528=LINE ( 'NONE', #52637, #97688 ) ;
#73539=EDGE_CURVE ( 'NONE', #154576, #183114, #43479, .T. ) ;
#73541=DIRECTION ( 'NONE',  ( -0.7070776581708965169, 0.7071359030027827286, 4.937903618720407826E-15 ) ) ;
#73545=EDGE_LOOP ( 'NONE', ( #200005, #70692, #132195, #96330 ) ) ;
#73564=EDGE_CURVE ( 'NONE', #198292, #257935, #190686, .T. ) ;
#73582=CARTESIAN_POINT ( 'NONE',  ( 20.94999999999999574, 74.16465844978819177, -191.8679561919614116 ) ) ;
#73614=EDGE_CURVE ( 'NONE', #67516, #129211, #211506, .T. ) ;
#73619=ADVANCED_FACE ( 'NONE', ( #117261 ), #80668, .T. ) ;
#73640=EDGE_LOOP ( 'NONE', ( #160978, #173554 ) ) ;
#73646=EDGE_CURVE ( 'NONE', #224589, #209479, #3715, .T. ) ;
#73659=EDGE_CURVE ( 'NONE', #37719, #85479, #28376, .T. ) ;
#73723=AXIS2_PLACEMENT_3D ( 'NONE', #151658, #253280, #214170 ) ;
#73750=EDGE_CURVE ( 'NONE', #227495, #200926, #178208, .T. ) ;
#73783=LINE ( 'NONE', #54177, #216060 ) ;
#73795=ADVANCED_FACE ( 'NONE', ( #169256 ), #71421, .T. ) ;
#73810=AXIS2_PLACEMENT_3D ( 'NONE', #215403, #195868, #176307 ) ;
#73849=ADVANCED_FACE ( 'NONE', ( #209626 ), #166681, .T. ) ;
#73877=AXIS2_PLACEMENT_3D ( 'NONE', #140860, #136996, #220401 ) ;
#73889=EDGE_CURVE ( 'NONE', #102120, #156136, #36572, .T. ) ;
#73911=AXIS2_PLACEMENT_3D ( 'NONE', #167713, #227646, #49015 ) ;
#73924=ORIENTED_EDGE ( 'NONE', *, *, #59631, .T. ) ;
#73947=DIRECTION ( 'NONE',  ( 1.000000000000000000, 0.000000000000000000, 0.000000000000000000 ) ) ;
#73976=EDGE_CURVE ( 'NONE', #257053, #3812, #61845, .T. ) ;
#73994=ADVANCED_FACE ( 'NONE', ( #212213 ), #251305, .T. ) ;
#74026=EDGE_LOOP ( 'NONE', ( #215767, #12029, #16615, #44783 ) ) ;
#74031=DIRECTION ( 'NONE',  ( 1.000000000000000000, 0.000000000000000000, 0.000000000000000000 ) ) ;
#74044=CARTESIAN_POINT ( 'NONE',  ( 21.05000000000000071, 87.65000000001268177, -203.5231074845243029 ) ) ;
#74061=DIRECTION ( 'NONE',  ( 0.000000000000000000, 0.6728971962617102953, 0.7397360091702507301 ) ) ;
#74083=CARTESIAN_POINT ( 'NONE',  ( -20.94999999999999929, 87.29603075034775372, -173.0710066441881452 ) ) ;
#74109=FACE_OUTER_BOUND ( 'NONE', #28767, .T. ) ;
#74120=AXIS2_PLACEMENT_3D ( 'NONE', #124371, #8276, #164774 ) ;
#74148=DIRECTION ( 'NONE',  ( 1.000000000000000000, 7.304098846218163263E-16, -4.217023435051627211E-16 ) ) ;
#74156=CONICAL_SURFACE ( 'NONE', #253171, 4.049999999999998046, 0.7853981633974604915 ) ;
#74158=EDGE_CURVE ( 'NONE', #133901, #133788, #188157, .T. ) ;
#74177=ADVANCED_FACE ( 'NONE', ( #231157 ), #227267, .T. ) ;
#74181=DIRECTION ( 'NONE',  ( 0.000000000000000000, 0.000000000000000000, 1.000000000000000000 ) ) ;
#74184=CARTESIAN_POINT ( 'NONE',  ( 21.12642695952774119, 75.90109671682336057, -209.8987674065595286 ) ) ;
#74190=AXIS2_PLACEMENT_3D ( 'NONE', #145181, #146460, #126922 ) ;
#74231=AXIS2_PLACEMENT_3D ( 'NONE', #233758, #57655, #74717 ) ;
#74253=DIRECTION ( 'NONE',  ( -0.000000000000000000, 0.1350103645451835865, 0.9908441862701605762 ) ) ;
#74254=DIRECTION ( 'NONE',  ( 1.000000000000000000, -2.952720810173289112E-16, -2.061873921506763405E-30 ) ) ;
#74262=ORIENTED_EDGE ( 'NONE', *, *, #115866, .T. ) ;
#74281=LINE ( 'NONE', #192918, #73411 ) ;
#74356=EDGE_CURVE ( 'NONE', #178668, #102259, #92442, .T. ) ;
#74357=AXIS2_PLACEMENT_3D ( 'NONE', #112200, #56018, #131738 ) ;
#74366=DIRECTION ( 'NONE',  ( 1.000000000000000000, -6.938893903907222067E-15, -4.845403715540888588E-29 ) ) ;
#74383=DIRECTION ( 'NONE',  ( -1.000000000000000000, 3.265361837132813093E-16, 2.280189983783949500E-30 ) ) ;
#74424=ORIENTED_EDGE ( 'NONE', *, *, #55927, .F. ) ;
#74428=LINE ( 'NONE', #16999, #179693 ) ;
#74443=ORIENTED_EDGE ( 'NONE', *, *, #158407, .F. ) ;
#74464=ORIENTED_EDGE ( 'NONE', *, *, #17479, .T. ) ;
#74480=EDGE_CURVE ( 'NONE', #153430, #219970, #119735, .T. ) ;
#74512=LINE ( 'NONE', #237397, #96211 ) ;
#74547=VECTOR ( 'NONE', #82964, 1000.000000000000000 ) ;
#74604=ORIENTED_EDGE ( 'NONE', *, *, #100048, .F. ) ;
#74628=CARTESIAN_POINT ( 'NONE',  ( -20.85000000000000142, 87.75000000001247713, -172.9231074845242802 ) ) ;
#74636=EDGE_CURVE ( 'NONE', #72890, #57467, #11982, .T. ) ;
#74639=ADVANCED_FACE ( 'NONE', ( #147575 ), #7881, .F. ) ;
#74643=ORIENTED_EDGE ( 'NONE', *, *, #57716, .T. ) ;
#74691=AXIS2_PLACEMENT_3D ( 'NONE', #227269, #31680, #107321 ) ;
#74717=DIRECTION ( 'NONE',  ( 1.000000000000000000, 0.000000000000000000, 0.000000000000000000 ) ) ;
#74731=ORIENTED_EDGE ( 'NONE', *, *, #202364, .T. ) ;
#74745=ADVANCED_FACE ( 'NONE', ( #190573 ), #172322, .F. ) ;
#74760=CARTESIAN_POINT ( 'NONE',  ( 23.15000000000000213, 85.00000000001251976, -179.9170766071767389 ) ) ;
#74766=CARTESIAN_POINT ( 'NONE',  ( -20.64999999999999858, 71.65000000001259650, -191.2731074845243882 ) ) ;
#74801=AXIS2_PLACEMENT_3D ( 'NONE', #59893, #45490, #82012 ) ;
#74808=TOROIDAL_SURFACE ( 'NONE', #29015, 0.2000000000000000111, 0.1000000000000000056 ) ;
#74820=CARTESIAN_POINT ( 'NONE',  ( -18.59999999999999787, 76.00000000001244871, -170.0231074845243597 ) ) ;
#74835=ORIENTED_EDGE ( 'NONE', *, *, #115990, .F. ) ;
#74839=ORIENTED_EDGE ( 'NONE', *, *, #205455, .T. ) ;
#74873=DIRECTION ( 'NONE',  ( -0.000000000000000000, -0.9876197685951290106, 0.1568667991644625281 ) ) ;
#74884=EDGE_LOOP ( 'NONE', ( #93047, #103600, #129647, #117540 ) ) ;
#74904=CARTESIAN_POINT ( 'NONE',  ( -20.64999999999999858, 85.50000000001251976, -179.9170766071767389 ) ) ;
#74911=AXIS2_PLACEMENT_3D ( 'NONE', #91228, #131623, #114630 ) ;
#74934=DIRECTION ( 'NONE',  ( -1.000000000000000000, 0.000000000000000000, 0.000000000000000000 ) ) ;
#74939=CARTESIAN_POINT ( 'NONE',  ( -20.64999999999999858, 74.05981308412474107, -190.6939882734710636 ) ) ;
#74940=CARTESIAN_POINT ( 'NONE',  ( -18.50000000000000000, 66.75000000001253397, -182.3731074845244393 ) ) ;
#74942=DIRECTION ( 'NONE',  ( -0.000000000000000000, -0.8660254037844420383, 0.4999999999999943379 ) ) ;
#74958=CARTESIAN_POINT ( 'NONE',  ( -18.31331870001069362, 85.53629471919325056, -163.1545287935392423 ) ) ;
#74995=VERTEX_POINT ( 'NONE', #213657 ) ;
#75007=EDGE_CURVE ( 'NONE', #165380, #210276, #54943, .T. ) ;
#75016=LINE ( 'NONE', #150678, #7558 ) ;
#75041=DIRECTION ( 'NONE',  ( 0.000000000000000000, -6.982962677686266711E-15, 1.000000000000000000 ) ) ;
#75048=AXIS2_PLACEMENT_3D ( 'NONE', #1907, #60600, #83979 ) ;
#75056=CARTESIAN_POINT ( 'NONE',  ( 21.14999999999999503, 64.25000000001269029, -203.5231074845244166 ) ) ;
#75097=CARTESIAN_POINT ( 'NONE',  ( 21.14999999999999858, 64.35000000001258513, -191.3731074845244393 ) ) ;
#75113=CARTESIAN_POINT ( 'NONE',  ( -20.54999999999999716, 71.65000000001253966, -182.3731074845244109 ) ) ;
#75120=DIRECTION ( 'NONE',  ( -1.000000000000000000, 0.000000000000000000, 0.000000000000000000 ) ) ;
#75138=CIRCLE ( 'NONE', #95936, 4.149999999999987033 ) ;
#75140=ORIENTED_EDGE ( 'NONE', *, *, #211235, .T. ) ;
#75178=ORIENTED_EDGE ( 'NONE', *, *, #237302, .F. ) ;
#75185=ORIENTED_EDGE ( 'NONE', *, *, #42629, .T. ) ;
#75195=CIRCLE ( 'NONE', #220897, 12.77500000000000924 ) ;
#75243=ORIENTED_EDGE ( 'NONE', *, *, #57716, .F. ) ;
#75288=EDGE_CURVE ( 'NONE', #10849, #177234, #126566, .T. ) ;
#75303=ORIENTED_EDGE ( 'NONE', *, *, #47565, .F. ) ;
#75338=VERTEX_POINT ( 'NONE', #136024 ) ;
#75339=DIRECTION ( 'NONE',  ( -0.000000000000000000, 1.000000000000000000, 6.982962677686266711E-15 ) ) ;
#75345=DIRECTION ( 'NONE',  ( 0.000000000000000000, 1.000000000000000000, 6.982962677686266711E-15 ) ) ;
#75405=DIRECTION ( 'NONE',  ( 0.000000000000000000, -0.7397360091702823714, 0.6728971962616756564 ) ) ;
#75434=ADVANCED_FACE ( 'NONE', ( #175230 ), #133132, .T. ) ;
#75446=VERTEX_POINT ( 'NONE', #193479 ) ;
#75462=EDGE_CURVE ( 'NONE', #25217, #34176, #237185, .T. ) ;
#75485=ORIENTED_EDGE ( 'NONE', *, *, #58772, .T. ) ;
#75486=FACE_OUTER_BOUND ( 'NONE', #246917, .T. ) ;
#75507=ORIENTED_EDGE ( 'NONE', *, *, #95977, .T. ) ;
#75522=CARTESIAN_POINT ( 'NONE',  ( 21.04999999999914806, 65.49746832288764153, -195.9642776674505456 ) ) ;
#75528=LINE ( 'NONE', #190336, #45372 ) ;
#75533=VECTOR ( 'NONE', #155239, 999.9999999999998863 ) ;
#75536=LINE ( 'NONE', #31294, #204198 ) ;
#75538=AXIS2_PLACEMENT_3D ( 'NONE', #130806, #210361, #192090 ) ;
#75541=CARTESIAN_POINT ( 'NONE',  ( -23.25000000000000000, 76.00000000001270450, -207.6731074845243370 ) ) ;
#75559=FACE_OUTER_BOUND ( 'NONE', #31489, .T. ) ;
#75567=DIRECTION ( 'NONE',  ( 0.000000000000000000, 0.000000000000000000, 1.000000000000000000 ) ) ;
#75576=VERTEX_POINT ( 'NONE', #241574 ) ;
#75589=CARTESIAN_POINT ( 'NONE',  ( 18.51024323315077069, 65.68895814178291914, -164.5026557862138645 ) ) ;
#75599=DIRECTION ( 'NONE',  ( 0.000000000000000000, 0.000000000000000000, 1.000000000000000000 ) ) ;
#75613=CARTESIAN_POINT ( 'NONE',  ( 21.00023020733504708, 76.00000000001273293, -209.9139767297927222 ) ) ;
#75624=DIRECTION ( 'NONE',  ( 0.000000000000000000, -7.056502275159890043E-15, 1.000000000000000000 ) ) ;
#75626=VECTOR ( 'NONE', #151854, 1000.000000000000000 ) ;
#75634=CARTESIAN_POINT ( 'NONE',  ( 18.59999999999999076, 69.35000000001254250, -182.2731074845244166 ) ) ;
#75647=CARTESIAN_POINT ( 'NONE',  ( 20.94999999999999929, 65.27628289530507288, -191.3731074845244393 ) ) ;
#75732=CARTESIAN_POINT ( 'NONE',  ( 22.57320508075688537, 64.25000000001267608, -203.5231074845244450 ) ) ;
#75763=ORIENTED_EDGE ( 'NONE', *, *, #38294, .F. ) ;
#75772=ORIENTED_EDGE ( 'NONE', *, *, #90031, .F. ) ;
#75774=DIRECTION ( 'NONE',  ( 1.000000000000000000, 0.000000000000000000, 0.000000000000000000 ) ) ;
#75781=CARTESIAN_POINT ( 'NONE',  ( 18.39999999999999858, 85.50000000001240608, -163.1084491415546154 ) ) ;
#75833=DIRECTION ( 'NONE',  ( 1.000000000000000000, 0.000000000000000000, 0.000000000000000000 ) ) ;
#75884=AXIS2_PLACEMENT_3D ( 'NONE', #89871, #32519, #208571 ) ;
#75893=VECTOR ( 'NONE', #199455, 1000.000000000000000 ) ;
#75903=DIRECTION ( 'NONE',  ( 0.000000000000000000, 1.000000000000000000, 6.982962677686266711E-15 ) ) ;
#75960=DIRECTION ( 'NONE',  ( 0.000000000000000000, -7.086529944415886769E-15, 1.000000000000000000 ) ) ;
#76004=( BOUNDED_SURFACE ( )  B_SPLINE_SURFACE ( 3, 2, ( 
 ( #246479, #46975, #189082 ),
 ( #169564, #130378, #67841 ),
 ( #204772, #185230, #146088 ),
 ( #225603, #27483, #228215 ),
 ( #127831, #6579, #149978 ),
 ( #147384, #226918, #187815 ) ),
 .UNSPECIFIED., .F., .F., .F. ) 
 B_SPLINE_SURFACE_WITH_KNOTS ( ( 4, 2, 4 ),
 ( 3, 3 ),
 ( 1.570796326794895448, 2.356194490192343505, 3.141592653589791784 ),
 ( 0.000000000000000000, 1.000000000000000000 ),
 .UNSPECIFIED. ) 
 GEOMETRIC_REPRESENTATION_ITEM ( )  RATIONAL_B_SPLINE_SURFACE ( (
 ( 1.000000000000000000, 0.7071067811865475727, 1.000000000000000000),
 ( 1.000000000000000000, 0.6611148371779083099, 1.000000000000000000),
 ( 1.000000000000000000, 0.6092287576696373552, 1.000000000000000000),
 ( 1.000000000000000000, 0.5278258667057376119, 1.000000000000000000),
 ( 1.000000000000000000, 0.4993418825332260891, 1.000000000000000000),
 ( 1.000000000000000000, 0.5000000000000456302, 1.000000000000000000) ) ) 
 REPRESENTATION_ITEM ( '' )  SURFACE ( )  );
#76038=CARTESIAN_POINT ( 'NONE',  ( 21.97500000000000497, 66.25000000001260503, -191.2731074845244166 ) ) ;
#76040=CARTESIAN_POINT ( 'NONE',  ( 20.94560253601876809, 64.25000000001249134, -177.0130239720093925 ) ) ;
#76082=AXIS2_PLACEMENT_3D ( 'NONE', #95, #242561, #160497 ) ;
#76086=EDGE_CURVE ( 'NONE', #206261, #144388, #123907, .T. ) ;
#76103=CIRCLE ( 'NONE', #5346, 12.87499999999999822 ) ;
#76131=AXIS2_PLACEMENT_3D ( 'NONE', #135633, #134341, #193067 ) ;
#76140=VERTEX_POINT ( 'NONE', #132891 ) ;
#76169=DIRECTION ( 'NONE',  ( 0.000000000000000000, 0.000000000000000000, 1.000000000000000000 ) ) ;
#76178=DIRECTION ( 'NONE',  ( 0.000000000000000000, -0.1495327102803283015, 0.9887567792719397231 ) ) ;
#76198=ADVANCED_FACE ( 'NONE', ( #172045 ), #135432, .T. ) ;
#76207=ORIENTED_EDGE ( 'NONE', *, *, #197311, .T. ) ;
#76218=LINE ( 'NONE', #20127, #115664 ) ;
#76225=FACE_OUTER_BOUND ( 'NONE', #70062, .T. ) ;
#76243=ORIENTED_EDGE ( 'NONE', *, *, #197737, .F. ) ;
#76272=CARTESIAN_POINT ( 'NONE',  ( -22.39999999999999858, 75.90000000001273861, -211.3138870828977645 ) ) ;
#76280=AXIS2_PLACEMENT_3D ( 'NONE', #172344, #73223, #154065 ) ;
#76306=DIRECTION ( 'NONE',  ( -0.7071067811865474617, 0.7071067811865474617, 5.142139384388980375E-15 ) ) ;
#76324=DIRECTION ( 'NONE',  ( 0.000000000000000000, -1.000000000000000000, 0.000000000000000000 ) ) ;
#76356=ORIENTED_EDGE ( 'NONE', *, *, #252204, .T. ) ;
#76358=DIRECTION ( 'NONE',  ( -0.000000000000000000, 6.982962677686266711E-15, -1.000000000000000000 ) ) ;
#76484=CARTESIAN_POINT ( 'NONE',  ( -18.59999999999999787, 76.00000000001244871, -170.0231074845243597 ) ) ;
#76500=ORIENTED_EDGE ( 'NONE', *, *, #64882, .F. ) ;
#76518=ORIENTED_EDGE ( 'NONE', *, *, #166501, .T. ) ;
#76527=EDGE_CURVE ( 'NONE', #218429, #13339, #90863, .T. ) ;
#76586=LINE ( 'NONE', #160005, #109028 ) ;
#76603=CARTESIAN_POINT ( 'NONE',  ( -21.05000000000000071, 69.58624026620243797, -203.4374944237204943 ) ) ;
#76612=DIRECTION ( 'NONE',  ( 0.000000000000000000, 1.000000000000000000, -5.551115123125777653E-14 ) ) ;
#76648=ORIENTED_EDGE ( 'NONE', *, *, #188234, .T. ) ;
#76708=CIRCLE ( 'NONE', #14210, 0.5000000000000004441 ) ;
#76721=DIRECTION ( 'NONE',  ( 1.000000000000000000, 0.000000000000000000, 0.000000000000000000 ) ) ;
#76727=DIRECTION ( 'NONE',  ( 1.000000000000000000, 0.000000000000000000, 0.000000000000000000 ) ) ;
#76747=CIRCLE ( 'NONE', #114355, 0.09999999999999938105 ) ;
#76752=DIRECTION ( 'NONE',  ( 0.000000000000000000, 1.181088324069314461E-14, -1.000000000000000000 ) ) ;
#76758=DIRECTION ( 'NONE',  ( 0.000000000000000000, 6.982962677686266711E-15, -1.000000000000000000 ) ) ;
#76802=CARTESIAN_POINT ( 'NONE',  ( 20.94999999999999574, 65.52661458509973613, -195.9444530202758870 ) ) ;
#76807=CARTESIAN_POINT ( 'NONE',  ( -22.59999999999999787, 64.25043287652329127, -203.6239658536231332 ) ) ;
#76823=CIRCLE ( 'NONE', #31084, 0.09999999999998898659 ) ;
#76827=ADVANCED_FACE ( 'NONE', ( #65863 ), #200244, .F. ) ;
#76839=DIRECTION ( 'NONE',  ( 0.000000000000000000, -6.982962677686267499E-15, 1.000000000000000000 ) ) ;
#76843=ORIENTED_EDGE ( 'NONE', *, *, #116918, .T. ) ;
#76845=DIRECTION ( 'NONE',  ( 0.000000000000000000, 1.000000000000000000, 6.688090509790097607E-15 ) ) ;
#76847=VECTOR ( 'NONE', #248833, 1000.000000000000000 ) ;
#76859=CARTESIAN_POINT ( 'NONE',  ( 22.47071067811864964, 75.90090754531013317, -211.2431822290224090 ) ) ;
#76863=ORIENTED_EDGE ( 'NONE', *, *, #149917, .T. ) ;
#76875=DIRECTION ( 'NONE',  ( -0.000000000000000000, 6.982962677686266711E-15, -1.000000000000000000 ) ) ;
#76877=ADVANCED_FACE ( 'NONE', ( #187126 ), #47570, .F. ) ;
#76881=DIRECTION ( 'NONE',  ( 0.000000000000000000, -6.352154140967427193E-15, 1.000000000000000000 ) ) ;
#76889=EDGE_CURVE ( 'NONE', #203961, #65541, #90555, .T. ) ;
#76901=DIRECTION ( 'NONE',  ( 1.000000000000000000, -7.304098846218134667E-16, -5.100424963727256530E-30 ) ) ;
#76903=AXIS2_PLACEMENT_3D ( 'NONE', #199497, #58652, #159088 ) ;
#76929=AXIS2_PLACEMENT_3D ( 'NONE', #90203, #69399, #229739 ) ;
#76931=CIRCLE ( 'NONE', #151982, 0.1000000000000028783 ) ;
#76978=DIRECTION ( 'NONE',  ( 0.000000000000000000, -0.9908441862701420355, -0.1350103645453197554 ) ) ;
#76981=ORIENTED_EDGE ( 'NONE', *, *, #250682, .T. ) ;
#76986=ORIENTED_EDGE ( 'NONE', *, *, #79460, .F. ) ;
#77001=ADVANCED_FACE ( 'NONE', ( #235218 ), #12691, .F. ) ;
#77018=VERTEX_POINT ( 'NONE', #198652 ) ;
#77022=ORIENTED_EDGE ( 'NONE', *, *, #38448, .F. ) ;
#77026=EDGE_LOOP ( 'NONE', ( #152505, #155338, #173461, #11195 ) ) ;
#77034=CARTESIAN_POINT ( 'NONE',  ( 20.94999999999999574, 67.07338541492552508, -195.0514244653012952 ) ) ;
#77061=EDGE_CURVE ( 'NONE', #207338, #56486, #59105, .T. ) ;
#77080=EDGE_CURVE ( 'NONE', #145161, #72156, #116717, .T. ) ;
#77086=CARTESIAN_POINT ( 'NONE',  ( 21.05000000000000071, 71.00000000001253397, -181.9283735034374843 ) ) ;
#77118=AXIS2_PLACEMENT_3D ( 'NONE', #200190, #101027, #202749 ) ;
#77120=CARTESIAN_POINT ( 'NONE',  ( -22.50000000000000000, 64.35042919246788529, -203.6231074845244393 ) ) ;
#77151=EDGE_LOOP ( 'NONE', ( #197700, #143779, #227479 ) ) ;
#77156=CARTESIAN_POINT ( 'NONE',  ( 23.14999999999999858, 76.00000000001267608, -203.5231074845243597 ) ) ;
#77167=DIRECTION ( 'NONE',  ( -1.040834085586054343E-13, 0.9999176327611370985, 0.01283462868040226822 ) ) ;
#77234=DIRECTION ( 'NONE',  ( 0.000000000000000000, -1.000000000000000000, -6.982962677686265922E-15 ) ) ;
#77259=FACE_OUTER_BOUND ( 'NONE', #130625, .T. ) ;
#77263=CARTESIAN_POINT ( 'NONE',  ( 22.45380639571440895, 75.99999985733725794, -215.2735403756365429 ) ) ;
#77271=AXIS2_PLACEMENT_3D ( 'NONE', #36930, #116438, #151733 ) ;
#77297=EDGE_CURVE ( 'NONE', #204733, #110754, #75536, .T. ) ;
#77321=FACE_OUTER_BOUND ( 'NONE', #124264, .T. ) ;
#77359=DIRECTION ( 'NONE',  ( 0.000000000000000000, 7.086529944415886769E-15, -1.000000000000000000 ) ) ;
#77376=VECTOR ( 'NONE', #55026, 1000.000000000000000 ) ;
#77379=AXIS2_PLACEMENT_3D ( 'NONE', #102583, #182165, #162606 ) ;
#77429=AXIS2_PLACEMENT_3D ( 'NONE', #120551, #15028, #56664 ) ;
#77437=VECTOR ( 'NONE', #53398, 1000.000000000000000 ) ;
#77455=EDGE_CURVE ( 'NONE', #183594, #13712, #221117, .T. ) ;
#77459=LINE ( 'NONE', #218261, #49512 ) ;
#77472=ORIENTED_EDGE ( 'NONE', *, *, #122385, .F. ) ;
#77481=VERTEX_POINT ( 'NONE', #20697 ) ;
#77484=DIRECTION ( 'NONE',  ( -1.000000000000000000, 0.000000000000000000, -0.000000000000000000 ) ) ;
#77503=VECTOR ( 'NONE', #234732, 1000.000000000000000 ) ;
#77523=LINE ( 'NONE', #157113, #244895 ) ;
#77527=EDGE_CURVE ( 'NONE', #199924, #46048, #42104, .T. ) ;
#77544=CARTESIAN_POINT ( 'NONE',  ( 18.49999999999998934, 65.75000000001251976, -178.7731074845244450 ) ) ;
#77567=ORIENTED_EDGE ( 'NONE', *, *, #98679, .F. ) ;
#77574=DIRECTION ( 'NONE',  ( 1.875376730785737719E-16, 1.000000000000000000, 6.982962677686266711E-15 ) ) ;
#77588=VECTOR ( 'NONE', #239214, 1000.000000000000000 ) ;
#77600=CYLINDRICAL_SURFACE ( 'NONE', #113759, 0.1000000000000028644 ) ;
#77621=FACE_OUTER_BOUND ( 'NONE', #20380, .T. ) ;
#77642=ADVANCED_FACE ( 'NONE', ( #133887 ), #191333, .T. ) ;
#77647=DIRECTION ( 'NONE',  ( 0.000000000000000000, -1.000000000000000000, -6.982962677686265922E-15 ) ) ;
#77668=ORIENTED_EDGE ( 'NONE', *, *, #128338, .F. ) ;
#77675=ORIENTED_EDGE ( 'NONE', *, *, #62639, .T. ) ;
#77687=CARTESIAN_POINT ( 'NONE',  ( 23.14999999999999858, 71.00000000001260503, -191.1178414656112921 ) ) ;
#77708=CARTESIAN_POINT ( 'NONE',  ( -20.94999999999999929, 77.85102823015347440, -191.8691942151018566 ) ) ;
#77769=DIRECTION ( 'NONE',  ( 0.000000000000000000, -1.000000000000000000, -6.982962677686265922E-15 ) ) ;
#77783=DIRECTION ( 'NONE',  ( 0.000000000000000000, 1.000000000000000000, 0.000000000000000000 ) ) ;
#77807=LINE ( 'NONE', #192650, #216874 ) ;
#77853=EDGE_CURVE ( 'NONE', #150964, #78372, #192768, .T. ) ;
#77863=ORIENTED_EDGE ( 'NONE', *, *, #110570, .T. ) ;
#77870=DIRECTION ( 'NONE',  ( -0.000000000000000000, 1.000000000000000000, 6.982962677686266711E-15 ) ) ;
#77895=EDGE_CURVE ( 'NONE', #28626, #19454, #193444, .T. ) ;
#77899=CARTESIAN_POINT ( 'NONE',  ( -21.05000000000000071, 87.29603075034795268, -200.4752083248604038 ) ) ;
#77908=DIRECTION ( 'NONE',  ( 1.000000000000000000, 0.000000000000000000, 0.000000000000000000 ) ) ;
#77911=AXIS2_PLACEMENT_3D ( 'NONE', #78471, #253257, #237568 ) ;
#77943=DIRECTION ( 'NONE',  ( 1.000000000000000000, 0.000000000000000000, 0.000000000000000000 ) ) ;
#77966=LINE ( 'NONE', #115827, #156209 ) ;
#77973=CARTESIAN_POINT ( 'NONE',  ( -20.05000000000000426, 66.75000000001253397, -182.2731074845244166 ) ) ;
#77976=EDGE_CURVE ( 'NONE', #72158, #256994, #126095, .T. ) ;
#77999=EDGE_CURVE ( 'NONE', #22816, #120125, #19943, .T. ) ;
#78019=DIRECTION ( 'NONE',  ( 1.000000000000000000, -0.000000000000000000, 0.000000000000000000 ) ) ;
#78031=EDGE_LOOP ( 'NONE', ( #22282, #103853, #124402, #244717 ) ) ;
#78039=DIRECTION ( 'NONE',  ( 1.000000000000000000, 0.000000000000000000, 0.000000000000000000 ) ) ;
#78053=CARTESIAN_POINT ( 'NONE',  ( 21.05000000000000071, 65.27628318601635726, -195.9287082486404756 ) ) ;
#78057=DIRECTION ( 'NONE',  ( 0.000000000000000000, -1.000000000000000000, -6.982962677686267499E-15 ) ) ;
#78062=DIRECTION ( 'NONE',  ( -1.000000000000000000, 1.836970198721029934E-16, 1.282749433769087757E-30 ) ) ;
#78109=DIRECTION ( 'NONE',  ( 0.000000000000000000, 1.000000000000000000, 6.982962677686267499E-15 ) ) ;
#78123=CARTESIAN_POINT ( 'NONE',  ( 18.59999999999999787, 70.10000000001267040, -193.3040077198679967 ) ) ;
#78134=CARTESIAN_POINT ( 'NONE',  ( -20.94999999999999929, 87.39257802171833589, -200.4491579046923277 ) ) ;
#78138=AXIS2_PLACEMENT_3D ( 'NONE', #213052, #74873, #37019 ) ;
#78159=CARTESIAN_POINT ( 'NONE',  ( 21.07933241753356768, 69.67135405163293171, -203.6164870749437057 ) ) ;
#78165=CARTESIAN_POINT ( 'NONE',  ( -21.05000000000000071, 76.00000000001270450, -207.8231074845243143 ) ) ;
#78188=DIRECTION ( 'NONE',  ( 0.000000000000000000, -7.272083257015735086E-15, 1.000000000000000000 ) ) ;
#78210=CARTESIAN_POINT ( 'NONE',  ( -23.15000000000000213, 85.00000000001261924, -194.1291383618718385 ) ) ;
#78250=CARTESIAN_POINT ( 'NONE',  ( 18.50000000000000000, 85.40000000001239755, -163.1410656363516125 ) ) ;
#78251=CIRCLE ( 'NONE', #70098, 0.2000000000000057288 ) ;
#78261=ORIENTED_EDGE ( 'NONE', *, *, #160854, .F. ) ;
#78266=DIRECTION ( 'NONE',  ( 1.000000000000000000, 0.000000000000000000, 0.000000000000000000 ) ) ;
#78270=CARTESIAN_POINT ( 'NONE',  ( 22.59999999999999432, 64.25043287652329127, -203.6239658536231616 ) ) ;
#78303=VERTEX_POINT ( 'NONE', #188138 ) ;
#78322=VECTOR ( 'NONE', #60394, 1000.000000000000000 ) ;
#78323=AXIS2_PLACEMENT_3D ( 'NONE', #164190, #83320, #207168 ) ;
#78372=VERTEX_POINT ( 'NONE', #233695 ) ;
#78392=CARTESIAN_POINT ( 'NONE',  ( -20.85000000000000142, 64.35000000001245724, -170.0231074845244166 ) ) ;
#78393=DIRECTION ( 'NONE',  ( 1.000000000000000000, 0.000000000000000000, 0.000000000000000000 ) ) ;
#78399=CARTESIAN_POINT ( 'NONE',  ( -23.25000000000000000, 77.83585931145600512, -158.5186683157258187 ) ) ;
#78418=FACE_OUTER_BOUND ( 'NONE', #193586, .T. ) ;
#78422=CIRCLE ( 'NONE', #207626, 0.5999999999999894307 ) ;
#78435=EDGE_CURVE ( 'NONE', #212797, #155749, #226039, .T. ) ;
#78446=ORIENTED_EDGE ( 'NONE', *, *, #193143, .T. ) ;
#78453=DIRECTION ( 'NONE',  ( 0.000000000000000000, 6.982962677686266711E-15, -1.000000000000000000 ) ) ;
#78454=CARTESIAN_POINT ( 'NONE',  ( -20.85000000000000142, 77.16412189325360771, -162.1082593989527254 ) ) ;
#78464=CIRCLE ( 'NONE', #49244, 0.09999999999998898659 ) ;
#78471=CARTESIAN_POINT ( 'NONE',  ( 21.05000000000000071, 85.00000000001251976, -179.5170766071767332 ) ) ;
#78498=ORIENTED_EDGE ( 'NONE', *, *, #147127, .T. ) ;
#78507=CARTESIAN_POINT ( 'NONE',  ( -23.25000000000000000, 76.00000000001244871, -170.0231074845243597 ) ) ;
#78510=EDGE_CURVE ( 'NONE', #213491, #177211, #19790, .T. ) ;
#78511=ORIENTED_EDGE ( 'NONE', *, *, #166415, .F. ) ;
#78560=VERTEX_POINT ( 'NONE', #160598 ) ;
#78606=EDGE_CURVE ( 'NONE', #241009, #87006, #197217, .T. ) ;
#78628=CARTESIAN_POINT ( 'NONE',  ( -18.45037301276614272, 85.49020044755479830, -196.5104333481092453 ) ) ;
#78656=EDGE_LOOP ( 'NONE', ( #225888, #254833, #227196, #169943 ) ) ;
#78675=DIRECTION ( 'NONE',  ( 1.000000000000000000, 0.000000000000000000, 0.000000000000000000 ) ) ;
#78683=ORIENTED_EDGE ( 'NONE', *, *, #153621, .T. ) ;
#78699=CARTESIAN_POINT ( 'NONE',  ( 21.05000000000000071, 69.69548367074820305, -203.5020041764652774 ) ) ;
#78703=AXIS2_PLACEMENT_3D ( 'NONE', #100570, #183994, #64048 ) ;
#78734=AXIS2_PLACEMENT_3D ( 'NONE', #236650, #20194, #160989 ) ;
#78737=DIRECTION ( 'NONE',  ( -0.000000000000000000, -6.982962677686266711E-15, 1.000000000000000000 ) ) ;
#78759=DIRECTION ( 'NONE',  ( 1.000000000000000000, 0.000000000000000000, 0.000000000000000000 ) ) ;
#78768=ORIENTED_EDGE ( 'NONE', *, *, #216551, .F. ) ;
#78770=CIRCLE ( 'NONE', #220464, 4.300000000000025580 ) ;
#78778=CARTESIAN_POINT ( 'NONE',  ( -20.54999999999999716, 68.85000000001254250, -182.3731074845244109 ) ) ;
#78805=CARTESIAN_POINT ( 'NONE',  ( -23.25000000000000000, 87.75000000001267608, -203.5231074845243029 ) ) ;
#78806=CYLINDRICAL_SURFACE ( 'NONE', #77429, 0.1000000000000028644 ) ;
#78807=CIRCLE ( 'NONE', #33103, 0.1000000000000072220 ) ;
#78834=AXIS2_PLACEMENT_3D ( 'NONE', #105283, #162748, #6207 ) ;
#78839=EDGE_CURVE ( 'NONE', #91470, #176502, #106570, .T. ) ;
#78879=CARTESIAN_POINT ( 'NONE',  ( 20.95512820512820440, 65.37615131630072085, -191.3731074845244393 ) ) ;
#78903=DIRECTION ( 'NONE',  ( 1.000000000000000000, 0.000000000000000000, 0.000000000000000000 ) ) ;
#78933=ORIENTED_EDGE ( 'NONE', *, *, #185717, .F. ) ;
#78940=DIRECTION ( 'NONE',  ( -0.000000000000000000, -6.982962677686266711E-15, 1.000000000000000000 ) ) ;
#78949=CARTESIAN_POINT ( 'NONE',  ( 23.14999999999999503, 64.35000000001249987, -177.0379132551783812 ) ) ;
#78972=DIRECTION ( 'NONE',  ( 0.7071067811865127117, 0.7071067811865821007, 0.000000000000000000 ) ) ;
#78982=FACE_OUTER_BOUND ( 'NONE', #50967, .T. ) ;
#78989=ORIENTED_EDGE ( 'NONE', *, *, #246951, .F. ) ;
#78998=CARTESIAN_POINT ( 'NONE',  ( -1.820710678118657944, 85.92928932189384739, -178.7731074845243029 ) ) ;
#79010=AXIS2_PLACEMENT_3D ( 'NONE', #216045, #200352, #161233 ) ;
#79020=ADVANCED_FACE ( 'NONE', ( #183359 ), #62126, .F. ) ;
#79032=DIRECTION ( 'NONE',  ( 0.000000000000000000, -7.086529944415886769E-15, 1.000000000000000000 ) ) ;
#79061=CARTESIAN_POINT ( 'NONE',  ( 23.14999999999999858, 76.00000000001244871, -170.0231074845243597 ) ) ;
#79083=CIRCLE ( 'NONE', #66647, 0.09999999999999971412 ) ;
#79093=CARTESIAN_POINT ( 'NONE',  ( -18.59999999999999787, 64.35000000001259934, -191.2731074845244450 ) ) ;
#79116=CARTESIAN_POINT ( 'NONE',  ( -20.54999999999999716, 85.00000000001261924, -193.6291383618718385 ) ) ;
#79128=VERTEX_POINT ( 'NONE', #210610 ) ;
#79147=EDGE_CURVE ( 'NONE', #80372, #25370, #225015, .T. ) ;
#79155=DIRECTION ( 'NONE',  ( 1.000000000000000000, 0.000000000000000000, 0.000000000000000000 ) ) ;
#79157=EDGE_CURVE ( 'NONE', #30344, #72156, #127228, .T. ) ;
#79164=DIRECTION ( 'NONE',  ( 0.000000000000000000, -0.008583690987162452199, 0.9999631594459053030 ) ) ;
#79177=CARTESIAN_POINT ( 'NONE',  ( -20.85000000000000142, 76.00000000001244871, -170.0231074845243597 ) ) ;
#79183=VECTOR ( 'NONE', #238962, 1000.000000000000000 ) ;
#79185=CIRCLE ( 'NONE', #33455, 0.09999999999998898659 ) ;
#79192=CIRCLE ( 'NONE', #224936, 0.09999999999999939493 ) ;
#79234=DIRECTION ( 'NONE',  ( 1.000000000000000000, 0.000000000000000000, 0.000000000000000000 ) ) ;
#79235=DIRECTION ( 'NONE',  ( 0.000000000000000000, 6.982962677686266711E-15, -1.000000000000000000 ) ) ;
#79259=CARTESIAN_POINT ( 'NONE',  ( -21.30740335185486245, 75.90106547423687289, -210.0797654065523545 ) ) ;
#79271=AXIS2_PLACEMENT_3D ( 'NONE', #208719, #189136, #168337 ) ;
#79282=ORIENTED_EDGE ( 'NONE', *, *, #114435, .F. ) ;
#79299=EDGE_CURVE ( 'NONE', #222338, #31357, #194302, .T. ) ;
#79301=CARTESIAN_POINT ( 'NONE',  ( -20.96077737575351918, 64.37609936600773608, -176.8823155274181147 ) ) ;
#79454=CARTESIAN_POINT ( 'NONE',  ( 23.24999999999999289, 64.35000000001275566, -215.2731074845244450 ) ) ;
#79455=CARTESIAN_POINT ( 'NONE',  ( -21.55000000000000071, 68.75000000001260503, -191.1731074845243938 ) ) ;
#79460=EDGE_CURVE ( 'NONE', #185078, #102497, #15212, .T. ) ;
#79482=ORIENTED_EDGE ( 'NONE', *, *, #206023, .T. ) ;
#79487=AXIS2_PLACEMENT_3D ( 'NONE', #97568, #239683, #16801 ) ;
#79491=DIRECTION ( 'NONE',  ( 0.000000000000000000, 0.000000000000000000, -1.000000000000000000 ) ) ;
#79551=CIRCLE ( 'NONE', #154617, 0.5000000000000004441 ) ;
#79553=EDGE_CURVE ( 'NONE', #255448, #253555, #202631, .T. ) ;
#79561=DIRECTION ( 'NONE',  ( -1.000000000000000000, 0.000000000000000000, 0.000000000000000000 ) ) ;
#79568=EDGE_CURVE ( 'NONE', #231047, #128423, #156782, .T. ) ;
#79581=FACE_OUTER_BOUND ( 'NONE', #254067, .T. ) ;
#79600=DIRECTION ( 'NONE',  ( 0.000000000000000000, 0.000000000000000000, -1.000000000000000000 ) ) ;
#79614=CIRCLE ( 'NONE', #225369, 0.09999999999999939493 ) ;
#79636=CIRCLE ( 'NONE', #530, 0.09999999999998898659 ) ;
#79652=VERTEX_POINT ( 'NONE', #176338 ) ;
#79661=DIRECTION ( 'NONE',  ( 1.000000000000000000, -0.000000000000000000, 0.000000000000000000 ) ) ;
#79667=DIRECTION ( 'NONE',  ( 0.000000000000000000, -1.000000000000000000, -6.982962677686266711E-15 ) ) ;
#79669=AXIS2_PLACEMENT_3D ( 'NONE', #25473, #81542, #125831 ) ;
#79674=DIRECTION ( 'NONE',  ( 1.000000000000000000, 0.000000000000000000, 0.000000000000000000 ) ) ;
#79703=EDGE_LOOP ( 'NONE', ( #252486, #180374, #149363, #231534 ) ) ;
#79705=ORIENTED_EDGE ( 'NONE', *, *, #192386, .F. ) ;
#79714=DIRECTION ( 'NONE',  ( 0.000000000000000000, -0.1350103645451807555, -0.9908441862701610203 ) ) ;
#79724=CARTESIAN_POINT ( 'NONE',  ( 20.04142135623730070, 64.35000000001275566, -215.2731074845244450 ) ) ;
#79807=DIRECTION ( 'NONE',  ( 1.000000000000000000, 0.000000000000000000, 0.000000000000000000 ) ) ;
#79808=EDGE_CURVE ( 'NONE', #228403, #175328, #10529, .T. ) ;
#79841=ORIENTED_EDGE ( 'NONE', *, *, #253248, .F. ) ;
#79847=LINE ( 'NONE', #159429, #79183 ) ;
#79866=DIRECTION ( 'NONE',  ( 0.000000000000000000, -0.6728971962617102953, -0.7397360091702507301 ) ) ;
#79913=DIRECTION ( 'NONE',  ( 2.952720810173289112E-16, 1.000000000000000000, 6.982962677686266711E-15 ) ) ;
#79946=ORIENTED_EDGE ( 'NONE', *, *, #100180, .T. ) ;
#79965=EDGE_CURVE ( 'NONE', #216782, #197918, #53500, .T. ) ;
#79975=CARTESIAN_POINT ( 'NONE',  ( 18.47073956224740954, 85.47172941248462052, -196.4144217317061134 ) ) ;
#79981=CARTESIAN_POINT ( 'NONE',  ( 21.05000000000000071, 75.90220970870393558, -209.7809220950004772 ) ) ;
#80010=ORIENTED_EDGE ( 'NONE', *, *, #47240, .F. ) ;
#80032=EDGE_CURVE ( 'NONE', #246278, #154279, #57236, .T. ) ;
#80048=CARTESIAN_POINT ( 'NONE',  ( 23.15000000000000213, 88.41227409416214300, -173.0231074845242745 ) ) ;
#80113=VECTOR ( 'NONE', #216072, 1000.000000000000000 ) ;
#80140=EDGE_LOOP ( 'NONE', ( #136213, #56469, #66117, #5914 ) ) ;
#80149=AXIS2_PLACEMENT_3D ( 'NONE', #247210, #9884, #51550 ) ;
#80165=CIRCLE ( 'NONE', #84245, 4.049999999999998046 ) ;
#80180=DIRECTION ( 'NONE',  ( -1.000000000000000000, -0.000000000000000000, -0.000000000000000000 ) ) ;
#80197=CARTESIAN_POINT ( 'NONE',  ( 20.77526135991769607, 67.06799098339227783, -195.0545389417991657 ) ) ;
#80234=DIRECTION ( 'NONE',  ( 2.952720810173289112E-16, 1.000000000000000000, -6.088138035986627436E-46 ) ) ;
#80257=AXIS2_PLACEMENT_3D ( 'NONE', #201351, #181796, #566 ) ;
#80273=ADVANCED_FACE ( 'NONE', ( #188848 ), #72789, .T. ) ;
#80311=FACE_OUTER_BOUND ( 'NONE', #248850, .T. ) ;
#80314=DIRECTION ( 'NONE',  ( 0.000000000000000000, -0.9908441862701420355, -0.1350103645453197554 ) ) ;
#80332=CARTESIAN_POINT ( 'NONE',  ( 18.46163235739469499, 85.48015080693069478, -163.3654969446463383 ) ) ;
#80360=CARTESIAN_POINT ( 'NONE',  ( 22.40736611211992368, 76.00000000001276135, -215.1726782920691505 ) ) ;
#80366=DIRECTION ( 'NONE',  ( -1.000000000000000000, -0.000000000000000000, -0.000000000000000000 ) ) ;
#80372=VERTEX_POINT ( 'NONE', #114449 ) ;
#80387=CARTESIAN_POINT ( 'NONE',  ( -21.07928932188134041, 75.90110485435833709, -209.8516241409176644 ) ) ;
#80410=CIRCLE ( 'NONE', #109663, 11.75000000000001066 ) ;
#80419=EDGE_CURVE ( 'NONE', #241603, #8263, #132267, .T. ) ;
#80423=CIRCLE ( 'NONE', #192902, 0.09999999999998898659 ) ;
#80432=CARTESIAN_POINT ( 'NONE',  ( -21.05000000000000071, 64.35000000001249987, -177.0379132551784096 ) ) ;
#80458=CARTESIAN_POINT ( 'NONE',  ( -23.15000000000000213, 64.25000000001260503, -191.2731074845244450 ) ) ;
#80460=ORIENTED_EDGE ( 'NONE', *, *, #256161, .F. ) ;
#80496=DIRECTION ( 'NONE',  ( 0.000000000000000000, -0.5000000000000016653, 0.8660254037844377084 ) ) ;
#80552=CARTESIAN_POINT ( 'NONE',  ( 23.14999999999999503, 64.35000000001249987, -177.0379132551783812 ) ) ;
#80565=ADVANCED_FACE ( 'NONE', ( #185972 ), #86849, .T. ) ;
#80574=CARTESIAN_POINT ( 'NONE',  ( -20.85000000000000142, 64.25000000001250555, -176.8069731475025321 ) ) ;
#80668=CYLINDRICAL_SURFACE ( 'NONE', #169856, 0.1000000000000028644 ) ;
#80707=ORIENTED_EDGE ( 'NONE', *, *, #79157, .T. ) ;
#80709=DIRECTION ( 'NONE',  ( -0.000000000000000000, -6.982962677686266711E-15, 1.000000000000000000 ) ) ;
#80738=TOROIDAL_SURFACE ( 'NONE', #130831, 7.800000000000000711, 0.1000000000000000056 ) ;
#80740=DIRECTION ( 'NONE',  ( -0.000000000000000000, 1.000000000000000000, 6.982962677686266711E-15 ) ) ;
#80744=CARTESIAN_POINT ( 'NONE',  ( -23.25000000000000000, 87.65000000001269598, -203.5231074845243029 ) ) ;
#80746=ORIENTED_EDGE ( 'NONE', *, *, #55290, .T. ) ;
#80765=EDGE_CURVE ( 'NONE', #222996, #64517, #78464, .T. ) ;
#80767=CARTESIAN_POINT ( 'NONE',  ( 22.49806830649814060, 64.35011034517360429, -203.6005718008499628 ) ) ;
#80781=CARTESIAN_POINT ( 'NONE',  ( 21.10710606213542562, 67.22310597611939897, -191.2821109581250028 ) ) ;
#80787=CYLINDRICAL_SURFACE ( 'NONE', #60041, 7.899999999999990585 ) ;
#80805=CARTESIAN_POINT ( 'NONE',  ( -20.94999999999999929, 74.16465844978819177, -191.9679561919613775 ) ) ;
#80817=DIRECTION ( 'NONE',  ( 0.000000000000000000, -0.8700118002898356018, 0.4930308989875170078 ) ) ;
#80833=EDGE_CURVE ( 'NONE', #217574, #14270, #90935, .T. ) ;
#80882=CIRCLE ( 'NONE', #189240, 0.09999999999999938105 ) ;
#80903=ORIENTED_EDGE ( 'NONE', *, *, #194790, .F. ) ;
#80905=VERTEX_POINT ( 'NONE', #186649 ) ;
#80916=ORIENTED_EDGE ( 'NONE', *, *, #35728, .F. ) ;
#80922=LINE ( 'NONE', #155379, #226261 ) ;
#80946=ORIENTED_EDGE ( 'NONE', *, *, #41970, .F. ) ;
#80951=DIRECTION ( 'NONE',  ( 1.000000000000000000, -0.000000000000000000, -0.000000000000000000 ) ) ;
#80958=CARTESIAN_POINT ( 'NONE',  ( -23.25000000000000000, 76.00000000001239187, -162.1231074845243825 ) ) ;
#80979=DIRECTION ( 'NONE',  ( -1.836970198721029934E-16, -1.000000000000000000, -6.982962677686266711E-15 ) ) ;
#80981=CARTESIAN_POINT ( 'NONE',  ( -18.50000000000000000, 76.00000000001244871, -170.0231074845243597 ) ) ;
#81041=LINE ( 'NONE', #160635, #232586 ) ;
#81067=EDGE_CURVE ( 'NONE', #199384, #248274, #91393, .T. ) ;
#81083=DIRECTION ( 'NONE',  ( 0.000000000000000000, 0.000000000000000000, 1.000000000000000000 ) ) ;
#81089=DIRECTION ( 'NONE',  ( 0.000000000000000000, 0.000000000000000000, 1.000000000000000000 ) ) ;
#81148=VECTOR ( 'NONE', #113003, 1000.000000000000000 ) ;
#81149=VERTEX_POINT ( 'NONE', #119967 ) ;
#81153=ADVANCED_FACE ( 'NONE', ( #40435 ), #138188, .F. ) ;
#81191=CARTESIAN_POINT ( 'NONE',  ( -18.50000000000000355, 85.40000000001262492, -196.2258477248610120 ) ) ;
#81196=EDGE_CURVE ( 'NONE', #100484, #25217, #161893, .T. ) ;
#81204=EDGE_CURVE ( 'NONE', #150814, #77481, #213497, .T. ) ;
#81219=CYLINDRICAL_SURFACE ( 'NONE', #160754, 0.09999999999998898659 ) ;
#81227=LINE ( 'NONE', #160819, #143043 ) ;
#81249=DIRECTION ( 'NONE',  ( 1.000000000000000000, 0.000000000000000000, 0.000000000000000000 ) ) ;
#81250=EDGE_LOOP ( 'NONE', ( #197438, #214361, #53055, #102344 ) ) ;
#81251=CIRCLE ( 'NONE', #156325, 7.900000000000003908 ) ;
#81289=DIRECTION ( 'NONE',  ( 0.000000000000000000, 6.982962677686266711E-15, -1.000000000000000000 ) ) ;
#81316=ORIENTED_EDGE ( 'NONE', *, *, #65525, .T. ) ;
#81323=ORIENTED_EDGE ( 'NONE', *, *, #188615, .F. ) ;
#81360=DIRECTION ( 'NONE',  ( 1.000000000000000000, 0.000000000000000000, 0.000000000000000000 ) ) ;
#81395=AXIS2_PLACEMENT_3D ( 'NONE', #161767, #104310, #225536 ) ;
#81432=DIRECTION ( 'NONE',  ( 0.000000000000000000, 1.000000000000000000, 6.982962677686266711E-15 ) ) ;
#81435=CARTESIAN_POINT ( 'NONE',  ( 20.94999999999999574, 74.16465844978819177, -191.9679561919613775 ) ) ;
#81439=AXIS2_PLACEMENT_3D ( 'NONE', #61119, #256706, #235898 ) ;
#81443=DIRECTION ( 'NONE',  ( 0.000000000000000000, 6.982962677686266711E-15, -1.000000000000000000 ) ) ;
#81454=AXIS2_PLACEMENT_3D ( 'NONE', #251095, #213260, #52906 ) ;
#81463=CARTESIAN_POINT ( 'NONE',  ( -20.85000000000000142, 64.25000000001250555, -176.8069731475025321 ) ) ;
#81491=PLANE ( 'NONE',  #118436 ) ;
#81505=VERTEX_POINT ( 'NONE', #23110 ) ;
#81509=DIRECTION ( 'NONE',  ( 0.000000000000000000, -1.000000000000000000, -6.982962677686266711E-15 ) ) ;
#81513=CIRCLE ( 'NONE', #89736, 0.09999999999999939493 ) ;
#81542=DIRECTION ( 'NONE',  ( -1.000000000000000000, 0.000000000000000000, -0.000000000000000000 ) ) ;
#81549=EDGE_CURVE ( 'NONE', #221772, #670, #232796, .T. ) ;
#81582=CIRCLE ( 'NONE', #223092, 0.09999999999998898659 ) ;
#81585=ORIENTED_EDGE ( 'NONE', *, *, #206206, .T. ) ;
#81586=ORIENTED_EDGE ( 'NONE', *, *, #129279, .T. ) ;
#81589=DIRECTION ( 'NONE',  ( -2.978066053179069723E-16, -1.000000000000000000, -4.764905685086511557E-15 ) ) ;
#81609=CARTESIAN_POINT ( 'NONE',  ( 18.48197441911657180, 85.51795479471881833, -163.1328958423161168 ) ) ;
#81619=CARTESIAN_POINT ( 'NONE',  ( 18.49999999999998934, 56.14960075277911500, -201.2428044267231257 ) ) ;
#81622=ORIENTED_EDGE ( 'NONE', *, *, #19691, .T. ) ;
#81636=FACE_OUTER_BOUND ( 'NONE', #129400, .T. ) ;
#81642=EDGE_CURVE ( 'NONE', #236908, #207747, #164454, .T. ) ;
#81643=DIRECTION ( 'NONE',  ( 1.000000000000000000, 0.000000000000000000, 0.000000000000000000 ) ) ;
#81656=VECTOR ( 'NONE', #78393, 1000.000000000000000 ) ;
#81672=VECTOR ( 'NONE', #99358, 1000.000000000000000 ) ;
#81695=VECTOR ( 'NONE', #36005, 1000.000000000000000 ) ;
#81701=CARTESIAN_POINT ( 'NONE',  ( -21.05000000000000071, 69.69257478044727350, -203.5062876161387635 ) ) ;
#81708=EDGE_CURVE ( 'NONE', #21234, #51100, #78807, .T. ) ;
#81763=PRODUCT_DEFINITION_CONTEXT ( 'detailed design', #139160, 'design' ) ;
#81784=AXIS2_PLACEMENT_3D ( 'NONE', #154455, #233950, #90575 ) ;
#81794=ADVANCED_FACE ( 'NONE', ( #90730 ), #32083, .T. ) ;
#81796=AXIS2_PLACEMENT_3D ( 'NONE', #12269, #209150, #30546 ) ;
#81802=CARTESIAN_POINT ( 'NONE',  ( -21.14999999999999858, 76.00000000001271871, -210.0637644362255969 ) ) ;
#81840=DIRECTION ( 'NONE',  ( 0.000000000000000000, 6.982962677686266711E-15, -1.000000000000000000 ) ) ;
#81897=VERTEX_POINT ( 'NONE', #191155 ) ;
#81921=ORIENTED_EDGE ( 'NONE', *, *, #243178, .T. ) ;
#81925=ORIENTED_EDGE ( 'NONE', *, *, #21664, .F. ) ;
#81926=FACE_OUTER_BOUND ( 'NONE', #200293, .T. ) ;
#81959=ADVANCED_FACE ( 'NONE', ( #58014 ), #37212, .F. ) ;
#81968=B_SPLINE_CURVE_WITH_KNOTS ( 'NONE', 3,
 ( #161565, #241102, #203232, #104110, #62451, #6304 ),
 .UNSPECIFIED., .F., .F.,
 ( 4, 2, 4 ),
 ( 0.000000000000000000, 0.0002113392456166052376, 0.0004226784912332104752 ),
 .UNSPECIFIED. ) ;
#81989=PLANE ( 'NONE',  #186277 ) ;
#82007=DIRECTION ( 'NONE',  ( 0.000000000000000000, 0.000000000000000000, -1.000000000000000000 ) ) ;
#82012=DIRECTION ( 'NONE',  ( 2.978066053179066272E-16, 1.000000000000000000, 9.529811370173012070E-15 ) ) ;
#82034=VECTOR ( 'NONE', #173182, 1000.000000000000000 ) ;
#82055=CARTESIAN_POINT ( 'NONE',  ( 21.13920837816993270, 67.21675294989267968, -191.2731074845244166 ) ) ;
#82071=TOROIDAL_SURFACE ( 'NONE', #115413, 12.97499999999999787, 0.1000000000000000056 ) ;
#82073=CARTESIAN_POINT ( 'NONE',  ( -22.50000000000000000, 76.00000000001276135, -215.1726782920691505 ) ) ;
#82112=DIRECTION ( 'NONE',  ( 1.000000000000000000, 0.000000000000000000, 0.000000000000000000 ) ) ;
#82115=LINE ( 'NONE', #162990, #197862 ) ;
#82131=DIRECTION ( 'NONE',  ( 1.000000000000000000, 7.304098846218134667E-16, 5.100424963727256530E-30 ) ) ;
#82141=VECTOR ( 'NONE', #256665, 1000.000000000000000 ) ;
#82145=CARTESIAN_POINT ( 'NONE',  ( 20.85000000000000142, 64.35000000001245724, -170.0231074845244166 ) ) ;
#82147=CARTESIAN_POINT ( 'NONE',  ( -20.64999999999999858, 84.73084112150785074, -179.6211822035086243 ) ) ;
#82185=ORIENTED_EDGE ( 'NONE', *, *, #179175, .T. ) ;
#82187=AXIS2_PLACEMENT_3D ( 'NONE', #104565, #47167, #66765 ) ;
#82195=DIRECTION ( 'NONE',  ( 1.000000000000000000, 0.000000000000000000, 0.000000000000000000 ) ) ;
#82228=AXIS2_PLACEMENT_3D ( 'NONE', #133483, #95628, #171374 ) ;
#82261=EDGE_CURVE ( 'NONE', #34777, #60192, #162424, .T. ) ;
#82262=CARTESIAN_POINT ( 'NONE',  ( -20.94999999999999929, 77.16270174995064224, -195.4231074845243370 ) ) ;
#82266=CARTESIAN_POINT ( 'NONE',  ( 18.59999999999999787, 77.26327546522965406, -162.1212428177779543 ) ) ;
#82290=ORIENTED_EDGE ( 'NONE', *, *, #83284, .T. ) ;
#82359=CARTESIAN_POINT ( 'NONE',  ( 20.95420533658165141, 65.45413552525306500, -195.9556014638312149 ) ) ;
#82360=ADVANCED_FACE ( 'NONE', ( #235107 ), #257171, .T. ) ;
#82410=ORIENTED_EDGE ( 'NONE', *, *, #446, .F. ) ;
#82411=EDGE_CURVE ( 'NONE', #241382, #178265, #79847, .T. ) ;
#82444=DIRECTION ( 'NONE',  ( 0.000000000000000000, 0.000000000000000000, -1.000000000000000000 ) ) ;
#82464=ORIENTED_EDGE ( 'NONE', *, *, #157619, .T. ) ;
#82472=DIRECTION ( 'NONE',  ( 0.000000000000000000, -6.982962677686266711E-15, 1.000000000000000000 ) ) ;
#82498=EDGE_CURVE ( 'NONE', #105444, #101145, #87381, .T. ) ;
#82499=AXIS2_PLACEMENT_3D ( 'NONE', #254116, #212456, #114621 ) ;
#82518=AXIS2_PLACEMENT_3D ( 'NONE', #246342, #205923, #164251 ) ;
#82533=VECTOR ( 'NONE', #215954, 1000.000000000000114 ) ;
#82544=LINE ( 'NONE', #245521, #140241 ) ;
#82546=AXIS2_PLACEMENT_3D ( 'NONE', #214202, #229906, #189504 ) ;
#82608=ORIENTED_EDGE ( 'NONE', *, *, #183288, .T. ) ;
#82645=CIRCLE ( 'NONE', #195139, 0.09999999999998898659 ) ;
#82653=CARTESIAN_POINT ( 'NONE',  ( 20.94999999999999574, 87.48912529308871910, -200.6231074845242688 ) ) ;
#82657=DIRECTION ( 'NONE',  ( 1.000000000000000000, 0.000000000000000000, 0.000000000000000000 ) ) ;
#82660=ADVANCED_FACE ( 'NONE', ( #88834 ), #104307, .F. ) ;
#82720=DIRECTION ( 'NONE',  ( 0.000000000000000000, -7.304098846218085561E-15, 1.000000000000000000 ) ) ;
#82724=EDGE_LOOP ( 'NONE', ( #10108, #152005, #143881, #123207, #240940 ) ) ;
#82731=VECTOR ( 'NONE', #4039, 1000.000000000000000 ) ;
#82749=ORIENTED_EDGE ( 'NONE', *, *, #51237, .F. ) ;
#82758=DIRECTION ( 'NONE',  ( -1.000000000000000000, -0.000000000000000000, -0.000000000000000000 ) ) ;
#82759=LINE ( 'NONE', #159783, #44848 ) ;
#82772=DIRECTION ( 'NONE',  ( -1.000000000000000000, -0.000000000000000000, -0.000000000000000000 ) ) ;
#82774=DIRECTION ( 'NONE',  ( 0.000000000000000000, 1.000000000000000000, 6.982962677686266711E-15 ) ) ;
#82823=ORIENTED_EDGE ( 'NONE', *, *, #139279, .T. ) ;
#82861=VERTEX_POINT ( 'NONE', #7387 ) ;
#82891=FACE_OUTER_BOUND ( 'NONE', #111951, .T. ) ;
#82925=LINE ( 'NONE', #38709, #70053 ) ;
#82934=ORIENTED_EDGE ( 'NONE', *, *, #143716, .F. ) ;
#82940=ORIENTED_EDGE ( 'NONE', *, *, #4048, .T. ) ;
#82958=AXIS2_PLACEMENT_3D ( 'NONE', #196197, #35862, #114082 ) ;
#82964=DIRECTION ( 'NONE',  ( -1.000000000000000000, 7.304098846218134667E-16, 5.100424963727256530E-30 ) ) ;
#83021=DIRECTION ( 'NONE',  ( 1.000000000000000000, -2.952720810173289112E-16, -2.061873921506763405E-30 ) ) ;
#83038=CIRCLE ( 'NONE', #183049, 0.09999999999998898659 ) ;
#83045=CARTESIAN_POINT ( 'NONE',  ( -22.47007471830799474, 68.27928934808619488, -203.5231074845244166 ) ) ;
#83109=DIRECTION ( 'NONE',  ( -2.915501640297152804E-16, -1.000000000000000000, -6.997203936713167125E-15 ) ) ;
#83130=ORIENTED_EDGE ( 'NONE', *, *, #96457, .F. ) ;
#83179=CARTESIAN_POINT ( 'NONE',  ( -18.50000000000000000, 66.65000000001259650, -191.1731074845244223 ) ) ;
#83193=ORIENTED_EDGE ( 'NONE', *, *, #167173, .F. ) ;
#83213=CARTESIAN_POINT ( 'NONE',  ( 18.59999999999999076, 76.00000000001244871, -170.0231074845243597 ) ) ;
#83215=ORIENTED_EDGE ( 'NONE', *, *, #173941, .F. ) ;
#83218=DIRECTION ( 'NONE',  ( 0.000000000000000000, -6.982962677686267499E-15, 1.000000000000000000 ) ) ;
#83284=EDGE_CURVE ( 'NONE', #12967, #143950, #211735, .T. ) ;
#83320=DIRECTION ( 'NONE',  ( -0.000000000000000000, -6.982962677686266711E-15, 1.000000000000000000 ) ) ;
#83325=SPHERICAL_SURFACE ( 'NONE', #134677, 0.1000000000000000056 ) ;
#83341=EDGE_CURVE ( 'NONE', #49841, #248091, #229992, .T. ) ;
#83342=CIRCLE ( 'NONE', #124886, 0.09999999999999939493 ) ;
#83359=TOROIDAL_SURFACE ( 'NONE', #125102, 0.2000000000000000111, 0.1000000000000000056 ) ;
#83390=FACE_OUTER_BOUND ( 'NONE', #104647, .T. ) ;
#83405=DIRECTION ( 'NONE',  ( -0.000000000000000000, -1.000000000000000000, -6.982962677686266711E-15 ) ) ;
#83413=DIRECTION ( 'NONE',  ( 0.000000000000000000, -7.487053152578134969E-15, 1.000000000000000000 ) ) ;
#83494=ORIENTED_EDGE ( 'NONE', *, *, #55409, .F. ) ;
#83510=ORIENTED_EDGE ( 'NONE', *, *, #170213, .T. ) ;
#83577=CARTESIAN_POINT ( 'NONE',  ( -18.39999999999999858, 85.68240343348880117, -163.3662641071115047 ) ) ;
#83597=ORIENTED_EDGE ( 'NONE', *, *, #131549, .T. ) ;
#83605=ORIENTED_EDGE ( 'NONE', *, *, #31700, .F. ) ;
#83615=ORIENTED_EDGE ( 'NONE', *, *, #215391, .T. ) ;
#83639=DIRECTION ( 'NONE',  ( -0.000000000000000000, -6.982962677686266711E-15, 1.000000000000000000 ) ) ;
#83659=VERTEX_POINT ( 'NONE', #105865 ) ;
#83662=CARTESIAN_POINT ( 'NONE',  ( -21.14999999999999858, 64.35000000001268461, -203.5231074845244166 ) ) ;
#83667=FACE_OUTER_BOUND ( 'NONE', #29359, .T. ) ;
#83670=DIRECTION ( 'NONE',  ( 0.000000000000000000, -6.982962677686266711E-15, 1.000000000000000000 ) ) ;
#83673=CARTESIAN_POINT ( 'NONE',  ( -22.47120815636973745, 75.97109617810887983, -215.1730394732778393 ) ) ;
#83718=CARTESIAN_POINT ( 'NONE',  ( -18.39999999999999858, 85.50000000001242029, -163.4229180933022576 ) ) ;
#83741=ORIENTED_EDGE ( 'NONE', *, *, #77297, .T. ) ;
#83752=EDGE_CURVE ( 'NONE', #255583, #41396, #190590, .T. ) ;
#83793=ORIENTED_EDGE ( 'NONE', *, *, #255873, .F. ) ;
#83819=CARTESIAN_POINT ( 'NONE',  ( -23.15000000000000213, 74.00000000001254818, -182.7477294072864709 ) ) ;
#83828=VERTEX_POINT ( 'NONE', #36665 ) ;
#83848=CIRCLE ( 'NONE', #13188, 0.09999999999998898659 ) ;
#83904=ORIENTED_EDGE ( 'NONE', *, *, #76086, .T. ) ;
#83936=CARTESIAN_POINT ( 'NONE',  ( -18.54148534481894117, 65.67467670974468774, -164.4531731826884879 ) ) ;
#83955=FACE_OUTER_BOUND ( 'NONE', #234477, .T. ) ;
#83975=DIRECTION ( 'NONE',  ( -1.000000000000000000, 0.000000000000000000, 0.000000000000000000 ) ) ;
#83979=DIRECTION ( 'NONE',  ( 0.000000000000000000, 0.000000000000000000, 1.000000000000000000 ) ) ;
#83980=DIRECTION ( 'NONE',  ( 0.000000000000000000, 0.000000000000000000, 1.000000000000000000 ) ) ;
#83991=ADVANCED_FACE ( 'NONE', ( #123883 ), #44346, .T. ) ;
#84001=CARTESIAN_POINT ( 'NONE',  ( 21.05000000000000071, 65.27628288308754634, -191.3468678833862668 ) ) ;
#84061=ORIENTED_EDGE ( 'NONE', *, *, #154228, .F. ) ;
#84090=ORIENTED_EDGE ( 'NONE', *, *, #254107, .T. ) ;
#84125=DIRECTION ( 'NONE',  ( 1.000000000000000000, 0.000000000000000000, 0.000000000000000000 ) ) ;
#84151=AXIS2_PLACEMENT_3D ( 'NONE', #118983, #56409, #134657 ) ;
#84185=DIRECTION ( 'NONE',  ( -1.000000000000000000, -0.000000000000000000, -0.000000000000000000 ) ) ;
#84202=CARTESIAN_POINT ( 'NONE',  ( 23.14999999999998437, 76.00000000001267608, -203.5231074845243597 ) ) ;
#84245=AXIS2_PLACEMENT_3D ( 'NONE', #84202, #208086, #206784 ) ;
#84254=ORIENTED_EDGE ( 'NONE', *, *, #17272, .F. ) ;
#84288=DIRECTION ( 'NONE',  ( -0.000000000000000000, -1.000000000000000000, -7.272083257015735086E-15 ) ) ;
#84298=VECTOR ( 'NONE', #235607, 1000.000000000000000 ) ;
#84299=( BOUNDED_SURFACE ( )  B_SPLINE_SURFACE ( 3, 2, ( 
 ( #164344, #123935, #104331 ),
 ( #43105, #45669, #108215 ),
 ( #241315, #206028, #24854 ),
 ( #67793, #28719, #3970 ) ),
 .UNSPECIFIED., .F., .F., .F. ) 
 B_SPLINE_SURFACE_WITH_KNOTS ( ( 4, 4 ),
 ( 3, 3 ),
 ( 0.0002700421466196637442, 0.0004789321604330607179 ),
 ( 0.000000000000000000, 1.000000000000000000 ),
 .UNSPECIFIED. ) 
 GEOMETRIC_REPRESENTATION_ITEM ( )  RATIONAL_B_SPLINE_SURFACE ( (
 ( 1.000000000000000000, 0.7071067811865475727, 1.000000000000000000),
 ( 1.000000000000000000, 0.7163411249511738577, 1.000000000000000000),
 ( 1.000000000000000000, 0.7221957104842052777, 1.000000000000000000),
 ( 1.000000000000000000, 0.7250110520819876836, 1.000000000000000000) ) ) 
 REPRESENTATION_ITEM ( '' )  SURFACE ( )  );
#84307=DIRECTION ( 'NONE',  ( -3.265361837132813093E-16, -1.000000000000000000, -6.982962677686266711E-15 ) ) ;
#84350=CARTESIAN_POINT ( 'NONE',  ( -21.09316766718153247, 75.96073659769805886, -209.8932607969990727 ) ) ;
#84423=CARTESIAN_POINT ( 'NONE',  ( -18.50000000000000000, 66.75000000001253397, -182.1731074845244223 ) ) ;
#84428=DIRECTION ( 'NONE',  ( 0.000000000000000000, 6.982962677686266711E-15, -1.000000000000000000 ) ) ;
#84435=ADVANCED_FACE ( 'NONE', ( #143102 ), #62804, .F. ) ;
#84460=DIRECTION ( 'NONE',  ( -1.000000000000000000, 2.952720810173289112E-16, 2.061873921506763405E-30 ) ) ;
#84478=DIRECTION ( 'NONE',  ( -1.000000000000000000, 2.952720810173289112E-16, 2.061873921506763405E-30 ) ) ;
#84488=LINE ( 'NONE', #167624, #198822 ) ;
#84505=CARTESIAN_POINT ( 'NONE',  ( 20.85000000000000142, 77.83585931145600512, -158.4186683157258244 ) ) ;
#84523=DIRECTION ( 'NONE',  ( 0.000000000000000000, 6.982962677686266711E-15, -1.000000000000000000 ) ) ;
#84526=AXIS2_PLACEMENT_3D ( 'NONE', #79061, #119520, #62103 ) ;
#84567=DIRECTION ( 'NONE',  ( -1.000000000000000000, 0.000000000000000000, -0.000000000000000000 ) ) ;
#84572=VECTOR ( 'NONE', #189170, 1000.000000000000000 ) ;
#84577=VECTOR ( 'NONE', #98243, 1000.000000000000000 ) ;
#84592=AXIS2_PLACEMENT_3D ( 'NONE', #202745, #140183, #219733 ) ;
#84622=AXIS2_PLACEMENT_3D ( 'NONE', #250868, #45307, #123562 ) ;
#84687=CARTESIAN_POINT ( 'NONE',  ( -20.54999999999999716, 76.00000000001267608, -203.5231074845243597 ) ) ;
#84706=FACE_OUTER_BOUND ( 'NONE', #199079, .T. ) ;
#84709=AXIS2_PLACEMENT_3D ( 'NONE', #21690, #118216, #77783 ) ;
#84710=VECTOR ( 'NONE', #205041, 1000.000000000000000 ) ;
#84715=FACE_OUTER_BOUND ( 'NONE', #52799, .T. ) ;
#84745=CARTESIAN_POINT ( 'NONE',  ( 21.05000000000000071, 76.00000000001244871, -170.0231074845243597 ) ) ;
#84762=ORIENTED_EDGE ( 'NONE', *, *, #213030, .F. ) ;
#84797=VECTOR ( 'NONE', #79913, 1000.000000000000000 ) ;
#84800=DIRECTION ( 'NONE',  ( 0.000000000000000000, -0.9908441862701791170, 0.1350103645450472789 ) ) ;
#84847=LINE ( 'NONE', #182723, #227412 ) ;
#84855=CARTESIAN_POINT ( 'NONE',  ( -18.52328366898032996, 85.64232108905365237, -163.3082881469542826 ) ) ;
#84868=CIRCLE ( 'NONE', #234948, 7.720710678118692272 ) ;
#84899=CIRCLE ( 'NONE', #134977, 0.09999999999999939493 ) ;
#84902=EDGE_CURVE ( 'NONE', #91774, #212797, #96282, .T. ) ;
#84905=VERTEX_POINT ( 'NONE', #112365 ) ;
#84908=CIRCLE ( 'NONE', #243157, 0.09999999999998898659 ) ;
#84913=LINE ( 'NONE', #87498, #115985 ) ;
#84942=CARTESIAN_POINT ( 'NONE',  ( -23.15000000000000213, 76.00000000001247713, -173.9231074845243654 ) ) ;
#84955=AXIS2_PLACEMENT_3D ( 'NONE', #205736, #70117, #68819 ) ;
#85008=ORIENTED_EDGE ( 'NONE', *, *, #134048, .F. ) ;
#85041=AXIS2_PLACEMENT_3D ( 'NONE', #6260, #84478, #45401 ) ;
#85076=DIRECTION ( 'NONE',  ( 1.000000000000000000, 0.000000000000000000, 0.000000000000000000 ) ) ;
#85123=ORIENTED_EDGE ( 'NONE', *, *, #166865, .F. ) ;
#85135=DIRECTION ( 'NONE',  ( -1.000000000000000000, 0.000000000000000000, 0.000000000000000000 ) ) ;
#85147=CARTESIAN_POINT ( 'NONE',  ( -20.85000000000000142, 77.16412189325360771, -162.1082593989527254 ) ) ;
#85148=LINE ( 'NONE', #100849, #25074 ) ;
#85162=DIRECTION ( 'NONE',  ( -1.000000000000000000, 0.000000000000000000, 0.000000000000000000 ) ) ;
#85201=EDGE_LOOP ( 'NONE', ( #38027, #128983, #214274, #146032, #7569, #172399 ) ) ;
#85224=AXIS2_PLACEMENT_3D ( 'NONE', #85296, #146562, #26662 ) ;
#85232=CYLINDRICAL_SURFACE ( 'NONE', #125622, 0.09999999999998898659 ) ;
#85248=CIRCLE ( 'NONE', #231054, 0.1000000000000033362 ) ;
#85296=CARTESIAN_POINT ( 'NONE',  ( 20.94999999999999929, 76.00000000001244871, -170.0231074845243597 ) ) ;
#85338=CARTESIAN_POINT ( 'NONE',  ( 20.59588692710267921, 65.63127657884351152, -195.8840263900140144 ) ) ;
#85345=CARTESIAN_POINT ( 'NONE',  ( 21.07928932188134397, 75.90110485435809551, -209.8516241409230645 ) ) ;
#85364=VECTOR ( 'NONE', #15400, 1000.000000000000114 ) ;
#85369=CARTESIAN_POINT ( 'NONE',  ( -23.15000000000000213, 85.00000000001261924, -193.6291383618718385 ) ) ;
#85370=DIRECTION ( 'NONE',  ( 0.000000000000000000, 0.000000000000000000, 1.000000000000000000 ) ) ;
#85394=EDGE_LOOP ( 'NONE', ( #56165, #10170, #236336 ) ) ;
#85399=VECTOR ( 'NONE', #209801, 1000.000000000000114 ) ;
#85414=CARTESIAN_POINT ( 'NONE',  ( -20.85882249326303040, 65.66751761918722252, -164.4282609406112670 ) ) ;
#85440=DIRECTION ( 'NONE',  ( 1.000000000000000000, -0.000000000000000000, 0.000000000000000000 ) ) ;
#85458=CARTESIAN_POINT ( 'NONE',  ( -21.08479644141222664, 69.65496134228079939, -203.5816619270885610 ) ) ;
#85467=DIRECTION ( 'NONE',  ( 0.000000000000000000, -6.938893903907030216E-14, 1.000000000000000000 ) ) ;
#85479=VERTEX_POINT ( 'NONE', #50463 ) ;
#85491=DIRECTION ( 'NONE',  ( 0.000000000000000000, -7.304098846218085561E-15, 1.000000000000000000 ) ) ;
#85501=CARTESIAN_POINT ( 'NONE',  ( 21.14999999999999858, 76.00000000001271871, -210.0637644362255969 ) ) ;
#85529=CARTESIAN_POINT ( 'NONE',  ( -20.85000000000000142, 77.14957036958807635, -162.2071950000224092 ) ) ;
#85542=DIRECTION ( 'NONE',  ( -0.000000000000000000, 6.982962677686266711E-15, -1.000000000000000000 ) ) ;
#85543=ADVANCED_FACE ( 'NONE', ( #234251 ), #193864, .F. ) ;
#85555=EDGE_CURVE ( 'NONE', #10156, #2919, #30965, .T. ) ;
#85585=EDGE_CURVE ( 'NONE', #49859, #19071, #125867, .T. ) ;
#85590=DIRECTION ( 'NONE',  ( -1.000000000000000000, 0.000000000000000000, 0.000000000000000000 ) ) ;
#85602=AXIS2_PLACEMENT_3D ( 'NONE', #150890, #225268, #226552 ) ;
#85649=CARTESIAN_POINT ( 'NONE',  ( -21.13498764882296044, 75.99834360528140564, -210.0187256279983217 ) ) ;
#85661=DIRECTION ( 'NONE',  ( 0.000000000000000000, -7.304098846218085561E-15, 1.000000000000000000 ) ) ;
#85669=CIRCLE ( 'NONE', #244106, 7.899999999999990585 ) ;
#85698=VERTEX_POINT ( 'NONE', #218523 ) ;
#85699=CARTESIAN_POINT ( 'NONE',  ( 21.05000000000000071, 84.66355140188177586, -193.9990063664569959 ) ) ;
#85722=CYLINDRICAL_SURFACE ( 'NONE', #106705, 0.1000000000000106914 ) ;
#85731=DIRECTION ( 'NONE',  ( 1.000000000000000000, -0.000000000000000000, 0.000000000000000000 ) ) ;
#85760=ORIENTED_EDGE ( 'NONE', *, *, #127016, .T. ) ;
#85795=ORIENTED_EDGE ( 'NONE', *, *, #221891, .F. ) ;
#85817=CARTESIAN_POINT ( 'NONE',  ( 18.59999999999999076, 76.00000000001244871, -170.0231074845243597 ) ) ;
#85823=ORIENTED_EDGE ( 'NONE', *, *, #79553, .F. ) ;
#85834=CARTESIAN_POINT ( 'NONE',  ( -21.05000000000000071, 77.85102823015347440, -191.8691942151018566 ) ) ;
#85840=CARTESIAN_POINT ( 'NONE',  ( 21.05000000000000071, 74.83729825007462466, -195.6231074845243540 ) ) ;
#85919=FACE_OUTER_BOUND ( 'NONE', #239260, .T. ) ;
#85925=TOROIDAL_SURFACE ( 'NONE', #127660, 11.70000000000000107, 0.1000000000000000056 ) ;
#85927=CARTESIAN_POINT ( 'NONE',  ( 18.59999999999999076, 76.00000000001244871, -170.0231074845243597 ) ) ;
#85929=DIRECTION ( 'NONE',  ( -2.952720810173289605E-16, -1.000000000000000000, -7.086529944415894657E-15 ) ) ;
#85940=ORIENTED_EDGE ( 'NONE', *, *, #99537, .T. ) ;
#85944=CARTESIAN_POINT ( 'NONE',  ( 21.05000000000000071, 67.22371710472015138, -195.0351067629400461 ) ) ;
#85947=ORIENTED_EDGE ( 'NONE', *, *, #77895, .T. ) ;
#85992=DIRECTION ( 'NONE',  ( -1.000000000000000000, 0.000000000000000000, 0.000000000000000000 ) ) ;
#85996=DIRECTION ( 'NONE',  ( 9.044546369203337730E-15, 0.7397360091702647189, 0.6728971962616949742 ) ) ;
#86001=ORIENTED_EDGE ( 'NONE', *, *, #97566, .F. ) ;
#86024=ORIENTED_EDGE ( 'NONE', *, *, #164400, .T. ) ;
#86025=DIRECTION ( 'NONE',  ( 0.000000000000000000, -1.000000000000000000, 0.000000000000000000 ) ) ;
#86027=ORIENTED_EDGE ( 'NONE', *, *, #78510, .T. ) ;
#86029=ADVANCED_FACE ( 'NONE', ( #131005 ), #175995, .T. ) ;
#86055=VECTOR ( 'NONE', #250760, 1000.000000000000000 ) ;
#86086=CARTESIAN_POINT ( 'NONE',  ( -20.94999999999999929, 77.16270174995064224, -195.5231074845243313 ) ) ;
#86113=DIRECTION ( 'NONE',  ( 1.000000000000000000, 0.000000000000000000, 0.000000000000000000 ) ) ;
#86131=CARTESIAN_POINT ( 'NONE',  ( 20.94999999999999929, 85.00000000001251976, -179.9170766071767389 ) ) ;
#86141=ORIENTED_EDGE ( 'NONE', *, *, #214239, .T. ) ;
#86147=DIRECTION ( 'NONE',  ( 0.000000000000000000, 0.000000000000000000, 1.000000000000000000 ) ) ;
#86163=DIRECTION ( 'NONE',  ( 2.952720810173289605E-16, 1.000000000000000000, 7.086529944415894657E-15 ) ) ;
#86186=DIRECTION ( 'NONE',  ( 0.000000000000000000, -7.147358527629766941E-15, 1.000000000000000000 ) ) ;
#86238=EDGE_CURVE ( 'NONE', #221522, #222996, #80423, .T. ) ;
#86256=CARTESIAN_POINT ( 'NONE',  ( -22.49756042579671700, 75.92195366299559112, -215.1729724456266979 ) ) ;
#86279=ORIENTED_EDGE ( 'NONE', *, *, #44048, .F. ) ;
#86284=CARTESIAN_POINT ( 'NONE',  ( -22.47071067811865319, 76.00000000001267608, -203.5231074845243597 ) ) ;
#86314=ORIENTED_EDGE ( 'NONE', *, *, #211559, .T. ) ;
#86323=AXIS2_PLACEMENT_3D ( 'NONE', #131349, #90937, #210890 ) ;
#86332=VECTOR ( 'NONE', #239489, 1000.000000000000000 ) ;
#86399=CARTESIAN_POINT ( 'NONE',  ( -23.15000000000000213, 76.00000000001242029, -166.1231074845243825 ) ) ;
#86435=DIRECTION ( 'NONE',  ( 0.000000000000000000, 0.000000000000000000, -1.000000000000000000 ) ) ;
#86479=DIRECTION ( 'NONE',  ( 2.952720810173289112E-16, 1.000000000000000000, 6.938893903907222067E-15 ) ) ;
#86515=CARTESIAN_POINT ( 'NONE',  ( -20.94999999999999929, 87.65000000001266756, -200.6231074845242688 ) ) ;
#86549=CARTESIAN_POINT ( 'NONE',  ( -21.05000000000000071, 74.83729825007462466, -195.4231074845243654 ) ) ;
#86577=VECTOR ( 'NONE', #182374, 1000.000000000000000 ) ;
#86622=CARTESIAN_POINT ( 'NONE',  ( 20.97250901189795513, 65.37543196631075659, -195.8585617675574611 ) ) ;
#86630=CARTESIAN_POINT ( 'NONE',  ( 21.04999999999999361, 75.90156250001241744, -209.8223383946166507 ) ) ;
#86634=DIRECTION ( 'NONE',  ( 0.000000000000000000, 0.000000000000000000, 1.000000000000000000 ) ) ;
#86650=CARTESIAN_POINT ( 'NONE',  ( 21.12400222705963415, 67.22148809293538818, -191.2731074845244166 ) ) ;
#86651=EDGE_LOOP ( 'NONE', ( #38732, #181746, #129200, #206444, #120782, #175373, #59722, #103508, #13259, #38666, #215743, #46498 ) ) ;
#86712=CARTESIAN_POINT ( 'NONE',  ( -20.88420186297724257, 65.66974365629718591, -164.4360145562605453 ) ) ;
#86738=CIRCLE ( 'NONE', #128294, 0.2000000000000057288 ) ;
#86752=ORIENTED_EDGE ( 'NONE', *, *, #64122, .F. ) ;
#86761=CARTESIAN_POINT ( 'NONE',  ( 18.44208962362762705, 85.55234049692037956, -163.1809344290608976 ) ) ;
#86788=CARTESIAN_POINT ( 'NONE',  ( -20.54999999999999716, 85.40000000001252545, -179.9170766071767389 ) ) ;
#86848=CARTESIAN_POINT ( 'NONE',  ( 22.60000000000000142, 76.00000000001267608, -203.5231074845243597 ) ) ;
#86849=CYLINDRICAL_SURFACE ( 'NONE', #144907, 0.1000000000000028644 ) ;
#86863=ORIENTED_EDGE ( 'NONE', *, *, #245568, .F. ) ;
#86878=EDGE_CURVE ( 'NONE', #65312, #69180, #188800, .T. ) ;
#86895=ORIENTED_EDGE ( 'NONE', *, *, #201011, .F. ) ;
#86911=DIRECTION ( 'NONE',  ( -1.000000000000000000, -0.000000000000000000, -0.000000000000000000 ) ) ;
#86913=DIRECTION ( 'NONE',  ( -1.000000000000000000, 0.000000000000000000, 0.000000000000000000 ) ) ;
#86930=CARTESIAN_POINT ( 'NONE',  ( -20.64999999999999858, 71.65000000001259650, -191.1731074845243654 ) ) ;
#86944=CARTESIAN_POINT ( 'NONE',  ( -21.08376601933334271, 75.93622398908284765, -209.8650547558000881 ) ) ;
#86953=CARTESIAN_POINT ( 'NONE',  ( -18.59999999999999787, 77.16412189325360771, -162.1082593989527254 ) ) ;
#86962=ORIENTED_EDGE ( 'NONE', *, *, #236960, .F. ) ;
#86975=ORIENTED_EDGE ( 'NONE', *, *, #54698, .T. ) ;
#87006=VERTEX_POINT ( 'NONE', #209296 ) ;
#87017=EDGE_CURVE ( 'NONE', #113112, #97927, #176527, .T. ) ;
#87022=DIRECTION ( 'NONE',  ( 0.000000000000000000, -0.8660254037844419273, 0.4999999999999942824 ) ) ;
#87033=DIRECTION ( 'NONE',  ( -1.000000000000000000, 2.952720810173289112E-16, 2.061873921506763405E-30 ) ) ;
#87083=ADVANCED_FACE ( 'NONE', ( #245864 ), #47635, .T. ) ;
#87116=ORIENTED_EDGE ( 'NONE', *, *, #1258, .F. ) ;
#87123=CARTESIAN_POINT ( 'NONE',  ( -21.09096482362091507, 75.96055172123860189, -209.8866518499290521 ) ) ;
#87125=VECTOR ( 'NONE', #32070, 1000.000000000000000 ) ;
#87133=ORIENTED_EDGE ( 'NONE', *, *, #34969, .T. ) ;
#87141=DIRECTION ( 'NONE',  ( 1.000000000000000000, 0.000000000000000000, 0.000000000000000000 ) ) ;
#87144=CARTESIAN_POINT ( 'NONE',  ( -23.15000000000000213, 71.85000000001276987, -215.2731074845243882 ) ) ;
#87146=DIRECTION ( 'NONE',  ( 0.000000000000000000, 1.000000000000000000, 6.352154140967427193E-15 ) ) ;
#87244=VERTEX_POINT ( 'NONE', #200020 ) ;
#87255=DIRECTION ( 'NONE',  ( 0.000000000000000000, 0.000000000000000000, 1.000000000000000000 ) ) ;
#87260=ORIENTED_EDGE ( 'NONE', *, *, #157529, .T. ) ;
#87271=ORIENTED_EDGE ( 'NONE', *, *, #245568, .T. ) ;
#87284=ORIENTED_EDGE ( 'NONE', *, *, #142939, .F. ) ;
#87291=MECHANICAL_DESIGN_GEOMETRIC_PRESENTATION_REPRESENTATION('',(#220586),#149873);
#87297=AXIS2_PLACEMENT_3D ( 'NONE', #209292, #50205, #111483 ) ;
#87304=ADVANCED_FACE ( 'NONE', ( #38375 ), #218266, .F. ) ;
#87319=AXIS2_PLACEMENT_3D ( 'NONE', #188572, #129873, #206857 ) ;
#87324=ORIENTED_EDGE ( 'NONE', *, *, #168618, .T. ) ;
#87339=DIRECTION ( 'NONE',  ( 1.000000000000000000, 0.000000000000000000, 0.000000000000000000 ) ) ;
#87349=LINE ( 'NONE', #88625, #213230 ) ;
#87372=CARTESIAN_POINT ( 'NONE',  ( 18.49999999999999289, 64.25000000001277556, -215.2731074845244450 ) ) ;
#87374=DIRECTION ( 'NONE',  ( 0.000000000000000000, 0.000000000000000000, 1.000000000000000000 ) ) ;
#87381=CIRCLE ( 'NONE', #233171, 0.1000000000000043771 ) ;
#87397=VERTEX_POINT ( 'NONE', #188162 ) ;
#87402=PLANE ( 'NONE',  #141370 ) ;
#87411=EDGE_LOOP ( 'NONE', ( #150773, #232740, #89751, #97193 ) ) ;
#87418=EDGE_CURVE ( 'NONE', #227800, #115127, #147655, .T. ) ;
#87429=EDGE_CURVE ( 'NONE', #17720, #197918, #151779, .T. ) ;
#87434=CYLINDRICAL_SURFACE ( 'NONE', #192286, 0.5000000000000004441 ) ;
#87461=FACE_OUTER_BOUND ( 'NONE', #68004, .T. ) ;
#87471=AXIS2_PLACEMENT_3D ( 'NONE', #245557, #188146, #190743 ) ;
#87496=SPHERICAL_SURFACE ( 'NONE', #123325, 0.1000000000000000056 ) ;
#87498=CARTESIAN_POINT ( 'NONE',  ( 18.50000000000000000, 86.35479209693788505, -176.2665665014505407 ) ) ;
#87506=CIRCLE ( 'NONE', #70807, 0.09999999999998986089 ) ;
#87510=FACE_OUTER_BOUND ( 'NONE', #85394, .T. ) ;
#87517=CARTESIAN_POINT ( 'NONE',  ( -20.85000000000000142, 76.00000000001244871, -170.0231074845243597 ) ) ;
#87534=EDGE_CURVE ( 'NONE', #153680, #43270, #173787, .T. ) ;
#87546=VERTEX_POINT ( 'NONE', #73378 ) ;
#87548=CARTESIAN_POINT ( 'NONE',  ( -22.47886152344871036, 75.96249906115107819, -215.1730961275723075 ) ) ;
#87556=DIRECTION ( 'NONE',  ( -1.000000000000000000, -0.000000000000000000, -0.000000000000000000 ) ) ;
#87558=EDGE_LOOP ( 'NONE', ( #79946, #7373 ) ) ;
#87568=AXIS2_PLACEMENT_3D ( 'NONE', #232767, #33308, #155808 ) ;
#87580=VECTOR ( 'NONE', #234282, 1000.000000000000000 ) ;
#87620=ORIENTED_EDGE ( 'NONE', *, *, #131989, .T. ) ;
#87632=ORIENTED_EDGE ( 'NONE', *, *, #43437, .T. ) ;
#87633=FACE_OUTER_BOUND ( 'NONE', #173847, .T. ) ;
#87639=DIRECTION ( 'NONE',  ( 1.000000000000000000, 0.000000000000000000, 0.000000000000000000 ) ) ;
#87655=FACE_OUTER_BOUND ( 'NONE', #166794, .T. ) ;
#87687=AXIS2_PLACEMENT_3D ( 'NONE', #222322, #5857, #202790 ) ;
#87691=ORIENTED_EDGE ( 'NONE', *, *, #59752, .F. ) ;
#87693=FACE_OUTER_BOUND ( 'NONE', #205026, .T. ) ;
#87698=CARTESIAN_POINT ( 'NONE',  ( -18.42554971533676778, 85.49715966945035461, -196.4832805709756656 ) ) ;
#87717=CARTESIAN_POINT ( 'NONE',  ( 21.05000000000000071, 71.18691588786300883, -181.9646252410481964 ) ) ;
#87728=CARTESIAN_POINT ( 'NONE',  ( 21.00000000000000000, 66.25000000001253397, -182.3731074845244393 ) ) ;
#87736=FACE_OUTER_BOUND ( 'NONE', #197723, .T. ) ;
#87796=CARTESIAN_POINT ( 'NONE',  ( -21.05000000000000071, 77.83534155023700407, -191.9679561919613491 ) ) ;
#87834=EDGE_CURVE ( 'NONE', #85698, #51100, #67904, .T. ) ;
#87835=CARTESIAN_POINT ( 'NONE',  ( 20.94999999999999929, 84.66355140188177586, -193.9990063664569959 ) ) ;
#87844=ORIENTED_EDGE ( 'NONE', *, *, #11649, .F. ) ;
#87880=CARTESIAN_POINT ( 'NONE',  ( 21.14999999999999858, 65.28660755661270798, -191.2731074845244166 ) ) ;
#87889=CARTESIAN_POINT ( 'NONE',  ( -18.59999999999999787, 68.97833521811233481, -166.2895420826271220 ) ) ;
#87905=EDGE_CURVE ( 'NONE', #193233, #14270, #144187, .T. ) ;
#87914=ADVANCED_FACE ( 'NONE', ( #11816 ), #193000, .F. ) ;
#87917=CARTESIAN_POINT ( 'NONE',  ( -23.15000000000000213, 64.35000000001258513, -191.2731074845244450 ) ) ;
#87925=CARTESIAN_POINT ( 'NONE',  ( -20.64999999999999858, 74.07476635515273244, -182.7533510176504876 ) ) ;
#87939=FACE_OUTER_BOUND ( 'NONE', #128862, .T. ) ;
#87954=DIRECTION ( 'NONE',  ( 0.000000000000000000, -7.026728003956695223E-15, 1.000000000000000000 ) ) ;
#87974=DIRECTION ( 'NONE',  ( 1.000000000000000000, 0.000000000000000000, 0.000000000000000000 ) ) ;
#87986=EDGE_CURVE ( 'NONE', #116802, #152824, #61686, .T. ) ;
#87999=CARTESIAN_POINT ( 'NONE',  ( -21.05000000000000071, 75.90220970870393558, -209.7809220950004772 ) ) ;
#88003=AXIS2_PLACEMENT_3D ( 'NONE', #559, #224435, #217038 ) ;
#88021=VERTEX_POINT ( 'NONE', #95173 ) ;
#88033=CARTESIAN_POINT ( 'NONE',  ( 18.49999999999999289, 69.55000000001261640, -193.5060803140843859 ) ) ;
#88064=DIRECTION ( 'NONE',  ( 3.265361837132813093E-16, 1.000000000000000000, 6.982962677686266711E-15 ) ) ;
#88067=PLANE ( 'NONE',  #41530 ) ;
#88094=AXIS2_PLACEMENT_3D ( 'NONE', #86848, #6033, #47726 ) ;
#88106=CARTESIAN_POINT ( 'NONE',  ( -20.54999999999999716, 73.50000000001259082, -190.2984855617622770 ) ) ;
#88119=CARTESIAN_POINT ( 'NONE',  ( -21.44999999999999929, 68.85000000001259934, -191.2731074845244166 ) ) ;
#88148=CARTESIAN_POINT ( 'NONE',  ( 18.59999999999999076, 65.50857864377520912, -178.7731074845244450 ) ) ;
#88189=CARTESIAN_POINT ( 'NONE',  ( -22.00356870141228427, 68.74575763752110902, -203.5231074845244450 ) ) ;
#88217=ORIENTED_EDGE ( 'NONE', *, *, #215826, .T. ) ;
#88235=DIRECTION ( 'NONE',  ( 0.000000000000000000, 6.982962677686266711E-15, -1.000000000000000000 ) ) ;
#88286=CARTESIAN_POINT ( 'NONE',  ( 19.75857864376268935, 64.25000000001250555, -178.6731074845244507 ) ) ;
#88306=FACE_OUTER_BOUND ( 'NONE', #123944, .T. ) ;
#88313=CIRCLE ( 'NONE', #104875, 0.09999999999998898659 ) ;
#88318=AXIS2_PLACEMENT_3D ( 'NONE', #48562, #131952, #8170 ) ;
#88354=ORIENTED_EDGE ( 'NONE', *, *, #87017, .F. ) ;
#88359=ORIENTED_EDGE ( 'NONE', *, *, #99329, .T. ) ;
#88375=ORIENTED_EDGE ( 'NONE', *, *, #124761, .T. ) ;
#88377=DIRECTION ( 'NONE',  ( 7.304098846218134667E-16, 1.000000000000000000, 6.982962677686267499E-15 ) ) ;
#88390=ORIENTED_EDGE ( 'NONE', *, *, #213553, .F. ) ;
#88396=TOROIDAL_SURFACE ( 'NONE', #192477, 6.258578643762700899, 0.1000000000000000056 ) ;
#88405=ORIENTED_EDGE ( 'NONE', *, *, #55797, .T. ) ;
#88436=ORIENTED_EDGE ( 'NONE', *, *, #58117, .T. ) ;
#88440=DIRECTION ( 'NONE',  ( 0.000000000000000000, 0.1298341882519953583, 0.9915357197604862671 ) ) ;
#88442=ADVANCED_FACE ( 'NONE', ( #248170 ), #244302, .T. ) ;
#88455=AXIS2_PLACEMENT_3D ( 'NONE', #102979, #60002, #220392 ) ;
#88461=CARTESIAN_POINT ( 'NONE',  ( 23.15000000000000213, 87.65000000001246860, -173.1231074845242688 ) ) ;
#88462=CARTESIAN_POINT ( 'NONE',  ( -23.15000000000000213, 70.10000000001251408, -180.2422072491807796 ) ) ;
#88502=DIRECTION ( 'NONE',  ( 4.336808689942128965E-15, -0.8660254037844367092, 0.5000000000000037748 ) ) ;
#88529=CARTESIAN_POINT ( 'NONE',  ( -18.59999999999999787, 77.83585931145600512, -158.5186683157258187 ) ) ;
#88564=AXIS2_PLACEMENT_3D ( 'NONE', #257763, #141714, #79164 ) ;
#88569=CIRCLE ( 'NONE', #167722, 4.000000000000003553 ) ;
#88571=DIRECTION ( 'NONE',  ( 1.000000000000000000, 0.000000000000000000, 0.000000000000000000 ) ) ;
#88598=DIRECTION ( 'NONE',  ( 0.000000000000000000, 0.000000000000000000, 1.000000000000000000 ) ) ;
#88600=ORIENTED_EDGE ( 'NONE', *, *, #128672, .F. ) ;
#88613=ORIENTED_EDGE ( 'NONE', *, *, #70333, .F. ) ;
#88616=EDGE_CURVE ( 'NONE', #247736, #242182, #219393, .T. ) ;
#88625=CARTESIAN_POINT ( 'NONE',  ( -23.15000000000000213, 87.41227409416215721, -173.0231074845243029 ) ) ;
#88629=DIRECTION ( 'NONE',  ( -1.000000000000000000, 0.000000000000000000, 0.000000000000000000 ) ) ;
#88711=CARTESIAN_POINT ( 'NONE',  ( 23.15000000000000213, 87.48912529308852015, -173.1231074845242688 ) ) ;
#88761=ADVANCED_FACE ( 'NONE', ( #139750 ), #219304, .T. ) ;
#88780=CARTESIAN_POINT ( 'NONE',  ( 21.05000000000000071, 76.00000000001242029, -166.0231074845243597 ) ) ;
#88781=DIRECTION ( 'NONE',  ( 0.000000000000000000, 6.982962677686266711E-15, -1.000000000000000000 ) ) ;
#88801=EDGE_CURVE ( 'NONE', #186491, #203708, #22289, .T. ) ;
#88808=FACE_OUTER_BOUND ( 'NONE', #51110, .T. ) ;
#88817=DIRECTION ( 'NONE',  ( 0.000000000000000000, 0.000000000000000000, 1.000000000000000000 ) ) ;
#88830=FACE_OUTER_BOUND ( 'NONE', #164250, .T. ) ;
#88834=FACE_OUTER_BOUND ( 'NONE', #185447, .T. ) ;
#88836=EDGE_CURVE ( 'NONE', #82861, #33906, #255360, .T. ) ;
#88862=AXIS2_PLACEMENT_3D ( 'NONE', #127980, #10602, #172281 ) ;
#88864=ORIENTED_EDGE ( 'NONE', *, *, #228388, .F. ) ;
#88866=EDGE_CURVE ( 'NONE', #53690, #33906, #222152, .T. ) ;
#88872=AXIS2_PLACEMENT_3D ( 'NONE', #95686, #257283, #136080 ) ;
#88897=ORIENTED_EDGE ( 'NONE', *, *, #50551, .T. ) ;
#88912=CIRCLE ( 'NONE', #109766, 0.5000000000000004441 ) ;
#88913=EDGE_LOOP ( 'NONE', ( #205010, #217469, #9125, #79841 ) ) ;
#88984=DIRECTION ( 'NONE',  ( 0.000000000000000000, 0.000000000000000000, 1.000000000000000000 ) ) ;
#88991=ORIENTED_EDGE ( 'NONE', *, *, #204191, .T. ) ;
#89003=DIRECTION ( 'NONE',  ( 0.1538461538461484146, -0.9880948137434723000, 0.000000000000000000 ) ) ;
#89027=AXIS2_PLACEMENT_3D ( 'NONE', #14438, #32731, #56076 ) ;
#89045=( BOUNDED_CURVE ( )  B_SPLINE_CURVE ( 3, ( #165158, #166470, #67335, #88148 ),
 .UNSPECIFIED., .F., .F. ) 
 B_SPLINE_CURVE_WITH_KNOTS ( ( 4, 4 ),
 ( 3.141592653589778461, 4.712388980384686121 ),
 .UNSPECIFIED. ) 
 CURVE ( )  GEOMETRIC_REPRESENTATION_ITEM ( )  RATIONAL_B_SPLINE_CURVE ( ( 1.000000000000000000, 0.8047378541243622729, 0.8047378541243622729, 1.000000000000000000 ) ) 
 REPRESENTATION_ITEM ( '' )  );
#89047=ADVANCED_FACE ( 'NONE', ( #144599 ), #83325, .T. ) ;
#89052=AXIS2_PLACEMENT_3D ( 'NONE', #158786, #19243, #101288 ) ;
#89065=CARTESIAN_POINT ( 'NONE',  ( 23.24999999999999645, 76.00000000001244871, -170.0231074845243597 ) ) ;
#89093=DIRECTION ( 'NONE',  ( -1.000000000000000000, 0.000000000000000000, -0.000000000000000000 ) ) ;
#89097=CARTESIAN_POINT ( 'NONE',  ( 20.94999999999999929, 69.45000000001259366, -191.2731074845244166 ) ) ;
#89109=DIRECTION ( 'NONE',  ( 1.000000000000000000, 0.000000000000000000, 0.000000000000000000 ) ) ;
#89111=ADVANCED_FACE ( 'NONE', ( #203314 ), #238751, .F. ) ;
#89117=LINE ( 'NONE', #109960, #216931 ) ;
#89121=FACE_OUTER_BOUND ( 'NONE', #135473, .T. ) ;
#89164=CARTESIAN_POINT ( 'NONE',  ( 18.49999999999999645, 77.29973367124354411, -213.4949779616549392 ) ) ;
#89169=CIRCLE ( 'NONE', #168344, 0.09999999999998898659 ) ;
#89170=TOROIDAL_SURFACE ( 'NONE', #218325, 11.65000000000000036, 0.1000000000000000056 ) ;
#89171=DIRECTION ( 'NONE',  ( 0.000000000000000000, 0.000000000000000000, 1.000000000000000000 ) ) ;
#89212=CARTESIAN_POINT ( 'NONE',  ( 20.86036036209898015, 65.37895722344167382, -195.8567590660222208 ) ) ;
#89235=AXIS2_PLACEMENT_3D ( 'NONE', #154060, #135711, #171055 ) ;
#89265=CARTESIAN_POINT ( 'NONE',  ( 23.14999999999999503, 69.35000000001259934, -191.3731074845244109 ) ) ;
#89282=VERTEX_POINT ( 'NONE', #28578 ) ;
#89287=EDGE_CURVE ( 'NONE', #89282, #152832, #118326, .T. ) ;
#89295=FACE_OUTER_BOUND ( 'NONE', #146260, .T. ) ;
#89305=ORIENTED_EDGE ( 'NONE', *, *, #156993, .F. ) ;
#89317=ORIENTED_EDGE ( 'NONE', *, *, #221324, .F. ) ;
#89338=EDGE_LOOP ( 'NONE', ( #255865, #104837, #18697, #235150 ) ) ;
#89365=CARTESIAN_POINT ( 'NONE',  ( 20.94999999999999929, 76.00000000001243450, -168.1231074845243540 ) ) ;
#89398=CIRCLE ( 'NONE', #105951, 11.90000000000000746 ) ;
#89423=CARTESIAN_POINT ( 'NONE',  ( -20.64999999999999858, 68.75000000001253397, -182.2731074845244166 ) ) ;
#89501=ORIENTED_EDGE ( 'NONE', *, *, #251423, .F. ) ;
#89504=DIRECTION ( 'NONE',  ( 0.000000000000000000, -0.9654727137038715545, 0.2605042016806676242 ) ) ;
#89519=AXIS2_PLACEMENT_3D ( 'NONE', #123273, #25468, #39911 ) ;
#89521=EDGE_LOOP ( 'NONE', ( #112521, #11021, #63319, #227819 ) ) ;
#89539=LINE ( 'NONE', #209496, #202591 ) ;
#89560=SPHERICAL_SURFACE ( 'NONE', #123304, 0.1000000000000000056 ) ;
#89610=DIRECTION ( 'NONE',  ( 0.000000000000000000, 1.000000000000000000, 6.982962677686267499E-15 ) ) ;
#89645=FACE_BOUND ( 'NONE', #141262, .T. ) ;
#89666=ORIENTED_EDGE ( 'NONE', *, *, #82411, .F. ) ;
#89681=EDGE_CURVE ( 'NONE', #44979, #209410, #80882, .T. ) ;
#89711=CARTESIAN_POINT ( 'NONE',  ( 22.50000000000000000, 76.00000000001267608, -203.5231074845243597 ) ) ;
#89731=CARTESIAN_POINT ( 'NONE',  ( -20.54999999999999716, 71.65000000001253966, -182.2731074845243882 ) ) ;
#89736=AXIS2_PLACEMENT_3D ( 'NONE', #174588, #59686, #137947 ) ;
#89751=ORIENTED_EDGE ( 'NONE', *, *, #139178, .T. ) ;
#89760=CARTESIAN_POINT ( 'NONE',  ( 18.49999999999999645, 77.36242903720570041, -162.1342262366031548 ) ) ;
#89761=AXIS2_PLACEMENT_3D ( 'NONE', #161071, #61966, #141489 ) ;
#89763=CARTESIAN_POINT ( 'NONE',  ( -21.05000000000000071, 74.16465844978819177, -191.9679561919613775 ) ) ;
#89780=( BOUNDED_CURVE ( )  B_SPLINE_CURVE ( 3, ( #76802, #212486, #113372, #135479 ),
 .UNSPECIFIED., .F., .T. ) 
 B_SPLINE_CURVE_WITH_KNOTS ( ( 4, 4 ),
 ( 0.06456096931748350753, 3.077031684272309775 ),
 .UNSPECIFIED. ) 
 CURVE ( )  GEOMETRIC_REPRESENTATION_ITEM ( )  RATIONAL_B_SPLINE_CURVE ( ( 1.000000000000000000, 0.3763440860215095940, 0.3763440860215095940, 1.000000000000000000 ) ) 
 REPRESENTATION_ITEM ( '' )  );
#89797=DIRECTION ( 'NONE',  ( 1.000000000000000000, 0.000000000000000000, 0.000000000000000000 ) ) ;
#89845=ORIENTED_EDGE ( 'NONE', *, *, #94539, .T. ) ;
#89871=CARTESIAN_POINT ( 'NONE',  ( -23.15000000000000213, 74.00000000001259082, -190.2984855617622770 ) ) ;
#89893=ADVANCED_FACE ( 'NONE', ( #83667 ), #64153, .F. ) ;
#90005=DIRECTION ( 'NONE',  ( 0.000000000000000000, -6.853228547068871147E-15, 1.000000000000000000 ) ) ;
#90031=EDGE_CURVE ( 'NONE', #56183, #257629, #43669, .T. ) ;
#90037=AXIS2_PLACEMENT_3D ( 'NONE', #79724, #78453, #158055 ) ;
#90063=VERTEX_POINT ( 'NONE', #54833 ) ;
#90065=CARTESIAN_POINT ( 'NONE',  ( -20.64999999999999858, 68.85000000001259934, -191.1731074845243938 ) ) ;
#90081=CARTESIAN_POINT ( 'NONE',  ( 21.05000000000000071, 70.50000000001253397, -182.4283735034374843 ) ) ;
#90104=DIRECTION ( 'NONE',  ( 0.000000000000000000, 1.000000000000000000, 6.982962677686266711E-15 ) ) ;
#90123=DIRECTION ( 'NONE',  ( 0.000000000000000000, -1.000000000000000000, -7.272083257015735086E-15 ) ) ;
#90131=CARTESIAN_POINT ( 'NONE',  ( 18.59999999999999076, 69.35000000001254250, -182.3731074845244109 ) ) ;
#90147=ADVANCED_FACE ( 'NONE', ( #34045 ), #113542, .F. ) ;
#90152=ORIENTED_EDGE ( 'NONE', *, *, #6666, .F. ) ;
#90173=ORIENTED_EDGE ( 'NONE', *, *, #256831, .T. ) ;
#90189=AXIS2_PLACEMENT_3D ( 'NONE', #119357, #35975, #197590 ) ;
#90198=ORIENTED_EDGE ( 'NONE', *, *, #52889, .F. ) ;
#90203=CARTESIAN_POINT ( 'NONE',  ( 21.97500000000000497, 66.25000000001260503, -191.1731074845244223 ) ) ;
#90216=CARTESIAN_POINT ( 'NONE',  ( -21.05000000000000071, 69.45934304831143891, -203.4231074845244223 ) ) ;
#90228=ORIENTED_EDGE ( 'NONE', *, *, #235057, .F. ) ;
#90252=VECTOR ( 'NONE', #160546, 1000.000000000000114 ) ;
#90288=VERTEX_POINT ( 'NONE', #219045 ) ;
#90340=CARTESIAN_POINT ( 'NONE',  ( -23.15000000000000213, 64.25000000001260503, -191.3731074845244393 ) ) ;
#90363=ADVANCED_FACE ( 'NONE', ( #12876 ), #234820, .T. ) ;
#90364=VECTOR ( 'NONE', #123777, 1000.000000000000000 ) ;
#90375=DIRECTION ( 'NONE',  ( 0.000000000000000000, -6.982962677686266711E-15, 1.000000000000000000 ) ) ;
#90399=CARTESIAN_POINT ( 'NONE',  ( 21.05000000000000071, 71.00000000001253397, -182.4283735034374843 ) ) ;
#90405=ORIENTED_EDGE ( 'NONE', *, *, #77853, .T. ) ;
#90408=AXIS2_PLACEMENT_3D ( 'NONE', #171862, #33645, #157432 ) ;
#90436=CARTESIAN_POINT ( 'NONE',  ( -23.15000000000000213, 85.50000000001251976, -179.9170766071767389 ) ) ;
#90440=EDGE_LOOP ( 'NONE', ( #37025, #70578, #227584, #137144 ) ) ;
#90444=CARTESIAN_POINT ( 'NONE',  ( -21.05000000000000071, 64.25000000001249134, -177.0379132551784096 ) ) ;
#90447=CIRCLE ( 'NONE', #94535, 12.87499999999999822 ) ;
#90448=VECTOR ( 'NONE', #181692, 1000.000000000000000 ) ;
#90471=CIRCLE ( 'NONE', #169646, 0.09999999999998898659 ) ;
#90487=ADVANCED_FACE ( 'NONE', ( #153705 ), #174548, .T. ) ;
#90504=EDGE_CURVE ( 'NONE', #106612, #221154, #18338, .T. ) ;
#90540=DIRECTION ( 'NONE',  ( 0.000000000000000000, 0.000000000000000000, 1.000000000000000000 ) ) ;
#90543=ORIENTED_EDGE ( 'NONE', *, *, #5548, .T. ) ;
#90544=CARTESIAN_POINT ( 'NONE',  ( -21.05000000000000071, 77.83534155023700407, -191.8679561919613832 ) ) ;
#90546=DIRECTION ( 'NONE',  ( 1.000000000000000000, 0.000000000000000000, 0.000000000000000000 ) ) ;
#90547=CIRCLE ( 'NONE', #248981, 0.09999999999998900047 ) ;
#90555=LINE ( 'NONE', #127124, #75626 ) ;
#90575=DIRECTION ( 'NONE',  ( 0.000000000000000000, 0.000000000000000000, 1.000000000000000000 ) ) ;
#90627=DIRECTION ( 'NONE',  ( 1.000000000000000000, 0.000000000000000000, 0.000000000000000000 ) ) ;
#90639=ADVANCED_FACE ( 'NONE', ( #119663 ), #179641, .F. ) ;
#90642=ORIENTED_EDGE ( 'NONE', *, *, #149212, .F. ) ;
#90706=CARTESIAN_POINT ( 'NONE',  ( 20.94999999999999574, 74.15091558138558980, -191.8670969630772447 ) ) ;
#90729=CARTESIAN_POINT ( 'NONE',  ( -20.64999999999999858, 73.50000000001259082, -190.2984855617622770 ) ) ;
#90730=FACE_OUTER_BOUND ( 'NONE', #184799, .T. ) ;
#90734=DIRECTION ( 'NONE',  ( 1.000000000000000000, 1.110223024625155531E-13, 0.000000000000000000 ) ) ;
#90794=CIRCLE ( 'NONE', #99167, 0.09999999999998898659 ) ;
#90797=ADVANCED_FACE ( 'NONE', ( #126047 ), #230292, .T. ) ;
#90800=ORIENTED_EDGE ( 'NONE', *, *, #154187, .F. ) ;
#90807=AXIS2_PLACEMENT_3D ( 'NONE', #51328, #16114, #14834 ) ;
#90824=ORIENTED_EDGE ( 'NONE', *, *, #7065, .F. ) ;
#90851=DIRECTION ( 'NONE',  ( 0.000000000000000000, 0.000000000000000000, -1.000000000000000000 ) ) ;
#90863=LINE ( 'NONE', #189977, #208318 ) ;
#90870=CARTESIAN_POINT ( 'NONE',  ( 21.07094088545303734, 69.67983277809619835, -203.6220011870766200 ) ) ;
#90881=CARTESIAN_POINT ( 'NONE',  ( 20.04142135623730070, 64.35000000001254250, -182.2731074845244450 ) ) ;
#90885=CARTESIAN_POINT ( 'NONE',  ( -20.64999999999999858, 85.50000000001251976, -179.9170766071767389 ) ) ;
#90930=ORIENTED_EDGE ( 'NONE', *, *, #86878, .T. ) ;
#90935=CIRCLE ( 'NONE', #61723, 0.9750000000000036415 ) ;
#90937=DIRECTION ( 'NONE',  ( 0.000000000000000000, -1.000000000000000000, -6.982962677686266711E-15 ) ) ;
#90943=DIRECTION ( 'NONE',  ( 0.000000000000000000, -0.9908441862701420355, -0.1350103645453197554 ) ) ;
#90957=AXIS2_PLACEMENT_3D ( 'NONE', #82653, #1841, #257412 ) ;
#90969=DIRECTION ( 'NONE',  ( 0.000000000000000000, 0.000000000000000000, 1.000000000000000000 ) ) ;
#90981=LINE ( 'NONE', #113121, #162693 ) ;
#90999=FACE_OUTER_BOUND ( 'NONE', #25339, .T. ) ;
#91003=DIRECTION ( 'NONE',  ( 0.000000000000000000, 0.3738317757009942399, -0.9274965247785252886 ) ) ;
#91005=DIRECTION ( 'NONE',  ( 0.000000000000000000, 0.9915357197604982575, -0.1298341882519033486 ) ) ;
#91017=VERTEX_POINT ( 'NONE', #81463 ) ;
#91025=AXIS2_PLACEMENT_3D ( 'NONE', #9263, #10563, #185337 ) ;
#91029=DIRECTION ( 'NONE',  ( -1.000000000000000000, 0.000000000000000000, -0.000000000000000000 ) ) ;
#91053=VECTOR ( 'NONE', #187905, 1000.000000000000000 ) ;
#91068=DIRECTION ( 'NONE',  ( 0.000000000000000000, -0.9908441862701420355, -0.1350103645453197554 ) ) ;
#91079=CARTESIAN_POINT ( 'NONE',  ( 22.50000000000000000, 76.00000000001267608, -203.5231074845243597 ) ) ;
#91106=DIRECTION ( 'NONE',  ( 0.000000000000000000, 0.000000000000000000, -1.000000000000000000 ) ) ;
#91109=FACE_OUTER_BOUND ( 'NONE', #136764, .T. ) ;
#91116=ADVANCED_FACE ( 'NONE', ( #204011 ), #151820, .T. ) ;
#91135=CIRCLE ( 'NONE', #236875, 12.87499999999999822 ) ;
#91175=CIRCLE ( 'NONE', #236916, 0.09999999999998898659 ) ;
#91199=ORIENTED_EDGE ( 'NONE', *, *, #110570, .F. ) ;
#91228=CARTESIAN_POINT ( 'NONE',  ( 21.05000000000000071, 87.65000000001246860, -172.9231074845242802 ) ) ;
#91250=CARTESIAN_POINT ( 'NONE',  ( 20.94999999999999929, 85.40000000001252545, -179.9170766071767389 ) ) ;
#91251=ORIENTED_EDGE ( 'NONE', *, *, #8709, .F. ) ;
#91254=DIRECTION ( 'NONE',  ( -0.000000000000000000, -6.982962677686266711E-15, 1.000000000000000000 ) ) ;
#91257=ORIENTED_EDGE ( 'NONE', *, *, #4195, .T. ) ;
#91286=CARTESIAN_POINT ( 'NONE',  ( 20.85000000000000142, 77.83585931145600512, -158.5186683157258187 ) ) ;
#91305=CARTESIAN_POINT ( 'NONE',  ( -21.05000000000000071, 77.26178616857765746, -195.4366085209788935 ) ) ;
#91357=DIRECTION ( 'NONE',  ( 0.000000000000000000, 1.000000000000000000, 0.000000000000000000 ) ) ;
#91369=DIRECTION ( 'NONE',  ( 0.000000000000000000, 0.000000000000000000, 1.000000000000000000 ) ) ;
#91374=CIRCLE ( 'NONE', #174803, 0.4000000000000114575 ) ;
#91376=CARTESIAN_POINT ( 'NONE',  ( 20.94999999999999929, 71.18691588786300883, -181.9646252410481964 ) ) ;
#91393=LINE ( 'NONE', #14443, #249359 ) ;
#91404=EDGE_CURVE ( 'NONE', #99703, #172803, #197291, .T. ) ;
#91407=VERTEX_POINT ( 'NONE', #59031 ) ;
#91470=VERTEX_POINT ( 'NONE', #4218 ) ;
#91477=CARTESIAN_POINT ( 'NONE',  ( -21.05000000000000071, 87.41227409416235616, -200.5231074845242745 ) ) ;
#91519=CARTESIAN_POINT ( 'NONE',  ( 23.15000000000000213, 85.00000000001251976, -179.9170766071767389 ) ) ;
#91522=VECTOR ( 'NONE', #233553, 1000.000000000000000 ) ;
#91525=EDGE_LOOP ( 'NONE', ( #176807, #154837, #159488, #174042 ) ) ;
#91527=ORIENTED_EDGE ( 'NONE', *, *, #94340, .F. ) ;
#91597=( NAMED_UNIT ( * ) SI_UNIT ( $, .STERADIAN. ) SOLID_ANGLE_UNIT ( ) );
#91605=DIRECTION ( 'NONE',  ( -1.000000000000000000, -0.000000000000000000, -0.000000000000000000 ) ) ;
#91608=DIRECTION ( 'NONE',  ( -0.7071067811865474617, 0.7071067811865474617, 4.937700262164531476E-15 ) ) ;
#91615=DIRECTION ( 'NONE',  ( 0.000000000000000000, 0.000000000000000000, 1.000000000000000000 ) ) ;
#91650=CARTESIAN_POINT ( 'NONE',  ( 23.14999999999999503, 61.90000000001248992, -175.6234050956638271 ) ) ;
#91689=FACE_OUTER_BOUND ( 'NONE', #85201, .T. ) ;
#91725=EDGE_LOOP ( 'NONE', ( #143440, #255681, #156977, #248105, #13138 ) ) ;
#91762=CARTESIAN_POINT ( 'NONE',  ( -23.25000000000000000, 76.00000000001267608, -203.5231074845243597 ) ) ;
#91774=VERTEX_POINT ( 'NONE', #20614 ) ;
#91850=ORIENTED_EDGE ( 'NONE', *, *, #109079, .T. ) ;
#91868=CYLINDRICAL_SURFACE ( 'NONE', #216007, 0.09999999999999939493 ) ;
#91891=EDGE_LOOP ( 'NONE', ( #123116, #110558, #1377, #54231 ) ) ;
#91917=CARTESIAN_POINT ( 'NONE',  ( -20.00857864376270001, 66.75000000001253397, -182.2731074845244166 ) ) ;
#91927=ADVANCED_FACE ( 'NONE', ( #166551 ), #8734, .F. ) ;
#91932=VECTOR ( 'NONE', #174462, 1000.000000000000000 ) ;
#91990=DIRECTION ( 'NONE',  ( 0.000000000000000000, 0.1350103645451807832, 0.9908441862701610203 ) ) ;
#91997=EDGE_CURVE ( 'NONE', #248551, #145935, #148068, .T. ) ;
#92012=DIRECTION ( 'NONE',  ( 1.836970198721029934E-16, 1.000000000000000000, 6.982962677686266711E-15 ) ) ;
#92037=AXIS2_PLACEMENT_3D ( 'NONE', #224427, #233128, #65357 ) ;
#92068=CIRCLE ( 'NONE', #163028, 0.09999999999999939493 ) ;
#92072=CYLINDRICAL_SURFACE ( 'NONE', #111281, 0.09999999999998898659 ) ;
#92096=EDGE_CURVE ( 'NONE', #53042, #109261, #202767, .T. ) ;
#92169=ORIENTED_EDGE ( 'NONE', *, *, #208165, .F. ) ;
#92171=DIRECTION ( 'NONE',  ( 1.000000000000000000, -3.265361837132813093E-16, -2.280189983783949500E-30 ) ) ;
#92179=TOROIDAL_SURFACE ( 'NONE', #183960, 11.89999999999999858, 0.1000000000000000056 ) ;
#92210=EDGE_LOOP ( 'NONE', ( #252974, #180352, #83193, #241918 ) ) ;
#92223=ORIENTED_EDGE ( 'NONE', *, *, #147949, .T. ) ;
#92235=ORIENTED_EDGE ( 'NONE', *, *, #185181, .F. ) ;
#92239=ORIENTED_EDGE ( 'NONE', *, *, #241559, .F. ) ;
#92258=AXIS2_PLACEMENT_3D ( 'NONE', #135558, #230848, #14373 ) ;
#92260=CARTESIAN_POINT ( 'NONE',  ( -21.05000000000000071, 76.08579911628717696, -209.9370863660123518 ) ) ;
#92277=DIRECTION ( 'NONE',  ( 0.000000000000000000, -7.086529944415886769E-15, 1.000000000000000000 ) ) ;
#92280=DIRECTION ( 'NONE',  ( 0.000000000000000000, -0.9274965247785323941, -0.3738317757009769760 ) ) ;
#92314=FACE_OUTER_BOUND ( 'NONE', #15566, .T. ) ;
#92340=CARTESIAN_POINT ( 'NONE',  ( -18.59999999999999787, 72.08710075277916474, -192.0412845115134246 ) ) ;
#92365=TOROIDAL_SURFACE ( 'NONE', #213162, 11.90000000000000391, 0.1000000000000000056 ) ;
#92375=CARTESIAN_POINT ( 'NONE',  ( -20.95000000000000284, 64.35000000001251408, -177.0379132551784096 ) ) ;
#92383=DIRECTION ( 'NONE',  ( 0.000000000000000000, -6.467318590049456648E-15, 1.000000000000000000 ) ) ;
#92412=DIRECTION ( 'NONE',  ( -1.000000000000000000, -0.000000000000000000, -0.000000000000000000 ) ) ;
#92442=LINE ( 'NONE', #29945, #182664 ) ;
#92450=AXIS2_PLACEMENT_3D ( 'NONE', #29812, #109290, #188845 ) ;
#92467=ORIENTED_EDGE ( 'NONE', *, *, #197398, .T. ) ;
#92471=CARTESIAN_POINT ( 'NONE',  ( -23.15000000000000213, 70.05000000001251692, -180.3288097895592159 ) ) ;
#92504=ORIENTED_EDGE ( 'NONE', *, *, #176462, .T. ) ;
#92548=ORIENTED_EDGE ( 'NONE', *, *, #77455, .F. ) ;
#92551=ORIENTED_EDGE ( 'NONE', *, *, #162699, .F. ) ;
#92598=FACE_BOUND ( 'NONE', #87558, .T. ) ;
#92623=ADVANCED_FACE ( 'NONE', ( #40859 ), #69340, .F. ) ;
#92671=ORIENTED_EDGE ( 'NONE', *, *, #104644, .T. ) ;
#92675=AXIS2_PLACEMENT_3D ( 'NONE', #152022, #92012, #251077 ) ;
#92680=ORIENTED_EDGE ( 'NONE', *, *, #74636, .F. ) ;
#92741=CYLINDRICAL_SURFACE ( 'NONE', #76280, 0.09999999999998898659 ) ;
#92753=CARTESIAN_POINT ( 'NONE',  ( 23.14999999999999858, 71.00000000001253397, -181.9283735034374843 ) ) ;
#92770=EDGE_CURVE ( 'NONE', #37719, #45489, #140676, .T. ) ;
#92780=VERTEX_POINT ( 'NONE', #78123 ) ;
#92871=VERTEX_POINT ( 'NONE', #84505 ) ;
#92876=CARTESIAN_POINT ( 'NONE',  ( -18.59999999999999787, 77.13501884592258762, -162.3061306010920362 ) ) ;
#92884=CARTESIAN_POINT ( 'NONE',  ( -20.64999999999999858, 68.85000000001259934, -191.1731074845243938 ) ) ;
#92898=ORIENTED_EDGE ( 'NONE', *, *, #181862, .F. ) ;
#92906=VERTEX_POINT ( 'NONE', #225325 ) ;
#92917=DIRECTION ( 'NONE',  ( 0.000000000000000000, 0.4999999999999608646, 0.8660254037844612451 ) ) ;
#92922=DIRECTION ( 'NONE',  ( -1.000000000000000000, 0.000000000000000000, -0.000000000000000000 ) ) ;
#92945=AXIS2_PLACEMENT_3D ( 'NONE', #101031, #219743, #188025 ) ;
#92951=CARTESIAN_POINT ( 'NONE',  ( 20.89878130938411616, 65.67252876774583115, -164.4457041994994881 ) ) ;
#92967=CARTESIAN_POINT ( 'NONE',  ( 18.59999999999999432, 74.83729825007462466, -195.4231074845243654 ) ) ;
#93047=ORIENTED_EDGE ( 'NONE', *, *, #201177, .F. ) ;
#93102=EDGE_CURVE ( 'NONE', #253555, #3812, #157012, .T. ) ;
#93139=DIRECTION ( 'NONE',  ( 0.000000000000000000, -1.000000000000000000, -6.982962677686266711E-15 ) ) ;
#93196=CARTESIAN_POINT ( 'NONE',  ( -18.44204374631836174, 85.49103638961074125, -163.3969062143033000 ) ) ;
#93224=DIRECTION ( 'NONE',  ( 1.000000000000000000, 0.000000000000000000, 0.000000000000000000 ) ) ;
#93246=CARTESIAN_POINT ( 'NONE',  ( -23.25000000000000000, 74.00000000001259082, -190.2984855617622770 ) ) ;
#93253=CARTESIAN_POINT ( 'NONE',  ( 20.94999999999999574, 77.83534155023700407, -191.9679561919613491 ) ) ;
#93255=DIRECTION ( 'NONE',  ( -1.000000000000000000, -0.000000000000000000, -0.000000000000000000 ) ) ;
#93258=TOROIDAL_SURFACE ( 'NONE', #34855, 0.2000000000000000111, 0.1000000000000000056 ) ;
#93286=ORIENTED_EDGE ( 'NONE', *, *, #71539, .F. ) ;
#93313=CARTESIAN_POINT ( 'NONE',  ( 21.00000000000000000, 66.25000000001260503, -191.1731074845244223 ) ) ;
#93322=CARTESIAN_POINT ( 'NONE',  ( 18.59999999999999076, 69.60000000001261355, -193.5926828544628222 ) ) ;
#93332=ORIENTED_EDGE ( 'NONE', *, *, #105332, .F. ) ;
#93356=ORIENTED_EDGE ( 'NONE', *, *, #75462, .F. ) ;
#93381=AXIS2_PLACEMENT_3D ( 'NONE', #132271, #151869, #231389 ) ;
#93385=ADVANCED_FACE ( 'NONE', ( #244592 ), #185910, .F. ) ;
#93391=CARTESIAN_POINT ( 'NONE',  ( 20.94999999999999929, 71.00000000001253397, -182.4283735034374843 ) ) ;
#93453=CARTESIAN_POINT ( 'NONE',  ( -18.59999999999999787, 77.16412189325360771, -162.2082593989527197 ) ) ;
#93456=CARTESIAN_POINT ( 'NONE',  ( 21.04999999999998650, 69.35000000001259934, -191.2731074845243882 ) ) ;
#93459=ORIENTED_EDGE ( 'NONE', *, *, #204015, .T. ) ;
#93463=DIRECTION ( 'NONE',  ( 0.000000000000000000, 0.000000000000000000, 1.000000000000000000 ) ) ;
#93485=DIRECTION ( 'NONE',  ( 0.000000000000000000, -6.982962677686266711E-15, 1.000000000000000000 ) ) ;
#93523=AXIS2_PLACEMENT_3D ( 'NONE', #222953, #44343, #88571 ) ;
#93563=CYLINDRICAL_SURFACE ( 'NONE', #156530, 0.09999999999998898659 ) ;
#93568=CARTESIAN_POINT ( 'NONE',  ( -23.25000000000000000, 76.00000000001244871, -170.0231074845243597 ) ) ;
#93593=ORIENTED_EDGE ( 'NONE', *, *, #187633, .F. ) ;
#93607=EDGE_CURVE ( 'NONE', #33906, #226219, #76218, .T. ) ;
#93639=AXIS2_PLACEMENT_3D ( 'NONE', #75097, #234128, #230275 ) ;
#93655=CIRCLE ( 'NONE', #6149, 0.09999999999999939493 ) ;
#93667=FACE_OUTER_BOUND ( 'NONE', #116317, .T. ) ;
#93671=LINE ( 'NONE', #12881, #162236 ) ;
#93677=ORIENTED_EDGE ( 'NONE', *, *, #131899, .F. ) ;
#93697=EDGE_LOOP ( 'NONE', ( #159594, #77472, #217876 ) ) ;
#93698=CARTESIAN_POINT ( 'NONE',  ( -22.39999999999999858, 64.25000000001269029, -203.6231074845244393 ) ) ;
#93703=ADVANCED_FACE ( 'NONE', ( #98321 ), #177920, .F. ) ;
#93706=ORIENTED_EDGE ( 'NONE', *, *, #38643, .T. ) ;
#93743=DIRECTION ( 'NONE',  ( 0.000000000000000000, -0.1350103645451557199, -0.9908441862701644620 ) ) ;
#93748=EDGE_CURVE ( 'NONE', #50255, #99797, #153302, .T. ) ;
#93763=CARTESIAN_POINT ( 'NONE',  ( -21.05000000000000071, 87.75000000001247713, -172.9231074845242802 ) ) ;
#93769=DIRECTION ( 'NONE',  ( 0.000000000000000000, 1.000000000000000000, 0.000000000000000000 ) ) ;
#93801=DIRECTION ( 'NONE',  ( 1.000000000000000000, 0.000000000000000000, 0.000000000000000000 ) ) ;
#93803=CARTESIAN_POINT ( 'NONE',  ( -22.39999999999999858, 76.10085836911147794, -215.2726746080137445 ) ) ;
#93807=DIRECTION ( 'NONE',  ( -0.000000000000000000, -6.982962677686266711E-15, 1.000000000000000000 ) ) ;
#93818=DIRECTION ( 'NONE',  ( 0.000000000000000000, -2.771150684185008344E-14, -1.000000000000000000 ) ) ;
#93820=VERTEX_POINT ( 'NONE', #222131 ) ;
#93834=CARTESIAN_POINT ( 'NONE',  ( 18.59117750673696534, 65.66751761918722252, -164.4282609406112670 ) ) ;
#93835=DIRECTION ( 'NONE',  ( 1.000000000000000000, -0.000000000000000000, 0.000000000000000000 ) ) ;
#93848=CARTESIAN_POINT ( 'NONE',  ( 18.59999999999999076, 69.55000000001253113, -182.3731074845244109 ) ) ;
#93861=CARTESIAN_POINT ( 'NONE',  ( 22.00356870071856363, 76.00000000003105072, -210.7773498462513260 ) ) ;
#93873=CARTESIAN_POINT ( 'NONE',  ( -20.94999999999999929, 76.00000000001267608, -203.5231074845243597 ) ) ;
#93880=DIRECTION ( 'NONE',  ( 0.000000000000000000, 0.000000000000000000, 1.000000000000000000 ) ) ;
#93896=DIRECTION ( 'NONE',  ( 0.000000000000000000, 0.000000000000000000, 1.000000000000000000 ) ) ;
#93898=CARTESIAN_POINT ( 'NONE',  ( 18.59999999999999787, 77.83534155023700407, -191.9679561919613491 ) ) ;
#93930=DIRECTION ( 'NONE',  ( 0.000000000000000000, -7.429790795770644761E-15, 1.000000000000000000 ) ) ;
#93937=DIRECTION ( 'NONE',  ( 1.000000000000000000, 0.000000000000000000, 0.000000000000000000 ) ) ;
#93953=ORIENTED_EDGE ( 'NONE', *, *, #241839, .T. ) ;
#93964=FACE_OUTER_BOUND ( 'NONE', #168672, .T. ) ;
#93971=ORIENTED_EDGE ( 'NONE', *, *, #199661, .T. ) ;
#93975=ORIENTED_EDGE ( 'NONE', *, *, #73659, .T. ) ;
#93978=AXIS2_PLACEMENT_3D ( 'NONE', #99978, #239531, #41352 ) ;
#93986=VERTEX_POINT ( 'NONE', #55058 ) ;
#94005=CARTESIAN_POINT ( 'NONE',  ( 20.94999999999999929, 76.00000000001244871, -170.0231074845243597 ) ) ;
#94008=VERTEX_POINT ( 'NONE', #98027 ) ;
#94027=AXIS2_PLACEMENT_3D ( 'NONE', #141136, #242780, #143684 ) ;
#94060=DIRECTION ( 'NONE',  ( 0.000000000000000000, 1.000000000000000000, 0.000000000000000000 ) ) ;
#94115=VERTEX_POINT ( 'NONE', #1515 ) ;
#94119=EDGE_CURVE ( 'NONE', #128423, #239176, #81041, .T. ) ;
#94143=EDGE_LOOP ( 'NONE', ( #247764, #165284, #121384, #233540, #154437 ) ) ;
#94149=CARTESIAN_POINT ( 'NONE',  ( -20.54999999999999716, 68.75000000001253397, -182.2731074845244166 ) ) ;
#94172=FACE_OUTER_BOUND ( 'NONE', #176983, .T. ) ;
#94187=DIRECTION ( 'NONE',  ( 0.000000000000000000, -7.429790795770644761E-15, 1.000000000000000000 ) ) ;
#94193=EDGE_LOOP ( 'NONE', ( #189645, #243392, #254590, #137062 ) ) ;
#94211=DIRECTION ( 'NONE',  ( 0.000000000000000000, -1.000000000000000000, -6.982962677686265922E-15 ) ) ;
#94250=LINE ( 'NONE', #134643, #86055 ) ;
#94256=CARTESIAN_POINT ( 'NONE',  ( -20.85000000000000142, 77.16412189325360771, -162.1082593989527254 ) ) ;
#94265=CARTESIAN_POINT ( 'NONE',  ( 20.94999999999999929, 85.00000000001251976, -179.9170766071767389 ) ) ;
#94288=CARTESIAN_POINT ( 'NONE',  ( 18.47654891039378455, 85.46527494839494921, -196.3971315793296526 ) ) ;
#94318=TOROIDAL_SURFACE ( 'NONE', #219221, 0.4000000000000009104, 0.1000000000000000056 ) ;
#94323=CARTESIAN_POINT ( 'NONE',  ( -18.39999999999999858, 85.50000000001263345, -196.4910380878246201 ) ) ;
#94340=EDGE_CURVE ( 'NONE', #118551, #181442, #134296, .T. ) ;
#94359=EDGE_LOOP ( 'NONE', ( #203643, #150915 ) ) ;
#94367=ORIENTED_EDGE ( 'NONE', *, *, #246951, .T. ) ;
#94393=VERTEX_POINT ( 'NONE', #15686 ) ;
#94394=CARTESIAN_POINT ( 'NONE',  ( 23.24999999999999645, 76.00000000001244871, -170.0231074845243597 ) ) ;
#94472=CARTESIAN_POINT ( 'NONE',  ( -20.00857864376270001, 66.65000000001259650, -191.1731074845244223 ) ) ;
#94489=ADVANCED_FACE ( 'NONE', ( #100300 ), #111953, .T. ) ;
#94509=VERTEX_POINT ( 'NONE', #192377 ) ;
#94519=EDGE_CURVE ( 'NONE', #223652, #10686, #207832, .T. ) ;
#94535=AXIS2_PLACEMENT_3D ( 'NONE', #146909, #127377, #128668 ) ;
#94539=EDGE_CURVE ( 'NONE', #11973, #181359, #194963, .T. ) ;
#94566=ORIENTED_EDGE ( 'NONE', *, *, #27732, .F. ) ;
#94579=CYLINDRICAL_SURFACE ( 'NONE', #181860, 0.09999999999998898659 ) ;
#94628=UNCERTAINTY_MEASURE_WITH_UNIT (LENGTH_MEASURE( 1.000000000000000082E-05 ), #172462, 'distance_accuracy_value', 'NONE');
#94635=DIRECTION ( 'NONE',  ( -3.265361837132813093E-16, -1.000000000000000000, -6.982962677686266711E-15 ) ) ;
#94652=ADVANCED_FACE ( 'NONE', ( #160967 ), #69877, .F. ) ;
#94658=EDGE_LOOP ( 'NONE', ( #21084, #107553, #45058, #252702 ) ) ;
#94689=CARTESIAN_POINT ( 'NONE',  ( -18.50000000000000000, 77.13501884592258762, -162.3061306010920362 ) ) ;
#94710=DIRECTION ( 'NONE',  ( 0.000000000000000000, 1.999342311295302429E-14, -1.000000000000000000 ) ) ;
#94722=ORIENTED_EDGE ( 'NONE', *, *, #153278, .F. ) ;
#94725=TOROIDAL_SURFACE ( 'NONE', #32217, 0.2000000000000000111, 0.1000000000000000056 ) ;
#94748=AXIS2_PLACEMENT_3D ( 'NONE', #113376, #132954, #129092 ) ;
#94751=DIRECTION ( 'NONE',  ( 0.000000000000000000, 0.000000000000000000, 1.000000000000000000 ) ) ;
#94769=ORIENTED_EDGE ( 'NONE', *, *, #140464, .F. ) ;
#94778=DIRECTION ( 'NONE',  ( 1.000000000000000000, 0.000000000000000000, 0.000000000000000000 ) ) ;
#94801=CARTESIAN_POINT ( 'NONE',  ( -20.54999999999999716, 74.00000000001254818, -183.2477294072864709 ) ) ;
#94862=CYLINDRICAL_SURFACE ( 'NONE', #218996, 0.09999999999999939493 ) ;
#94898=DIRECTION ( 'NONE',  ( 0.000000000000000000, 6.982962677686266711E-15, -1.000000000000000000 ) ) ;
#94900=CARTESIAN_POINT ( 'NONE',  ( -18.59999999999999787, 68.97833521811233481, -166.1895420826271277 ) ) ;
#94906=FACE_OUTER_BOUND ( 'NONE', #81250, .T. ) ;
#94920=CARTESIAN_POINT ( 'NONE',  ( 23.15000000000000213, 84.59626168225560150, -194.0729799673740104 ) ) ;
#94946=ORIENTED_EDGE ( 'NONE', *, *, #35618, .F. ) ;
#94968=AXIS2_PLACEMENT_3D ( 'NONE', #11442, #247462, #128817 ) ;
#94970=ORIENTED_EDGE ( 'NONE', *, *, #126454, .F. ) ;
#94971=ORIENTED_EDGE ( 'NONE', *, *, #160181, .T. ) ;
#94982=ADVANCED_FACE ( 'NONE', ( #152986 ), #232509, .T. ) ;
#95028=ADVANCED_FACE ( 'NONE', ( #91689 ), #211655, .F. ) ;
#95055=CARTESIAN_POINT ( 'NONE',  ( 21.05000000000000071, 65.31570632562542755, -195.9964335458869300 ) ) ;
#95078=AXIS2_PLACEMENT_3D ( 'NONE', #242577, #82195, #200892 ) ;
#95103=DIRECTION ( 'NONE',  ( 0.000000000000000000, 0.9915357197604982575, -0.1298341882519033486 ) ) ;
#95124=CARTESIAN_POINT ( 'NONE',  ( 18.55121869061587958, 65.67252876774583115, -164.4457041994994881 ) ) ;
#95169=AXIS2_PLACEMENT_3D ( 'NONE', #210909, #117893, #191380 ) ;
#95173=CARTESIAN_POINT ( 'NONE',  ( 18.50000000000000000, 85.40000000001263913, -196.2258477248609836 ) ) ;
#95211=DIRECTION ( 'NONE',  ( -1.000000000000000000, -0.000000000000000000, 0.000000000000000000 ) ) ;
#95213=ORIENTED_EDGE ( 'NONE', *, *, #73614, .F. ) ;
#95216=ADVANCED_FACE ( 'NONE', ( #5393 ), #128317, .T. ) ;
#95262=FACE_OUTER_BOUND ( 'NONE', #139197, .T. ) ;
#95270=DIRECTION ( 'NONE',  ( 1.000000000000000000, -2.952720810173289112E-16, -2.061873921506763405E-30 ) ) ;
#95272=CIRCLE ( 'NONE', #241020, 0.1000000000000028644 ) ;
#95277=ADVANCED_FACE ( 'NONE', ( #87510 ), #141095, .T. ) ;
#95282=CARTESIAN_POINT ( 'NONE',  ( 22.50014994444005367, 64.25028026812066173, -203.6061876412436504 ) ) ;
#95293=CIRCLE ( 'NONE', #241054, 0.1000000000000072220 ) ;
#95298=DIRECTION ( 'NONE',  ( 1.000000000000000000, 0.000000000000000000, 0.000000000000000000 ) ) ;
#95304=DIRECTION ( 'NONE',  ( -1.000000000000000000, -0.000000000000000000, -0.000000000000000000 ) ) ;
#95308=VERTEX_POINT ( 'NONE', #90081 ) ;
#95321=CARTESIAN_POINT ( 'NONE',  ( -20.64999999999999858, 74.00000000001254818, -183.2477294072864709 ) ) ;
#95326=CIRCLE ( 'NONE', #249458, 0.09999999999998898659 ) ;
#95327=SPHERICAL_SURFACE ( 'NONE', #230810, 0.1000000000000000056 ) ;
#95387=EDGE_CURVE ( 'NONE', #241424, #35186, #70570, .T. ) ;
#95388=ORIENTED_EDGE ( 'NONE', *, *, #139706, .T. ) ;
#95392=ORIENTED_EDGE ( 'NONE', *, *, #142129, .T. ) ;
#95404=EDGE_CURVE ( 'NONE', #235019, #92906, #217725, .T. ) ;
#95421=PLANE ( 'NONE',  #56329 ) ;
#95449=TOROIDAL_SURFACE ( 'NONE', #128774, 0.4000000000000005773, 0.1000000000000000056 ) ;
#95475=ORIENTED_EDGE ( 'NONE', *, *, #29012, .T. ) ;
#95497=CIRCLE ( 'NONE', #166262, 0.09999999999998898659 ) ;
#95514=DIRECTION ( 'NONE',  ( 1.000000000000000000, 0.000000000000000000, 0.000000000000000000 ) ) ;
#95533=EDGE_LOOP ( 'NONE', ( #50688, #95596, #184320, #186378 ) ) ;
#95545=DIRECTION ( 'NONE',  ( 1.000000000000000000, 0.000000000000000000, 0.000000000000000000 ) ) ;
#95575=ORIENTED_EDGE ( 'NONE', *, *, #249854, .T. ) ;
#95596=ORIENTED_EDGE ( 'NONE', *, *, #83341, .T. ) ;
#95597=EDGE_CURVE ( 'NONE', #233373, #221772, #57739, .T. ) ;
#95604=DIRECTION ( 'NONE',  ( 0.000000000000000000, 0.000000000000000000, 1.000000000000000000 ) ) ;
#95625=CONICAL_SURFACE ( 'NONE', #212164, 4.049999999999998046, 0.7853981633974604915 ) ;
#95628=DIRECTION ( 'NONE',  ( 1.836970198721029934E-16, 1.000000000000000000, 6.982962677686266711E-15 ) ) ;
#95629=CARTESIAN_POINT ( 'NONE',  ( -18.60000000000000142, 85.32100840337393777, -196.2871692354464130 ) ) ;
#95651=VECTOR ( 'NONE', #76306, 1000.000000000000114 ) ;
#95686=CARTESIAN_POINT ( 'NONE',  ( -20.94999999999999929, 76.00000000001244871, -170.0231074845243597 ) ) ;
#95696=ADVANCED_FACE ( 'NONE', ( #108081 ), #27289, .T. ) ;
#95702=CIRCLE ( 'NONE', #29133, 0.09999999999998898659 ) ;
#95714=CARTESIAN_POINT ( 'NONE',  ( -21.05000000000000071, 87.65000000001246860, -173.1231074845242688 ) ) ;
#95725=ORIENTED_EDGE ( 'NONE', *, *, #255199, .T. ) ;
#95763=ORIENTED_EDGE ( 'NONE', *, *, #115932, .F. ) ;
#95775=DIRECTION ( 'NONE',  ( -1.000000000000000000, 0.000000000000000000, -0.000000000000000000 ) ) ;
#95805=CARTESIAN_POINT ( 'NONE',  ( 22.39999999999999858, 68.20922040163929978, -203.6231074845244109 ) ) ;
#95847=EDGE_CURVE ( 'NONE', #28569, #235019, #247582, .T. ) ;
#95871=CARTESIAN_POINT ( 'NONE',  ( -21.37071067811865532, 67.92928932189394686, -191.2731074845244166 ) ) ;
#95885=LINE ( 'NONE', #622, #118611 ) ;
#95891=FACE_OUTER_BOUND ( 'NONE', #129627, .T. ) ;
#95924=DIRECTION ( 'NONE',  ( 0.000000000000000000, -7.086529944415886769E-15, 1.000000000000000000 ) ) ;
#95936=AXIS2_PLACEMENT_3D ( 'NONE', #29456, #248468, #69849 ) ;
#95948=VERTEX_POINT ( 'NONE', #102587 ) ;
#95977=EDGE_CURVE ( 'NONE', #106612, #210954, #132965, .T. ) ;
#96020=AXIS2_PLACEMENT_3D ( 'NONE', #34935, #114438, #50590 ) ;
#96025=CIRCLE ( 'NONE', #154358, 0.1000000000000000888 ) ;
#96033=ORIENTED_EDGE ( 'NONE', *, *, #4055, .F. ) ;
#96063=CARTESIAN_POINT ( 'NONE',  ( 18.33683296300426235, 85.51114997114527227, -163.1174000718142452 ) ) ;
#96095=EDGE_LOOP ( 'NONE', ( #46191, #150879, #64447, #175491, #162470 ) ) ;
#96116=EDGE_CURVE ( 'NONE', #59470, #93820, #8241, .T. ) ;
#96126=AXIS2_PLACEMENT_3D ( 'NONE', #111883, #170617, #124068 ) ;
#96130=CARTESIAN_POINT ( 'NONE',  ( -18.59999999999999787, 74.14897176987174987, -191.8691942151018850 ) ) ;
#96144=CARTESIAN_POINT ( 'NONE',  ( 21.07928932188134397, 76.00000000001267608, -203.5231074845243597 ) ) ;
#96149=CYLINDRICAL_SURFACE ( 'NONE', #200977, 4.049999999999998046 ) ;
#96164=CONICAL_SURFACE ( 'NONE', #58744, 7.750000000000034639, 0.7853981633974531640 ) ;
#96176=FACE_OUTER_BOUND ( 'NONE', #40443, .T. ) ;
#96211=VECTOR ( 'NONE', #213983, 1000.000000000000000 ) ;
#96257=VERTEX_POINT ( 'NONE', #252380 ) ;
#96281=DIRECTION ( 'NONE',  ( 0.000000000000000000, 0.1350103645451807555, 0.9908441862701609093 ) ) ;
#96282=CIRCLE ( 'NONE', #597, 0.09999999999998898659 ) ;
#96287=VERTEX_POINT ( 'NONE', #93322 ) ;
#96303=CARTESIAN_POINT ( 'NONE',  ( 23.14999999999999503, 69.45000000001259366, -191.1731074845243938 ) ) ;
#96330=ORIENTED_EDGE ( 'NONE', *, *, #87905, .F. ) ;
#96356=PLANE ( 'NONE',  #119855 ) ;
#96372=EDGE_LOOP ( 'NONE', ( #227101, #152063, #51059, #133278 ) ) ;
#96385=DIRECTION ( 'NONE',  ( 0.000000000000000000, -1.000000000000000000, -6.860497997771532351E-15 ) ) ;
#96387=EDGE_CURVE ( 'NONE', #91407, #87397, #203852, .T. ) ;
#96392=CIRCLE ( 'NONE', #146451, 11.64999999999999325 ) ;
#96399=DIRECTION ( 'NONE',  ( 0.000000000000000000, 6.982962677686266711E-15, -1.000000000000000000 ) ) ;
#96410=CARTESIAN_POINT ( 'NONE',  ( 21.14999999999999858, 65.28660755661270798, -191.2731074845244166 ) ) ;
#96415=ORIENTED_EDGE ( 'NONE', *, *, #145636, .T. ) ;
#96427=CARTESIAN_POINT ( 'NONE',  ( -20.94999999999999929, 87.65000000001246860, -172.9231074845242802 ) ) ;
#96457=EDGE_CURVE ( 'NONE', #193233, #24117, #228815, .T. ) ;
#96471=EDGE_CURVE ( 'NONE', #125507, #133309, #70801, .T. ) ;
#96478=CARTESIAN_POINT ( 'NONE',  ( -23.15000000000000213, 64.25000000001259082, -191.3731074845244393 ) ) ;
#96501=VERTEX_POINT ( 'NONE', #118784 ) ;
#96511=LINE ( 'NONE', #176104, #63768 ) ;
#96536=CIRCLE ( 'NONE', #92450, 2.099999999999990763 ) ;
#96566=LINE ( 'NONE', #58721, #10694 ) ;
#96618=DIRECTION ( 'NONE',  ( 0.000000000000000000, 0.8777080977375655291, -0.4791956752370622463 ) ) ;
#96645=EDGE_LOOP ( 'NONE', ( #227941, #83615, #125201, #36853 ) ) ;
#96648=CARTESIAN_POINT ( 'NONE',  ( -22.49436431346200038, 64.35004905235922479, -203.5900110142466986 ) ) ;
#96688=DIRECTION ( 'NONE',  ( 1.000000000000000000, 0.000000000000000000, 0.000000000000000000 ) ) ;
#96691=EDGE_CURVE ( 'NONE', #17720, #63242, #246423, .T. ) ;
#96711=DIRECTION ( 'NONE',  ( -0.000000000000000000, 1.000000000000000000, 6.352154140967427193E-15 ) ) ;
#96764=ORIENTED_EDGE ( 'NONE', *, *, #134117, .T. ) ;
#96769=ORIENTED_EDGE ( 'NONE', *, *, #108778, .T. ) ;
#96787=ORIENTED_EDGE ( 'NONE', *, *, #131899, .T. ) ;
#96807=ADVANCED_FACE ( 'NONE', ( #174640 ), #113326, .T. ) ;
#96829=ORIENTED_EDGE ( 'NONE', *, *, #233697, .F. ) ;
#96846=AXIS2_PLACEMENT_3D ( 'NONE', #114661, #194228, #233353 ) ;
#96866=ORIENTED_EDGE ( 'NONE', *, *, #244867, .F. ) ;
#96917=EDGE_CURVE ( 'NONE', #69180, #218291, #37654, .T. ) ;
#96958=CARTESIAN_POINT ( 'NONE',  ( 23.14999999999999858, 70.40000000001253966, -182.4283735034374843 ) ) ;
#96965=DIRECTION ( 'NONE',  ( -0.000000000000000000, 1.000000000000000000, 6.982962677686266711E-15 ) ) ;
#97010=DIRECTION ( 'NONE',  ( 0.000000000000000000, 6.769652589177795712E-15, -1.000000000000000000 ) ) ;
#97014=CARTESIAN_POINT ( 'NONE',  ( -18.48408745364673678, 85.66432225867556838, -163.3400289511960466 ) ) ;
#97035=CIRCLE ( 'NONE', #213796, 0.09999999999998898659 ) ;
#97037=CARTESIAN_POINT ( 'NONE',  ( 21.05000000000000071, 76.00000000001244871, -170.0231074845243597 ) ) ;
#97039=DIRECTION ( 'NONE',  ( 0.000000000000000000, 6.982962677686266711E-15, -1.000000000000000000 ) ) ;
#97093=PLANE ( 'NONE',  #29800 ) ;
#97134=CIRCLE ( 'NONE', #189340, 0.09999999999998898659 ) ;
#97149=TOROIDAL_SURFACE ( 'NONE', #38961, 0.4000000000000003553, 0.1000000000000000056 ) ;
#97150=ORIENTED_EDGE ( 'NONE', *, *, #167437, .F. ) ;
#97167=CARTESIAN_POINT ( 'NONE',  ( -20.94999999999999929, 74.73821383144760944, -195.4366085209788935 ) ) ;
#97171=EDGE_LOOP ( 'NONE', ( #88217, #180558 ) ) ;
#97177=CARTESIAN_POINT ( 'NONE',  ( -23.25000000000000000, 71.85000000001259934, -191.1731074845243654 ) ) ;
#97180=AXIS2_PLACEMENT_3D ( 'NONE', #54905, #173649, #253107 ) ;
#97185=ORIENTED_EDGE ( 'NONE', *, *, #205661, .F. ) ;
#97193=ORIENTED_EDGE ( 'NONE', *, *, #131418, .T. ) ;
#97198=VERTEX_POINT ( 'NONE', #53035 ) ;
#97228=CARTESIAN_POINT ( 'NONE',  ( 20.94999999999999929, 70.60000000001259934, -191.1178414656113205 ) ) ;
#97239=CARTESIAN_POINT ( 'NONE',  ( 20.94999999999999929, 70.50000000001253397, -182.4283735034374843 ) ) ;
#97248=ORIENTED_EDGE ( 'NONE', *, *, #116006, .T. ) ;
#97254=ORIENTED_EDGE ( 'NONE', *, *, #226337, .T. ) ;
#97296=ORIENTED_EDGE ( 'NONE', *, *, #50583, .F. ) ;
#97351=CYLINDRICAL_SURFACE ( 'NONE', #3367, 0.09999999999999939493 ) ;
#97355=DIRECTION ( 'NONE',  ( 1.000000000000000000, 0.000000000000000000, 0.000000000000000000 ) ) ;
#97356=CARTESIAN_POINT ( 'NONE',  ( 23.15000000000000213, 87.75000000001247713, -173.1231074845242688 ) ) ;
#97362=CARTESIAN_POINT ( 'NONE',  ( 23.24999999999999289, 64.25000000001269029, -203.4231074845244507 ) ) ;
#97449=EDGE_CURVE ( 'NONE', #75576, #135228, #167497, .T. ) ;
#97477=DIRECTION ( 'NONE',  ( 2.952720810173289112E-16, 1.000000000000000000, 6.530723674265620862E-15 ) ) ;
#97511=EDGE_LOOP ( 'NONE', ( #44374, #25608, #93356 ) ) ;
#97556=AXIS2_PLACEMENT_3D ( 'NONE', #231853, #208444, #212289 ) ;
#97566=EDGE_CURVE ( 'NONE', #210954, #186763, #17603, .T. ) ;
#97568=CARTESIAN_POINT ( 'NONE',  ( 18.59999999999999432, 70.30054753569118020, -216.0653814410942175 ) ) ;
#97572=ORIENTED_EDGE ( 'NONE', *, *, #73005, .F. ) ;
#97576=ORIENTED_EDGE ( 'NONE', *, *, #31700, .T. ) ;
#97583=ORIENTED_EDGE ( 'NONE', *, *, #157731, .F. ) ;
#97587=DIRECTION ( 'NONE',  ( 1.000000000000000000, 7.304098846218134667E-16, 4.639676173203993355E-30 ) ) ;
#97651=ORIENTED_EDGE ( 'NONE', *, *, #21664, .T. ) ;
#97656=DIRECTION ( 'NONE',  ( -0.000000000000000000, 1.000000000000000000, 7.272083257015735086E-15 ) ) ;
#97663=CARTESIAN_POINT ( 'NONE',  ( 18.49999999999998934, 65.70711192142415769, -164.5651054685122858 ) ) ;
#97676=EDGE_CURVE ( 'NONE', #221772, #90288, #52269, .T. ) ;
#97688=VECTOR ( 'NONE', #249579, 1000.000000000000000 ) ;
#97704=CARTESIAN_POINT ( 'NONE',  ( -21.05000000000000071, 77.16270174995064224, -195.4231074845243370 ) ) ;
#97707=DIRECTION ( 'NONE',  ( 0.000000000000000000, 0.000000000000000000, -1.000000000000000000 ) ) ;
#97721=AXIS2_PLACEMENT_3D ( 'NONE', #221138, #218566, #239444 ) ;
#97728=DIRECTION ( 'NONE',  ( 0.000000000000000000, 0.000000000000000000, 1.000000000000000000 ) ) ;
#97730=EDGE_LOOP ( 'NONE', ( #136800, #207578, #50295, #42888 ) ) ;
#97743=CARTESIAN_POINT ( 'NONE',  ( -23.25000000000000000, 64.35000000001249987, -177.0379132551784096 ) ) ;
#97761=DIRECTION ( 'NONE',  ( 0.000000000000000000, -1.000000000000000000, -6.982962677686265922E-15 ) ) ;
#97780=EDGE_CURVE ( 'NONE', #218193, #145161, #26146, .T. ) ;
#97784=DIRECTION ( 'NONE',  ( 1.000000000000000000, 0.000000000000000000, 0.000000000000000000 ) ) ;
#97806=DIRECTION ( 'NONE',  ( 1.000000000000000000, 7.304098846218135653E-16, 5.100424963727256530E-30 ) ) ;
#97818=ORIENTED_EDGE ( 'NONE', *, *, #119195, .T. ) ;
#97927=VERTEX_POINT ( 'NONE', #131648 ) ;
#97937=TOROIDAL_SURFACE ( 'NONE', #89761, 0.2000000000000000111, 0.1000000000000000056 ) ;
#97945=VERTEX_POINT ( 'NONE', #132948 ) ;
#97948=EDGE_CURVE ( 'NONE', #133309, #176065, #89780, .T. ) ;
#97949=CARTESIAN_POINT ( 'NONE',  ( -20.85000000000000142, 64.25000000001250555, -176.8647081744215086 ) ) ;
#97961=DIRECTION ( 'NONE',  ( 1.000000000000000000, 0.000000000000000000, 0.000000000000000000 ) ) ;
#97962=DIRECTION ( 'NONE',  ( 1.000000000000000000, 0.000000000000000000, 0.000000000000000000 ) ) ;
#97996=ORIENTED_EDGE ( 'NONE', *, *, #10522, .F. ) ;
#98027=CARTESIAN_POINT ( 'NONE',  ( -18.59999999999999787, 64.40000000001263913, -196.5949042542488883 ) ) ;
#98056=CARTESIAN_POINT ( 'NONE',  ( 23.14999999999999858, 64.35000000001249987, -177.0379132551783812 ) ) ;
#98058=CARTESIAN_POINT ( 'NONE',  ( 20.04142135623731136, 64.25000000001250555, -178.7559501969990947 ) ) ;
#98086=CARTESIAN_POINT ( 'NONE',  ( 22.40000000000010516, 76.00000000001371347, -215.1726782920694632 ) ) ;
#98102=FACE_OUTER_BOUND ( 'NONE', #126861, .T. ) ;
#98107=ORIENTED_EDGE ( 'NONE', *, *, #198397, .F. ) ;
#98154=TOROIDAL_SURFACE ( 'NONE', #48306, 4.099999999999999645, 0.1000000000000000056 ) ;
#98157=CIRCLE ( 'NONE', #68995, 4.000000000000003553 ) ;
#98168=CIRCLE ( 'NONE', #27525, 0.1999999999999987899 ) ;
#98171=CARTESIAN_POINT ( 'NONE',  ( -18.40000000000000213, 85.50000000001264766, -196.5237453873442064 ) ) ;
#98197=CARTESIAN_POINT ( 'NONE',  ( -20.94999999999999929, 76.00000000001264766, -200.6231074845243825 ) ) ;
#98198=CIRCLE ( 'NONE', #160631, 0.09999999999998898659 ) ;
#98204=LINE ( 'NONE', #211789, #232300 ) ;
#98215=CYLINDRICAL_SURFACE ( 'NONE', #223921, 4.049999999999998046 ) ;
#98243=DIRECTION ( 'NONE',  ( -0.000000000000000000, -1.000000000000000000, -6.982962677686266711E-15 ) ) ;
#98256=EDGE_CURVE ( 'NONE', #165093, #160597, #221968, .T. ) ;
#98283=DIRECTION ( 'NONE',  ( 4.026293107431335996E-15, 0.8700118002898393765, -0.4930308989875104575 ) ) ;
#98321=FACE_OUTER_BOUND ( 'NONE', #28429, .T. ) ;
#98338=CARTESIAN_POINT ( 'NONE',  ( -22.59999999999999787, 64.25043287652329127, -203.6239658536231332 ) ) ;
#98373=AXIS2_PLACEMENT_3D ( 'NONE', #252948, #74366, #151317 ) ;
#98417=AXIS2_PLACEMENT_3D ( 'NONE', #125849, #31929, #67179 ) ;
#98431=EDGE_CURVE ( 'NONE', #110754, #154576, #217067, .T. ) ;
#98466=CARTESIAN_POINT ( 'NONE',  ( 20.74625933824084711, 67.11708647892832857, -194.9679364604013188 ) ) ;
#98487=LINE ( 'NONE', #17699, #30514 ) ;
#98498=ORIENTED_EDGE ( 'NONE', *, *, #79808, .F. ) ;
#98499=CARTESIAN_POINT ( 'NONE',  ( -23.25000000000000000, 76.00000000001247713, -173.9231074845243654 ) ) ;
#98503=CARTESIAN_POINT ( 'NONE',  ( -20.94999999999999929, 77.36087058720467269, -195.4501095574333931 ) ) ;
#98517=DIRECTION ( 'NONE',  ( 0.000000000000000000, -6.982962677686266711E-15, 1.000000000000000000 ) ) ;
#98537=CIRCLE ( 'NONE', #81796, 0.2000000000000057288 ) ;
#98605=ORIENTED_EDGE ( 'NONE', *, *, #74356, .F. ) ;
#98611=ORIENTED_EDGE ( 'NONE', *, *, #19339, .F. ) ;
#98638=ORIENTED_EDGE ( 'NONE', *, *, #155095, .T. ) ;
#98679=EDGE_CURVE ( 'NONE', #15467, #226290, #167056, .T. ) ;
#98688=CARTESIAN_POINT ( 'NONE',  ( 20.94999999999999929, 77.83534155023701828, -191.9679561919613491 ) ) ;
#98732=DIRECTION ( 'NONE',  ( 0.000000000000000000, 0.5907332058517377193, -0.8068669527896954463 ) ) ;
#98744=AXIS2_PLACEMENT_3D ( 'NONE', #146492, #10863, #227330 ) ;
#98764=ORIENTED_EDGE ( 'NONE', *, *, #37036, .T. ) ;
#98765=ORIENTED_EDGE ( 'NONE', *, *, #108778, .F. ) ;
#98788=ADVANCED_FACE ( 'NONE', ( #54052 ), #55302, .F. ) ;
#98801=ADVANCED_FACE ( 'NONE', ( #38356 ), #20081, .F. ) ;
#98809=DIRECTION ( 'NONE',  ( 1.000000000000000000, 0.000000000000000000, -0.000000000000000000 ) ) ;
#98826=DIRECTION ( 'NONE',  ( 1.000000000000000000, -3.265361837132813093E-16, -2.280189983783949500E-30 ) ) ;
#98827=VERTEX_POINT ( 'NONE', #176595 ) ;
#98839=AXIS2_PLACEMENT_3D ( 'NONE', #179852, #161580, #138117 ) ;
#98871=DIRECTION ( 'NONE',  ( -1.000000000000000000, 0.000000000000000000, 0.000000000000000000 ) ) ;
#98875=CARTESIAN_POINT ( 'NONE',  ( -21.14999999999999858, 76.00000000001276135, -215.1726782920691505 ) ) ;
#98885=VERTEX_POINT ( 'NONE', #244232 ) ;
#98892=ADVANCED_FACE ( 'NONE', ( #46042 ), #48611, .F. ) ;
#98897=AXIS2_PLACEMENT_3D ( 'NONE', #202388, #23785, #197250 ) ;
#98903=ORIENTED_EDGE ( 'NONE', *, *, #155710, .T. ) ;
#98908=CARTESIAN_POINT ( 'NONE',  ( -20.64999999999999858, 85.40000000001252545, -179.9170766071767389 ) ) ;
#98909=EDGE_CURVE ( 'NONE', #65963, #32434, #206409, .T. ) ;
#98918=DIRECTION ( 'NONE',  ( 4.504528286903032433E-15, 0.1298341882520054891, 0.9915357197604850459 ) ) ;
#98926=LINE ( 'NONE', #41582, #196842 ) ;
#98934=ORIENTED_EDGE ( 'NONE', *, *, #18790, .T. ) ;
#98947=EDGE_LOOP ( 'NONE', ( #247025, #198039, #109466, #161129 ) ) ;
#98957=CARTESIAN_POINT ( 'NONE',  ( 23.14999999999999858, 64.35000000001249987, -177.0379132551783812 ) ) ;
#98967=AXIS2_PLACEMENT_3D ( 'NONE', #7139, #30594, #69716 ) ;
#98985=ADVANCED_FACE ( 'NONE', ( #29104 ), #9485, .T. ) ;
#99026=EDGE_LOOP ( 'NONE', ( #108185, #180806, #63031, #119669 ) ) ;
#99036=EDGE_CURVE ( 'NONE', #72156, #156620, #751, .T. ) ;
#99057=CARTESIAN_POINT ( 'NONE',  ( 21.14999999999999858, 67.21339244341248786, -191.2731074845244166 ) ) ;
#99075=EDGE_CURVE ( 'NONE', #228147, #151955, #50656, .T. ) ;
#99113=ORIENTED_EDGE ( 'NONE', *, *, #248602, .F. ) ;
#99138=CARTESIAN_POINT ( 'NONE',  ( 23.24999999999999645, 71.22429906543310096, -181.8718755885703615 ) ) ;
#99156=ORIENTED_EDGE ( 'NONE', *, *, #27473, .F. ) ;
#99167=AXIS2_PLACEMENT_3D ( 'NONE', #94256, #250766, #192103 ) ;
#99173=CARTESIAN_POINT ( 'NONE',  ( 20.94999999999999929, 87.39257802171813694, -173.0970570643562212 ) ) ;
#99181=CARTESIAN_POINT ( 'NONE',  ( 20.94999999999999574, 65.57661458509971908, -196.0310555606543517 ) ) ;
#99184=VERTEX_POINT ( 'NONE', #199390 ) ;
#99206=DIRECTION ( 'NONE',  ( 0.000000000000000000, 0.000000000000000000, -1.000000000000000000 ) ) ;
#99228=CARTESIAN_POINT ( 'NONE',  ( -20.64999999999999858, 68.75000000001253397, -182.3731074845244109 ) ) ;
#99238=CARTESIAN_POINT ( 'NONE',  ( -21.05000000000000426, 76.02103547655286775, -209.8275633064720296 ) ) ;
#99274=DIRECTION ( 'NONE',  ( 0.000000000000000000, -1.565658005757035267E-14, 1.000000000000000000 ) ) ;
#99283=ORIENTED_EDGE ( 'NONE', *, *, #162615, .F. ) ;
#99329=EDGE_CURVE ( 'NONE', #104754, #196694, #8606, .T. ) ;
#99336=AXIS2_PLACEMENT_3D ( 'NONE', #62129, #84185, #85491 ) ;
#99340=DIRECTION ( 'NONE',  ( 0.000000000000000000, -0.9654727137038715545, -0.2605042016806676242 ) ) ;
#99342=DIRECTION ( 'NONE',  ( 0.000000000000000000, 6.982962677686266711E-15, -1.000000000000000000 ) ) ;
#99358=DIRECTION ( 'NONE',  ( -0.000000000000000000, 6.982962677686266711E-15, -1.000000000000000000 ) ) ;
#99364=CARTESIAN_POINT ( 'NONE',  ( 20.95017935633852346, 65.52451072038731184, -195.9456676871339482 ) ) ;
#99372=CARTESIAN_POINT ( 'NONE',  ( -23.24999999999999645, 85.60000000001240039, -163.4229180933022576 ) ) ;
#99397=LINE ( 'NONE', #308, #53250 ) ;
#99436=CARTESIAN_POINT ( 'NONE',  ( 20.94999999999999929, 64.25000000001249134, -176.8069731475025890 ) ) ;
#99437=CARTESIAN_POINT ( 'NONE',  ( 18.49999999999999645, 74.27191306321832087, -216.6386724793566145 ) ) ;
#99476=FACE_OUTER_BOUND ( 'NONE', #196355, .T. ) ;
#99483=VERTEX_POINT ( 'NONE', #113103 ) ;
#99486=LINE ( 'NONE', #179091, #84797 ) ;
#99518=VECTOR ( 'NONE', #118693, 999.9999999999998863 ) ;
#99521=DIRECTION ( 'NONE',  ( 0.000000000000000000, -1.000000000000000000, -6.982962677686265922E-15 ) ) ;
#99537=EDGE_CURVE ( 'NONE', #37631, #92871, #77807, .T. ) ;
#99550=CARTESIAN_POINT ( 'NONE',  ( -23.25000000000000000, 64.25000000001269029, -203.5231074845244166 ) ) ;
#99554=AXIS2_PLACEMENT_3D ( 'NONE', #119544, #97355, #176964 ) ;
#99558=( BOUNDED_SURFACE ( )  B_SPLINE_SURFACE ( 3, 2, ( 
 ( #110437, #204390, #166594 ),
 ( #249956, #128730, #229110 ),
 ( #67458, #71338, #10054 ),
 ( #90870, #148286, #208273 ) ),
 .UNSPECIFIED., .F., .F., .F. ) 
 B_SPLINE_SURFACE_WITH_KNOTS ( ( 4, 4 ),
 ( 3, 3 ),
 ( 0.04058434257139476031, 0.04256401539001599538 ),
 ( 0.000000000000000000, 1.000000000000000000 ),
 .UNSPECIFIED. ) 
 GEOMETRIC_REPRESENTATION_ITEM ( )  RATIONAL_B_SPLINE_SURFACE ( (
 ( 1.000000000000000000, 0.7103081912007810361, 1.000000000000000000),
 ( 1.000000000000000000, 0.7104998333556836743, 1.000000000000000000),
 ( 1.000000000000000000, 0.7107238315753999780, 1.000000000000000000),
 ( 1.000000000000000000, 0.7110073749539779220, 1.000000000000000000) ) ) 
 REPRESENTATION_ITEM ( '' )  SURFACE ( )  );
#99572=DIRECTION ( 'NONE',  ( 0.000000000000000000, -6.982962677686266711E-15, 1.000000000000000000 ) ) ;
#99593=CARTESIAN_POINT ( 'NONE',  ( -18.36527282682052586, 85.50000060001187308, -163.1009585200215781 ) ) ;
#99625=EDGE_CURVE ( 'NONE', #100336, #144129, #8785, .T. ) ;
#99703=VERTEX_POINT ( 'NONE', #29447 ) ;
#99725=DIRECTION ( 'NONE',  ( 0.000000000000000000, -7.109473446599835262E-15, 1.000000000000000000 ) ) ;
#99738=VERTEX_POINT ( 'NONE', #86788 ) ;
#99769=CARTESIAN_POINT ( 'NONE',  ( 20.97107704358301916, 67.12452184799133192, -194.9641342551351784 ) ) ;
#99776=CARTESIAN_POINT ( 'NONE',  ( 21.14999999999999858, 64.25000000001259082, -191.3731074845244393 ) ) ;
#99794=EDGE_CURVE ( 'NONE', #229203, #226175, #129600, .T. ) ;
#99795=DIRECTION ( 'NONE',  ( 0.000000000000000000, -1.000000000000000000, -6.982962677686265922E-15 ) ) ;
#99797=VERTEX_POINT ( 'NONE', #5968 ) ;
#99812=DIRECTION ( 'NONE',  ( 0.000000000000000000, 0.000000000000000000, -1.000000000000000000 ) ) ;
#99833=AXIS2_PLACEMENT_3D ( 'NONE', #209968, #13063, #31356 ) ;
#99868=ORIENTED_EDGE ( 'NONE', *, *, #124362, .T. ) ;
#99878=CARTESIAN_POINT ( 'NONE',  ( -18.59999999999999787, 74.36282728704222222, -191.9409541190523498 ) ) ;
#99880=ORIENTED_EDGE ( 'NONE', *, *, #224505, .T. ) ;
#99895=CARTESIAN_POINT ( 'NONE',  ( 18.43630871534869797, 85.67980087481544160, -163.3624754165403772 ) ) ;
#99908=DIRECTION ( 'NONE',  ( 0.000000000000000000, 0.000000000000000000, 1.000000000000000000 ) ) ;
#99978=CARTESIAN_POINT ( 'NONE',  ( 21.05000000000000071, 70.60000000001251408, -179.9170766071768526 ) ) ;
#99979=CARTESIAN_POINT ( 'NONE',  ( -20.94999999999999929, 64.35000000001245724, -170.0231074845244166 ) ) ;
#99988=DIRECTION ( 'NONE',  ( -0.000000000000000000, 1.000000000000000000, 6.982962677686266711E-15 ) ) ;
#100048=EDGE_CURVE ( 'NONE', #30084, #165694, #160922, .T. ) ;
#100064=CARTESIAN_POINT ( 'NONE',  ( 18.59999999999999076, 65.50857864377520912, -178.7731074845244450 ) ) ;
#100072=AXIS2_PLACEMENT_3D ( 'NONE', #85817, #244925, #116975 ) ;
#100073=DIRECTION ( 'NONE',  ( -0.000000000000000000, -6.982962677686266711E-15, 1.000000000000000000 ) ) ;
#100114=DIRECTION ( 'NONE',  ( 0.000000000000000000, -7.429790795770644761E-15, 1.000000000000000000 ) ) ;
#100119=DIRECTION ( 'NONE',  ( 1.000000000000000000, 0.000000000000000000, 0.000000000000000000 ) ) ;
#100147=EDGE_LOOP ( 'NONE', ( #201249, #42797, #185136, #145741 ) ) ;
#100148=CARTESIAN_POINT ( 'NONE',  ( 20.94999999999999929, 85.00000000001251976, -179.4170766071767389 ) ) ;
#100165=CARTESIAN_POINT ( 'NONE',  ( -21.45000000000000284, 68.29142135624984178, -182.2731074845244166 ) ) ;
#100180=EDGE_CURVE ( 'NONE', #165186, #174151, #71540, .T. ) ;
#100182=CYLINDRICAL_SURFACE ( 'NONE', #177072, 0.09999999999998898659 ) ;
#100229=DIRECTION ( 'NONE',  ( 0.000000000000000000, -7.056502275159890043E-15, 1.000000000000000000 ) ) ;
#100230=ADVANCED_FACE ( 'NONE', ( #29149 ), #100697, .T. ) ;
#100232=ORIENTED_EDGE ( 'NONE', *, *, #33252, .T. ) ;
#100263=EDGE_CURVE ( 'NONE', #60084, #141837, #107056, .T. ) ;
#100287=CIRCLE ( 'NONE', #108692, 11.64999999999999325 ) ;
#100300=FACE_OUTER_BOUND ( 'NONE', #39076, .T. ) ;
#100305=FACE_OUTER_BOUND ( 'NONE', #151094, .T. ) ;
#100322=DIRECTION ( 'NONE',  ( 0.000000000000000000, 0.000000000000000000, 1.000000000000000000 ) ) ;
#100336=VERTEX_POINT ( 'NONE', #250427 ) ;
#100337=CIRCLE ( 'NONE', #162735, 2.100000000000004530 ) ;
#100359=VECTOR ( 'NONE', #211075, 1000.000000000000000 ) ;
#100436=CIRCLE ( 'NONE', #71452, 0.5000000000000004441 ) ;
#100440=CARTESIAN_POINT ( 'NONE',  ( 18.59999999999999432, 77.16270174995064224, -195.4231074845243370 ) ) ;
#100442=PLANE ( 'NONE',  #197359 ) ;
#100448=AXIS2_PLACEMENT_3D ( 'NONE', #76484, #214717, #195192 ) ;
#100484=VERTEX_POINT ( 'NONE', #97743 ) ;
#100507=CARTESIAN_POINT ( 'NONE',  ( -21.05000000000000071, 75.96636726467907863, -209.7819246792057868 ) ) ;
#100534=ORIENTED_EDGE ( 'NONE', *, *, #227326, .T. ) ;
#100547=DIRECTION ( 'NONE',  ( 0.000000000000000000, 6.982962677686266711E-15, -1.000000000000000000 ) ) ;
#100552=EDGE_CURVE ( 'NONE', #226290, #117519, #40410, .T. ) ;
#100569=AXIS2_PLACEMENT_3D ( 'NONE', #28955, #208827, #169738 ) ;
#100570=CARTESIAN_POINT ( 'NONE',  ( 23.15000000000000213, 87.75000000001251976, -182.1731074845242802 ) ) ;
#100577=EDGE_CURVE ( 'NONE', #103860, #4003, #162914, .T. ) ;
#100589=CARTESIAN_POINT ( 'NONE',  ( 20.94999999999999929, 76.00000000001247713, -174.0231074845243882 ) ) ;
#100608=DIRECTION ( 'NONE',  ( 0.000000000000000000, 1.000000000000000000, 0.000000000000000000 ) ) ;
#100634=CARTESIAN_POINT ( 'NONE',  ( 21.05000000000000071, 87.48912529308852015, -173.1231074845242688 ) ) ;
#100648=DIRECTION ( 'NONE',  ( 1.000000000000000000, 0.000000000000000000, 0.000000000000000000 ) ) ;
#100673=ORIENTED_EDGE ( 'NONE', *, *, #110435, .T. ) ;
#100697=TOROIDAL_SURFACE ( 'NONE', #63301, 11.65000000000000036, 0.1000000000000000056 ) ;
#100714=CARTESIAN_POINT ( 'NONE',  ( -18.44448725179914916, 85.49008171549576218, -163.3941471904618083 ) ) ;
#100733=CARTESIAN_POINT ( 'NONE',  ( -18.46946985241234529, 85.50931722872408614, -196.5364449190244613 ) ) ;
#100771=ORIENTED_EDGE ( 'NONE', *, *, #113320, .F. ) ;
#100784=ORIENTED_EDGE ( 'NONE', *, *, #79157, .F. ) ;
#100793=EDGE_CURVE ( 'NONE', #6205, #156110, #209236, .T. ) ;
#100807=CARTESIAN_POINT ( 'NONE',  ( 18.51565452909167675, 85.35285933884784981, -196.3281981632918587 ) ) ;
#100849=CARTESIAN_POINT ( 'NONE',  ( -18.59999999999999787, 61.95000000001265050, -198.0094124137634708 ) ) ;
#100850=LINE ( 'NONE', #219548, #28360 ) ;
#100865=VERTEX_POINT ( 'NONE', #25334 ) ;
#100911=CIRCLE ( 'NONE', #155177, 0.2000000000000057288 ) ;
#100950=CARTESIAN_POINT ( 'NONE',  ( 21.05000000000000071, 76.10000000001268461, -203.5231074845243597 ) ) ;
#100958=VERTEX_POINT ( 'NONE', #111277 ) ;
#101010=CARTESIAN_POINT ( 'NONE',  ( -20.99142135623731065, 64.40000000001249703, -176.9513107147999449 ) ) ;
#101016=DIRECTION ( 'NONE',  ( -1.000000000000000000, 3.265361837132813093E-16, 2.280189983783949500E-30 ) ) ;
#101023=VECTOR ( 'NONE', #110947, 1000.000000000000227 ) ;
#101027=DIRECTION ( 'NONE',  ( 1.000000000000000000, 0.000000000000000000, 0.000000000000000000 ) ) ;
#101031=CARTESIAN_POINT ( 'NONE',  ( -20.85000000000000142, 77.16412189325360771, -162.1082593989527254 ) ) ;
#101054=AXIS2_PLACEMENT_3D ( 'NONE', #38858, #115818, #37577 ) ;
#101058=ORIENTED_EDGE ( 'NONE', *, *, #105269, .T. ) ;
#101063=CARTESIAN_POINT ( 'NONE',  ( -20.94999999999999929, 87.65000000001266756, -200.5231074845242745 ) ) ;
#101090=TOROIDAL_SURFACE ( 'NONE', #92945, 0.2000000000000000111, 0.1000000000000000056 ) ;
#101145=VERTEX_POINT ( 'NONE', #215501 ) ;
#101146=ORIENTED_EDGE ( 'NONE', *, *, #207561, .T. ) ;
#101153=DIRECTION ( 'NONE',  ( 0.000000000000000000, 0.9893560106964510714, -0.1455152366551481502 ) ) ;
#101172=CIRCLE ( 'NONE', #230397, 11.80000000000000426 ) ;
#101184=AXIS2_PLACEMENT_3D ( 'NONE', #177087, #256534, #77943 ) ;
#101222=DIRECTION ( 'NONE',  ( 0.000000000000000000, -5.880418562633242623E-15, 1.000000000000000000 ) ) ;
#101236=CARTESIAN_POINT ( 'NONE',  ( 21.05000000000000071, 74.65091558138561822, -195.5366085209788878 ) ) ;
#101240=FACE_OUTER_BOUND ( 'NONE', #180256, .T. ) ;
#101270=TOROIDAL_SURFACE ( 'NONE', #72123, 0.2000000000000000111, 0.1000000000000000056 ) ;
#101288=DIRECTION ( 'NONE',  ( 0.000000000000000000, -0.4999999999999088507, 0.8660254037844913322 ) ) ;
#101335=AXIS2_PLACEMENT_3D ( 'NONE', #129061, #74253, #148635 ) ;
#101362=EDGE_LOOP ( 'NONE', ( #74731, #242556, #253527, #169615 ) ) ;
#101363=FACE_OUTER_BOUND ( 'NONE', #162571, .T. ) ;
#101381=CARTESIAN_POINT ( 'NONE',  ( -23.15000000000000213, 64.35000000001254250, -182.1731074845244507 ) ) ;
#101386=ORIENTED_EDGE ( 'NONE', *, *, #171852, .T. ) ;
#101394=ORIENTED_EDGE ( 'NONE', *, *, #189787, .T. ) ;
#101420=FACE_OUTER_BOUND ( 'NONE', #232348, .T. ) ;
#101468=FACE_OUTER_BOUND ( 'NONE', #71798, .T. ) ;
#101483=CARTESIAN_POINT ( 'NONE',  ( 23.14999999999999147, 80.15000000001268177, -203.5231074845243313 ) ) ;
#101491=CARTESIAN_POINT ( 'NONE',  ( -21.05000000000000071, 64.25000000001250555, -176.8647081744215370 ) ) ;
#101494=CIRCLE ( 'NONE', #5644, 0.09999999999999489853 ) ;
#101509=DIRECTION ( 'NONE',  ( -0.000000000000000000, 1.000000000000000000, 6.982962677686266711E-15 ) ) ;
#101523=EDGE_CURVE ( 'NONE', #228133, #161032, #35318, .T. ) ;
#101592=FACE_OUTER_BOUND ( 'NONE', #80140, .T. ) ;
#101612=CARTESIAN_POINT ( 'NONE',  ( 21.07964655665547227, 67.22511038503405700, -191.3011909015603749 ) ) ;
#101628=DIRECTION ( 'NONE',  ( 0.7071067811865474617, -0.7071067811865474617, -4.937700262164531476E-15 ) ) ;
#101688=FACE_OUTER_BOUND ( 'NONE', #50481, .T. ) ;
#101696=ORIENTED_EDGE ( 'NONE', *, *, #228286, .F. ) ;
#101705=DIRECTION ( 'NONE',  ( 0.000000000000000000, -6.467318590049456648E-15, 1.000000000000000000 ) ) ;
#101714=EDGE_CURVE ( 'NONE', #188196, #110731, #184838, .T. ) ;
#101748=ORIENTED_EDGE ( 'NONE', *, *, #208697, .T. ) ;
#101760=CARTESIAN_POINT ( 'NONE',  ( 18.59999999999999076, 65.79142135624982757, -178.8731074845244109 ) ) ;
#101788=CARTESIAN_POINT ( 'NONE',  ( -21.05000000000000071, 75.90220970870393558, -209.7809220950004772 ) ) ;
#101804=ORIENTED_EDGE ( 'NONE', *, *, #166583, .F. ) ;
#101823=AXIS2_PLACEMENT_3D ( 'NONE', #180696, #138953, #218498 ) ;
#101840=FACE_OUTER_BOUND ( 'NONE', #133879, .T. ) ;
#101854=CARTESIAN_POINT ( 'NONE',  ( 18.59999999999999076, 61.95000000001263629, -198.0094124137634708 ) ) ;
#101867=ADVANCED_FACE ( 'NONE', ( #85919 ), #93258, .T. ) ;
#101894=DIRECTION ( 'NONE',  ( 0.7071067811865475727, -0.7071067811865475727, -4.937700262164531476E-15 ) ) ;
#101962=CARTESIAN_POINT ( 'NONE',  ( -22.49072729836729678, 75.94351806727914322, -215.1731157336793103 ) ) ;
#101970=EDGE_CURVE ( 'NONE', #156620, #228338, #171951, .T. ) ;
#101998=ORIENTED_EDGE ( 'NONE', *, *, #27407, .F. ) ;
#102077=FACE_OUTER_BOUND ( 'NONE', #190337, .T. ) ;
#102087=ORIENTED_EDGE ( 'NONE', *, *, #127522, .T. ) ;
#102089=CARTESIAN_POINT ( 'NONE',  ( 20.94999999999999929, 87.48912529308852015, -173.0231074845243029 ) ) ;
#102100=ORIENTED_EDGE ( 'NONE', *, *, #171509, .F. ) ;
#102113=CARTESIAN_POINT ( 'NONE',  ( -23.25000000000000000, 77.14957036958807635, -162.2071950000224092 ) ) ;
#102115=FACE_OUTER_BOUND ( 'NONE', #251918, .T. ) ;
#102120=VERTEX_POINT ( 'NONE', #140468 ) ;
#102123=CYLINDRICAL_SURFACE ( 'NONE', #215543, 0.1000000000000106914 ) ;
#102127=DIRECTION ( 'NONE',  ( 0.000000000000000000, 0.4999999999999088507, 0.8660254037844913322 ) ) ;
#102133=CARTESIAN_POINT ( 'NONE',  ( -21.65000000000000213, 68.25000000001260503, -191.1731074845243938 ) ) ;
#102140=DIRECTION ( 'NONE',  ( 0.000000000000000000, 6.982962677686266711E-15, -1.000000000000000000 ) ) ;
#102141=DIRECTION ( 'NONE',  ( 1.000000000000000000, 0.000000000000000000, 0.000000000000000000 ) ) ;
#102146=DIRECTION ( 'NONE',  ( 1.000000000000000000, 0.000000000000000000, 0.000000000000000000 ) ) ;
#102164=ORIENTED_EDGE ( 'NONE', *, *, #201124, .F. ) ;
#102176=CARTESIAN_POINT ( 'NONE',  ( 18.49999999999996803, 68.92903212821357783, -166.2765432626560766 ) ) ;
#102259=VERTEX_POINT ( 'NONE', #50338 ) ;
#102293=ORIENTED_EDGE ( 'NONE', *, *, #236537, .F. ) ;
#102304=EDGE_CURVE ( 'NONE', #150964, #200908, #189142, .T. ) ;
#102328=CYLINDRICAL_SURFACE ( 'NONE', #77118, 0.09999999999998898659 ) ;
#102336=EDGE_CURVE ( 'NONE', #96257, #36482, #135123, .T. ) ;
#102341=EDGE_CURVE ( 'NONE', #118551, #133788, #197674, .T. ) ;
#102344=ORIENTED_EDGE ( 'NONE', *, *, #253384, .F. ) ;
#102354=CARTESIAN_POINT ( 'NONE',  ( 21.09546886439536451, 67.12144688699764572, -191.2860136339689632 ) ) ;
#102358=DIRECTION ( 'NONE',  ( 3.265361837132813093E-16, 1.000000000000000000, 6.982962677686266711E-15 ) ) ;
#102363=CARTESIAN_POINT ( 'NONE',  ( 19.90621891164687440, 64.25000000001250555, -178.6946622066474504 ) ) ;
#102423=CARTESIAN_POINT ( 'NONE',  ( 18.49999999999999645, 74.83729825007462466, -195.4231074845243654 ) ) ;
#102481=VECTOR ( 'NONE', #137155, 1000.000000000000000 ) ;
#102486=CARTESIAN_POINT ( 'NONE',  ( 22.46250603428203618, 75.97885582387397108, -215.1729705818644334 ) ) ;
#102497=VERTEX_POINT ( 'NONE', #245392 ) ;
#102583=CARTESIAN_POINT ( 'NONE',  ( -20.85000000000000142, 75.83895117929372987, -170.3072973288845731 ) ) ;
#102587=CARTESIAN_POINT ( 'NONE',  ( 21.05000000000000071, 87.75000000001247713, -173.1231074845242688 ) ) ;
#102604=ORIENTED_EDGE ( 'NONE', *, *, #207512, .T. ) ;
#102606=VERTEX_POINT ( 'NONE', #53601 ) ;
#102615=FACE_OUTER_BOUND ( 'NONE', #28022, .T. ) ;
#102649=CIRCLE ( 'NONE', #73504, 0.1000000000000028644 ) ;
#102657=CARTESIAN_POINT ( 'NONE',  ( -21.08134388332232589, 75.92418108250575415, -209.8577880650423140 ) ) ;
#102674=CARTESIAN_POINT ( 'NONE',  ( -22.59066674512268946, 64.25000000001267608, -203.5536116081548244 ) ) ;
#102741=CARTESIAN_POINT ( 'NONE',  ( 21.05000000000000071, 87.65000000001246860, -172.9231074845242802 ) ) ;
#102747=CARTESIAN_POINT ( 'NONE',  ( -23.15000000000000213, 85.00000000001261924, -193.6291383618718385 ) ) ;
#102794=AXIS2_PLACEMENT_3D ( 'NONE', #189964, #11323, #150830 ) ;
#102829=DIRECTION ( 'NONE',  ( 1.000000000000000000, 7.304098846218133681E-16, 5.311601492717083645E-30 ) ) ;
#102839=DIRECTION ( 'NONE',  ( 1.000000000000000000, 0.000000000000000000, 0.000000000000000000 ) ) ;
#102892=EDGE_CURVE ( 'NONE', #75446, #220769, #82115, .T. ) ;
#102896=LINE ( 'NONE', #127625, #90364 ) ;
#102948=CARTESIAN_POINT ( 'NONE',  ( 21.10642757222115407, 65.27684371085399562, -191.2824099607392156 ) ) ;
#102974=EDGE_CURVE ( 'NONE', #152549, #50255, #252032, .T. ) ;
#102978=EDGE_CURVE ( 'NONE', #196419, #191888, #130244, .T. ) ;
#102979=CARTESIAN_POINT ( 'NONE',  ( -18.59999999999999787, 66.65000000001259650, -191.1731074845244223 ) ) ;
#103012=EDGE_CURVE ( 'NONE', #177267, #50255, #171997, .T. ) ;
#103043=FACE_OUTER_BOUND ( 'NONE', #253712, .T. ) ;
#103048=ORIENTED_EDGE ( 'NONE', *, *, #132873, .F. ) ;
#103094=ORIENTED_EDGE ( 'NONE', *, *, #140030, .T. ) ;
#103108=CARTESIAN_POINT ( 'NONE',  ( -21.05000000000000071, 76.00000000001244871, -170.0231074845243597 ) ) ;
#103109=CARTESIAN_POINT ( 'NONE',  ( -22.39999999999999858, 76.00000000001267608, -203.5231074845243597 ) ) ;
#103134=EDGE_CURVE ( 'NONE', #75338, #71516, #77966, .T. ) ;
#103156=CARTESIAN_POINT ( 'NONE',  ( 20.12500000000000000, 66.25000000001263345, -195.4113362024101548 ) ) ;
#103167=DIRECTION ( 'NONE',  ( -1.000000000000000000, 0.000000000000000000, -0.000000000000000000 ) ) ;
#103194=ORIENTED_EDGE ( 'NONE', *, *, #103134, .T. ) ;
#103218=CARTESIAN_POINT ( 'NONE',  ( 23.14999999999999503, 64.25000000001276135, -215.2731074845244450 ) ) ;
#103250=AXIS2_PLACEMENT_3D ( 'NONE', #214769, #59516, #38716 ) ;
#103253=CARTESIAN_POINT ( 'NONE',  ( -22.50000000000000000, 75.90736249940329117, -215.1728046915651191 ) ) ;
#103254=VECTOR ( 'NONE', #14884, 1000.000000000000114 ) ;
#103276=CIRCLE ( 'NONE', #149104, 4.099999999999992539 ) ;
#103299=VECTOR ( 'NONE', #216312, 1000.000000000000000 ) ;
#103301=ORIENTED_EDGE ( 'NONE', *, *, #74356, .T. ) ;
#103402=DIRECTION ( 'NONE',  ( 0.000000000000000000, 0.000000000000000000, 1.000000000000000000 ) ) ;
#103448=CARTESIAN_POINT ( 'NONE',  ( -21.29999999999995808, 76.00000000001267608, -203.5231074845243597 ) ) ;
#103467=ORIENTED_EDGE ( 'NONE', *, *, #171295, .T. ) ;
#103474=DIRECTION ( 'NONE',  ( -1.000000000000000000, -0.000000000000000000, -0.000000000000000000 ) ) ;
#103508=ORIENTED_EDGE ( 'NONE', *, *, #93607, .T. ) ;
#103510=AXIS2_PLACEMENT_3D ( 'NONE', #23985, #185606, #6962 ) ;
#103515=AXIS2_PLACEMENT_3D ( 'NONE', #10268, #109333, #11557 ) ;
#103544=EDGE_LOOP ( 'NONE', ( #121661, #204294, #252989, #235574 ) ) ;
#103576=ADVANCED_FACE ( 'NONE', ( #253725 ), #38551, .T. ) ;
#103594=EDGE_CURVE ( 'NONE', #52949, #178394, #197655, .T. ) ;
#103600=ORIENTED_EDGE ( 'NONE', *, *, #43173, .T. ) ;
#103617=AXIS2_PLACEMENT_3D ( 'NONE', #50969, #174849, #130526 ) ;
#103622=CARTESIAN_POINT ( 'NONE',  ( 20.21494484322215968, 66.69682926214377972, -195.1828422927512179 ) ) ;
#103651=CARTESIAN_POINT ( 'NONE',  ( -22.50047199487871197, 75.95509394808482284, -215.2731549034355680 ) ) ;
#103711=AXIS2_PLACEMENT_3D ( 'NONE', #246681, #249272, #107172 ) ;
#103747=CARTESIAN_POINT ( 'NONE',  ( -21.13614978966382196, 69.50089529817890366, -203.5231074845243882 ) ) ;
#103758=CIRCLE ( 'NONE', #132846, 0.5000000000000004441 ) ;
#103787=ORIENTED_EDGE ( 'NONE', *, *, #208715, .F. ) ;
#103799=AXIS2_PLACEMENT_3D ( 'NONE', #155270, #233507, #234768 ) ;
#103833=VECTOR ( 'NONE', #52468, 1000.000000000000000 ) ;
#103853=ORIENTED_EDGE ( 'NONE', *, *, #174835, .F. ) ;
#103860=VERTEX_POINT ( 'NONE', #87917 ) ;
#103881=CIRCLE ( 'NONE', #253731, 0.5000000000000004441 ) ;
#103917=ORIENTED_EDGE ( 'NONE', *, *, #87905, .T. ) ;
#103929=AXIS2_PLACEMENT_3D ( 'NONE', #52895, #152030, #132441 ) ;
#103931=ORIENTED_EDGE ( 'NONE', *, *, #212427, .T. ) ;
#103971=SPHERICAL_SURFACE ( 'NONE', #43441, 0.1000000000000000056 ) ;
#103999=CARTESIAN_POINT ( 'NONE',  ( 23.24999999999999289, 64.35000000001258513, -191.3731074845244393 ) ) ;
#104022=CIRCLE ( 'NONE', #137350, 0.09999999999999939493 ) ;
#104077=CARTESIAN_POINT ( 'NONE',  ( -20.64999999999999858, 85.50000000001261924, -193.6291383618718385 ) ) ;
#104110=CARTESIAN_POINT ( 'NONE',  ( 21.04999999999999716, 65.31569084252754465, -195.9964106941975786 ) ) ;
#104123=DIRECTION ( 'NONE',  ( -1.000000000000000000, 0.000000000000000000, 0.000000000000000000 ) ) ;
#104176=DIRECTION ( 'NONE',  ( 1.000000000000000000, 7.304098846218135653E-16, 5.311601492717085047E-30 ) ) ;
#104203=DIRECTION ( 'NONE',  ( 1.000000000000000000, 0.000000000000000000, 0.000000000000000000 ) ) ;
#104210=CIRCLE ( 'NONE', #208285, 0.09999999999998898659 ) ;
#104211=VERTEX_POINT ( 'NONE', #30936 ) ;
#104220=ORIENTED_EDGE ( 'NONE', *, *, #135608, .T. ) ;
#104223=CARTESIAN_POINT ( 'NONE',  ( -21.05000000000000071, 64.25000000001249134, -177.0379132551784096 ) ) ;
#104235=CARTESIAN_POINT ( 'NONE',  ( 21.05000000000000071, 67.12338541492553645, -195.1380270056797599 ) ) ;
#104240=ORIENTED_EDGE ( 'NONE', *, *, #200378, .T. ) ;
#104276=VERTEX_POINT ( 'NONE', #77708 ) ;
#104307=TOROIDAL_SURFACE ( 'NONE', #29360, 0.2000000000000000111, 0.1000000000000000056 ) ;
#104310=DIRECTION ( 'NONE',  ( 0.000000000000000000, -1.000000000000000000, -6.982962677686265922E-15 ) ) ;
#104331=CARTESIAN_POINT ( 'NONE',  ( 20.94999999999999929, 67.07338541492552508, -195.0514244653012952 ) ) ;
#104371=ORIENTED_EDGE ( 'NONE', *, *, #30050, .F. ) ;
#104374=DIRECTION ( 'NONE',  ( -0.000000000000000000, -0.1350103645451835865, -0.9908441862701606873 ) ) ;
#104385=DIRECTION ( 'NONE',  ( 1.000000000000000000, 0.000000000000000000, 0.000000000000000000 ) ) ;
#104389=EDGE_CURVE ( 'NONE', #98885, #172803, #227070, .T. ) ;
#104409=CARTESIAN_POINT ( 'NONE',  ( -21.05000000000000071, 77.25000000001263345, -195.5231074845243313 ) ) ;
#104420=DIRECTION ( 'NONE',  ( 0.000000000000000000, 6.982962677686266711E-15, -1.000000000000000000 ) ) ;
#104432=LINE ( 'NONE', #1496, #37432 ) ;
#104442=DIRECTION ( 'NONE',  ( 0.000000000000000000, 7.026728003956695223E-15, -1.000000000000000000 ) ) ;
#104478=CARTESIAN_POINT ( 'NONE',  ( 21.05000000000000071, 76.00000000001267608, -203.5231074845243597 ) ) ;
#104495=DIRECTION ( 'NONE',  ( 1.000000000000000000, 0.000000000000000000, 0.000000000000000000 ) ) ;
#104516=ORIENTED_EDGE ( 'NONE', *, *, #77976, .T. ) ;
#104517=AXIS2_PLACEMENT_3D ( 'NONE', #66374, #22133, #162928 ) ;
#104519=LINE ( 'NONE', #26310, #209128 ) ;
#104565=CARTESIAN_POINT ( 'NONE',  ( -18.59999999999999787, 64.35000000001259934, -191.3731074845244393 ) ) ;
#104614=ORIENTED_EDGE ( 'NONE', *, *, #112946, .F. ) ;
#104644=EDGE_CURVE ( 'NONE', #132574, #236269, #167905, .T. ) ;
#104647=EDGE_LOOP ( 'NONE', ( #15858, #167920, #229473, #228562 ) ) ;
#104682=CARTESIAN_POINT ( 'NONE',  ( 20.94999999999999574, 62.00000000001264056, -198.0960149541419071 ) ) ;
#104687=CARTESIAN_POINT ( 'NONE',  ( -20.64999999999999858, 76.00000000001244871, -170.0231074845243597 ) ) ;
#104746=AXIS2_PLACEMENT_3D ( 'NONE', #189120, #10491, #90005 ) ;
#104754=VERTEX_POINT ( 'NONE', #66854 ) ;
#104794=FACE_OUTER_BOUND ( 'NONE', #54879, .T. ) ;
#104798=DIRECTION ( 'NONE',  ( 0.000000000000000000, 6.982962677686266711E-15, -1.000000000000000000 ) ) ;
#104800=FACE_OUTER_BOUND ( 'NONE', #105112, .T. ) ;
#104837=ORIENTED_EDGE ( 'NONE', *, *, #221272, .F. ) ;
#104840=EDGE_LOOP ( 'NONE', ( #120643, #26596, #46637, #66026 ) ) ;
#104875=AXIS2_PLACEMENT_3D ( 'NONE', #238520, #63734, #239824 ) ;
#104891=CARTESIAN_POINT ( 'NONE',  ( 20.11144452914042802, 66.06638914889266800, -195.6328140305747070 ) ) ;
#104903=DIRECTION ( 'NONE',  ( 0.000000000000000000, -0.8700118002898357128, 0.4930308989875171188 ) ) ;
#104947=( BOUNDED_SURFACE ( )  B_SPLINE_SURFACE ( 3, 2, ( 
 ( #130875, #111329, #151759 ),
 ( #193443, #14818, #167471 ),
 ( #147889, #179038, #76040 ),
 ( #255910, #219390, #59011 ),
 ( #348, #16099, #40803 ),
 ( #35669, #99436, #253394 ) ),
 .UNSPECIFIED., .F., .F., .F. ) 
 B_SPLINE_SURFACE_WITH_KNOTS ( ( 4, 2, 4 ),
 ( 3, 3 ),
 ( -1.776356839400250465E-15, 0.7853981633974468357, 1.570796326794895448 ),
 ( 0.000000000000000000, 1.000000000000000000 ),
 .UNSPECIFIED. ) 
 GEOMETRIC_REPRESENTATION_ITEM ( )  RATIONAL_B_SPLINE_SURFACE ( (
 ( 1.000000000000000000, 0.5000000000000456302, 1.000000000000000000),
 ( 1.000000000000000000, 0.4993418825340405487, 1.000000000000000000),
 ( 1.000000000000000000, 0.5278258667052666553, 1.000000000000000000),
 ( 1.000000000000000000, 0.6092287576700228247, 1.000000000000000000),
 ( 1.000000000000000000, 0.6611148371775413812, 1.000000000000000000),
 ( 1.000000000000000000, 0.7071067811865597852, 1.000000000000000000) ) ) 
 REPRESENTATION_ITEM ( '' )  SURFACE ( )  );
#104973=DIRECTION ( 'NONE',  ( 0.000000000000000000, 6.982962677686266711E-15, -1.000000000000000000 ) ) ;
#105003=CARTESIAN_POINT ( 'NONE',  ( 21.14999999999999858, 69.74218538953655866, -203.6208977758331855 ) ) ;
#105014=CARTESIAN_POINT ( 'NONE',  ( -21.12230431290519306, 69.54243334671967602, -203.5283173362134335 ) ) ;
#105039=EDGE_CURVE ( 'NONE', #198292, #57380, #36750, .T. ) ;
#105041=CARTESIAN_POINT ( 'NONE',  ( -23.15000000000000213, 74.00000000001254818, -182.6477294072865050 ) ) ;
#105054=DIRECTION ( 'NONE',  ( -1.000000000000000000, 0.000000000000000000, 0.000000000000000000 ) ) ;
#105094=EDGE_LOOP ( 'NONE', ( #180488, #35342, #120603, #178698, #24 ) ) ;
#105097=EDGE_CURVE ( 'NONE', #257555, #101145, #108284, .T. ) ;
#105098=AXIS2_PLACEMENT_3D ( 'NONE', #117873, #18774, #134850 ) ;
#105112=EDGE_LOOP ( 'NONE', ( #215090, #198232, #67796, #200619 ) ) ;
#105115=CARTESIAN_POINT ( 'NONE',  ( -21.04999999999999716, 85.60000000001264198, -196.4910380878246201 ) ) ;
#105136=FACE_OUTER_BOUND ( 'NONE', #255950, .T. ) ;
#105168=CARTESIAN_POINT ( 'NONE',  ( 18.59999999999999076, 64.35000000001275566, -215.2731074845244450 ) ) ;
#105180=ORIENTED_EDGE ( 'NONE', *, *, #80419, .F. ) ;
#105269=EDGE_CURVE ( 'NONE', #129083, #118551, #19340, .T. ) ;
#105273=CIRCLE ( 'NONE', #26800, 0.09999999999998898659 ) ;
#105278=ORIENTED_EDGE ( 'NONE', *, *, #30494, .F. ) ;
#105282=EDGE_LOOP ( 'NONE', ( #254975, #56672, #228712, #152880 ) ) ;
#105283=CARTESIAN_POINT ( 'NONE',  ( 20.94999999999999929, 69.35000000001262777, -193.5060803140843859 ) ) ;
#105284=DIRECTION ( 'NONE',  ( -1.000000000000000000, 0.000000000000000000, 0.000000000000000000 ) ) ;
#105286=DIRECTION ( 'NONE',  ( -0.000000000000000000, -6.982962677686266711E-15, 1.000000000000000000 ) ) ;
#105292=CIRCLE ( 'NONE', #26243, 7.720710678118663850 ) ;
#105310=DIRECTION ( 'NONE',  ( -0.000000000000000000, 1.000000000000000000, 6.982962677686266711E-15 ) ) ;
#105316=CARTESIAN_POINT ( 'NONE',  ( -23.25000000000000000, 87.65000000001246860, -173.1231074845242688 ) ) ;
#105327=DIRECTION ( 'NONE',  ( 0.000000000000000000, 1.000000000000000000, 6.982962677686266711E-15 ) ) ;
#105328=ADVANCED_FACE ( 'NONE', ( #229481 ), #129093, .T. ) ;
#105332=EDGE_CURVE ( 'NONE', #197918, #76140, #190367, .T. ) ;
#105394=ORIENTED_EDGE ( 'NONE', *, *, #198640, .F. ) ;
#105404=EDGE_CURVE ( 'NONE', #184335, #99738, #119479, .T. ) ;
#105419=CARTESIAN_POINT ( 'NONE',  ( -20.85000000000000142, 65.66751761918720831, -164.4282609406112670 ) ) ;
#105425=VERTEX_POINT ( 'NONE', #213755 ) ;
#105427=LINE ( 'NONE', #65054, #130029 ) ;
#105444=VERTEX_POINT ( 'NONE', #76807 ) ;
#105450=AXIS2_PLACEMENT_3D ( 'NONE', #86930, #46529, #145632 ) ;
#105454=CARTESIAN_POINT ( 'NONE',  ( 21.05000000000000071, 76.00000000001267608, -203.5231074845243597 ) ) ;
#105459=LINE ( 'NONE', #226717, #186294 ) ;
#105473=ADVANCED_FACE ( 'NONE', ( #75559 ), #160996, .T. ) ;
#105519=VERTEX_POINT ( 'NONE', #108882 ) ;
#105520=DIRECTION ( 'NONE',  ( 0.000000000000000000, -1.000000000000000000, -6.352154140967427193E-15 ) ) ;
#105530=CARTESIAN_POINT ( 'NONE',  ( 20.04142135623730070, 64.25000000001277556, -215.2731074845244450 ) ) ;
#105626=ORIENTED_EDGE ( 'NONE', *, *, #167753, .F. ) ;
#105640=ORIENTED_EDGE ( 'NONE', *, *, #216804, .T. ) ;
#105699=DIRECTION ( 'NONE',  ( 0.000000000000000000, 0.000000000000000000, 1.000000000000000000 ) ) ;
#105705=CARTESIAN_POINT ( 'NONE',  ( -20.64999999999999858, 85.00000000001251976, -179.5170766071767332 ) ) ;
#105713=DIRECTION ( 'NONE',  ( -0.000000000000000000, -6.982962677686266711E-15, 1.000000000000000000 ) ) ;
#105749=FACE_OUTER_BOUND ( 'NONE', #166929, .T. ) ;
#105756=AXIS2_PLACEMENT_3D ( 'NONE', #213012, #73541, #119063 ) ;
#105781=ORIENTED_EDGE ( 'NONE', *, *, #36188, .F. ) ;
#105787=ADVANCED_FACE ( 'NONE', ( #1762 ), #18765, .T. ) ;
#105864=ADVANCED_FACE ( 'NONE', ( #123022 ), #219600, .F. ) ;
#105865=CARTESIAN_POINT ( 'NONE',  ( 21.05000000000000071, 76.10000000001272724, -210.0637644362255969 ) ) ;
#105885=ORIENTED_EDGE ( 'NONE', *, *, #35919, .F. ) ;
#105902=VERTEX_POINT ( 'NONE', #87717 ) ;
#105951=AXIS2_PLACEMENT_3D ( 'NONE', #217508, #98826, #83109 ) ;
#105969=CARTESIAN_POINT ( 'NONE',  ( -18.50000000000000000, 85.40000000001263913, -196.2258477248610120 ) ) ;
#105991=VECTOR ( 'NONE', #250959, 1000.000000000000000 ) ;
#106005=DIRECTION ( 'NONE',  ( -1.000000000000000000, 0.000000000000000000, -0.000000000000000000 ) ) ;
#106020=DIRECTION ( 'NONE',  ( 0.000000000000000000, 6.982962677686266711E-15, -1.000000000000000000 ) ) ;
#106025=AXIS2_PLACEMENT_3D ( 'NONE', #60275, #21194, #61575 ) ;
#106034=ADVANCED_FACE ( 'NONE', ( #248089 ), #55005, .T. ) ;
#106059=ORIENTED_EDGE ( 'NONE', *, *, #75462, .T. ) ;
#106072=AXIS2_PLACEMENT_3D ( 'NONE', #15196, #132570, #94710 ) ;
#106108=DIRECTION ( 'NONE',  ( -1.000000000000000000, 0.000000000000000000, -0.000000000000000000 ) ) ;
#106143=DIRECTION ( 'NONE',  ( 1.000000000000000000, 0.000000000000000000, 0.000000000000000000 ) ) ;
#106148=ORIENTED_EDGE ( 'NONE', *, *, #162096, .T. ) ;
#106149=CARTESIAN_POINT ( 'NONE',  ( 23.15000000000000213, 84.59626168225550202, -179.4732350016745954 ) ) ;
#106206=CARTESIAN_POINT ( 'NONE',  ( -18.59999999999999787, 102.4393534156134962, -185.3815988770167280 ) ) ;
#106209=ORIENTED_EDGE ( 'NONE', *, *, #174879, .F. ) ;
#106222=AXIS2_PLACEMENT_3D ( 'NONE', #105003, #45080, #123342 ) ;
#106223=ADVANCED_FACE ( 'NONE', ( #234963 ), #135836, .T. ) ;
#106248=CARTESIAN_POINT ( 'NONE',  ( -22.47071067811865319, 68.27992525551462677, -203.6221999392270448 ) ) ;
#106260=ORIENTED_EDGE ( 'NONE', *, *, #66953, .T. ) ;
#106310=AXIS2_PLACEMENT_3D ( 'NONE', #199625, #41837, #62668 ) ;
#106330=ORIENTED_EDGE ( 'NONE', *, *, #161012, .F. ) ;
#106342=EDGE_LOOP ( 'NONE', ( #103787, #231276, #1893, #257711 ) ) ;
#106345=ADVANCED_FACE ( 'NONE', ( #190411 ), #191708, .F. ) ;
#106369=ADVANCED_FACE ( 'NONE', ( #108293 ), #73049, .F. ) ;
#106405=AXIS2_PLACEMENT_3D ( 'NONE', #200004, #106005, #86435 ) ;
#106475=CARTESIAN_POINT ( 'NONE',  ( -23.15000000000000213, 74.00000000001259082, -190.7984855617622770 ) ) ;
#106494=VECTOR ( 'NONE', #145335, 1000.000000000000000 ) ;
#106504=CARTESIAN_POINT ( 'NONE',  ( -21.05000000000000071, 87.65000000001246860, -173.0231074845243029 ) ) ;
#106511=DIRECTION ( 'NONE',  ( 0.000000000000000000, 6.982962677686266711E-15, -1.000000000000000000 ) ) ;
#106570=CIRCLE ( 'NONE', #135800, 0.09999999999998712696 ) ;
#106612=VERTEX_POINT ( 'NONE', #45435 ) ;
#106620=ORIENTED_EDGE ( 'NONE', *, *, #81549, .F. ) ;
#106635=FACE_BOUND ( 'NONE', #207693, .T. ) ;
#106679=CARTESIAN_POINT ( 'NONE',  ( -21.05000000000253024, 75.94867256767116714, -209.8232908208007927 ) ) ;
#106680=CARTESIAN_POINT ( 'NONE',  ( -20.64999999999999858, 76.00000000001244871, -170.0231074845243597 ) ) ;
#106705=AXIS2_PLACEMENT_3D ( 'NONE', #180065, #87022, #148311 ) ;
#106719=DIRECTION ( 'NONE',  ( 0.000000000000000000, 0.000000000000000000, -1.000000000000000000 ) ) ;
#106724=FACE_OUTER_BOUND ( 'NONE', #94143, .T. ) ;
#106736=AXIS2_PLACEMENT_3D ( 'NONE', #21683, #101153, #201583 ) ;
#106770=VERTEX_POINT ( 'NONE', #97356 ) ;
#106772=TOROIDAL_SURFACE ( 'NONE', #114973, 2.100000000000002309, 0.1000000000000000056 ) ;
#106778=EDGE_CURVE ( 'NONE', #188810, #249694, #16003, .T. ) ;
#106797=CARTESIAN_POINT ( 'NONE',  ( -20.93284271247462058, 64.25000000001250555, -177.0379132551783812 ) ) ;
#106816=CYLINDRICAL_SURFACE ( 'NONE', #208822, 0.09999999999999939493 ) ;
#106848=CARTESIAN_POINT ( 'NONE',  ( -23.25000000000000000, 87.65000000001276703, -215.2731074845242745 ) ) ;
#106869=ORIENTED_EDGE ( 'NONE', *, *, #204550, .F. ) ;
#106883=VERTEX_POINT ( 'NONE', #40025 ) ;
#106888=ORIENTED_EDGE ( 'NONE', *, *, #61373, .T. ) ;
#106935=ORIENTED_EDGE ( 'NONE', *, *, #81642, .F. ) ;
#106943=CARTESIAN_POINT ( 'NONE',  ( 18.40000000000000213, 85.50000000001264766, -196.5237453873441495 ) ) ;
#106950=ORIENTED_EDGE ( 'NONE', *, *, #151462, .T. ) ;
#106966=FACE_OUTER_BOUND ( 'NONE', #47481, .T. ) ;
#106968=CARTESIAN_POINT ( 'NONE',  ( 18.49999999999999289, 64.35000000001245724, -170.0231074845244166 ) ) ;
#106973=DIRECTION ( 'NONE',  ( -1.000000000000000000, 1.836970198721029934E-16, 1.282749433769087757E-30 ) ) ;
#106997=EDGE_CURVE ( 'NONE', #200607, #251965, #174432, .T. ) ;
#107042=AXIS2_PLACEMENT_3D ( 'NONE', #82147, #85996, #161745 ) ;
#107056=LINE ( 'NONE', #169659, #138130 ) ;
#107076=DIRECTION ( 'NONE',  ( 1.000000000000000000, 0.000000000000000000, 0.000000000000000000 ) ) ;
#107123=CARTESIAN_POINT ( 'NONE',  ( -22.49510344025093644, 75.93287232181852175, -215.1730775896386376 ) ) ;
#107133=ORIENTED_EDGE ( 'NONE', *, *, #73539, .T. ) ;
#107138=EDGE_CURVE ( 'NONE', #46518, #153680, #29743, .T. ) ;
#107172=DIRECTION ( 'NONE',  ( -1.000000000000000000, 0.000000000000000000, 0.000000000000000000 ) ) ;
#107227=ORIENTED_EDGE ( 'NONE', *, *, #204716, .F. ) ;
#107228=AXIS2_PLACEMENT_3D ( 'NONE', #203408, #3918, #19638 ) ;
#107229=CARTESIAN_POINT ( 'NONE',  ( -21.14999999999999858, 69.45934304831143891, -203.5231074845243882 ) ) ;
#107260=ORIENTED_EDGE ( 'NONE', *, *, #226161, .F. ) ;
#107267=EDGE_CURVE ( 'NONE', #137660, #210729, #108406, .T. ) ;
#107268=FACE_OUTER_BOUND ( 'NONE', #22300, .T. ) ;
#107308=CARTESIAN_POINT ( 'NONE',  ( -20.64999999999999858, 68.85000000001254250, -182.2731074845244166 ) ) ;
#107320=ADVANCED_FACE ( 'NONE', ( #87461 ), #166689, .T. ) ;
#107321=DIRECTION ( 'NONE',  ( -0.7071067811865127117, -0.7071067811865821007, 0.000000000000000000 ) ) ;
#107326=DIRECTION ( 'NONE',  ( 1.000000000000000000, 0.000000000000000000, 0.000000000000000000 ) ) ;
#107348=DIRECTION ( 'NONE',  ( 0.000000000000000000, -5.551115123125777653E-14, 1.000000000000000000 ) ) ;
#107358=ADVANCED_FACE ( 'NONE', ( #256616 ), #137993, .T. ) ;
#107371=ORIENTED_EDGE ( 'NONE', *, *, #87429, .T. ) ;
#107411=VERTEX_POINT ( 'NONE', #3621 ) ;
#107417=AXIS2_PLACEMENT_3D ( 'NONE', #146354, #6860, #225873 ) ;
#107426=DIRECTION ( 'NONE',  ( -4.336808689942052446E-15, 0.8660254037844445918, 0.4999999999999896194 ) ) ;
#107435=ORIENTED_EDGE ( 'NONE', *, *, #66223, .T. ) ;
#107453=DIRECTION ( 'NONE',  ( -4.408576920032447355E-17, -0.1350103645451945777, 0.9908441862701589109 ) ) ;
#107454=ADVANCED_FACE ( 'NONE', ( #177175 ), #33463, .T. ) ;
#107457=ORIENTED_EDGE ( 'NONE', *, *, #115990, .T. ) ;
#107493=CARTESIAN_POINT ( 'NONE',  ( -18.59999999999999787, 77.83585931145600512, -158.5186683157258187 ) ) ;
#107501=CIRCLE ( 'NONE', #161708, 4.000000000000003553 ) ;
#107511=ORIENTED_EDGE ( 'NONE', *, *, #18643, .F. ) ;
#107529=DIRECTION ( 'NONE',  ( 0.000000000000000000, -1.000000000000000000, -7.272083257015735086E-15 ) ) ;
#107553=ORIENTED_EDGE ( 'NONE', *, *, #79299, .F. ) ;
#107578=CARTESIAN_POINT ( 'NONE',  ( -20.89192007715128341, 65.67101464000555211, -164.4404391622479977 ) ) ;
#107594=DIRECTION ( 'NONE',  ( -4.408576920032448588E-17, -0.1350103645451807832, -0.9908441862701610203 ) ) ;
#107631=ORIENTED_EDGE ( 'NONE', *, *, #34969, .F. ) ;
#107641=CIRCLE ( 'NONE', #224358, 0.09999999999999459321 ) ;
#107652=DIRECTION ( 'NONE',  ( -0.000000000000000000, 1.000000000000000000, 6.982962677686267499E-15 ) ) ;
#107657=CARTESIAN_POINT ( 'NONE',  ( 18.60000000000000142, 85.32100840337392356, -196.2871692354463846 ) ) ;
#107662=CARTESIAN_POINT ( 'NONE',  ( -18.50000000000000000, 77.36242903720570041, -162.1342262366031548 ) ) ;
#107674=EDGE_LOOP ( 'NONE', ( #131521, #2448, #222305 ) ) ;
#107737=DIRECTION ( 'NONE',  ( 0.000000000000000000, 0.8660254037844424824, 0.4999999999999934497 ) ) ;
#107758=ORIENTED_EDGE ( 'NONE', *, *, #56276, .F. ) ;
#107762=CIRCLE ( 'NONE', #166636, 0.09999999999998898659 ) ;
#107772=VECTOR ( 'NONE', #172241, 1000.000000000000114 ) ;
#107829=DIRECTION ( 'NONE',  ( 2.259780016855445309E-14, -0.9875055080513764905, 0.1575844902526679359 ) ) ;
#107966=AXIS2_PLACEMENT_3D ( 'NONE', #93848, #173453, #252919 ) ;
#107990=FACE_OUTER_BOUND ( 'NONE', #170706, .T. ) ;
#108005=FACE_OUTER_BOUND ( 'NONE', #248829, .T. ) ;
#108065=CARTESIAN_POINT ( 'NONE',  ( -23.15000000000000213, 76.00000000001267608, -203.5231074845243597 ) ) ;
#108066=CARTESIAN_POINT ( 'NONE',  ( 23.14999999999999858, 79.90000000001244018, -170.0231074845243313 ) ) ;
#108068=CARTESIAN_POINT ( 'NONE',  ( 18.49999999999999645, 77.63717271298298783, -191.9409541190523214 ) ) ;
#108081=FACE_OUTER_BOUND ( 'NONE', #91525, .T. ) ;
#108111=ORIENTED_EDGE ( 'NONE', *, *, #55615, .T. ) ;
#108143=CARTESIAN_POINT ( 'NONE',  ( 21.22070241538126467, 75.90108096947770377, -209.9930537573939660 ) ) ;
#108150=CARTESIAN_POINT ( 'NONE',  ( -18.59999999999999787, 64.35000000001264198, -196.5083017138704236 ) ) ;
#108151=CARTESIAN_POINT ( 'NONE',  ( -20.64999999999999858, 84.73084112150795022, -193.9250327655399531 ) ) ;
#108157=DIRECTION ( 'NONE',  ( 0.000000000000000000, 0.000000000000000000, 1.000000000000000000 ) ) ;
#108178=VERTEX_POINT ( 'NONE', #253560 ) ;
#108179=ADVANCED_FACE ( 'NONE', ( #155789 ), #177906, .T. ) ;
#108183=DIRECTION ( 'NONE',  ( 0.000000000000000000, -0.8660254037844468122, -0.4999999999999859557 ) ) ;
#108185=ORIENTED_EDGE ( 'NONE', *, *, #242993, .T. ) ;
#108188=LINE ( 'NONE', #32532, #218320 ) ;
#108215=CARTESIAN_POINT ( 'NONE',  ( 20.95263205890715952, 67.10425989211856290, -195.0335990775828066 ) ) ;
#108267=CARTESIAN_POINT ( 'NONE',  ( 20.94999999999999574, 87.39257802171833589, -200.4491579046923277 ) ) ;
#108284=B_SPLINE_CURVE_WITH_KNOTS ( 'NONE', 3,
 ( #137097, #195815, #17171, #96648, #236191, #255712, #77120 ),
 .UNSPECIFIED., .F., .F.,
 ( 4, 3, 4 ),
 ( 0.000000000000000000, 1.860045280646148997E-05, 5.251155757305322482E-05 ),
 .UNSPECIFIED. ) ;
#108293=FACE_OUTER_BOUND ( 'NONE', #138942, .T. ) ;
#108304=DIRECTION ( 'NONE',  ( 0.000000000000000000, 0.000000000000000000, 1.000000000000000000 ) ) ;
#108315=CARTESIAN_POINT ( 'NONE',  ( 23.14999999999999503, 69.35000000001259934, -191.2731074845243882 ) ) ;
#108351=CARTESIAN_POINT ( 'NONE',  ( 18.59999999999999076, 65.79142135624984178, -182.1731074845244223 ) ) ;
#108372=DIRECTION ( 'NONE',  ( 1.000000000000000000, 0.000000000000000000, 0.000000000000000000 ) ) ;
#108386=LINE ( 'NONE', #210063, #101023 ) ;
#108401=EDGE_LOOP ( 'NONE', ( #78683, #88436, #134524, #100232 ) ) ;
#108406=CIRCLE ( 'NONE', #245767, 11.74999999999999645 ) ;
#108410=ORIENTED_EDGE ( 'NONE', *, *, #207947, .F. ) ;
#108416=AXIS2_PLACEMENT_3D ( 'NONE', #141598, #257633, #79032 ) ;
#108422=ORIENTED_EDGE ( 'NONE', *, *, #56948, .T. ) ;
#108507=CARTESIAN_POINT ( 'NONE',  ( -18.59999999999999787, 76.00000000001239187, -162.1231074845243825 ) ) ;
#108517=CARTESIAN_POINT ( 'NONE',  ( -21.05000000000000071, 69.52192177891770086, -203.4231075492199352 ) ) ;
#108533=CARTESIAN_POINT ( 'NONE',  ( 23.24999999999999645, 70.40000000001276703, -215.2731074845243882 ) ) ;
#108541=ORIENTED_EDGE ( 'NONE', *, *, #237600, .T. ) ;
#108566=ADVANCED_FACE ( 'NONE', ( #58582 ), #14694, .T. ) ;
#108599=CARTESIAN_POINT ( 'NONE',  ( 18.57071067811864040, 65.82071067813119214, -182.2731074845244450 ) ) ;
#108618=CARTESIAN_POINT ( 'NONE',  ( 18.59999999999999076, 65.79142135624984178, -182.1731074845244223 ) ) ;
#108652=CARTESIAN_POINT ( 'NONE',  ( 18.59999999999999076, 77.83585931145600512, -158.4186683157258244 ) ) ;
#108683=DIRECTION ( 'NONE',  ( 0.000000000000000000, 0.000000000000000000, -1.000000000000000000 ) ) ;
#108691=CARTESIAN_POINT ( 'NONE',  ( -18.58222699835055280, 65.66799936921584901, -164.4299399888601272 ) ) ;
#108692=AXIS2_PLACEMENT_3D ( 'NONE', #144889, #163198, #86186 ) ;
#108696=CIRCLE ( 'NONE', #171096, 7.800000000000001599 ) ;
#108697=ORIENTED_EDGE ( 'NONE', *, *, #161702, .F. ) ;
#108715=FACE_OUTER_BOUND ( 'NONE', #138886, .T. ) ;
#108758=CARTESIAN_POINT ( 'NONE',  ( 21.30740335185486245, 69.44334207798469549, -203.6220420103002766 ) ) ;
#108778=EDGE_CURVE ( 'NONE', #221154, #186763, #11400, .T. ) ;
#108797=ADVANCED_FACE ( 'NONE', ( #90999 ), #170597, .T. ) ;
#108829=EDGE_CURVE ( 'NONE', #145161, #47017, #230524, .T. ) ;
#108882=CARTESIAN_POINT ( 'NONE',  ( -20.64999999999999858, 71.75000000001253397, -182.3731074845244109 ) ) ;
#108908=CARTESIAN_POINT ( 'NONE',  ( -18.50000000000000000, 85.40000000001241176, -163.1410656363516125 ) ) ;
#108925=AXIS2_PLACEMENT_3D ( 'NONE', #245548, #149027, #75599 ) ;
#108953=EDGE_LOOP ( 'NONE', ( #152847, #76207, #36025, #244921 ) ) ;
#108984=CARTESIAN_POINT ( 'NONE',  ( -21.14999999999999858, 75.90220970870393558, -209.7809220950004772 ) ) ;
#109012=CARTESIAN_POINT ( 'NONE',  ( -21.00857864376268935, 64.40000000001263913, -196.5949042542488598 ) ) ;
#109028=VECTOR ( 'NONE', #217366, 1000.000000000000000 ) ;
#109030=DIRECTION ( 'NONE',  ( -0.000000000000000000, 6.982962677686266711E-15, -1.000000000000000000 ) ) ;
#109038=EDGE_CURVE ( 'NONE', #96287, #58661, #186383, .T. ) ;
#109079=EDGE_CURVE ( 'NONE', #135406, #58809, #115620, .T. ) ;
#109083=VERTEX_POINT ( 'NONE', #48991 ) ;
#109096=VERTEX_POINT ( 'NONE', #166413 ) ;
#109121=FACE_OUTER_BOUND ( 'NONE', #140549, .T. ) ;
#109126=ORIENTED_EDGE ( 'NONE', *, *, #216804, .F. ) ;
#109210=CARTESIAN_POINT ( 'NONE',  ( -21.53699400384058293, 75.99999999999440092, -210.3108192777700367 ) ) ;
#109229=ORIENTED_EDGE ( 'NONE', *, *, #173040, .F. ) ;
#109246=VERTEX_POINT ( 'NONE', #172847 ) ;
#109261=VERTEX_POINT ( 'NONE', #71149 ) ;
#109290=DIRECTION ( 'NONE',  ( 1.000000000000000000, 0.000000000000000000, 0.000000000000000000 ) ) ;
#109303=EDGE_LOOP ( 'NONE', ( #93459, #244449, #140939, #63191 ) ) ;
#109326=CARTESIAN_POINT ( 'NONE',  ( 18.59999999999999432, 77.29973367124354411, -213.4949779616549392 ) ) ;
#109330=ORIENTED_EDGE ( 'NONE', *, *, #509, .F. ) ;
#109333=DIRECTION ( 'NONE',  ( 1.000000000000000000, 0.000000000000000000, 0.000000000000000000 ) ) ;
#109341=EDGE_CURVE ( 'NONE', #163056, #226489, #165724, .T. ) ;
#109363=CIRCLE ( 'NONE', #1012, 0.09999999999998898659 ) ;
#109399=CIRCLE ( 'NONE', #255101, 0.1000000000000033362 ) ;
#109406=CARTESIAN_POINT ( 'NONE',  ( 21.17356465864818915, 75.90108875899885277, -209.9459106107660489 ) ) ;
#109445=ORIENTED_EDGE ( 'NONE', *, *, #114435, .T. ) ;
#109466=ORIENTED_EDGE ( 'NONE', *, *, #192718, .F. ) ;
#109486=EDGE_LOOP ( 'NONE', ( #176093, #254913, #244494, #46449 ) ) ;
#109514=CIRCLE ( 'NONE', #22065, 4.000000000000003553 ) ;
#109565=B_SPLINE_CURVE_WITH_KNOTS ( 'NONE', 3,
 ( #124597, #46315, #47596, #67181, #187151, #244521, #7185, #64598, #222363, #247081, #68471, #148004, #128438, #107578, #86712, #188405, #125851, #85414, #223665 ),
 .UNSPECIFIED., .F., .F.,
 ( 4, 3, 3, 3, 3, 3, 4 ),
 ( -2.000416914646550933E-06, 4.235164736271501695E-22, 4.714008503745888536E-05, 9.979203887778544059E-05, 0.0001372215519229606556, 0.0001635031576221011721, 0.0001900083748504231092 ),
 .UNSPECIFIED. ) ;
#109587=CARTESIAN_POINT ( 'NONE',  ( 21.97500000000000497, 66.25000000001253397, -182.3731074845244393 ) ) ;
#109597=DIRECTION ( 'NONE',  ( 0.000000000000000000, 1.000000000000000000, 6.982962677686266711E-15 ) ) ;
#109609=EDGE_CURVE ( 'NONE', #4179, #189559, #86738, .T. ) ;
#109610=ADVANCED_FACE ( 'NONE', ( #193354 ), #74156, .F. ) ;
#109630=EDGE_LOOP ( 'NONE', ( #172096, #119, #127384, #92239, #62154 ) ) ;
#109638=CARTESIAN_POINT ( 'NONE',  ( -18.59999999999999787, 74.25000000001259082, -191.8535959266227451 ) ) ;
#109654=CARTESIAN_POINT ( 'NONE',  ( 23.14999999999998792, 64.35000000001268461, -203.5231074845244166 ) ) ;
#109663=AXIS2_PLACEMENT_3D ( 'NONE', #186058, #174239, #95924 ) ;
#109688=DIRECTION ( 'NONE',  ( 0.000000000000000000, 0.000000000000000000, 1.000000000000000000 ) ) ;
#109697=VERTEX_POINT ( 'NONE', #199778 ) ;
#109698=AXIS2_PLACEMENT_3D ( 'NONE', #226833, #45639, #185143 ) ;
#109715=VECTOR ( 'NONE', #122747, 1000.000000000000000 ) ;
#109725=DIRECTION ( 'NONE',  ( 1.000000000000000000, 0.000000000000000000, 0.000000000000000000 ) ) ;
#109738=ORIENTED_EDGE ( 'NONE', *, *, #162795, .T. ) ;
#109748=ORIENTED_EDGE ( 'NONE', *, *, #50257, .T. ) ;
#109766=AXIS2_PLACEMENT_3D ( 'NONE', #242715, #199776, #21144 ) ;
#109786=VECTOR ( 'NONE', #196400, 999.9999999999998863 ) ;
#109789=ADVANCED_FACE ( 'NONE', ( #116379 ), #235040, .T. ) ;
#109790=CARTESIAN_POINT ( 'NONE',  ( -21.05000000000282512, 69.50298221358175965, -203.5085617939581653 ) ) ;
#109810=CARTESIAN_POINT ( 'NONE',  ( -23.15000000000000213, 64.35000000001258513, -191.3731074845244393 ) ) ;
#109812=ORIENTED_EDGE ( 'NONE', *, *, #6986, .T. ) ;
#109832=DIRECTION ( 'NONE',  ( -4.801466763864314121E-15, 0.2605042016806606298, 0.9654727137038736640 ) ) ;
#109858=AXIS2_PLACEMENT_3D ( 'NONE', #130545, #87556, #27644 ) ;
#109881=FACE_OUTER_BOUND ( 'NONE', #91725, .T. ) ;
#109896=VECTOR ( 'NONE', #140150, 1000.000000000000000 ) ;
#109938=VECTOR ( 'NONE', #165448, 1000.000000000000114 ) ;
#109944=CARTESIAN_POINT ( 'NONE',  ( -20.94999999999999929, 70.15000000001266756, -193.3906102602464330 ) ) ;
#109949=DIRECTION ( 'NONE',  ( 0.000000000000000000, -1.000000000000000000, -6.982962677686265922E-15 ) ) ;
#109951=CIRCLE ( 'NONE', #1793, 0.09999999999999939493 ) ;
#109952=ORIENTED_EDGE ( 'NONE', *, *, #10489, .T. ) ;
#109958=CARTESIAN_POINT ( 'NONE',  ( 18.49999999999999289, 65.79142135624982757, -178.7559501969990663 ) ) ;
#109960=CARTESIAN_POINT ( 'NONE',  ( -21.14999999999999858, 64.25000000001263345, -196.7969768484652491 ) ) ;
#109971=FACE_OUTER_BOUND ( 'NONE', #151704, .T. ) ;
#110004=EDGE_CURVE ( 'NONE', #150814, #178668, #207475, .T. ) ;
#110076=FACE_OUTER_BOUND ( 'NONE', #88913, .T. ) ;
#110102=AXIS2_PLACEMENT_3D ( 'NONE', #48725, #128283, #5728 ) ;
#110113=TOROIDAL_SURFACE ( 'NONE', #160217, 0.6000000000000015321, 0.1000000000000000056 ) ;
#110122=DIRECTION ( 'NONE',  ( 1.000000000000000000, 0.000000000000000000, 0.000000000000000000 ) ) ;
#110146=DIRECTION ( 'NONE',  ( 0.000000000000000000, 6.982962677686266711E-15, -1.000000000000000000 ) ) ;
#110150=FACE_OUTER_BOUND ( 'NONE', #95533, .T. ) ;
#110151=DIRECTION ( 'NONE',  ( 0.000000000000000000, 6.982962677686266711E-15, -1.000000000000000000 ) ) ;
#110167=VERTEX_POINT ( 'NONE', #144588 ) ;
#110188=CARTESIAN_POINT ( 'NONE',  ( -18.44232395689961734, 85.55228255706272478, -163.1808554997175520 ) ) ;
#110269=FACE_OUTER_BOUND ( 'NONE', #92210, .T. ) ;
#110278=EDGE_LOOP ( 'NONE', ( #9613, #97651, #161826 ) ) ;
#110298=EDGE_CURVE ( 'NONE', #8118, #116802, #193693, .T. ) ;
#110306=CARTESIAN_POINT ( 'NONE',  ( 23.25000000000000000, 85.60000000001252829, -179.9170766071767389 ) ) ;
#110313=ORIENTED_EDGE ( 'NONE', *, *, #116006, .F. ) ;
#110318=EDGE_CURVE ( 'NONE', #178265, #106770, #8045, .T. ) ;
#110333=DIRECTION ( 'NONE',  ( -0.000000000000000000, 1.000000000000000000, 6.982962677686267499E-15 ) ) ;
#110344=DIRECTION ( 'NONE',  ( 0.000000000000000000, 3.528251137579945416E-15, -1.000000000000000000 ) ) ;
#110360=DIRECTION ( 'NONE',  ( -0.000000000000000000, 0.2605042016806385363, 0.9654727137038795481 ) ) ;
#110386=EDGE_CURVE ( 'NONE', #92871, #156136, #116203, .T. ) ;
#110393=DIRECTION ( 'NONE',  ( -1.000000000000000000, 0.000000000000000000, 0.000000000000000000 ) ) ;
#110409=DIRECTION ( 'NONE',  ( 1.000000000000000000, 0.000000000000000000, 0.000000000000000000 ) ) ;
#110435=EDGE_CURVE ( 'NONE', #176502, #248551, #137028, .T. ) ;
#110437=CARTESIAN_POINT ( 'NONE',  ( 22.47071067811864609, 68.27992525551464098, -203.6221999392270448 ) ) ;
#110454=EDGE_CURVE ( 'NONE', #195444, #14366, #240515, .T. ) ;
#110467=ORIENTED_EDGE ( 'NONE', *, *, #55179, .T. ) ;
#110480=ORIENTED_EDGE ( 'NONE', *, *, #77895, .F. ) ;
#110482=DIRECTION ( 'NONE',  ( 1.000000000000000000, -2.952720810173289112E-16, -2.061873921506763405E-30 ) ) ;
#110499=FACE_OUTER_BOUND ( 'NONE', #221467, .T. ) ;
#110502=CIRCLE ( 'NONE', #143814, 12.97499999999998721 ) ;
#110558=ORIENTED_EDGE ( 'NONE', *, *, #60262, .T. ) ;
#110569=CARTESIAN_POINT ( 'NONE',  ( -20.00857864376270001, 66.85000000001254250, -182.3731074845244393 ) ) ;
#110570=EDGE_CURVE ( 'NONE', #256994, #129211, #202666, .T. ) ;
#110581=CARTESIAN_POINT ( 'NONE',  ( -23.15000000000000213, 84.59626168225560150, -194.0729799673740104 ) ) ;
#110585=ADVANCED_FACE ( 'NONE', ( #83955 ), #243075, .T. ) ;
#110611=ADVANCED_FACE ( 'NONE', ( #18456 ), #241370, .F. ) ;
#110616=ORIENTED_EDGE ( 'NONE', *, *, #12507, .F. ) ;
#110631=DIRECTION ( 'NONE',  ( 0.000000000000000000, 0.000000000000000000, 1.000000000000000000 ) ) ;
#110686=CARTESIAN_POINT ( 'NONE',  ( -20.54999999999999716, 76.00000000001246292, -172.0231074845243597 ) ) ;
#110702=CARTESIAN_POINT ( 'NONE',  ( -20.00857864376270001, 66.65000000001259650, -191.2731074845244166 ) ) ;
#110704=DIRECTION ( 'NONE',  ( 0.000000000000000000, 0.000000000000000000, 1.000000000000000000 ) ) ;
#110731=VERTEX_POINT ( 'NONE', #46984 ) ;
#110739=EDGE_LOOP ( 'NONE', ( #207585, #103094, #54208, #217085 ) ) ;
#110742=ADVANCED_FACE ( 'NONE', ( #223068 ), #129118, .T. ) ;
#110754=VERTEX_POINT ( 'NONE', #106968 ) ;
#110767=CIRCLE ( 'NONE', #206630, 0.2000000000000057288 ) ;
#110802=DIRECTION ( 'NONE',  ( 1.000000000000000000, -1.836970198721029934E-16, -1.282749433769087582E-30 ) ) ;
#110856=DIRECTION ( 'NONE',  ( 1.000000000000000000, 0.000000000000000000, -0.000000000000000000 ) ) ;
#110905=CARTESIAN_POINT ( 'NONE',  ( -23.15000000000000213, 87.39257802171813694, -173.0970570643562212 ) ) ;
#110932=CARTESIAN_POINT ( 'NONE',  ( 22.59999999999999787, 64.35042919246788529, -203.6231074845244393 ) ) ;
#110947=DIRECTION ( 'NONE',  ( 0.000000000000000000, -0.8700118002898354908, 0.4930308989875170078 ) ) ;
#110952=DIRECTION ( 'NONE',  ( 0.000000000000000000, 0.000000000000000000, -1.000000000000000000 ) ) ;
#110981=ORIENTED_EDGE ( 'NONE', *, *, #148049, .T. ) ;
#110995=ORIENTED_EDGE ( 'NONE', *, *, #187693, .T. ) ;
#110997=CARTESIAN_POINT ( 'NONE',  ( 21.05000000000000426, 69.58617371119972006, -203.4373665474910240 ) ) ;
#111085=DIRECTION ( 'NONE',  ( 0.000000000000000000, -6.454785026890406770E-15, 1.000000000000000000 ) ) ;
#111132=DIRECTION ( 'NONE',  ( -1.000000000000000000, 0.000000000000000000, -0.000000000000000000 ) ) ;
#111137=CARTESIAN_POINT ( 'NONE',  ( -18.59999999999999787, 74.83729825007462466, -195.4231074845243654 ) ) ;
#111141=EDGE_CURVE ( 'NONE', #32289, #188196, #174286, .T. ) ;
#111192=EDGE_LOOP ( 'NONE', ( #196784, #109445, #20610, #138306 ) ) ;
#111212=FACE_OUTER_BOUND ( 'NONE', #209387, .T. ) ;
#111232=ADVANCED_FACE ( 'NONE', ( #228229 ), #157723, .T. ) ;
#111238=DIRECTION ( 'NONE',  ( 0.000000000000000000, 0.000000000000000000, 1.000000000000000000 ) ) ;
#111240=CARTESIAN_POINT ( 'NONE',  ( 20.94983749550516450, 65.70233904877071041, -164.5487410911968595 ) ) ;
#111277=CARTESIAN_POINT ( 'NONE',  ( 20.84999999999998721, 87.75000000001246292, -170.0231074845242745 ) ) ;
#111281=AXIS2_PLACEMENT_3D ( 'NONE', #75113, #232901, #34697 ) ;
#111288=EDGE_CURVE ( 'NONE', #92871, #177284, #116184, .T. ) ;
#111304=CARTESIAN_POINT ( 'NONE',  ( 21.05000000000000071, 87.65000000001268177, -203.5231074845243029 ) ) ;
#111316=EDGE_CURVE ( 'NONE', #175328, #114775, #12134, .T. ) ;
#111329=CARTESIAN_POINT ( 'NONE',  ( 21.05000000000000071, 64.25000000001249134, -176.8647081744215370 ) ) ;
#111331=AXIS2_PLACEMENT_3D ( 'NONE', #90065, #169668, #7993 ) ;
#111400=EDGE_CURVE ( 'NONE', #182617, #193318, #55972, .T. ) ;
#111412=CARTESIAN_POINT ( 'NONE',  ( -21.05000000000000071, 87.48912529308871910, -200.4231074845242802 ) ) ;
#111427=VECTOR ( 'NONE', #14400, 1000.000000000000000 ) ;
#111430=ORIENTED_EDGE ( 'NONE', *, *, #130877, .F. ) ;
#111435=FACE_OUTER_BOUND ( 'NONE', #137940, .T. ) ;
#111441=CARTESIAN_POINT ( 'NONE',  ( -18.50000000000000000, 64.35000000001259934, -191.3731074845244393 ) ) ;
#111471=CARTESIAN_POINT ( 'NONE',  ( -23.25000000000000000, 69.06610602788607878, -166.2374616501508342 ) ) ;
#111483=DIRECTION ( 'NONE',  ( 0.000000000000000000, 0.000000000000000000, 1.000000000000000000 ) ) ;
#111485=CARTESIAN_POINT ( 'NONE',  ( -18.47130263965431141, 85.47115558597647578, -163.3397027190475512 ) ) ;
#111493=DIRECTION ( 'NONE',  ( 1.000000000000000000, -3.265361837132813093E-16, -2.280189983783949500E-30 ) ) ;
#111494=VECTOR ( 'NONE', #54038, 1000.000000000000000 ) ;
#111512=CARTESIAN_POINT ( 'NONE',  ( -20.54999999999999716, 71.65000000001253966, -182.3731074845244109 ) ) ;
#111517=CARTESIAN_POINT ( 'NONE',  ( -20.54999999999999716, 85.50000000001251976, -179.9170766071767389 ) ) ;
#111523=AXIS2_PLACEMENT_3D ( 'NONE', #236342, #95545, #112560 ) ;
#111612=AXIS2_PLACEMENT_3D ( 'NONE', #79116, #159987, #137808 ) ;
#111658=CARTESIAN_POINT ( 'NONE',  ( 23.24999999999999645, 71.22429906543317202, -191.6743393804784148 ) ) ;
#111659=VERTEX_POINT ( 'NONE', #54072 ) ;
#111720=EDGE_LOOP ( 'NONE', ( #36771, #219724, #195123, #226903, #75140 ) ) ;
#111739=CARTESIAN_POINT ( 'NONE',  ( -21.05000000000000071, 74.14897176987174987, -191.8691942151018850 ) ) ;
#111765=ORIENTED_EDGE ( 'NONE', *, *, #128614, .T. ) ;
#111800=PLANE ( 'NONE',  #44675 ) ;
#111882=LINE ( 'NONE', #233127, #91932 ) ;
#111883=CARTESIAN_POINT ( 'NONE',  ( 20.85000000000000142, 77.83585931145600512, -158.5186683157258187 ) ) ;
#111913=CARTESIAN_POINT ( 'NONE',  ( -23.25000000000000000, 85.00000000001261924, -193.6291383618718385 ) ) ;
#111931=EDGE_CURVE ( 'NONE', #116410, #63242, #124723, .T. ) ;
#111949=EDGE_CURVE ( 'NONE', #166644, #60084, #153812, .T. ) ;
#111951=EDGE_LOOP ( 'NONE', ( #4228, #36278, #206714, #67666 ) ) ;
#111953=TOROIDAL_SURFACE ( 'NONE', #32866, 0.2000000000000000111, 0.1000000000000000056 ) ;
#111986=CARTESIAN_POINT ( 'NONE',  ( 21.00000000000000000, 66.25000000001253397, -182.2731074845244450 ) ) ;
#112138=DIRECTION ( 'NONE',  ( 0.000000000000000000, 0.000000000000000000, 1.000000000000000000 ) ) ;
#112156=CARTESIAN_POINT ( 'NONE',  ( 18.52928932188133970, 65.72071067813119782, -182.1731074845244223 ) ) ;
#112158=EDGE_CURVE ( 'NONE', #137948, #236913, #104432, .T. ) ;
#112178=CARTESIAN_POINT ( 'NONE',  ( 20.94999999999999574, 87.65000000001266756, -200.6231074845242688 ) ) ;
#112200=CARTESIAN_POINT ( 'NONE',  ( 21.05000000000000071, 87.65000000001246860, -173.1231074845242688 ) ) ;
#112204=PLANE ( 'NONE',  #54932 ) ;
#112222=CARTESIAN_POINT ( 'NONE',  ( 21.14999999999999858, 69.35000000001259934, -191.1731074845243938 ) ) ;
#112260=CIRCLE ( 'NONE', #195464, 0.1000000000000009492 ) ;
#112270=CIRCLE ( 'NONE', #203818, 0.1000000000000043771 ) ;
#112292=ORIENTED_EDGE ( 'NONE', *, *, #38577, .T. ) ;
#112293=CARTESIAN_POINT ( 'NONE',  ( 21.05000000000000071, 69.74218538953655866, -203.6208977758331855 ) ) ;
#112315=ADVANCED_FACE ( 'NONE', ( #131728 ), #245266, .F. ) ;
#112333=CARTESIAN_POINT ( 'NONE',  ( 20.95483826173899899, 67.12383379524264626, -194.9768319316249006 ) ) ;
#112361=AXIS2_PLACEMENT_3D ( 'NONE', #216419, #54772, #97728 ) ;
#112365=CARTESIAN_POINT ( 'NONE',  ( 20.85000000000000142, 76.00000000001239187, -162.1231074845243825 ) ) ;
#112437=DIRECTION ( 'NONE',  ( 1.040834085586049673E-13, 0.7899159663865300551, 0.6132151058540831201 ) ) ;
#112452=CARTESIAN_POINT ( 'NONE',  ( 21.13614978966381841, 76.00000000001270450, -210.0222121863581037 ) ) ;
#112480=CARTESIAN_POINT ( 'NONE',  ( -21.05000000000000071, 74.16465844978819177, -191.9679561919613775 ) ) ;
#112514=FACE_OUTER_BOUND ( 'NONE', #243536, .T. ) ;
#112521=ORIENTED_EDGE ( 'NONE', *, *, #231825, .T. ) ;
#112524=CARTESIAN_POINT ( 'NONE',  ( 23.24999999999999289, 69.35000000001259934, -191.1731074845243938 ) ) ;
#112548=CARTESIAN_POINT ( 'NONE',  ( -23.25000000000000000, 68.97833521811233481, -166.1895420826271277 ) ) ;
#112560=DIRECTION ( 'NONE',  ( 0.000000000000000000, -6.467318590049456648E-15, 1.000000000000000000 ) ) ;
#112582=ORIENTED_EDGE ( 'NONE', *, *, #211975, .F. ) ;
#112586=ORIENTED_EDGE ( 'NONE', *, *, #105097, .F. ) ;
#112627=CARTESIAN_POINT ( 'NONE',  ( 19.99999999999998934, 64.25000000001250555, -178.6731074845244507 ) ) ;
#112631=ADVANCED_FACE ( 'NONE', ( #65021 ), #229895, .T. ) ;
#112635=AXIS2_PLACEMENT_3D ( 'NONE', #29999, #40899, #88629 ) ;
#112673=DIRECTION ( 'NONE',  ( 0.000000000000000000, -6.982962677686266711E-15, 1.000000000000000000 ) ) ;
#112674=ORIENTED_EDGE ( 'NONE', *, *, #202847, .F. ) ;
#112704=ADVANCED_FACE ( 'NONE', ( #67594 ), #148430, .T. ) ;
#112711=EDGE_LOOP ( 'NONE', ( #230834, #31060, #197095, #11288 ) ) ;
#112713=TOROIDAL_SURFACE ( 'NONE', #21156, 11.70000000000000639, 0.1000000000000000056 ) ;
#112755=EDGE_CURVE ( 'NONE', #120584, #79652, #166730, .T. ) ;
#112758=ORIENTED_EDGE ( 'NONE', *, *, #250771, .T. ) ;
#112773=CARTESIAN_POINT ( 'NONE',  ( -18.33981767444326039, 85.56957578981658230, -163.2039456407995317 ) ) ;
#112806=ORIENTED_EDGE ( 'NONE', *, *, #59897, .T. ) ;
#112829=EDGE_CURVE ( 'NONE', #121003, #62333, #191938, .T. ) ;
#112840=DIRECTION ( 'NONE',  ( -1.000000000000000000, 0.000000000000000000, -0.000000000000000000 ) ) ;
#112888=EDGE_CURVE ( 'NONE', #228673, #57380, #146111, .T. ) ;
#112946=EDGE_CURVE ( 'NONE', #204385, #216335, #246081, .T. ) ;
#112947=CIRCLE ( 'NONE', #487, 0.09999999999999939493 ) ;
#112960=ORIENTED_EDGE ( 'NONE', *, *, #128020, .F. ) ;
#112999=EDGE_LOOP ( 'NONE', ( #188021, #49835, #87632, #85947 ) ) ;
#113003=DIRECTION ( 'NONE',  ( -0.000000000000000000, -1.000000000000000000, -6.982962677686266711E-15 ) ) ;
#113022=CARTESIAN_POINT ( 'NONE',  ( 21.05000000000000071, 71.18691588786307989, -191.5815897280005800 ) ) ;
#113024=DIRECTION ( 'NONE',  ( -1.000000000000000000, 0.000000000000000000, -0.000000000000000000 ) ) ;
#113027=CARTESIAN_POINT ( 'NONE',  ( 20.94999999999999574, 77.83534155023700407, -191.9679561919613491 ) ) ;
#113061=DIRECTION ( 'NONE',  ( 1.000000000000000000, 0.000000000000000000, 0.000000000000000000 ) ) ;
#113070=ORIENTED_EDGE ( 'NONE', *, *, #55927, .T. ) ;
#113085=DIRECTION ( 'NONE',  ( 0.000000000000000000, -0.1350103645451974088, 0.9908441862701587999 ) ) ;
#113089=CARTESIAN_POINT ( 'NONE',  ( -20.94999999999999929, 74.16465844978819177, -191.8679561919614116 ) ) ;
#113103=CARTESIAN_POINT ( 'NONE',  ( -20.54999999999999716, 85.40000000001262492, -193.6291383618718385 ) ) ;
#113106=CARTESIAN_POINT ( 'NONE',  ( -23.25000000000000000, 85.00000000001251976, -179.9170766071767389 ) ) ;
#113112=VERTEX_POINT ( 'NONE', #30749 ) ;
#113121=CARTESIAN_POINT ( 'NONE',  ( -21.05000000000000071, 70.15000000001266756, -193.3906102602464330 ) ) ;
#113148=FACE_OUTER_BOUND ( 'NONE', #225774, .T. ) ;
#113193=DIRECTION ( 'NONE',  ( 0.000000000000000000, -0.4999999999999088507, 0.8660254037844913322 ) ) ;
#113197=DIRECTION ( 'NONE',  ( 0.000000000000000000, -1.000000000000000000, 0.000000000000000000 ) ) ;
#113206=CARTESIAN_POINT ( 'NONE',  ( 20.99999999999997868, 76.00000000001267608, -203.5231074845243597 ) ) ;
#113210=CARTESIAN_POINT ( 'NONE',  ( -18.50000000000000000, 66.85000000001259934, -191.1731074845244223 ) ) ;
#113221=DIRECTION ( 'NONE',  ( 0.000000000000000000, 0.000000000000000000, 1.000000000000000000 ) ) ;
#113295=FACE_OUTER_BOUND ( 'NONE', #32602, .T. ) ;
#113320=EDGE_CURVE ( 'NONE', #253585, #119237, #126628, .T. ) ;
#113326=CYLINDRICAL_SURFACE ( 'NONE', #120874, 0.09999999999999939493 ) ;
#113337=DIRECTION ( 'NONE',  ( 0.000000000000000000, -7.116814260417676401E-15, 1.000000000000000000 ) ) ;
#113348=EDGE_CURVE ( 'NONE', #236840, #213491, #25678, .T. ) ;
#113355=ORIENTED_EDGE ( 'NONE', *, *, #203886, .F. ) ;
#113362=DIRECTION ( 'NONE',  ( 1.000000000000000000, 0.000000000000000000, 0.000000000000000000 ) ) ;
#113363=ADVANCED_FACE ( 'NONE', ( #138763 ), #39738, .F. ) ;
#113372=CARTESIAN_POINT ( 'NONE',  ( 19.58285714285715073, 66.98499851036405062, -195.1024546684426753 ) ) ;
#113376=CARTESIAN_POINT ( 'NONE',  ( 20.94999999999999929, 76.00000000001244871, -170.0231074845243597 ) ) ;
#113379=FACE_OUTER_BOUND ( 'NONE', #32940, .T. ) ;
#113394=CARTESIAN_POINT ( 'NONE',  ( -20.64999999999999858, 71.65000000001259650, -191.1731074845243654 ) ) ;
#113463=CARTESIAN_POINT ( 'NONE',  ( 23.25000000000000000, 84.59626168225560150, -194.0729799673740104 ) ) ;
#113475=ORIENTED_EDGE ( 'NONE', *, *, #8665, .T. ) ;
#113484=DIRECTION ( 'NONE',  ( 0.000000000000000000, 0.000000000000000000, -1.000000000000000000 ) ) ;
#113490=EDGE_CURVE ( 'NONE', #257629, #109697, #96392, .T. ) ;
#113512=FACE_OUTER_BOUND ( 'NONE', #31577, .T. ) ;
#113542=CYLINDRICAL_SURFACE ( 'NONE', #147721, 0.09999999999998898659 ) ;
#113579=CARTESIAN_POINT ( 'NONE',  ( 22.39999999999999503, 75.90000000001273861, -211.3138870828977360 ) ) ;
#113593=DIRECTION ( 'NONE',  ( -1.000000000000000000, -0.000000000000000000, -0.000000000000000000 ) ) ;
#113605=DIRECTION ( 'NONE',  ( 0.000000000000000000, 6.982962677686267499E-15, -1.000000000000000000 ) ) ;
#113648=ORIENTED_EDGE ( 'NONE', *, *, #197533, .F. ) ;
#113670=DIRECTION ( 'NONE',  ( 0.000000000000000000, 0.000000000000000000, 1.000000000000000000 ) ) ;
#113682=ORIENTED_EDGE ( 'NONE', *, *, #160854, .T. ) ;
#113724=SURFACE_STYLE_FILL_AREA ( #190726 ) ;
#113726=DIRECTION ( 'NONE',  ( 0.000000000000000000, -1.000000000000000000, -6.982962677686265922E-15 ) ) ;
#113746=ORIENTED_EDGE ( 'NONE', *, *, #57913, .T. ) ;
#113752=ORIENTED_EDGE ( 'NONE', *, *, #254355, .T. ) ;
#113754=CARTESIAN_POINT ( 'NONE',  ( -20.64999999999999858, 76.00000000001267608, -203.5231074845243597 ) ) ;
#113759=AXIS2_PLACEMENT_3D ( 'NONE', #18929, #239277, #157195 ) ;
#113763=AXIS2_PLACEMENT_3D ( 'NONE', #246035, #9986, #167806 ) ;
#113776=DIRECTION ( 'NONE',  ( -1.000000000000000000, 0.000000000000000000, 0.000000000000000000 ) ) ;
#113783=CARTESIAN_POINT ( 'NONE',  ( -21.05000000000000071, 76.00000000001242029, -166.0231074845243597 ) ) ;
#113791=VECTOR ( 'NONE', #236874, 1000.000000000000114 ) ;
#113792=DIRECTION ( 'NONE',  ( 0.000000000000000000, -1.000000000000000000, -6.982962677686265922E-15 ) ) ;
#113793=DIRECTION ( 'NONE',  ( 0.000000000000000000, 1.000000000000000000, 0.000000000000000000 ) ) ;
#113801=DIRECTION ( 'NONE',  ( -1.000000000000000000, -0.000000000000000000, -0.000000000000000000 ) ) ;
#113825=EDGE_LOOP ( 'NONE', ( #2104, #56136, #545, #38960 ) ) ;
#113836=CARTESIAN_POINT ( 'NONE',  ( -20.94999999999999929, 74.14897176987174987, -191.8691942151018850 ) ) ;
#113840=CIRCLE ( 'NONE', #205391, 11.80000000000000426 ) ;
#113845=CARTESIAN_POINT ( 'NONE',  ( 20.94999999999999929, 76.00000000001244871, -170.0231074845243597 ) ) ;
#113864=DIRECTION ( 'NONE',  ( -1.000000000000000000, 0.000000000000000000, -0.000000000000000000 ) ) ;
#113897=CARTESIAN_POINT ( 'NONE',  ( -23.25000000000000000, 64.25000000001277556, -215.2731074845244450 ) ) ;
#113903=CYLINDRICAL_SURFACE ( 'NONE', #90807, 0.09999999999998898659 ) ;
#113918=DIRECTION ( 'NONE',  ( 2.952720810173289112E-16, 1.000000000000000000, 6.938893903907222067E-15 ) ) ;
#113962=AXIS2_PLACEMENT_3D ( 'NONE', #203674, #163277, #43325 ) ;
#114007=FACE_OUTER_BOUND ( 'NONE', #155901, .T. ) ;
#114037=CARTESIAN_POINT ( 'NONE',  ( -18.33682934331497094, 85.51118559110597062, -163.1174527158505612 ) ) ;
#114041=AXIS2_PLACEMENT_3D ( 'NONE', #39581, #216885, #37002 ) ;
#114060=ORIENTED_EDGE ( 'NONE', *, *, #194790, .T. ) ;
#114068=FACE_OUTER_BOUND ( 'NONE', #52395, .T. ) ;
#114082=DIRECTION ( 'NONE',  ( 0.000000000000000000, 1.000000000000000000, 7.116814260417668513E-15 ) ) ;
#114083=B_SPLINE_CURVE_WITH_KNOTS ( 'NONE', 3,
 ( #77034, #236114, #37941, #57462, #137016, #216549, #32825, #232291, #112333, #191887 ),
 .UNSPECIFIED., .F., .F.,
 ( 4, 3, 3, 4 ),
 ( 0.000000000000000000, 3.394313611811463347E-05, 6.779740500699467213E-05, 0.0001049857339142579784 ),
 .UNSPECIFIED. ) ;
#114098=DIRECTION ( 'NONE',  ( 0.000000000000000000, 0.000000000000000000, -1.000000000000000000 ) ) ;
#114112=EDGE_CURVE ( 'NONE', #185078, #32552, #196719, .T. ) ;
#114120=CYLINDRICAL_SURFACE ( 'NONE', #5408, 0.09999999999999939493 ) ;
#114179=CARTESIAN_POINT ( 'NONE',  ( -21.05000000000000071, 76.00000000001244871, -170.0231074845243597 ) ) ;
#114213=CARTESIAN_POINT ( 'NONE',  ( -22.57320508075687115, 64.25000000001269029, -203.5231074845244166 ) ) ;
#114240=CIRCLE ( 'NONE', #235060, 0.5000000000000004441 ) ;
#114246=CARTESIAN_POINT ( 'NONE',  ( 21.05000000000000071, 71.00000000001253397, -182.4283735034374843 ) ) ;
#114263=EDGE_LOOP ( 'NONE', ( #207573, #8894, #47318 ) ) ;
#114264=CARTESIAN_POINT ( 'NONE',  ( -22.39999999999999858, 75.90000000001268177, -203.5231074845243597 ) ) ;
#114294=ORIENTED_EDGE ( 'NONE', *, *, #32952, .F. ) ;
#114308=FACE_OUTER_BOUND ( 'NONE', #12962, .T. ) ;
#114318=ORIENTED_EDGE ( 'NONE', *, *, #82261, .T. ) ;
#114355=AXIS2_PLACEMENT_3D ( 'NONE', #171992, #152414, #251474 ) ;
#114359=DIRECTION ( 'NONE',  ( -1.000000000000000000, 0.000000000000000000, 0.000000000000000000 ) ) ;
#114360=CARTESIAN_POINT ( 'NONE',  ( -21.45000000000000284, 68.29142135624984178, -182.3731074845244109 ) ) ;
#114363=CARTESIAN_POINT ( 'NONE',  ( 20.94999999999999574, 74.16465844978819177, -191.9679561919613775 ) ) ;
#114399=CARTESIAN_POINT ( 'NONE',  ( -20.94999999999999929, 77.26178616857765746, -195.4366085209788935 ) ) ;
#114435=EDGE_CURVE ( 'NONE', #36049, #228338, #30164, .T. ) ;
#114438=DIRECTION ( 'NONE',  ( 7.304098846218134667E-16, 1.000000000000000000, 6.982962677686266711E-15 ) ) ;
#114449=CARTESIAN_POINT ( 'NONE',  ( 18.59999999999999076, 64.35000000001251408, -178.7731074845244450 ) ) ;
#114452=DIRECTION ( 'NONE',  ( -1.000000000000000000, -0.000000000000000000, -0.000000000000000000 ) ) ;
#114468=ORIENTED_EDGE ( 'NONE', *, *, #81708, .F. ) ;
#114477=CARTESIAN_POINT ( 'NONE',  ( -23.15000000000000213, 71.75000000001259082, -191.1731074845243654 ) ) ;
#114478=CARTESIAN_POINT ( 'NONE',  ( -22.50000000000000000, 76.00000000001276135, -215.1726782920691505 ) ) ;
#114518=ADVANCED_FACE ( 'NONE', ( #36667 ), #174919, .F. ) ;
#114532=ORIENTED_EDGE ( 'NONE', *, *, #4078, .T. ) ;
#114535=AXIS2_PLACEMENT_3D ( 'NONE', #37318, #179395, #238056 ) ;
#114610=ORIENTED_EDGE ( 'NONE', *, *, #175092, .T. ) ;
#114621=DIRECTION ( 'NONE',  ( 0.000000000000000000, 1.000000000000000000, 6.853228547068871147E-15 ) ) ;
#114630=DIRECTION ( 'NONE',  ( -1.000000000000000000, 0.000000000000000000, 0.000000000000000000 ) ) ;
#114639=EDGE_CURVE ( 'NONE', #176065, #107411, #114083, .T. ) ;
#114641=ADVANCED_FACE ( 'NONE', ( #13236 ), #92741, .T. ) ;
#114643=LINE ( 'NONE', #134193, #69530 ) ;
#114661=CARTESIAN_POINT ( 'NONE',  ( 21.05000000000000071, 85.00000000001261924, -193.6291383618718385 ) ) ;
#114664=EDGE_CURVE ( 'NONE', #233248, #116470, #76103, .T. ) ;
#114677=ORIENTED_EDGE ( 'NONE', *, *, #149871, .F. ) ;
#114687=CARTESIAN_POINT ( 'NONE',  ( 18.51697539158856642, 65.68434038414410736, -164.4866880726065972 ) ) ;
#114729=AXIS2_PLACEMENT_3D ( 'NONE', #34989, #37528, #77908 ) ;
#114735=DIRECTION ( 'NONE',  ( 0.000000000000000000, 0.000000000000000000, 1.000000000000000000 ) ) ;
#114775=VERTEX_POINT ( 'NONE', #164297 ) ;
#114814=DIRECTION ( 'NONE',  ( 4.377807931758639578E-15, -0.2605042016806606298, -0.9654727137038736640 ) ) ;
#114847=EDGE_CURVE ( 'NONE', #72156, #19640, #144703, .T. ) ;
#114851=EDGE_CURVE ( 'NONE', #207747, #252194, #187719, .T. ) ;
#114864=CARTESIAN_POINT ( 'NONE',  ( 21.51976009735019346, 69.08954155835347422, -203.5231074845243882 ) ) ;
#114957=CARTESIAN_POINT ( 'NONE',  ( 18.59999999999999432, 77.16270174995064224, -195.4231074845243370 ) ) ;
#114973=AXIS2_PLACEMENT_3D ( 'NONE', #20912, #162982, #183806 ) ;
#115017=AXIS2_PLACEMENT_3D ( 'NONE', #27468, #207357, #87374 ) ;
#115022=ORIENTED_EDGE ( 'NONE', *, *, #153677, .F. ) ;
#115065=ORIENTED_EDGE ( 'NONE', *, *, #226672, .T. ) ;
#115079=VERTEX_POINT ( 'NONE', #136691 ) ;
#115127=VERTEX_POINT ( 'NONE', #132219 ) ;
#115129=EDGE_CURVE ( 'NONE', #52715, #96287, #59698, .T. ) ;
#115151=CARTESIAN_POINT ( 'NONE',  ( -20.94999999999999929, 68.97833521811233481, -166.1895420826271277 ) ) ;
#115161=CARTESIAN_POINT ( 'NONE',  ( -21.05000000000000071, 76.00000000001244871, -170.0231074845243597 ) ) ;
#115172=ORIENTED_EDGE ( 'NONE', *, *, #145017, .F. ) ;
#115203=CARTESIAN_POINT ( 'NONE',  ( -18.49346865148325492, 85.44307379853751172, -196.3379112292089985 ) ) ;
#115216=EDGE_LOOP ( 'NONE', ( #147546, #242067, #73152, #76356 ) ) ;
#115222=EDGE_LOOP ( 'NONE', ( #83597, #82185, #110480, #90800, #71716, #204965 ) ) ;
#115226=B_SPLINE_CURVE_WITH_KNOTS ( 'NONE', 3,
 ( #93803, #196754, #215043, #255396, #36436, #115954 ),
 .UNSPECIFIED., .F., .F.,
 ( 4, 2, 4 ),
 ( 0.000000000000000000, 0.0001568709654583423218, 0.0003137419309166846436 ),
 .UNSPECIFIED. ) ;
#115263=VERTEX_POINT ( 'NONE', #218150 ) ;
#115355=LINE ( 'NONE', #232757, #38668 ) ;
#115367=EDGE_LOOP ( 'NONE', ( #245027, #12904, #234185 ) ) ;
#115376=DIRECTION ( 'NONE',  ( 0.000000000000000000, 0.000000000000000000, 1.000000000000000000 ) ) ;
#115413=AXIS2_PLACEMENT_3D ( 'NONE', #237305, #14428, #93930 ) ;
#115430=AXIS2_PLACEMENT_3D ( 'NONE', #93568, #214795, #92277 ) ;
#115439=ORIENTED_EDGE ( 'NONE', *, *, #241057, .F. ) ;
#115482=AXIS2_PLACEMENT_3D ( 'NONE', #79177, #139137, #117048 ) ;
#115488=CARTESIAN_POINT ( 'NONE',  ( -20.64999999999999858, 71.75000000001259082, -191.1731074845243654 ) ) ;
#115499=DIRECTION ( 'NONE',  ( 1.000000000000000000, -2.952720810173289112E-16, -2.061873921506763405E-30 ) ) ;
#115542=CARTESIAN_POINT ( 'NONE',  ( -23.25000000000000000, 64.25000000001244871, -170.0231074845244166 ) ) ;
#115554=DIRECTION ( 'NONE',  ( 0.000000000000000000, -6.938893903907222067E-15, 1.000000000000000000 ) ) ;
#115562=ADVANCED_FACE ( 'NONE', ( #87633 ), #8125, .T. ) ;
#115576=CIRCLE ( 'NONE', #86323, 0.09999999999998898659 ) ;
#115590=CARTESIAN_POINT ( 'NONE',  ( -20.54999999999999716, 74.00000000001259082, -190.2984855617622770 ) ) ;
#115598=VERTEX_POINT ( 'NONE', #208883 ) ;
#115620=CIRCLE ( 'NONE', #132382, 11.64999999999999325 ) ;
#115636=FACE_OUTER_BOUND ( 'NONE', #25801, .T. ) ;
#115639=CARTESIAN_POINT ( 'NONE',  ( -23.15000000000000213, 87.65000000001246860, -173.1231074845242688 ) ) ;
#115647=EDGE_CURVE ( 'NONE', #65528, #14901, #184233, .T. ) ;
#115664=VECTOR ( 'NONE', #38395, 1000.000000000000000 ) ;
#115678=DIRECTION ( 'NONE',  ( 1.000000000000000000, -3.265361837132813093E-16, -2.280189983783949500E-30 ) ) ;
#115682=EDGE_LOOP ( 'NONE', ( #114610, #18405, #53522, #231353 ) ) ;
#115684=EDGE_LOOP ( 'NONE', ( #248636, #126421, #25060, #254167, #214045 ) ) ;
#115708=DIRECTION ( 'NONE',  ( 0.000000000000000000, -6.853228547068871147E-15, 1.000000000000000000 ) ) ;
#115722=CARTESIAN_POINT ( 'NONE',  ( 20.95512820512820795, 67.12384868372447499, -191.3229346253956180 ) ) ;
#115730=LINE ( 'NONE', #15365, #188139 ) ;
#115732=ADVANCED_FACE ( 'NONE', ( #35422 ), #194483, .T. ) ;
#115756=DIRECTION ( 'NONE',  ( 2.710505431213777355E-16, 1.000000000000000000, 6.982962677686266711E-15 ) ) ;
#115797=CARTESIAN_POINT ( 'NONE',  ( -20.00857864376270001, 66.75000000001253397, -182.3731074845244393 ) ) ;
#115818=DIRECTION ( 'NONE',  ( 0.000000000000000000, 6.982962677686266711E-15, -1.000000000000000000 ) ) ;
#115827=CARTESIAN_POINT ( 'NONE',  ( -21.05000000000000071, 76.00000000001264766, -200.6231074845243825 ) ) ;
#115866=EDGE_CURVE ( 'NONE', #34288, #135228, #205254, .T. ) ;
#115875=DIRECTION ( 'NONE',  ( -0.000000000000000000, 6.982962677686266711E-15, -1.000000000000000000 ) ) ;
#115897=AXIS2_PLACEMENT_3D ( 'NONE', #45152, #25603, #26909 ) ;
#115908=ORIENTED_EDGE ( 'NONE', *, *, #100577, .T. ) ;
#115913=EDGE_CURVE ( 'NONE', #161829, #183594, #167702, .T. ) ;
#115932=EDGE_CURVE ( 'NONE', #249694, #120125, #109399, .T. ) ;
#115954=CARTESIAN_POINT ( 'NONE',  ( -22.59999999999999787, 75.89914163091405896, -215.2726746080137445 ) ) ;
#115959=FACE_OUTER_BOUND ( 'NONE', #206922, .T. ) ;
#115965=AXIS2_PLACEMENT_3D ( 'NONE', #211, #4068, #138418 ) ;
#115985=VECTOR ( 'NONE', #207484, 1000.000000000000227 ) ;
#115986=DIRECTION ( 'NONE',  ( -1.000000000000000000, 2.952720810173289112E-16, 2.061873921506763405E-30 ) ) ;
#115990=EDGE_CURVE ( 'NONE', #126474, #192558, #126140, .T. ) ;
#115994=ORIENTED_EDGE ( 'NONE', *, *, #85555, .T. ) ;
#116006=EDGE_CURVE ( 'NONE', #15467, #239176, #230210, .T. ) ;
#116007=DIRECTION ( 'NONE',  ( 1.000000000000000000, -3.469446951953718318E-14, 2.003086131649645455E-14 ) ) ;
#116015=CARTESIAN_POINT ( 'NONE',  ( 20.95512820512820440, 67.12384868372447499, -191.3731074845244109 ) ) ;
#116017=DIRECTION ( 'NONE',  ( -0.7071067811865127117, -0.7071067811865821007, 0.000000000000000000 ) ) ;
#116071=DIRECTION ( 'NONE',  ( 0.000000000000000000, 1.000000000000000000, 1.387778780781444413E-14 ) ) ;
#116090=ORIENTED_EDGE ( 'NONE', *, *, #197086, .F. ) ;
#116092=DIRECTION ( 'NONE',  ( 0.000000000000000000, -6.982962677686266711E-15, 1.000000000000000000 ) ) ;
#116093=CARTESIAN_POINT ( 'NONE',  ( -22.50000000000000000, 64.35000000001268461, -203.5231074845244166 ) ) ;
#116105=VECTOR ( 'NONE', #148708, 1000.000000000000000 ) ;
#116107=VECTOR ( 'NONE', #74148, 1000.000000000000000 ) ;
#116116=LINE ( 'NONE', #15754, #126487 ) ;
#116146=CARTESIAN_POINT ( 'NONE',  ( 22.48660254037845618, 64.25000000001269029, -203.5731074845244564 ) ) ;
#116149=EDGE_CURVE ( 'NONE', #30084, #152240, #13924, .T. ) ;
#116172=EDGE_LOOP ( 'NONE', ( #39508, #46000, #53294, #191219 ) ) ;
#116184=CIRCLE ( 'NONE', #232698, 0.09999999999998898659 ) ;
#116195=DIRECTION ( 'NONE',  ( 0.000000000000000000, -1.000000000000000000, -6.352154140967427193E-15 ) ) ;
#116198=EDGE_CURVE ( 'NONE', #164331, #186491, #220139, .T. ) ;
#116203=CIRCLE ( 'NONE', #187116, 0.09999999999998898659 ) ;
#116220=ORIENTED_EDGE ( 'NONE', *, *, #34449, .T. ) ;
#116223=VERTEX_POINT ( 'NONE', #88286 ) ;
#116225=DIRECTION ( 'NONE',  ( 0.000000000000000000, 0.4930308989874980785, 0.8700118002898462599 ) ) ;
#116255=ORIENTED_EDGE ( 'NONE', *, *, #170864, .F. ) ;
#116260=DIRECTION ( 'NONE',  ( 0.000000000000000000, 0.000000000000000000, 1.000000000000000000 ) ) ;
#116266=ORIENTED_EDGE ( 'NONE', *, *, #77976, .F. ) ;
#116298=ORIENTED_EDGE ( 'NONE', *, *, #51237, .T. ) ;
#116309=ORIENTED_EDGE ( 'NONE', *, *, #61159, .F. ) ;
#116317=EDGE_LOOP ( 'NONE', ( #67947, #21590, #148663, #247699 ) ) ;
#116337=ADVANCED_FACE ( 'NONE', ( #208282 ), #68763, .T. ) ;
#116348=DIRECTION ( 'NONE',  ( 0.000000000000000000, 0.9915357197604862671, -0.1298341882519953583 ) ) ;
#116379=FACE_OUTER_BOUND ( 'NONE', #210513, .T. ) ;
#116381=EDGE_LOOP ( 'NONE', ( #69122, #75185, #205759, #211420 ) ) ;
#116405=LINE ( 'NONE', #173854, #30091 ) ;
#116410=VERTEX_POINT ( 'NONE', #90881 ) ;
#116428=EDGE_CURVE ( 'NONE', #19640, #213808, #255027, .T. ) ;
#116438=DIRECTION ( 'NONE',  ( 0.7071067811865475727, -0.7071067811865475727, -4.937700262164531476E-15 ) ) ;
#116446=VERTEX_POINT ( 'NONE', #152174 ) ;
#116450=DIRECTION ( 'NONE',  ( -1.000000000000000000, 0.000000000000000000, -0.000000000000000000 ) ) ;
#116458=CIRCLE ( 'NONE', #99833, 0.1000000000000046685 ) ;
#116459=EDGE_LOOP ( 'NONE', ( #145822, #237759, #20243, #179122 ) ) ;
#116461=CIRCLE ( 'NONE', #74801, 11.65000000000000746 ) ;
#116470=VERTEX_POINT ( 'NONE', #113022 ) ;
#116528=DIRECTION ( 'NONE',  ( 0.000000000000000000, 0.000000000000000000, -1.000000000000000000 ) ) ;
#116547=ORIENTED_EDGE ( 'NONE', *, *, #67942, .F. ) ;
#116561=ORIENTED_EDGE ( 'NONE', *, *, #73659, .F. ) ;
#116582=DIRECTION ( 'NONE',  ( 0.000000000000000000, 1.000000000000000000, 0.000000000000000000 ) ) ;
#116619=VECTOR ( 'NONE', #206720, 1000.000000000000000 ) ;
#116622=ADVANCED_FACE ( 'NONE', ( #162435 ), #8489, .F. ) ;
#116634=CIRCLE ( 'NONE', #179207, 0.1000000000000028644 ) ;
#116680=DIRECTION ( 'NONE',  ( 0.000000000000000000, 6.982962677686267499E-15, -1.000000000000000000 ) ) ;
#116703=AXIS2_PLACEMENT_3D ( 'NONE', #138217, #117396, #76978 ) ;
#116717=CIRCLE ( 'NONE', #112635, 0.09999999999999939493 ) ;
#116743=B_SPLINE_CURVE_WITH_KNOTS ( 'NONE', 3,
 ( #101788, #100507, #99238, #223050, #22316, #177552 ),
 .UNSPECIFIED., .F., .F.,
 ( 4, 2, 4 ),
 ( 0.000000000000000000, 0.0001891491689349488760, 0.0003782983378698977521 ),
 .UNSPECIFIED. ) ;
#116775=ORIENTED_EDGE ( 'NONE', *, *, #248602, .T. ) ;
#116802=VERTEX_POINT ( 'NONE', #14916 ) ;
#116830=ORIENTED_EDGE ( 'NONE', *, *, #220438, .F. ) ;
#116832=DIRECTION ( 'NONE',  ( 0.000000000000000000, -6.982962677686266711E-15, 1.000000000000000000 ) ) ;
#116839=EDGE_LOOP ( 'NONE', ( #87271, #230617, #77675, #20036, #16285 ) ) ;
#116890=ORIENTED_EDGE ( 'NONE', *, *, #144846, .T. ) ;
#116894=ORIENTED_EDGE ( 'NONE', *, *, #687, .T. ) ;
#116918=EDGE_CURVE ( 'NONE', #251509, #137582, #68455, .T. ) ;
#116924=EDGE_CURVE ( 'NONE', #212797, #4741, #211826, .T. ) ;
#116926=ORIENTED_EDGE ( 'NONE', *, *, #60814, .T. ) ;
#116954=AXIS2_PLACEMENT_3D ( 'NONE', #252535, #193868, #234255 ) ;
#116968=LINE ( 'NONE', #97362, #86332 ) ;
#116975=DIRECTION ( 'NONE',  ( -3.265361837132813093E-16, -1.000000000000000000, -7.086529944415894657E-15 ) ) ;
#116983=FACE_OUTER_BOUND ( 'NONE', #163891, .T. ) ;
#116991=CIRCLE ( 'NONE', #137815, 0.09999999999999939493 ) ;
#117048=DIRECTION ( 'NONE',  ( 0.000000000000000000, 7.086529944415886769E-15, -1.000000000000000000 ) ) ;
#117050=DIRECTION ( 'NONE',  ( 0.000000000000000000, -0.01562499999999307672, 0.9998779222360100194 ) ) ;
#117088=EDGE_CURVE ( 'NONE', #65528, #141019, #109951, .T. ) ;
#117105=EDGE_CURVE ( 'NONE', #163070, #67817, #208641, .T. ) ;
#117114=ORIENTED_EDGE ( 'NONE', *, *, #234694, .T. ) ;
#117151=( BOUNDED_SURFACE ( )  B_SPLINE_SURFACE ( 3, 2, ( 
 ( #37768, #33945, #76859 ),
 ( #194281, #93861, #117287 ),
 ( #258022, #192978, #118585 ),
 ( #75613, #155162, #54733 ) ),
 .UNSPECIFIED., .F., .F., .F. ) 
 B_SPLINE_SURFACE_WITH_KNOTS ( ( 4, 4 ),
 ( 3, 3 ),
 ( -3.469446951953614189E-18, 0.001979672783031532438 ),
 ( 0.000000000000000000, 1.000000000000000000 ),
 .UNSPECIFIED. ) 
 GEOMETRIC_REPRESENTATION_ITEM ( )  RATIONAL_B_SPLINE_SURFACE ( (
 ( 1.000000000000000000, 0.7103081912008384347, 1.000000000000000000),
 ( 1.000000000000000000, 0.7104998333558053547, 1.000000000000000000),
 ( 1.000000000000000000, 0.7107238315755477487, 1.000000000000000000),
 ( 1.000000000000000000, 0.7110073749539295163, 1.000000000000000000) ) ) 
 REPRESENTATION_ITEM ( '' )  SURFACE ( )  );
#117166=ORIENTED_EDGE ( 'NONE', *, *, #58530, .F. ) ;
#117188=VERTEX_POINT ( 'NONE', #52093 ) ;
#117231=CARTESIAN_POINT ( 'NONE',  ( -20.94999999999999929, 76.00000000001244871, -170.0231074845243597 ) ) ;
#117261=FACE_OUTER_BOUND ( 'NONE', #62609, .T. ) ;
#117271=VERTEX_POINT ( 'NONE', #233345 ) ;
#117287=CARTESIAN_POINT ( 'NONE',  ( 22.00411653889218400, 75.90096189422571626, -210.7765503521648327 ) ) ;
#117291=ORIENTED_EDGE ( 'NONE', *, *, #55797, .F. ) ;
#117307=CARTESIAN_POINT ( 'NONE',  ( 21.08884785362045378, 69.64280663258743687, -203.5728905795912453 ) ) ;
#117396=DIRECTION ( 'NONE',  ( -0.000000000000000000, 0.1350103645451974088, -0.9908441862701587999 ) ) ;
#117399=ADVANCED_FACE ( 'NONE', ( #38985, #4940 ), #63657, .F. ) ;
#117455=AXIS2_PLACEMENT_3D ( 'NONE', #22807, #81432, #83980 ) ;
#117483=ORIENTED_EDGE ( 'NONE', *, *, #209091, .F. ) ;
#117493=ORIENTED_EDGE ( 'NONE', *, *, #156037, .T. ) ;
#117512=DIRECTION ( 'NONE',  ( 0.000000000000000000, -0.4999999999999088507, 0.8660254037844913322 ) ) ;
#117517=CIRCLE ( 'NONE', #168021, 0.09999999999998898659 ) ;
#117519=VERTEX_POINT ( 'NONE', #105316 ) ;
#117522=ORIENTED_EDGE ( 'NONE', *, *, #213593, .T. ) ;
#117526=ORIENTED_EDGE ( 'NONE', *, *, #64702, .T. ) ;
#117534=AXIS2_PLACEMENT_3D ( 'NONE', #93698, #251481, #127705 ) ;
#117540=ORIENTED_EDGE ( 'NONE', *, *, #155649, .F. ) ;
#117543=ORIENTED_EDGE ( 'NONE', *, *, #199219, .F. ) ;
#117555=DIRECTION ( 'NONE',  ( 0.000000000000000000, -1.000000000000000000, -6.982962677686265922E-15 ) ) ;
#117576=AXIS2_PLACEMENT_3D ( 'NONE', #187564, #125010, #204522 ) ;
#117600=TOROIDAL_SURFACE ( 'NONE', #234108, 1.900000000000002576, 0.1000000000000000056 ) ;
#117639=ADVANCED_FACE ( 'NONE', ( #150903 ), #53079, .T. ) ;
#117653=ORIENTED_EDGE ( 'NONE', *, *, #6057, .F. ) ;
#117665=CARTESIAN_POINT ( 'NONE',  ( 22.60000000000000142, 64.25043287652329127, -203.6239658536231332 ) ) ;
#117684=CARTESIAN_POINT ( 'NONE',  ( 22.45463910399148588, 76.00000000001365663, -215.1726782947082484 ) ) ;
#117696=AXIS2_PLACEMENT_3D ( 'NONE', #191008, #219519, #139966 ) ;
#117711=DIRECTION ( 'NONE',  ( 0.000000000000000000, 0.000000000000000000, -1.000000000000000000 ) ) ;
#117772=EDGE_LOOP ( 'NONE', ( #38656, #132050, #182896 ) ) ;
#117797=ORIENTED_EDGE ( 'NONE', *, *, #175324, .F. ) ;
#117807=DIRECTION ( 'NONE',  ( 0.7071067811865474617, -0.7071067811865474617, -4.937700262164531476E-15 ) ) ;
#117823=CYLINDRICAL_SURFACE ( 'NONE', #88872, 4.000000000000003553 ) ;
#117826=ORIENTED_EDGE ( 'NONE', *, *, #223944, .F. ) ;
#117828=DIRECTION ( 'NONE',  ( -1.000000000000000000, 7.304098846218164250E-16, -4.217023435051628197E-16 ) ) ;
#117829=ORIENTED_EDGE ( 'NONE', *, *, #228516, .T. ) ;
#117830=ORIENTED_EDGE ( 'NONE', *, *, #251332, .F. ) ;
#117839=LINE ( 'NONE', #171445, #155396 ) ;
#117863=ADVANCED_FACE ( 'NONE', ( #80311 ), #41803, .T. ) ;
#117871=ORIENTED_EDGE ( 'NONE', *, *, #1734, .F. ) ;
#117873=CARTESIAN_POINT ( 'NONE',  ( -22.57320508075687115, 64.35000000001268461, -203.5231074845243882 ) ) ;
#117886=CARTESIAN_POINT ( 'NONE',  ( 20.85000000000000142, 64.25000000001249134, -176.8069731475025321 ) ) ;
#117892=DIRECTION ( 'NONE',  ( -1.000000000000000000, 0.000000000000000000, 0.000000000000000000 ) ) ;
#117893=DIRECTION ( 'NONE',  ( 0.000000000000000000, 1.000000000000000000, 7.272083257015735086E-15 ) ) ;
#117967=CARTESIAN_POINT ( 'NONE',  ( 18.59999999999999787, 77.83585931145600512, -158.5186683157258187 ) ) ;
#118015=CARTESIAN_POINT ( 'NONE',  ( -18.50000000000000000, 77.16270174995064224, -195.4231074845243370 ) ) ;
#118021=ORIENTED_EDGE ( 'NONE', *, *, #224787, .T. ) ;
#118037=CARTESIAN_POINT ( 'NONE',  ( -22.50000000000000000, 64.35000000001269882, -203.5231074845244166 ) ) ;
#118045=ORIENTED_EDGE ( 'NONE', *, *, #188234, .F. ) ;
#118061=AXIS2_PLACEMENT_3D ( 'NONE', #177722, #232557, #154326 ) ;
#118098=CARTESIAN_POINT ( 'NONE',  ( 21.05000000000000071, 74.63912941282058000, -195.4501095574334215 ) ) ;
#118110=VECTOR ( 'NONE', #73207, 1000.000000000000000 ) ;
#118153=TOROIDAL_SURFACE ( 'NONE', #5695, 0.6000000000000009770, 0.1000000000000000056 ) ;
#118179=ADVANCED_FACE ( 'NONE', ( #206285 ), #210148, .T. ) ;
#118200=CARTESIAN_POINT ( 'NONE',  ( -23.25000000000000000, 64.35000000001275566, -215.2731074845244450 ) ) ;
#118216=DIRECTION ( 'NONE',  ( 3.616040088954490704E-32, 7.105427357601001859E-15, -1.000000000000000000 ) ) ;
#118249=ADVANCED_FACE ( 'NONE', ( #115959 ), #216158, .F. ) ;
#118251=ADVANCED_FACE ( 'NONE', ( #216321 ), #14310, .F. ) ;
#118279=CIRCLE ( 'NONE', #226579, 0.1000000000000028644 ) ;
#118280=CIRCLE ( 'NONE', #222478, 0.2000000000000057288 ) ;
#118282=ADVANCED_FACE ( 'NONE', ( #101468 ), #199631, .F. ) ;
#118314=CARTESIAN_POINT ( 'NONE',  ( -21.05000000000000426, 69.72991413632355773, -203.5579754875374761 ) ) ;
#118326=CIRCLE ( 'NONE', #139121, 0.1000000000000028644 ) ;
#118370=ORIENTED_EDGE ( 'NONE', *, *, #182440, .F. ) ;
#118380=DIRECTION ( 'NONE',  ( -0.000000000000000000, -1.000000000000000000, -6.982962677686266711E-15 ) ) ;
#118400=ADVANCED_FACE ( 'NONE', ( #218879 ), #40299, .T. ) ;
#118420=ADVANCED_FACE ( 'NONE', ( #13645 ), #210564, .F. ) ;
#118436=AXIS2_PLACEMENT_3D ( 'NONE', #58086, #257534, #159797 ) ;
#118448=CARTESIAN_POINT ( 'NONE',  ( 21.05000000000000071, 71.00000000001253397, -182.4283735034374843 ) ) ;
#118456=EDGE_LOOP ( 'NONE', ( #199103, #246427, #256588, #249734 ) ) ;
#118469=CARTESIAN_POINT ( 'NONE',  ( -20.96428641294330220, 64.25000000001250555, -176.8482143065820651 ) ) ;
#118491=CARTESIAN_POINT ( 'NONE',  ( -21.05000000000000071, 88.41227409416214300, -172.9231074845242802 ) ) ;
#118511=CIRCLE ( 'NONE', #110102, 0.09999999999998898659 ) ;
#118539=CARTESIAN_POINT ( 'NONE',  ( 21.00000000000000000, 66.25000000001260503, -191.1731074845244223 ) ) ;
#118551=VERTEX_POINT ( 'NONE', #253523 ) ;
#118562=EDGE_CURVE ( 'NONE', #81505, #180867, #83038, .T. ) ;
#118578=ADVANCED_FACE ( 'NONE', ( #215672 ), #177872, .F. ) ;
#118585=CARTESIAN_POINT ( 'NONE',  ( 21.53752568622135755, 75.90102553874190505, -210.3099153590729031 ) ) ;
#118588=AXIS2_PLACEMENT_3D ( 'NONE', #15452, #235751, #233224 ) ;
#118597=LINE ( 'NONE', #227948, #179360 ) ;
#118605=DIRECTION ( 'NONE',  ( 0.000000000000000000, 0.000000000000000000, 1.000000000000000000 ) ) ;
#118611=VECTOR ( 'NONE', #178025, 999.9999999999998863 ) ;
#118651=AXIS2_PLACEMENT_3D ( 'NONE', #77687, #159830, #80234 ) ;
#118673=CARTESIAN_POINT ( 'NONE',  ( 21.04999999999908411, 67.22371710472192774, -191.3651984818719143 ) ) ;
#118693=DIRECTION ( 'NONE',  ( -4.239556034732056743E-17, -0.1298341882519953583, -0.9915357197604862671 ) ) ;
#118695=AXIS2_PLACEMENT_3D ( 'NONE', #183015, #4344, #27815 ) ;
#118775=VECTOR ( 'NONE', #147248, 999.9999999999998863 ) ;
#118779=ORIENTED_EDGE ( 'NONE', *, *, #142900, .F. ) ;
#118784=CARTESIAN_POINT ( 'NONE',  ( 20.94999999999999574, 74.14897176987174987, -191.8691942151018850 ) ) ;
#118837=TOROIDAL_SURFACE ( 'NONE', #239626, 2.100000000000002309, 0.1000000000000000056 ) ;
#118870=ORIENTED_EDGE ( 'NONE', *, *, #109079, .F. ) ;
#118911=EDGE_LOOP ( 'NONE', ( #17132, #205627, #86001, #240305 ) ) ;
#118968=CARTESIAN_POINT ( 'NONE',  ( 20.94999999999999574, 65.52661458509973613, -195.9444530202758870 ) ) ;
#118983=CARTESIAN_POINT ( 'NONE',  ( 23.14999999999999503, 64.35000000001249987, -177.0379132551783812 ) ) ;
#118990=DIRECTION ( 'NONE',  ( 1.000000000000000000, -2.952720810173289112E-16, -2.061873921506763405E-30 ) ) ;
#119011=DIRECTION ( 'NONE',  ( 0.000000000000000000, 6.982962677686266711E-15, -1.000000000000000000 ) ) ;
#119022=ORIENTED_EDGE ( 'NONE', *, *, #162615, .T. ) ;
#119027=DIRECTION ( 'NONE',  ( -6.938893903907224433E-15, -1.000000000000000000, -6.982962677686266711E-15 ) ) ;
#119029=CARTESIAN_POINT ( 'NONE',  ( -23.25000000000000000, 87.75000000001247713, -173.1231074845242688 ) ) ;
#119063=DIRECTION ( 'NONE',  ( 0.7071359030027593029, 0.7070776581709197206, 0.000000000000000000 ) ) ;
#119064=ORIENTED_EDGE ( 'NONE', *, *, #73614, .T. ) ;
#119089=DIRECTION ( 'NONE',  ( 2.952720810173289112E-16, 1.000000000000000000, -6.088138035986627436E-46 ) ) ;
#119099=ADVANCED_FACE ( 'NONE', ( #101840 ), #45743, .F. ) ;
#119129=ORIENTED_EDGE ( 'NONE', *, *, #243795, .F. ) ;
#119140=VECTOR ( 'NONE', #105286, 1000.000000000000000 ) ;
#119142=CARTESIAN_POINT ( 'NONE',  ( 21.07954763557393818, 69.67070900997542537, -203.5889834031427483 ) ) ;
#119144=CARTESIAN_POINT ( 'NONE',  ( 18.45036689428337340, 85.49018414334143756, -196.5104116570379347 ) ) ;
#119164=CYLINDRICAL_SURFACE ( 'NONE', #190287, 0.1000000000000072220 ) ;
#119195=EDGE_CURVE ( 'NONE', #242379, #66129, #185261, .T. ) ;
#119205=EDGE_CURVE ( 'NONE', #131204, #204385, #29504, .T. ) ;
#119206=EDGE_CURVE ( 'NONE', #166854, #19071, #37679, .T. ) ;
#119212=VECTOR ( 'NONE', #246380, 1000.000000000000000 ) ;
#119237=VERTEX_POINT ( 'NONE', #15646 ) ;
#119238=CARTESIAN_POINT ( 'NONE',  ( 23.14999999999998437, 64.25000000001269029, -203.5231074845244166 ) ) ;
#119244=DIRECTION ( 'NONE',  ( 0.000000000000000000, 0.000000000000000000, -1.000000000000000000 ) ) ;
#119246=B_SPLINE_CURVE_WITH_KNOTS ( 'NONE', 3,
 ( #83718, #202424, #66773, #100714, #180295, #64203, #143727, #25100, #65473, #145001 ),
 .UNSPECIFIED., .F., .F.,
 ( 4, 2, 2, 2, 4 ),
 ( 0.000000000000000000, 4.221631689688417835E-05, 8.443263379376835670E-05, 0.0001688652675874643971, 0.0003377305351749477678 ),
 .UNSPECIFIED. ) ;
#119249=ORIENTED_EDGE ( 'NONE', *, *, #121745, .T. ) ;
#119274=EDGE_CURVE ( 'NONE', #148199, #236846, #191816, .T. ) ;
#119278=FACE_OUTER_BOUND ( 'NONE', #199237, .T. ) ;
#119302=VERTEX_POINT ( 'NONE', #96410 ) ;
#119303=CARTESIAN_POINT ( 'NONE',  ( 23.14999999999999858, 76.00000000001260503, -190.6481074845243597 ) ) ;
#119351=AXIS2_PLACEMENT_3D ( 'NONE', #253519, #55294, #214399 ) ;
#119357=CARTESIAN_POINT ( 'NONE',  ( -20.85000000000000142, 77.83585931145600512, -158.5186683157258187 ) ) ;
#119359=CARTESIAN_POINT ( 'NONE',  ( -23.15000000000000213, 64.25000000001253397, -182.1731074845244507 ) ) ;
#119380=CARTESIAN_POINT ( 'NONE',  ( 23.14999999999999858, 76.00000000001244871, -170.0231074845243597 ) ) ;
#119402=DIRECTION ( 'NONE',  ( -0.000000000000000000, -0.6132151058540604716, 0.7899159663865477077 ) ) ;
#119429=ADVANCED_FACE ( 'NONE', ( #160287 ), #5003, .F. ) ;
#119436=DIRECTION ( 'NONE',  ( -1.000000000000000000, 0.000000000000000000, 0.000000000000000000 ) ) ;
#119454=CARTESIAN_POINT ( 'NONE',  ( -23.15000000000000213, 64.25000000001249134, -176.8647081744214802 ) ) ;
#119457=CARTESIAN_POINT ( 'NONE',  ( -21.29999999999995808, 76.00000000001264766, -199.4731074845243484 ) ) ;
#119469=AXIS2_PLACEMENT_3D ( 'NONE', #1946, #39837, #257508 ) ;
#119479=CIRCLE ( 'NONE', #140291, 0.09999999999999939493 ) ;
#119509=CARTESIAN_POINT ( 'NONE',  ( 18.31325810956328937, 85.53638847601955320, -163.1546672782194491 ) ) ;
#119520=DIRECTION ( 'NONE',  ( -1.000000000000000000, 2.952720810173289112E-16, 2.061873921506763405E-30 ) ) ;
#119537=AXIS2_PLACEMENT_3D ( 'NONE', #105705, #180154, #1490 ) ;
#119539=CARTESIAN_POINT ( 'NONE',  ( 22.48508240969612615, 75.95372358549585101, -215.1731182160979188 ) ) ;
#119544=CARTESIAN_POINT ( 'NONE',  ( -20.94999999999999929, 87.48912529308871910, -200.4231074845242802 ) ) ;
#119564=ORIENTED_EDGE ( 'NONE', *, *, #4195, .F. ) ;
#119585=ORIENTED_EDGE ( 'NONE', *, *, #67944, .F. ) ;
#119601=LINE ( 'NONE', #99979, #142333 ) ;
#119610=ORIENTED_EDGE ( 'NONE', *, *, #210391, .F. ) ;
#119638=CARTESIAN_POINT ( 'NONE',  ( 18.59999999999999787, 85.40000000001239755, -163.1410656363516125 ) ) ;
#119663=FACE_OUTER_BOUND ( 'NONE', #29164, .T. ) ;
#119669=ORIENTED_EDGE ( 'NONE', *, *, #98431, .F. ) ;
#119692=AXIS2_PLACEMENT_3D ( 'NONE', #31009, #169236, #191360 ) ;
#119713=CARTESIAN_POINT ( 'NONE',  ( -22.50000000000000000, 64.35012909624849442, -203.6056273753975461 ) ) ;
#119732=CARTESIAN_POINT ( 'NONE',  ( -18.50000000000000000, 77.73625713161000306, -191.9544551555068495 ) ) ;
#119735=LINE ( 'NONE', #195431, #186949 ) ;
#119742=TOROIDAL_SURFACE ( 'NONE', #32259, 0.2000000000000000111, 0.1000000000000000056 ) ;
#119757=ORIENTED_EDGE ( 'NONE', *, *, #25219, .F. ) ;
#119761=ORIENTED_EDGE ( 'NONE', *, *, #200865, .F. ) ;
#119813=DIRECTION ( 'NONE',  ( -1.000000000000000000, -0.000000000000000000, -0.000000000000000000 ) ) ;
#119816=LINE ( 'NONE', #199345, #256917 ) ;
#119838=ORIENTED_EDGE ( 'NONE', *, *, #5805, .T. ) ;
#119849=AXIS2_PLACEMENT_3D ( 'NONE', #192752, #153674, #248866 ) ;
#119850=FACE_OUTER_BOUND ( 'NONE', #12969, .T. ) ;
#119855=AXIS2_PLACEMENT_3D ( 'NONE', #117231, #40294, #140630 ) ;
#119862=DIRECTION ( 'NONE',  ( 0.000000000000000000, 0.8660254037844420383, -0.4999999999999941713 ) ) ;
#119944=CARTESIAN_POINT ( 'NONE',  ( -18.50000000000000000, 64.35000000001259934, -191.2731074845244450 ) ) ;
#119963=ORIENTED_EDGE ( 'NONE', *, *, #168909, .F. ) ;
#119967=CARTESIAN_POINT ( 'NONE',  ( 20.84999999999998721, 65.66751761918722252, -164.4282609406112670 ) ) ;
#119983=ORIENTED_EDGE ( 'NONE', *, *, #128372, .F. ) ;
#119984=CARTESIAN_POINT ( 'NONE',  ( 23.24999999999999645, 76.00000000001244871, -170.0231074845243597 ) ) ;
#119996=PLANE ( 'NONE',  #141439 ) ;
#120070=SPHERICAL_SURFACE ( 'NONE', #14576, 0.1000000000000000056 ) ;
#120112=AXIS2_PLACEMENT_3D ( 'NONE', #206493, #169985, #89109 ) ;
#120125=VERTEX_POINT ( 'NONE', #184006 ) ;
#120141=DIRECTION ( 'NONE',  ( -1.000000000000000000, 0.000000000000000000, 0.000000000000000000 ) ) ;
#120144=CIRCLE ( 'NONE', #74357, 0.09999999999998898659 ) ;
#120172=DIRECTION ( 'NONE',  ( -0.7071067811865475727, 0.7071067811865475727, 4.937700262164531476E-15 ) ) ;
#120173=DIRECTION ( 'NONE',  ( 5.421010862427554711E-16, 1.000000000000000000, 1.023556919514279895E-14 ) ) ;
#120175=CARTESIAN_POINT ( 'NONE',  ( 23.14999999999999858, 76.00000000001242029, -166.0231074845243597 ) ) ;
#120233=CIRCLE ( 'NONE', #7781, 0.1000000000000070832 ) ;
#120234=CARTESIAN_POINT ( 'NONE',  ( -18.59999999999999787, 64.25000000001277556, -215.2731074845244450 ) ) ;
#120253=CARTESIAN_POINT ( 'NONE',  ( -23.25000000000000000, 87.65000000001266756, -200.4231074845242802 ) ) ;
#120262=ORIENTED_EDGE ( 'NONE', *, *, #221868, .T. ) ;
#120268=AXIS2_PLACEMENT_3D ( 'NONE', #233418, #13085, #114735 ) ;
#120278=CARTESIAN_POINT ( 'NONE',  ( 20.95539060131842746, 65.37613784235699654, -195.8693736708682422 ) ) ;
#120282=DIRECTION ( 'NONE',  ( -0.000000000000000000, 1.000000000000000000, 6.982962677686266711E-15 ) ) ;
#120334=ADVANCED_FACE ( 'NONE', ( #49634 ), #92365, .T. ) ;
#120338=ORIENTED_EDGE ( 'NONE', *, *, #103012, .T. ) ;
#120344=CARTESIAN_POINT ( 'NONE',  ( 22.60000000000000142, 75.89914163091405896, -215.2726746080137445 ) ) ;
#120359=ADVANCED_FACE ( 'NONE', ( #92598, #32692 ), #112204, .T. ) ;
#120407=ORIENTED_EDGE ( 'NONE', *, *, #155539, .F. ) ;
#120413=CYLINDRICAL_SURFACE ( 'NONE', #156480, 0.09999999999998898659 ) ;
#120429=DIRECTION ( 'NONE',  ( 0.000000000000000000, -7.116814260417660624E-15, 1.000000000000000000 ) ) ;
#120432=CARTESIAN_POINT ( 'NONE',  ( 20.94999999999999929, 65.70729864261056719, -164.5657455973725121 ) ) ;
#120434=TOROIDAL_SURFACE ( 'NONE', #195255, 0.2000000000000000111, 0.1000000000000000056 ) ;
#120494=B_SPLINE_CURVE_WITH_KNOTS ( 'NONE', 3,
 ( #173886, #254628, #214253, #94288, #133429, #51286, #175170, #153031, #171324, #35647 ),
 .UNSPECIFIED., .F., .F.,
 ( 4, 2, 2, 2, 4 ),
 ( 0.000000000000000000, 0.0001584437871624302908, 0.0002376656807436914470, 0.0002772766275343568009, 0.0003168875743250221277 ),
 .UNSPECIFIED. ) ;
#120518=EDGE_LOOP ( 'NONE', ( #162993, #23292, #212070, #146063 ) ) ;
#120551=CARTESIAN_POINT ( 'NONE',  ( -1.739115166359751801E-14, 64.35000000001252829, -178.6731074845244507 ) ) ;
#120553=LINE ( 'NONE', #215762, #257477 ) ;
#120583=VECTOR ( 'NONE', #223099, 1000.000000000000114 ) ;
#120584=VERTEX_POINT ( 'NONE', #181157 ) ;
#120597=AXIS2_PLACEMENT_3D ( 'NONE', #7723, #224179, #85929 ) ;
#120603=ORIENTED_EDGE ( 'NONE', *, *, #47339, .T. ) ;
#120631=LINE ( 'NONE', #3207, #109896 ) ;
#120643=ORIENTED_EDGE ( 'NONE', *, *, #87834, .F. ) ;
#120726=CARTESIAN_POINT ( 'NONE',  ( 18.59999999999998721, 69.15387683765983695, -166.2853812176745691 ) ) ;
#120780=ORIENTED_EDGE ( 'NONE', *, *, #200680, .T. ) ;
#120782=ORIENTED_EDGE ( 'NONE', *, *, #94519, .F. ) ;
#120834=AXIS2_PLACEMENT_3D ( 'NONE', #35227, #155174, #194294 ) ;
#120852=ORIENTED_EDGE ( 'NONE', *, *, #19339, .T. ) ;
#120874=AXIS2_PLACEMENT_3D ( 'NONE', #72951, #76758, #190310 ) ;
#120936=EDGE_CURVE ( 'NONE', #84905, #51335, #34330, .T. ) ;
#120948=ORIENTED_EDGE ( 'NONE', *, *, #196, .F. ) ;
#120983=LINE ( 'NONE', #964, #244565 ) ;
#120996=ADVANCED_FACE ( 'NONE', ( #110269 ), #184672, .F. ) ;
#121003=VERTEX_POINT ( 'NONE', #149429 ) ;
#121005=CARTESIAN_POINT ( 'NONE',  ( -20.54999999999999361, 64.35000000001254250, -182.1731074845244507 ) ) ;
#121023=CIRCLE ( 'NONE', #4456, 0.1000000000000043771 ) ;
#121050=CARTESIAN_POINT ( 'NONE',  ( -21.05315837477644436, 64.25000000001249134, -176.8647514783578742 ) ) ;
#121082=CARTESIAN_POINT ( 'NONE',  ( -23.15000000000000213, 71.65000000001259650, -191.3731074845243825 ) ) ;
#121087=DIRECTION ( 'NONE',  ( -1.836970198721029934E-16, -1.000000000000000000, -6.982962677686266711E-15 ) ) ;
#121118=DIRECTION ( 'NONE',  ( 0.000000000000000000, -0.9999631594459057471, 0.008583690987121077309 ) ) ;
#121143=CARTESIAN_POINT ( 'NONE',  ( -20.94999999999999929, 76.00000000001267608, -203.5231074845243597 ) ) ;
#121165=EDGE_LOOP ( 'NONE', ( #158740, #204396, #48171, #196946 ) ) ;
#121175=ADVANCED_FACE ( 'NONE', ( #51553 ), #114120, .T. ) ;
#121246=DIRECTION ( 'NONE',  ( 1.000000000000000000, 0.000000000000000000, 0.000000000000000000 ) ) ;
#121258=VERTEX_POINT ( 'NONE', #157133 ) ;
#121262=CARTESIAN_POINT ( 'NONE',  ( -21.14999999999999858, 76.00000000001271871, -210.0637644362255969 ) ) ;
#121263=CARTESIAN_POINT ( 'NONE',  ( 21.05095171578076574, 67.22382012124155892, -191.3572342078865347 ) ) ;
#121279=PLANE ( 'NONE',  #254603 ) ;
#121283=VERTEX_POINT ( 'NONE', #4444 ) ;
#121284=CARTESIAN_POINT ( 'NONE',  ( 18.59999999999999787, 77.25000000001239187, -162.2226267301092832 ) ) ;
#121286=DIRECTION ( 'NONE',  ( 0.000000000000000000, 0.000000000000000000, 1.000000000000000000 ) ) ;
#121367=CARTESIAN_POINT ( 'NONE',  ( 21.05000000000000071, 77.84908441863962025, -191.8670969630772163 ) ) ;
#121384=ORIENTED_EDGE ( 'NONE', *, *, #23673, .F. ) ;
#121391=EDGE_LOOP ( 'NONE', ( #36110, #201507, #18449, #219911 ) ) ;
#121419=CARTESIAN_POINT ( 'NONE',  ( 18.49505816908824229, 85.43787255322352792, -163.2454502828533975 ) ) ;
#121421=LINE ( 'NONE', #123964, #19010 ) ;
#121467=DIRECTION ( 'NONE',  ( 1.000000000000000000, -3.265361837132813093E-16, -2.280189983783949500E-30 ) ) ;
#121483=CARTESIAN_POINT ( 'NONE',  ( -20.54999999999999716, 85.00000000001251976, -179.5170766071767332 ) ) ;
#121497=EDGE_LOOP ( 'NONE', ( #216239, #73116, #188065, #191299 ) ) ;
#121498=AXIS2_PLACEMENT_3D ( 'NONE', #145873, #225404, #126317 ) ;
#121504=LINE ( 'NONE', #100589, #221976 ) ;
#121529=CARTESIAN_POINT ( 'NONE',  ( 18.59999999999999787, 76.00000000001267608, -203.5231074845243597 ) ) ;
#121538=AXIS2_PLACEMENT_3D ( 'NONE', #188785, #12749, #70157 ) ;
#121549=FACE_OUTER_BOUND ( 'NONE', #129791, .T. ) ;
#121572=CARTESIAN_POINT ( 'NONE',  ( 20.94999999999999929, 76.00000000001244871, -170.0231074845243597 ) ) ;
#121573=ADVANCED_FACE ( 'NONE', ( #77259 ), #158143, .F. ) ;
#121584=CIRCLE ( 'NONE', #104746, 4.049999999999998046 ) ;
#121593=ORIENTED_EDGE ( 'NONE', *, *, #249887, .F. ) ;
#121608=DIRECTION ( 'NONE',  ( -1.000000000000000000, 0.000000000000000000, -0.000000000000000000 ) ) ;
#121641=AXIS2_PLACEMENT_3D ( 'NONE', #212147, #154752, #15235 ) ;
#121653=ADVANCED_FACE ( 'NONE', ( #95891 ), #77600, .T. ) ;
#121661=ORIENTED_EDGE ( 'NONE', *, *, #99036, .T. ) ;
#121696=DIRECTION ( 'NONE',  ( -0.000000000000000000, -1.000000000000000000, -6.982962677686266711E-15 ) ) ;
#121704=VECTOR ( 'NONE', #6356, 1000.000000000000000 ) ;
#121722=CARTESIAN_POINT ( 'NONE',  ( 21.05000000000000071, 69.52244781751886649, -203.4231075192253115 ) ) ;
#121745=EDGE_CURVE ( 'NONE', #180641, #8118, #256193, .T. ) ;
#121749=DIRECTION ( 'NONE',  ( 1.000000000000000000, 0.000000000000000000, 0.000000000000000000 ) ) ;
#121754=CYLINDRICAL_SURFACE ( 'NONE', #170335, 0.09999999999999939493 ) ;
#121771=CARTESIAN_POINT ( 'NONE',  ( -23.15000000000000213, 87.48912529308852015, -173.0231074845243029 ) ) ;
#121798=DIRECTION ( 'NONE',  ( 1.000000000000000000, 0.000000000000000000, 0.000000000000000000 ) ) ;
#121859=FACE_OUTER_BOUND ( 'NONE', #197364, .T. ) ;
#121888=DIRECTION ( 'NONE',  ( 0.000000000000000000, -6.982962677686266711E-15, 1.000000000000000000 ) ) ;
#121926=CARTESIAN_POINT ( 'NONE',  ( 20.94999999999999574, 69.60000000001261355, -193.5926828544628222 ) ) ;
#121935=TOROIDAL_SURFACE ( 'NONE', #76131, 0.6000000000000013101, 0.1000000000000000056 ) ;
#121940=DIRECTION ( 'NONE',  ( 0.000000000000000000, -0.9887567792719351711, 0.1495327102803594987 ) ) ;
#121964=AXIS2_PLACEMENT_3D ( 'NONE', #60963, #144328, #140493 ) ;
#122024=CIRCLE ( 'NONE', #155382, 0.09999999999999134581 ) ;
#122028=ADVANCED_FACE ( 'NONE', ( #72212 ), #104947, .T. ) ;
#122040=ORIENTED_EDGE ( 'NONE', *, *, #241559, .T. ) ;
#122048=EDGE_CURVE ( 'NONE', #67817, #133612, #147265, .T. ) ;
#122073=CIRCLE ( 'NONE', #9641, 7.899999999999990585 ) ;
#122092=AXIS2_PLACEMENT_3D ( 'NONE', #234184, #254977, #195101 ) ;
#122098=DIRECTION ( 'NONE',  ( 1.000000000000000000, 0.000000000000000000, 0.000000000000000000 ) ) ;
#122134=EDGE_CURVE ( 'NONE', #241009, #151179, #84868, .T. ) ;
#122146=DIRECTION ( 'NONE',  ( -0.000000000000000000, 0.1350103645451945777, -0.9908441862701590219 ) ) ;
#122171=TOROIDAL_SURFACE ( 'NONE', #180425, 0.2000000000000000111, 0.1000000000000000056 ) ;
#122189=CARTESIAN_POINT ( 'NONE',  ( -21.14999999999999858, 69.74218538953657287, -203.6208977758331855 ) ) ;
#122212=ORIENTED_EDGE ( 'NONE', *, *, #114112, .F. ) ;
#122220=AXIS2_PLACEMENT_3D ( 'NONE', #70231, #186306, #205854 ) ;
#122246=DIRECTION ( 'NONE',  ( 1.387778780781405791E-13, 0.9999176327611370985, 0.01283462868040226822 ) ) ;
#122256=CIRCLE ( 'NONE', #226277, 0.09999999999999971412 ) ;
#122304=DIRECTION ( 'NONE',  ( -1.000000000000000000, 0.000000000000000000, -0.000000000000000000 ) ) ;
#122343=ADVANCED_FACE ( 'NONE', ( #191867 ), #172320, .F. ) ;
#122385=EDGE_CURVE ( 'NONE', #172249, #65541, #39334, .T. ) ;
#122388=EDGE_CURVE ( 'NONE', #116802, #97945, #8436, .T. ) ;
#122412=CARTESIAN_POINT ( 'NONE',  ( 20.94999999999999929, 70.15000000001252545, -180.1556047088023149 ) ) ;
#122431=ADVANCED_FACE ( 'NONE', ( #234812 ), #251686, .F. ) ;
#122512=ORIENTED_EDGE ( 'NONE', *, *, #100180, .F. ) ;
#122532=DIRECTION ( 'NONE',  ( 1.000000000000000000, 0.000000000000000000, 0.000000000000000000 ) ) ;
#122568=AXIS2_PLACEMENT_3D ( 'NONE', #126397, #122572, #82112 ) ;
#122572=DIRECTION ( 'NONE',  ( 0.000000000000000000, 6.982962677686266711E-15, -1.000000000000000000 ) ) ;
#122575=DIRECTION ( 'NONE',  ( 1.000000000000000000, 0.000000000000000000, 0.000000000000000000 ) ) ;
#122632=CARTESIAN_POINT ( 'NONE',  ( -20.54999999999999716, 85.50000000001251976, -179.9170766071767389 ) ) ;
#122652=ORIENTED_EDGE ( 'NONE', *, *, #26090, .T. ) ;
#122656=CIRCLE ( 'NONE', #126732, 0.09999999999998898659 ) ;
#122707=CARTESIAN_POINT ( 'NONE',  ( 18.59999999999999076, 69.55000000001261640, -193.5060803140843859 ) ) ;
#122722=DIRECTION ( 'NONE',  ( 0.000000000000000000, 0.000000000000000000, -1.000000000000000000 ) ) ;
#122740=TOROIDAL_SURFACE ( 'NONE', #222641, 4.149999999999999467, 0.1000000000000000056 ) ;
#122747=DIRECTION ( 'NONE',  ( 0.000000000000000000, 6.982962677686266711E-15, -1.000000000000000000 ) ) ;
#122787=VERTEX_POINT ( 'NONE', #234490 ) ;
#122809=EDGE_CURVE ( 'NONE', #34777, #172898, #97134, .T. ) ;
#122846=CARTESIAN_POINT ( 'NONE',  ( -18.59999999999999787, 77.73625713161000306, -191.9544551555068495 ) ) ;
#122852=DIRECTION ( 'NONE',  ( 0.000000000000000000, 6.982962677686266711E-15, -1.000000000000000000 ) ) ;
#122866=DIRECTION ( 'NONE',  ( 0.000000000000000000, 0.8660254037844420383, -0.4999999999999943379 ) ) ;
#122880=AXIS2_PLACEMENT_3D ( 'NONE', #88711, #7930, #105699 ) ;
#122927=DIRECTION ( 'NONE',  ( 0.000000000000000000, 0.000000000000000000, -1.000000000000000000 ) ) ;
#122970=CARTESIAN_POINT ( 'NONE',  ( 21.14999999999999858, 69.45000000001259366, -191.3731074845244109 ) ) ;
#122999=CARTESIAN_POINT ( 'NONE',  ( 21.05000000000000426, 69.69981666374641804, -203.5744349168663518 ) ) ;
#123012=CARTESIAN_POINT ( 'NONE',  ( -20.85000000000000142, 68.97833521811233481, -166.1895420826271277 ) ) ;
#123022=FACE_OUTER_BOUND ( 'NONE', #184839, .T. ) ;
#123061=CARTESIAN_POINT ( 'NONE',  ( 22.50000000000000000, 64.35042919246788529, -203.6231074845244393 ) ) ;
#123116=ORIENTED_EDGE ( 'NONE', *, *, #110298, .F. ) ;
#123119=CARTESIAN_POINT ( 'NONE',  ( 23.14999999999999858, 74.00000000001244871, -170.0231074845243882 ) ) ;
#123129=ORIENTED_EDGE ( 'NONE', *, *, #18212, .F. ) ;
#123133=ADVANCED_FACE ( 'NONE', ( #168810 ), #41811, .T. ) ;
#123145=ORIENTED_EDGE ( 'NONE', *, *, #47322, .T. ) ;
#123207=ORIENTED_EDGE ( 'NONE', *, *, #139590, .F. ) ;
#123227=CARTESIAN_POINT ( 'NONE',  ( 21.04999999999999716, 76.01454569058479649, -210.0201252709573794 ) ) ;
#123241=CARTESIAN_POINT ( 'NONE',  ( 21.13461538461538325, 67.11458296203812779, -191.2731074845244166 ) ) ;
#123270=AXIS2_PLACEMENT_3D ( 'NONE', #165806, #143639, #146203 ) ;
#123273=CARTESIAN_POINT ( 'NONE',  ( 20.85000000000000142, 77.83585931145600512, -158.5186683157258187 ) ) ;
#123274=ORIENTED_EDGE ( 'NONE', *, *, #78606, .T. ) ;
#123281=AXIS2_PLACEMENT_3D ( 'NONE', #112222, #134310, #161294 ) ;
#123288=CARTESIAN_POINT ( 'NONE',  ( 21.05000000000000071, 76.08561306081669784, -209.9368672183346405 ) ) ;
#123293=EDGE_LOOP ( 'NONE', ( #109952, #29145, #83605, #1464 ) ) ;
#123304=AXIS2_PLACEMENT_3D ( 'NONE', #169148, #170448, #209521 ) ;
#123325=AXIS2_PLACEMENT_3D ( 'NONE', #164501, #65382, #108372 ) ;
#123342=DIRECTION ( 'NONE',  ( 0.000000000000000000, -0.9998779222360104635, -0.01562499999996343723 ) ) ;
#123358=DIRECTION ( 'NONE',  ( 0.000000000000000000, 0.000000000000000000, 1.000000000000000000 ) ) ;
#123396=CARTESIAN_POINT ( 'NONE',  ( 21.08078803292166015, 69.66698703557557337, -203.6022934716821737 ) ) ;
#123417=EDGE_CURVE ( 'NONE', #200908, #252901, #35048, .T. ) ;
#123505=CIRCLE ( 'NONE', #11075, 4.300000000000025580 ) ;
#123540=CARTESIAN_POINT ( 'NONE',  ( -21.11927991906891222, 75.99091632053885803, -209.9716006030158724 ) ) ;
#123548=DIRECTION ( 'NONE',  ( -0.000000000000000000, 1.000000000000000000, 7.525063763929033127E-15 ) ) ;
#123549=ORIENTED_EDGE ( 'NONE', *, *, #180656, .F. ) ;
#123561=EDGE_LOOP ( 'NONE', ( #64030, #217213, #211394, #57723 ) ) ;
#123562=DIRECTION ( 'NONE',  ( 0.000000000000000000, -2.775557561563196798E-13, -1.000000000000000000 ) ) ;
#123567=EDGE_CURVE ( 'NONE', #160419, #70041, #177484, .T. ) ;
#123694=CARTESIAN_POINT ( 'NONE',  ( -20.64999999999999858, 73.60000000001254250, -183.2477294072864709 ) ) ;
#123713=ORIENTED_EDGE ( 'NONE', *, *, #252808, .F. ) ;
#123727=CARTESIAN_POINT ( 'NONE',  ( 18.49999999999999289, 65.79142135392936552, -178.8206006188949004 ) ) ;
#123728=DIRECTION ( 'NONE',  ( 0.000000000000000000, -7.147358527629766941E-15, 1.000000000000000000 ) ) ;
#123742=ORIENTED_EDGE ( 'NONE', *, *, #123567, .F. ) ;
#123777=DIRECTION ( 'NONE',  ( -0.000000000000000000, 0.8660254037844377084, 0.5000000000000016653 ) ) ;
#123798=CIRCLE ( 'NONE', #11179, 11.70000000000001528 ) ;
#123801=EDGE_CURVE ( 'NONE', #145080, #255597, #108188, .T. ) ;
#123816=DIRECTION ( 'NONE',  ( 0.000000000000000000, 7.116814260417668513E-15, -1.000000000000000000 ) ) ;
#123824=DIRECTION ( 'NONE',  ( 0.000000000000000000, 6.982962677686267499E-15, -1.000000000000000000 ) ) ;
#123840=CARTESIAN_POINT ( 'NONE',  ( -20.64999999999999858, 68.85000000001259934, -191.2731074845244166 ) ) ;
#123871=SPHERICAL_SURFACE ( 'NONE', #57256, 0.1000000000000000056 ) ;
#123883=FACE_OUTER_BOUND ( 'NONE', #224964, .T. ) ;
#123902=CYLINDRICAL_SURFACE ( 'NONE', #68380, 4.000000000000003553 ) ;
#123907=LINE ( 'NONE', #187738, #183563 ) ;
#123921=VERTEX_POINT ( 'NONE', #252810 ) ;
#123935=CARTESIAN_POINT ( 'NONE',  ( 21.05000000000000071, 67.07338541492552508, -195.0514244653012952 ) ) ;
#123944=EDGE_LOOP ( 'NONE', ( #253769, #92898, #29666, #211048 ) ) ;
#123964=CARTESIAN_POINT ( 'NONE',  ( 23.14999999999999503, 61.95000000001248708, -175.5368025552853624 ) ) ;
#123966=CARTESIAN_POINT ( 'NONE',  ( -21.05000000000000071, 64.40000000001249703, -176.9513107147999449 ) ) ;
#123999=AXIS2_PLACEMENT_3D ( 'NONE', #125535, #172411, #113670 ) ;
#124006=( BOUNDED_SURFACE ( )  B_SPLINE_SURFACE ( 3, 2, ( 
 ( #193011, #247751, #40914 ),
 ( #126524, #100807, #139957 ),
 ( #198666, #66555, #125243 ),
 ( #79975, #27470, #46963 ),
 ( #144778, #159556, #146072 ),
 ( #180400, #119144, #26152 ),
 ( #206059, #246466, #207358 ),
 ( #239088, #106943, #224334 ) ),
 .UNSPECIFIED., .F., .F., .F. ) 
 B_SPLINE_SURFACE_WITH_KNOTS ( ( 4, 2, 2, 4 ),
 ( 3, 3 ),
 ( 0.0001704874539069695018, 0.0003809798300636461129, 0.0004862260181419844184, 0.0005914722062203227240 ),
 ( 0.000000000000000000, 1.000000000000000000 ),
 .UNSPECIFIED. ) 
 GEOMETRIC_REPRESENTATION_ITEM ( )  RATIONAL_B_SPLINE_SURFACE ( (
 ( 1.000000000000000000, 0.7071067811865302533, 1.000000000000000000),
 ( 1.000000000000000000, 0.7670648383570790596, 1.000000000000000000),
 ( 1.000000000000000000, 0.8204820770259678708, 1.000000000000000000),
 ( 1.000000000000000000, 0.8877218296110218620, 1.000000000000000000),
 ( 1.000000000000000000, 0.9080815932661593370, 1.000000000000000000),
 ( 1.000000000000000000, 0.9395541505865371290, 1.000000000000000000),
 ( 1.000000000000000000, 0.9506520335376564823, 1.000000000000000000),
 ( 1.000000000000000000, 0.9504532311154358926, 1.000000000000000000) ) ) 
 REPRESENTATION_ITEM ( '' )  SURFACE ( )  );
#124068=DIRECTION ( 'NONE',  ( 0.000000000000000000, 0.000000000000000000, 1.000000000000000000 ) ) ;
#124087=EDGE_LOOP ( 'NONE', ( #110467, #184984, #241627, #58412 ) ) ;
#124105=CARTESIAN_POINT ( 'NONE',  ( 20.95576188350343116, 65.39101945504923208, -195.9118737617701242 ) ) ;
#124114=CARTESIAN_POINT ( 'NONE',  ( 23.14999999999999147, 76.00000000001267608, -203.5231074845243597 ) ) ;
#124119=AXIS2_PLACEMENT_3D ( 'NONE', #242199, #123548, #64844 ) ;
#124151=CARTESIAN_POINT ( 'NONE',  ( 21.05000000000000071, 71.00000000001260503, -191.1178414656112921 ) ) ;
#124169=VECTOR ( 'NONE', #62819, 999.9999999999998863 ) ;
#124174=DIRECTION ( 'NONE',  ( 1.000000000000000000, 0.000000000000000000, 0.000000000000000000 ) ) ;
#124181=CIRCLE ( 'NONE', #123999, 0.09999999999998898659 ) ;
#124207=EDGE_LOOP ( 'NONE', ( #254411, #225132, #161651, #149419 ) ) ;
#124223=EDGE_CURVE ( 'NONE', #51521, #11973, #58130, .T. ) ;
#124257=EDGE_CURVE ( 'NONE', #119302, #118551, #217211, .T. ) ;
#124262=ORIENTED_EDGE ( 'NONE', *, *, #148542, .F. ) ;
#124264=EDGE_LOOP ( 'NONE', ( #181926, #164408, #167232, #20705, #174448, #230433, #187624, #202881, #203209, #126701, #251871, #97818 ) ) ;
#124281=CARTESIAN_POINT ( 'NONE',  ( 21.05000000000000071, 88.41227409416215721, -173.0231074845242745 ) ) ;
#124283=CARTESIAN_POINT ( 'NONE',  ( -20.94999999999999929, 87.48912529308871910, -200.6231074845242688 ) ) ;
#124290=CARTESIAN_POINT ( 'NONE',  ( -18.49499033040906681, 85.43814877175731226, -196.3249542586008829 ) ) ;
#124302=ORIENTED_EDGE ( 'NONE', *, *, #205455, .F. ) ;
#124319=LINE ( 'NONE', #46049, #198504 ) ;
#124354=CARTESIAN_POINT ( 'NONE',  ( -23.15000000000000213, 76.00000000001267608, -203.5231074845243597 ) ) ;
#124362=EDGE_CURVE ( 'NONE', #128423, #130315, #135311, .T. ) ;
#124371=CARTESIAN_POINT ( 'NONE',  ( 21.05000000000000071, 76.00000000001267608, -203.5231074845243597 ) ) ;
#124402=ORIENTED_EDGE ( 'NONE', *, *, #57912, .F. ) ;
#124414=CYLINDRICAL_SURFACE ( 'NONE', #253114, 0.1000000000000070832 ) ;
#124429=EDGE_CURVE ( 'NONE', #35701, #156136, #56197, .T. ) ;
#124445=ORIENTED_EDGE ( 'NONE', *, *, #48442, .F. ) ;
#124479=AXIS2_PLACEMENT_3D ( 'NONE', #132092, #211641, #236474 ) ;
#124484=CARTESIAN_POINT ( 'NONE',  ( 21.04116576186320486, 65.37533692126123697, -191.1945257158966740 ) ) ;
#124506=CARTESIAN_POINT ( 'NONE',  ( 20.94999999999999574, 77.16270174995064224, -195.5231074845243313 ) ) ;
#124528=TOROIDAL_SURFACE ( 'NONE', #66270, 12.77499999999999858, 0.1000000000000000056 ) ;
#124535=ORIENTED_EDGE ( 'NONE', *, *, #141194, .T. ) ;
#124537=CARTESIAN_POINT ( 'NONE',  ( 21.06086055315980232, 67.22529248505637156, -191.3207853293704090 ) ) ;
#124553=CARTESIAN_POINT ( 'NONE',  ( 22.60000000000000142, 64.25043287652329127, -203.6239658536231332 ) ) ;
#124556=CARTESIAN_POINT ( 'NONE',  ( -23.15000000000000213, 76.00000000001253397, -181.8231074845243711 ) ) ;
#124568=ORIENTED_EDGE ( 'NONE', *, *, #73564, .T. ) ;
#124586=ADVANCED_FACE ( 'NONE', ( #228804 ), #30613, .F. ) ;
#124597=CARTESIAN_POINT ( 'NONE',  ( -20.94999999999999929, 65.70729864261056719, -164.5657455973725121 ) ) ;
#124623=LINE ( 'NONE', #127191, #116619 ) ;
#124643=DIRECTION ( 'NONE',  ( -1.000000000000000000, -0.000000000000000000, -0.000000000000000000 ) ) ;
#124676=ORIENTED_EDGE ( 'NONE', *, *, #124223, .T. ) ;
#124685=ORIENTED_EDGE ( 'NONE', *, *, #65525, .F. ) ;
#124723=CIRCLE ( 'NONE', #74691, 0.1000000000000026007 ) ;
#124732=CIRCLE ( 'NONE', #12317, 0.2000000000000057288 ) ;
#124741=EDGE_CURVE ( 'NONE', #68342, #201210, #189679, .T. ) ;
#124747=CARTESIAN_POINT ( 'NONE',  ( -18.59999999999999787, 70.05000000001267324, -193.2174051794895320 ) ) ;
#124753=AXIS2_PLACEMENT_3D ( 'NONE', #182901, #158229, #122927 ) ;
#124761=EDGE_CURVE ( 'NONE', #33564, #14366, #56381, .T. ) ;
#124785=EDGE_CURVE ( 'NONE', #248274, #76140, #222984, .T. ) ;
#124796=DIRECTION ( 'NONE',  ( -0.000000000000000000, 6.982962677686266711E-15, -1.000000000000000000 ) ) ;
#124832=CARTESIAN_POINT ( 'NONE',  ( -20.94999999999999929, 76.00000000001244871, -170.0231074845243597 ) ) ;
#124852=DIRECTION ( 'NONE',  ( -1.000000000000000000, 0.000000000000000000, -0.000000000000000000 ) ) ;
#124859=ORIENTED_EDGE ( 'NONE', *, *, #252808, .T. ) ;
#124886=AXIS2_PLACEMENT_3D ( 'NONE', #250720, #128222, #207776 ) ;
#124894=ORIENTED_EDGE ( 'NONE', *, *, #206377, .F. ) ;
#124895=CARTESIAN_POINT ( 'NONE',  ( 23.15000000000000213, 84.66355140188177586, -193.9990063664569959 ) ) ;
#124908=VERTEX_POINT ( 'NONE', #246446 ) ;
#124921=FACE_OUTER_BOUND ( 'NONE', #152106, .T. ) ;
#124924=ORIENTED_EDGE ( 'NONE', *, *, #68496, .T. ) ;
#124945=VERTEX_POINT ( 'NONE', #52075 ) ;
#124951=CARTESIAN_POINT ( 'NONE',  ( -21.64999999999999858, 68.75000000001260503, -191.2731074845244166 ) ) ;
#124978=DIRECTION ( 'NONE',  ( 1.000000000000000000, -0.000000000000000000, 0.000000000000000000 ) ) ;
#125010=DIRECTION ( 'NONE',  ( -1.000000000000000000, 0.000000000000000000, -0.000000000000000000 ) ) ;
#125015=CARTESIAN_POINT ( 'NONE',  ( 18.49999999999999289, 65.75000000001250555, -178.8731074845244109 ) ) ;
#125024=VERTEX_POINT ( 'NONE', #187771 ) ;
#125027=DIRECTION ( 'NONE',  ( -1.000000000000000000, 0.000000000000000000, -0.000000000000000000 ) ) ;
#125036=B_SPLINE_CURVE_WITH_KNOTS ( 'NONE', 3,
 ( #189499, #30434, #10862, #173832, #171265, #232493, #92951, #150380, #51233, #72130, #130794, #210349, #212910, #31738, #111240, #34300, #252025, #190811, #12165 ),
 .UNSPECIFIED., .F., .F.,
 ( 4, 3, 3, 3, 3, 3, 4 ),
 ( 1.387778780781445521E-17, 2.646747978909188838E-05, 5.271166642128437155E-05, 9.008788829884586393E-05, 0.0001426648776560943404, 0.0001897378458659839079, 0.0001917382627806266040 ),
 .UNSPECIFIED. ) ;
#125059=TOROIDAL_SURFACE ( 'NONE', #100072, 11.65000000000000036, 0.1000000000000000056 ) ;
#125090=ORIENTED_EDGE ( 'NONE', *, *, #86238, .F. ) ;
#125096=DIRECTION ( 'NONE',  ( -1.000000000000000000, 2.952720810173289112E-16, 2.061873921506763405E-30 ) ) ;
#125102=AXIS2_PLACEMENT_3D ( 'NONE', #85147, #46051, #66904 ) ;
#125105=CARTESIAN_POINT ( 'NONE',  ( -20.94999999999999929, 87.48912529308852015, -172.9231074845242802 ) ) ;
#125110=CARTESIAN_POINT ( 'NONE',  ( 21.05000000000000071, 77.73625713161000306, -191.9544551555068495 ) ) ;
#125136=EDGE_LOOP ( 'NONE', ( #84090, #165860, #13522, #181886 ) ) ;
#125156=AXIS2_PLACEMENT_3D ( 'NONE', #70488, #28803, #9187 ) ;
#125201=ORIENTED_EDGE ( 'NONE', *, *, #134463, .T. ) ;
#125205=CIRCLE ( 'NONE', #25259, 0.09999999999998898659 ) ;
#125211=DIRECTION ( 'NONE',  ( -0.000000000000000000, -6.982962677686266711E-15, 1.000000000000000000 ) ) ;
#125235=ORIENTED_EDGE ( 'NONE', *, *, #32590, .F. ) ;
#125243=CARTESIAN_POINT ( 'NONE',  ( 18.58703555225034876, 85.40633674080154947, -196.3981628432776461 ) ) ;
#125247=PLANE ( 'NONE',  #61036 ) ;
#125271=DIRECTION ( 'NONE',  ( 1.000000000000000000, 0.000000000000000000, 0.000000000000000000 ) ) ;
#125285=DIRECTION ( 'NONE',  ( 1.000000000000000000, 0.000000000000000000, 0.000000000000000000 ) ) ;
#125300=EDGE_LOOP ( 'NONE', ( #66100, #62658, #127589, #233462 ) ) ;
#125317=CARTESIAN_POINT ( 'NONE',  ( 20.46382478191414833, 65.40137955871524866, -195.8452930151790099 ) ) ;
#125347=EDGE_CURVE ( 'NONE', #222996, #188810, #17293, .T. ) ;
#125358=EDGE_CURVE ( 'NONE', #63948, #48255, #238901, .T. ) ;
#125389=CARTESIAN_POINT ( 'NONE',  ( 20.85000000000000142, 77.26327546522965406, -162.1212428177779543 ) ) ;
#125487=VERTEX_POINT ( 'NONE', #88780 ) ;
#125507=VERTEX_POINT ( 'NONE', #247877 ) ;
#125532=EDGE_LOOP ( 'NONE', ( #209012, #222695, #28265, #221896 ) ) ;
#125535=CARTESIAN_POINT ( 'NONE',  ( -20.94999999999999929, 77.83534155023700407, -191.9679561919613491 ) ) ;
#125557=AXIS2_PLACEMENT_3D ( 'NONE', #71511, #191469, #251402 ) ;
#125622=AXIS2_PLACEMENT_3D ( 'NONE', #164814, #46135, #141382 ) ;
#125633=DIRECTION ( 'NONE',  ( 0.000000000000000000, -7.086529944415886769E-15, 1.000000000000000000 ) ) ;
#125641=EDGE_LOOP ( 'NONE', ( #28944, #183136, #192862, #44172 ) ) ;
#125680=CARTESIAN_POINT ( 'NONE',  ( -18.59999999999999787, 65.66751761918722252, -164.4282609406112670 ) ) ;
#125761=ORIENTED_EDGE ( 'NONE', *, *, #162795, .F. ) ;
#125769=CARTESIAN_POINT ( 'NONE',  ( 20.19326291201646129, 65.84393901210869160, -195.7612456769175253 ) ) ;
#125780=CARTESIAN_POINT ( 'NONE',  ( 21.04999999999999716, 75.94851711813100792, -209.8232873024375635 ) ) ;
#125798=CARTESIAN_POINT ( 'NONE',  ( 20.95512828230159030, 67.12384868768731394, -191.3206772190213485 ) ) ;
#125800=ORIENTED_EDGE ( 'NONE', *, *, #161407, .T. ) ;
#125815=CARTESIAN_POINT ( 'NONE',  ( -23.25000000000000000, 76.00000000001244871, -170.0231074845243597 ) ) ;
#125831=DIRECTION ( 'NONE',  ( 0.000000000000000000, 6.938893903907222067E-15, -1.000000000000000000 ) ) ;
#125849=CARTESIAN_POINT ( 'NONE',  ( 20.94999999999999929, 85.50000000001251976, -179.9170766071767389 ) ) ;
#125851=CARTESIAN_POINT ( 'NONE',  ( -20.86777300164944648, 65.66799936921584901, -164.4299399888601556 ) ) ;
#125867=CIRCLE ( 'NONE', #159231, 0.09999999999999938105 ) ;
#125896=CARTESIAN_POINT ( 'NONE',  ( -21.14999999999999858, 69.45934304831143891, -203.5231074845243882 ) ) ;
#125905=ADVANCED_FACE ( 'NONE', ( #194999 ), #94579, .F. ) ;
#125923=CARTESIAN_POINT ( 'NONE',  ( 18.59999999999999076, 65.75000000001251976, -178.7731074845244450 ) ) ;
#125926=DIRECTION ( 'NONE',  ( 0.000000000000000000, 6.982962677686266711E-15, -1.000000000000000000 ) ) ;
#125954=DIRECTION ( 'NONE',  ( 0.000000000000000000, -7.147358527629766941E-15, 1.000000000000000000 ) ) ;
#125996=FACE_OUTER_BOUND ( 'NONE', #123293, .T. ) ;
#126046=CARTESIAN_POINT ( 'NONE',  ( -21.53752568617682783, 69.21319212550889688, -203.6220819458087306 ) ) ;
#126047=FACE_OUTER_BOUND ( 'NONE', #134990, .T. ) ;
#126095=CIRCLE ( 'NONE', #167648, 0.09999999999998712696 ) ;
#126107=DIRECTION ( 'NONE',  ( 1.000000000000000000, 0.000000000000000000, 0.000000000000000000 ) ) ;
#126140=CIRCLE ( 'NONE', #13731, 12.87499999999999822 ) ;
#126156=DIRECTION ( 'NONE',  ( -1.000000000000000000, 0.000000000000000000, 0.000000000000000000 ) ) ;
#126157=FACE_OUTER_BOUND ( 'NONE', #250559, .T. ) ;
#126205=CARTESIAN_POINT ( 'NONE',  ( -23.15000000000000213, 71.65000000001253966, -182.1731074845243938 ) ) ;
#126229=ORIENTED_EDGE ( 'NONE', *, *, #151169, .F. ) ;
#126241=CARTESIAN_POINT ( 'NONE',  ( -20.94999999999999929, 74.26374286841520700, -191.9544551555068779 ) ) ;
#126267=DIRECTION ( 'NONE',  ( 1.000000000000000000, -2.952720810173289112E-16, -2.061873921506763405E-30 ) ) ;
#126271=CIRCLE ( 'NONE', #17929, 0.09999999999999939493 ) ;
#126303=EDGE_LOOP ( 'NONE', ( #62542, #23790, #206374, #173634 ) ) ;
#126317=DIRECTION ( 'NONE',  ( 0.000000000000000000, -0.9908441862701791170, 0.1350103645450472789 ) ) ;
#126318=AXIS2_PLACEMENT_3D ( 'NONE', #142042, #24701, #79491 ) ;
#126328=CIRCLE ( 'NONE', #63795, 0.09999999999998898659 ) ;
#126342=ORIENTED_EDGE ( 'NONE', *, *, #183129, .T. ) ;
#126373=FACE_OUTER_BOUND ( 'NONE', #74884, .T. ) ;
#126378=CARTESIAN_POINT ( 'NONE',  ( -21.05000000000000071, 77.26178616857765746, -195.4366085209788935 ) ) ;
#126397=CARTESIAN_POINT ( 'NONE',  ( 21.14999999999999858, 64.35000000001275566, -215.2731074845244450 ) ) ;
#126400=CARTESIAN_POINT ( 'NONE',  ( -20.94999999999999929, 77.25000000001263345, -195.5231074845243313 ) ) ;
#126414=CARTESIAN_POINT ( 'NONE',  ( -20.85000000000000142, 69.06610602788607878, -166.2374616501508342 ) ) ;
#126421=ORIENTED_EDGE ( 'NONE', *, *, #69411, .F. ) ;
#126426=DIRECTION ( 'NONE',  ( 1.000000000000000000, 0.000000000000000000, 0.000000000000000000 ) ) ;
#126454=EDGE_CURVE ( 'NONE', #28788, #105519, #207528, .T. ) ;
#126464=EDGE_CURVE ( 'NONE', #116410, #7857, #61604, .T. ) ;
#126474=VERTEX_POINT ( 'NONE', #242775 ) ;
#126487=VECTOR ( 'NONE', #35324, 1000.000000000000000 ) ;
#126506=CIRCLE ( 'NONE', #247101, 0.5000000000000004441 ) ;
#126521=DIRECTION ( 'NONE',  ( 2.557131231893037478E-16, 0.8660254037844420383, -0.4999999999999943379 ) ) ;
#126524=CARTESIAN_POINT ( 'NONE',  ( 18.50000000000000355, 85.42145614550778987, -196.2811254005050330 ) ) ;
#126529=LINE ( 'NONE', #147375, #148548 ) ;
#126551=DIRECTION ( 'NONE',  ( 0.000000000000000000, -7.034366652768095332E-15, 1.000000000000000000 ) ) ;
#126554=DIRECTION ( 'NONE',  ( -1.836970198721029934E-16, -1.000000000000000000, -6.982962677686266711E-15 ) ) ;
#126566=B_SPLINE_CURVE_WITH_KNOTS ( 'NONE', 3,
 ( #240921, #67411, #42714, #7429, #243478, #102657, #184787, #86944, #64834, #166545, #84350, #165229, #204341, #4838, #123540, #220072, #85649, #63551, #81802 ),
 .UNSPECIFIED., .F., .F.,
 ( 4, 3, 3, 3, 3, 3, 4 ),
 ( 0.000000000000000000, 1.655171619026472822E-05, 2.773500582848447909E-05, 5.941817267378178010E-05, 0.0001114174635873323616, 0.0001914169455916120898, 0.0002627181070750313511 ),
 .UNSPECIFIED. ) ;
#126579=DIRECTION ( 'NONE',  ( 1.000000000000000000, 0.000000000000000000, 0.000000000000000000 ) ) ;
#126618=ORIENTED_EDGE ( 'NONE', *, *, #59620, .F. ) ;
#126628=LINE ( 'NONE', #78805, #237869 ) ;
#126662=DIRECTION ( 'NONE',  ( 1.000000000000000000, 0.000000000000000000, 0.000000000000000000 ) ) ;
#126663=LINE ( 'NONE', #9283, #184601 ) ;
#126679=AXIS2_PLACEMENT_3D ( 'NONE', #84687, #6467, #83413 ) ;
#126701=ORIENTED_EDGE ( 'NONE', *, *, #162393, .T. ) ;
#126732=AXIS2_PLACEMENT_3D ( 'NONE', #130687, #111132, #231103 ) ;
#126733=ORIENTED_EDGE ( 'NONE', *, *, #254182, .F. ) ;
#126793=AXIS2_PLACEMENT_3D ( 'NONE', #213768, #52106, #36441 ) ;
#126805=CYLINDRICAL_SURFACE ( 'NONE', #60703, 0.09999999999999939493 ) ;
#126806=AXIS2_PLACEMENT_3D ( 'NONE', #18796, #257350, #78759 ) ;
#126817=VECTOR ( 'NONE', #199263, 1000.000000000000000 ) ;
#126829=AXIS2_PLACEMENT_3D ( 'NONE', #246355, #12902, #87255 ) ;
#126837=EDGE_CURVE ( 'NONE', #37214, #113112, #222903, .T. ) ;
#126861=EDGE_LOOP ( 'NONE', ( #183266, #94970, #85123, #96829 ) ) ;
#126865=DIRECTION ( 'NONE',  ( 0.000000000000000000, 0.000000000000000000, -1.000000000000000000 ) ) ;
#126922=DIRECTION ( 'NONE',  ( 0.000000000000000000, 0.9908441862701791170, -0.1350103645450472789 ) ) ;
#126930=DIRECTION ( 'NONE',  ( 1.000000000000000000, 0.000000000000000000, 0.000000000000000000 ) ) ;
#126960=DIRECTION ( 'NONE',  ( 0.000000000000000000, -6.982962677686266711E-15, 1.000000000000000000 ) ) ;
#126984=CIRCLE ( 'NONE', #14579, 7.791421356237310469 ) ;
#126992=DIRECTION ( 'NONE',  ( -0.000000000000000000, -6.982962677686266711E-15, 1.000000000000000000 ) ) ;
#127016=EDGE_CURVE ( 'NONE', #44671, #46048, #93671, .T. ) ;
#127032=ORIENTED_EDGE ( 'NONE', *, *, #201790, .T. ) ;
#127047=DIRECTION ( 'NONE',  ( 1.000000000000000000, 0.000000000000000000, 0.000000000000000000 ) ) ;
#127111=FACE_OUTER_BOUND ( 'NONE', #252425, .T. ) ;
#127123=VERTEX_POINT ( 'NONE', #106475 ) ;
#127124=CARTESIAN_POINT ( 'NONE',  ( 22.39999999999999503, 76.00000000001273293, -211.2731074845243882 ) ) ;
#127163=EDGE_LOOP ( 'NONE', ( #86895, #150731, #201771, #209529, #192202 ) ) ;
#127166=ORIENTED_EDGE ( 'NONE', *, *, #111316, .T. ) ;
#127183=ORIENTED_EDGE ( 'NONE', *, *, #193492, .F. ) ;
#127191=CARTESIAN_POINT ( 'NONE',  ( -21.05000000000000071, 87.75000000001247713, -173.0231074845243029 ) ) ;
#127207=DIRECTION ( 'NONE',  ( 0.000000000000000000, -0.01562499999996560217, -0.9998779222360102414 ) ) ;
#127209=CARTESIAN_POINT ( 'NONE',  ( 18.49999999999999289, 64.25000000001251976, -178.6731074845244507 ) ) ;
#127222=AXIS2_PLACEMENT_3D ( 'NONE', #39255, #58761, #41821 ) ;
#127228=LINE ( 'NONE', #227600, #231694 ) ;
#127267=DIRECTION ( 'NONE',  ( 0.000000000000000000, 0.000000000000000000, 1.000000000000000000 ) ) ;
#127268=ORIENTED_EDGE ( 'NONE', *, *, #48694, .T. ) ;
#127272=EDGE_CURVE ( 'NONE', #126474, #74995, #66539, .T. ) ;
#127279=DIRECTION ( 'NONE',  ( 0.000000000000000000, 0.1350103645451945777, -0.9908441862701591329 ) ) ;
#127289=EDGE_CURVE ( 'NONE', #217036, #177234, #167796, .T. ) ;
#127305=CARTESIAN_POINT ( 'NONE',  ( -18.50000000000000000, 66.65000000001253966, -182.1731074845244223 ) ) ;
#127342=ORIENTED_EDGE ( 'NONE', *, *, #150912, .T. ) ;
#127362=DIRECTION ( 'NONE',  ( 0.000000000000000000, 0.000000000000000000, -1.000000000000000000 ) ) ;
#127377=DIRECTION ( 'NONE',  ( 1.000000000000000000, 0.000000000000000000, 0.000000000000000000 ) ) ;
#127384=ORIENTED_EDGE ( 'NONE', *, *, #48480, .F. ) ;
#127406=ORIENTED_EDGE ( 'NONE', *, *, #197316, .F. ) ;
#127436=ORIENTED_EDGE ( 'NONE', *, *, #247201, .T. ) ;
#127465=EDGE_CURVE ( 'NONE', #75338, #36049, #216558, .T. ) ;
#127469=CIRCLE ( 'NONE', #6656, 0.09999999999999646672 ) ;
#127475=DIRECTION ( 'NONE',  ( 0.000000000000000000, 0.000000000000000000, 1.000000000000000000 ) ) ;
#127522=EDGE_CURVE ( 'NONE', #4003, #11973, #169746, .T. ) ;
#127548=ORIENTED_EDGE ( 'NONE', *, *, #140322, .F. ) ;
#127556=AXIS2_PLACEMENT_3D ( 'NONE', #196166, #235283, #20112 ) ;
#127558=ORIENTED_EDGE ( 'NONE', *, *, #136394, .F. ) ;
#127559=CIRCLE ( 'NONE', #15131, 0.2000000000000057288 ) ;
#127571=CYLINDRICAL_SURFACE ( 'NONE', #170738, 0.09999999999999939493 ) ;
#127585=CARTESIAN_POINT ( 'NONE',  ( -20.54999999999999716, 74.07476635515278929, -190.7928639513982318 ) ) ;
#127589=ORIENTED_EDGE ( 'NONE', *, *, #213553, .T. ) ;
#127609=ORIENTED_EDGE ( 'NONE', *, *, #11767, .T. ) ;
#127625=CARTESIAN_POINT ( 'NONE',  ( 21.05000000000000071, 67.17357026049543833, -195.1090527715807070 ) ) ;
#127660=AXIS2_PLACEMENT_3D ( 'NONE', #115161, #151747, #13502 ) ;
#127693=DIRECTION ( 'NONE',  ( 1.000000000000000000, 0.000000000000000000, -0.000000000000000000 ) ) ;
#127705=DIRECTION ( 'NONE',  ( 1.000000000000000000, 0.000000000000000000, 0.000000000000000000 ) ) ;
#127720=ORIENTED_EDGE ( 'NONE', *, *, #221891, .T. ) ;
#127735=DIRECTION ( 'NONE',  ( 0.000000000000000000, -1.000000000000000000, -8.717686153663073805E-15 ) ) ;
#127754=DIRECTION ( 'NONE',  ( -1.000000000000000000, 1.836970198721029934E-16, 1.282749433769087582E-30 ) ) ;
#127798=EDGE_CURVE ( 'NONE', #223140, #77481, #65463, .T. ) ;
#127802=ADVANCED_FACE ( 'NONE', ( #101688 ), #221650, .F. ) ;
#127827=ADVANCED_FACE ( 'NONE', ( #44331 ), #123871, .T. ) ;
#127831=CARTESIAN_POINT ( 'NONE',  ( -20.97625342178413277, 64.39999999919218965, -196.5949042547225645 ) ) ;
#127868=DIRECTION ( 'NONE',  ( 0.000000000000000000, -5.270046002967521614E-15, 1.000000000000000000 ) ) ;
#127974=DIRECTION ( 'NONE',  ( 0.000000000000000000, 1.000000000000000000, 6.982962677686266711E-15 ) ) ;
#127980=CARTESIAN_POINT ( 'NONE',  ( -18.59999999999999787, 85.40000000001241176, -163.1410656363516125 ) ) ;
#128004=DIRECTION ( 'NONE',  ( 1.000000000000000000, 0.000000000000000000, 0.000000000000000000 ) ) ;
#128020=EDGE_CURVE ( 'NONE', #125487, #218291, #52001, .T. ) ;
#128088=CARTESIAN_POINT ( 'NONE',  ( -21.05000000000000071, 69.74218538953117275, -203.6208977758336118 ) ) ;
#128163=CIRCLE ( 'NONE', #98897, 0.09999999999999459321 ) ;
#128179=DIRECTION ( 'NONE',  ( 0.000000000000000000, 0.000000000000000000, 1.000000000000000000 ) ) ;
#128190=EDGE_CURVE ( 'NONE', #179110, #124908, #253078, .T. ) ;
#128214=ORIENTED_EDGE ( 'NONE', *, *, #194691, .F. ) ;
#128222=DIRECTION ( 'NONE',  ( -2.602085213965226419E-14, 6.982962677686266711E-15, -1.000000000000000000 ) ) ;
#128234=DIRECTION ( 'NONE',  ( 0.000000000000000000, 6.853228547068871147E-15, -1.000000000000000000 ) ) ;
#128240=CYLINDRICAL_SURFACE ( 'NONE', #48591, 0.09999999999998898659 ) ;
#128241=DIRECTION ( 'NONE',  ( -1.000000000000000000, 0.000000000000000000, -0.000000000000000000 ) ) ;
#128242=DIRECTION ( 'NONE',  ( 0.000000000000000000, -0.8660254037844377084, -0.5000000000000016653 ) ) ;
#128245=CIRCLE ( 'NONE', #44849, 4.099999999999992539 ) ;
#128279=AXIS2_PLACEMENT_3D ( 'NONE', #248302, #129639, #10976 ) ;
#128282=EDGE_CURVE ( 'NONE', #117519, #144953, #236512, .T. ) ;
#128283=DIRECTION ( 'NONE',  ( 1.000000000000000000, 0.000000000000000000, 0.000000000000000000 ) ) ;
#128294=AXIS2_PLACEMENT_3D ( 'NONE', #112524, #13426, #113793 ) ;
#128295=ORIENTED_EDGE ( 'NONE', *, *, #11767, .F. ) ;
#128317=TOROIDAL_SURFACE ( 'NONE', #157567, 0.6000000000000017542, 0.1000000000000000056 ) ;
#128337=CARTESIAN_POINT ( 'NONE',  ( 22.47071067811865319, 68.27992525551464098, -203.6221999392270448 ) ) ;
#128338=EDGE_CURVE ( 'NONE', #218193, #19640, #65823, .T. ) ;
#128372=EDGE_CURVE ( 'NONE', #223851, #116446, #77523, .T. ) ;
#128399=DIRECTION ( 'NONE',  ( 1.000000000000000000, 0.000000000000000000, 0.000000000000000000 ) ) ;
#128423=VERTEX_POINT ( 'NONE', #38429 ) ;
#128425=DIRECTION ( 'NONE',  ( -0.000000000000000000, 0.9908441862701591329, 0.1350103645451946055 ) ) ;
#128438=CARTESIAN_POINT ( 'NONE',  ( -20.89878130938411616, 65.67252876774583115, -164.4457041994994881 ) ) ;
#128439=CARTESIAN_POINT ( 'NONE',  ( 20.94999999999999929, 76.00000000001242029, -165.9231074845243654 ) ) ;
#128444=EDGE_LOOP ( 'NONE', ( #230762, #67289, #45920, #88359, #183718, #135337 ) ) ;
#128474=SURFACE_STYLE_FILL_AREA ( #168931 ) ;
#128517=CARTESIAN_POINT ( 'NONE',  ( -20.64999999999999858, 71.65000000001259650, -191.1731074845243654 ) ) ;
#128545=LINE ( 'NONE', #148112, #224026 ) ;
#128590=CARTESIAN_POINT ( 'NONE',  ( 23.25000000000000000, 87.48912529308852015, -173.1231074845242688 ) ) ;
#128614=EDGE_CURVE ( 'NONE', #252148, #106883, #45169, .T. ) ;
#128668=DIRECTION ( 'NONE',  ( 0.000000000000000000, -6.467318590049456648E-15, 1.000000000000000000 ) ) ;
#128672=EDGE_CURVE ( 'NONE', #242161, #139303, #178472, .T. ) ;
#128680=DIRECTION ( 'NONE',  ( 1.000000000000000000, 0.000000000000000000, 0.000000000000000000 ) ) ;
#128682=( BOUNDED_CURVE ( )  B_SPLINE_CURVE ( 3, ( #17291, #98058, #159371, #60242 ),
 .UNSPECIFIED., .F., .T. ) 
 B_SPLINE_CURVE_WITH_KNOTS ( ( 4, 4 ),
 ( 0.000000000000000000, 1.570796326794908992 ),
 .UNSPECIFIED. ) 
 CURVE ( )  GEOMETRIC_REPRESENTATION_ITEM ( )  RATIONAL_B_SPLINE_CURVE ( ( 1.000000000000000000, 0.8047378541243619399, 0.8047378541243619399, 1.000000000000000000 ) ) 
 REPRESENTATION_ITEM ( '' )  );
#128701=CARTESIAN_POINT ( 'NONE',  ( -23.25000000000000000, 76.00000000001267608, -203.5231074845243597 ) ) ;
#128728=ORIENTED_EDGE ( 'NONE', *, *, #37036, .F. ) ;
#128730=CARTESIAN_POINT ( 'NONE',  ( 22.00356870141233401, 68.74575763752109481, -203.5231074845244450 ) ) ;
#128735=VECTOR ( 'NONE', #74942, 999.9999999999998863 ) ;
#128745=ORIENTED_EDGE ( 'NONE', *, *, #71824, .T. ) ;
#128774=AXIS2_PLACEMENT_3D ( 'NONE', #73163, #152700, #190536 ) ;
#128800=DIRECTION ( 'NONE',  ( 0.000000000000000000, -6.982962677686266711E-15, 1.000000000000000000 ) ) ;
#128817=DIRECTION ( 'NONE',  ( 1.000000000000000000, 0.000000000000000000, 0.000000000000000000 ) ) ;
#128839=DIRECTION ( 'NONE',  ( 0.000000000000000000, -6.938893903907222067E-15, 1.000000000000000000 ) ) ;
#128861=CARTESIAN_POINT ( 'NONE',  ( -20.15000000000000568, 66.70857864377522617, -182.2731074845244166 ) ) ;
#128862=EDGE_LOOP ( 'NONE', ( #58031, #50068, #22499, #135475 ) ) ;
#128865=CARTESIAN_POINT ( 'NONE',  ( -18.39999999999999858, 85.40000000001276703, -215.2731074845243029 ) ) ;
#128887=ADVANCED_FACE ( 'NONE', ( #102077 ), #245083, .T. ) ;
#128939=AXIS2_PLACEMENT_3D ( 'NONE', #97704, #39071, #118605 ) ;
#128978=LINE ( 'NONE', #110686, #100359 ) ;
#128979=CARTESIAN_POINT ( 'NONE',  ( -18.59999999999999787, 77.14957036958807635, -162.2071950000224092 ) ) ;
#128983=ORIENTED_EDGE ( 'NONE', *, *, #204957, .T. ) ;
#129053=DIRECTION ( 'NONE',  ( -1.000000000000000000, -0.000000000000000000, -0.000000000000000000 ) ) ;
#129059=DIRECTION ( 'NONE',  ( 1.000000000000000000, 0.000000000000000000, 0.000000000000000000 ) ) ;
#129061=CARTESIAN_POINT ( 'NONE',  ( -18.59999999999999787, 77.16270174995064224, -195.4231074845243370 ) ) ;
#129083=VERTEX_POINT ( 'NONE', #217546 ) ;
#129092=DIRECTION ( 'NONE',  ( 0.000000000000000000, -6.982962677686266711E-15, 1.000000000000000000 ) ) ;
#129093=CYLINDRICAL_SURFACE ( 'NONE', #140117, 0.1000000000000028644 ) ;
#129102=AXIS2_PLACEMENT_3D ( 'NONE', #20090, #203843, #159598 ) ;
#129109=ORIENTED_EDGE ( 'NONE', *, *, #114851, .F. ) ;
#129118=SPHERICAL_SURFACE ( 'NONE', #216301, 0.1000000000000000056 ) ;
#129157=AXIS2_PLACEMENT_3D ( 'NONE', #246219, #187549, #10181 ) ;
#129200=ORIENTED_EDGE ( 'NONE', *, *, #135602, .F. ) ;
#129208=DIRECTION ( 'NONE',  ( 1.000000000000000000, -2.952720810173289112E-16, -2.061873921506763405E-30 ) ) ;
#129211=VERTEX_POINT ( 'NONE', #124895 ) ;
#129242=AXIS2_PLACEMENT_3D ( 'NONE', #14776, #171305, #194699 ) ;
#129260=EDGE_CURVE ( 'NONE', #146901, #46606, #200570, .T. ) ;
#129279=EDGE_CURVE ( 'NONE', #102259, #192523, #228722, .T. ) ;
#129360=AXIS2_PLACEMENT_3D ( 'NONE', #231210, #31742, #249483 ) ;
#129366=DIRECTION ( 'NONE',  ( 0.000000000000000000, 1.000000000000000000, 6.982962677686266711E-15 ) ) ;
#129400=EDGE_LOOP ( 'NONE', ( #239932, #93593, #207156, #98107 ) ) ;
#129401=VECTOR ( 'NONE', #200827, 1000.000000000000000 ) ;
#129406=CARTESIAN_POINT ( 'NONE',  ( -23.25000000000000000, 76.00000000001244871, -170.0231074845243597 ) ) ;
#129415=CARTESIAN_POINT ( 'NONE',  ( -23.25000000000000000, 73.40000000001259650, -190.2984855617622770 ) ) ;
#129425=ADVANCED_FACE ( 'NONE', ( #191313 ), #53728, .T. ) ;
#129522=DIRECTION ( 'NONE',  ( 0.000000000000000000, 0.4999999999999088507, -0.8660254037844913322 ) ) ;
#129526=CIRCLE ( 'NONE', #171269, 0.09999999999999939493 ) ;
#129529=CARTESIAN_POINT ( 'NONE',  ( -20.94999999999999929, 74.75000000001261924, -195.5231074845243597 ) ) ;
#129543=EDGE_CURVE ( 'NONE', #25370, #38969, #136402, .T. ) ;
#129585=DIRECTION ( 'NONE',  ( -1.000000000000000000, -0.000000000000000000, -0.000000000000000000 ) ) ;
#129600=CIRCLE ( 'NONE', #225233, 0.09999999999998898659 ) ;
#129613=CARTESIAN_POINT ( 'NONE',  ( 21.13461538461538325, 65.38541703798705385, -191.2731074845244166 ) ) ;
#129616=DIRECTION ( 'NONE',  ( -0.000000000000000000, 7.172728831056617961E-15, -1.000000000000000000 ) ) ;
#129627=EDGE_LOOP ( 'NONE', ( #161118, #24556, #207840, #41722 ) ) ;
#129639=DIRECTION ( 'NONE',  ( -1.000000000000000000, 2.952720810173289112E-16, 2.061873921506763405E-30 ) ) ;
#129647=ORIENTED_EDGE ( 'NONE', *, *, #224111, .F. ) ;
#129702=EDGE_CURVE ( 'NONE', #42819, #69180, #107501, .T. ) ;
#129726=( BOUNDED_SURFACE ( )  B_SPLINE_SURFACE ( 3, 2, ( 
 ( #241901, #142785, #243186 ),
 ( #144074, #4566, #60687 ),
 ( #159825, #180661, #102363 ),
 ( #39890, #2000, #222314 ),
 ( #219767, #140219, #161105 ),
 ( #62004, #181944, #702 ) ),
 .UNSPECIFIED., .F., .F., .T. ) 
 B_SPLINE_SURFACE_WITH_KNOTS ( ( 4, 2, 4 ),
 ( 3, 3 ),
 ( 4.712388980384689674, 5.497787143782137953, 6.283185307179586232 ),
 ( 0.000000000000000000, 1.000000000000000000 ),
 .UNSPECIFIED. ) 
 GEOMETRIC_REPRESENTATION_ITEM ( )  RATIONAL_B_SPLINE_SURFACE ( (
 ( 1.000000000000000000, 0.7071067811865475727, 1.000000000000000000),
 ( 1.000000000000000000, 0.7727932973489580748, 1.000000000000000000),
 ( 1.000000000000000000, 0.8282379607652672338, 1.000000000000000000),
 ( 1.000000000000000000, 0.9038128468036616958, 1.000000000000000000),
 ( 1.000000000000000000, 0.9240297172245867108, 1.000000000000000000),
 ( 1.000000000000000000, 0.9238795325112961754, 1.000000000000000000) ) ) 
 REPRESENTATION_ITEM ( '' )  SURFACE ( )  );
#129737=FACE_OUTER_BOUND ( 'NONE', #21942, .T. ) ;
#129779=ORIENTED_EDGE ( 'NONE', *, *, #252873, .F. ) ;
#129791=EDGE_LOOP ( 'NONE', ( #210903, #5116, #241821, #159203 ) ) ;
#129814=CIRCLE ( 'NONE', #88094, 11.75000000000001066 ) ;
#129818=ADVANCED_FACE ( 'NONE', ( #111435 ), #91868, .F. ) ;
#129853=CIRCLE ( 'NONE', #146412, 0.1000000000000026007 ) ;
#129861=CARTESIAN_POINT ( 'NONE',  ( -20.94999999999999929, 64.40000000001263913, -196.5949042542488883 ) ) ;
#129873=DIRECTION ( 'NONE',  ( 0.000000000000000000, -1.000000000000000000, -6.860497997771531562E-15 ) ) ;
#129929=DIRECTION ( 'NONE',  ( 2.840903330521633255E-16, 0.8700118002898357128, -0.4930308989875171188 ) ) ;
#129990=DIRECTION ( 'NONE',  ( 0.000000000000000000, 1.000000000000000000, 0.000000000000000000 ) ) ;
#130012=ORIENTED_EDGE ( 'NONE', *, *, #19691, .F. ) ;
#130020=CIRCLE ( 'NONE', #75884, 0.5000000000000004441 ) ;
#130029=VECTOR ( 'NONE', #84567, 1000.000000000000000 ) ;
#130050=DIRECTION ( 'NONE',  ( 1.734723475976817507E-14, -6.982962677686266711E-15, 1.000000000000000000 ) ) ;
#130076=DIRECTION ( 'NONE',  ( 0.000000000000000000, 0.000000000000000000, -1.000000000000000000 ) ) ;
#130081=VECTOR ( 'NONE', #48121, 1000.000000000000000 ) ;
#130084=EDGE_LOOP ( 'NONE', ( #193436, #158925, #196622, #89666 ) ) ;
#130090=DIRECTION ( 'NONE',  ( 1.000000000000000000, 0.000000000000000000, 0.000000000000000000 ) ) ;
#130102=ORIENTED_EDGE ( 'NONE', *, *, #102336, .F. ) ;
#130129=DIRECTION ( 'NONE',  ( 0.000000000000000000, 6.982962677686267499E-15, -1.000000000000000000 ) ) ;
#130132=ORIENTED_EDGE ( 'NONE', *, *, #242993, .F. ) ;
#130143=FACE_OUTER_BOUND ( 'NONE', #145035, .T. ) ;
#130162=AXIS2_PLACEMENT_3D ( 'NONE', #148595, #168193, #12950 ) ;
#130171=CIRCLE ( 'NONE', #38607, 0.4000000000000114575 ) ;
#130219=CARTESIAN_POINT ( 'NONE',  ( 21.00000000000000000, 66.25000000001260503, -191.1731074845244223 ) ) ;
#130221=LINE ( 'NONE', #71574, #116107 ) ;
#130227=DIRECTION ( 'NONE',  ( 1.000000000000000000, 0.000000000000000000, 0.000000000000000000 ) ) ;
#130244=LINE ( 'NONE', #148547, #85399 ) ;
#130249=AXIS2_PLACEMENT_3D ( 'NONE', #155366, #154096, #94060 ) ;
#130315=VERTEX_POINT ( 'NONE', #172436 ) ;
#130355=CARTESIAN_POINT ( 'NONE',  ( 18.59999999999999432, 77.83585931145600512, -158.5186683157258187 ) ) ;
#130359=DIRECTION ( 'NONE',  ( 1.000000000000000000, 0.000000000000000000, 0.000000000000000000 ) ) ;
#130378=CARTESIAN_POINT ( 'NONE',  ( -21.03571358705832850, 64.25000000001264766, -196.6980006624660859 ) ) ;
#130382=ORIENTED_EDGE ( 'NONE', *, *, #39594, .F. ) ;
#130414=CIRCLE ( 'NONE', #22109, 0.1999999999999987899 ) ;
#130419=CARTESIAN_POINT ( 'NONE',  ( 21.05000000000000071, 84.73084112150783653, -179.6211822035086527 ) ) ;
#130452=DIRECTION ( 'NONE',  ( 0.000000000000000000, 0.000000000000000000, 1.000000000000000000 ) ) ;
#130465=DIRECTION ( 'NONE',  ( 1.000000000000000000, -2.952720810173289112E-16, -2.061873921506763405E-30 ) ) ;
#130482=DIRECTION ( 'NONE',  ( 1.000000000000000000, 0.000000000000000000, 0.000000000000000000 ) ) ;
#130526=DIRECTION ( 'NONE',  ( -3.265361837132813093E-16, -1.000000000000000000, -6.938893903907229955E-15 ) ) ;
#130545=CARTESIAN_POINT ( 'NONE',  ( 20.85000000000000142, 76.00000000001244871, -170.0231074845243597 ) ) ;
#130549=CARTESIAN_POINT ( 'NONE',  ( 21.05000000000000071, 69.45934304831143891, -203.4231074845244223 ) ) ;
#130559=EDGE_LOOP ( 'NONE', ( #127166, #81316, #205960, #97254, #21035, #106148, #14689, #146880, #234888, #41233, #11918 ) ) ;
#130577=ORIENTED_EDGE ( 'NONE', *, *, #117105, .T. ) ;
#130581=DIRECTION ( 'NONE',  ( 0.000000000000000000, -6.608470384673580212E-15, 1.000000000000000000 ) ) ;
#130587=ADVANCED_FACE ( 'NONE', ( #106966 ), #87402, .F. ) ;
#130625=EDGE_LOOP ( 'NONE', ( #134377, #207101, #184646, #161452, #179528 ) ) ;
#130632=ORIENTED_EDGE ( 'NONE', *, *, #216392, .T. ) ;
#130645=CARTESIAN_POINT ( 'NONE',  ( -21.07928932188134041, 69.67148334361398554, -203.6220026301790540 ) ) ;
#130684=DIRECTION ( 'NONE',  ( 0.000000000000000000, -7.026728003956695223E-15, 1.000000000000000000 ) ) ;
#130687=CARTESIAN_POINT ( 'NONE',  ( -20.64999999999999858, 68.85000000001254250, -182.3731074845244109 ) ) ;
#130756=ORIENTED_EDGE ( 'NONE', *, *, #182375, .F. ) ;
#130769=CARTESIAN_POINT ( 'NONE',  ( 21.05000000000000071, 76.00000000001244871, -170.0231074845243597 ) ) ;
#130794=CARTESIAN_POINT ( 'NONE',  ( 20.93302460841142931, 65.68434038414410736, -164.4866880726065972 ) ) ;
#130806=CARTESIAN_POINT ( 'NONE',  ( -23.15000000000000213, 64.35000000001254250, -182.1731074845244507 ) ) ;
#130827=CARTESIAN_POINT ( 'NONE',  ( 22.49999999999999645, 75.90000000001276703, -215.1726782920691505 ) ) ;
#130831=AXIS2_PLACEMENT_3D ( 'NONE', #148204, #45255, #246030 ) ;
#130847=ORIENTED_EDGE ( 'NONE', *, *, #251298, .F. ) ;
#130873=ORIENTED_EDGE ( 'NONE', *, *, #203575, .T. ) ;
#130875=CARTESIAN_POINT ( 'NONE',  ( 21.05000000000000071, 64.40000000001248281, -176.9513107147999449 ) ) ;
#130877=EDGE_CURVE ( 'NONE', #222999, #243219, #153916, .T. ) ;
#130882=CARTESIAN_POINT ( 'NONE',  ( 21.12400247839514122, 65.27851195598221068, -191.2731074845244166 ) ) ;
#130912=CIRCLE ( 'NONE', #135168, 0.09999999999999939493 ) ;
#130943=EDGE_LOOP ( 'NONE', ( #257514, #187270, #239671, #86752 ) ) ;
#130952=TOROIDAL_SURFACE ( 'NONE', #35137, 6.258578643762712446, 0.1000000000000000056 ) ;
#130962=CIRCLE ( 'NONE', #135027, 0.1000000000000033362 ) ;
#131005=FACE_OUTER_BOUND ( 'NONE', #252179, .T. ) ;
#131012=CYLINDRICAL_SURFACE ( 'NONE', #119351, 7.899999999999990585 ) ;
#131073=CARTESIAN_POINT ( 'NONE',  ( 18.58685178364170199, 85.40673308381690276, -196.3986870154365363 ) ) ;
#131103=DIRECTION ( 'NONE',  ( -1.000000000000000000, -0.000000000000000000, 0.000000000000000000 ) ) ;
#131181=ADVANCED_FACE ( 'NONE', ( #160894 ), #241694, .F. ) ;
#131189=UNCERTAINTY_MEASURE_WITH_UNIT (LENGTH_MEASURE( 1.000000000000000082E-05 ), #9804, 'distance_accuracy_value', 'NONE');
#131204=VERTEX_POINT ( 'NONE', #121771 ) ;
#131238=EDGE_CURVE ( 'NONE', #51100, #94008, #85148, .T. ) ;
#131245=ORIENTED_EDGE ( 'NONE', *, *, #50223, .T. ) ;
#131252=ORIENTED_EDGE ( 'NONE', *, *, #184548, .T. ) ;
#131256=EDGE_CURVE ( 'NONE', #109697, #43253, #168637, .T. ) ;
#131263=ORIENTED_EDGE ( 'NONE', *, *, #155308, .F. ) ;
#131349=CARTESIAN_POINT ( 'NONE',  ( -18.59999999999999787, 64.35000000001259934, -191.3731074845244393 ) ) ;
#131367=DIRECTION ( 'NONE',  ( 0.000000000000000000, -7.147358527629766941E-15, 1.000000000000000000 ) ) ;
#131410=DIRECTION ( 'NONE',  ( -0.000000000000000000, 0.1298341882520009927, 0.9915357197604854900 ) ) ;
#131418=EDGE_CURVE ( 'NONE', #141019, #113112, #154204, .T. ) ;
#131427=CARTESIAN_POINT ( 'NONE',  ( -18.59999999999999787, 77.16412189325360771, -162.1082593989527254 ) ) ;
#131434=LINE ( 'NONE', #54462, #239737 ) ;
#131472=DIRECTION ( 'NONE',  ( 1.000000000000000000, 0.000000000000000000, 0.000000000000000000 ) ) ;
#131476=CARTESIAN_POINT ( 'NONE',  ( -23.15000000000000213, 76.00000000001264766, -199.3731074845243540 ) ) ;
#131502=CARTESIAN_POINT ( 'NONE',  ( -23.15000000000000213, 71.75000000001253397, -182.3731074845244109 ) ) ;
#131514=ADVANCED_FACE ( 'NONE', ( #34238 ), #162604, .F. ) ;
#131521=ORIENTED_EDGE ( 'NONE', *, *, #227280, .T. ) ;
#131547=CARTESIAN_POINT ( 'NONE',  ( -20.85000000000000142, 77.26327546522965406, -162.1212428177779543 ) ) ;
#131549=EDGE_CURVE ( 'NONE', #137582, #51105, #79185, .T. ) ;
#131551=CARTESIAN_POINT ( 'NONE',  ( 21.78635804494511419, 75.90099493450505008, -210.5587689696775442 ) ) ;
#131581=EDGE_LOOP ( 'NONE', ( #39270, #141817, #116309, #235177 ) ) ;
#131623=DIRECTION ( 'NONE',  ( -1.836970198721029934E-16, -1.000000000000000000, -6.982962677686266711E-15 ) ) ;
#131648=CARTESIAN_POINT ( 'NONE',  ( 23.14999999999999858, 71.18691588786307989, -191.5815897280005800 ) ) ;
#131701=VERTEX_POINT ( 'NONE', #165734 ) ;
#131703=AXIS2_PLACEMENT_3D ( 'NONE', #90399, #8322, #47411 ) ;
#131719=DIRECTION ( 'NONE',  ( 6.938893903907222067E-15, 1.000000000000000000, 6.982962677686266711E-15 ) ) ;
#131728=FACE_OUTER_BOUND ( 'NONE', #132528, .T. ) ;
#131729=DIRECTION ( 'NONE',  ( 0.000000000000000000, -7.116814260417668513E-15, 1.000000000000000000 ) ) ;
#131736=AXIS2_PLACEMENT_3D ( 'NONE', #121143, #20744, #100229 ) ;
#131738=DIRECTION ( 'NONE',  ( 0.000000000000000000, 0.000000000000000000, -1.000000000000000000 ) ) ;
#131796=ADVANCED_FACE ( 'NONE', ( #14372 ), #112713, .F. ) ;
#131845=DIRECTION ( 'NONE',  ( 0.000000000000000000, -1.000000000000000000, 0.000000000000000000 ) ) ;
#131880=ORIENTED_EDGE ( 'NONE', *, *, #64882, .T. ) ;
#131899=EDGE_CURVE ( 'NONE', #24117, #97198, #221505, .T. ) ;
#131939=DIRECTION ( 'NONE',  ( 0.000000000000000000, 6.982962677686266711E-15, -1.000000000000000000 ) ) ;
#131952=DIRECTION ( 'NONE',  ( -0.000000000000000000, 0.4791956752371485107, 0.8777080977375185666 ) ) ;
#131979=EDGE_CURVE ( 'NONE', #236913, #241424, #116991, .T. ) ;
#131989=EDGE_CURVE ( 'NONE', #257935, #99184, #17052, .T. ) ;
#132005=EDGE_CURVE ( 'NONE', #102497, #137660, #118597, .T. ) ;
#132008=ORIENTED_EDGE ( 'NONE', *, *, #100793, .T. ) ;
#132011=DIRECTION ( 'NONE',  ( 1.000000000000000000, 0.000000000000000000, 0.000000000000000000 ) ) ;
#132028=DIRECTION ( 'NONE',  ( -1.000000000000000000, 7.304098846218134667E-16, 5.100424963727256530E-30 ) ) ;
#132050=ORIENTED_EDGE ( 'NONE', *, *, #236537, .T. ) ;
#132055=DIRECTION ( 'NONE',  ( 0.000000000000000000, 0.8660254037844420383, -0.4999999999999943379 ) ) ;
#132065=DIRECTION ( 'NONE',  ( 0.000000000000000000, 1.000000000000000000, 1.321694076934707365E-14 ) ) ;
#132066=CARTESIAN_POINT ( 'NONE',  ( -21.37071067811865532, 67.92928932189387581, -182.3731074845244393 ) ) ;
#132084=ORIENTED_EDGE ( 'NONE', *, *, #13196, .T. ) ;
#132092=CARTESIAN_POINT ( 'NONE',  ( 20.85000000000000142, 77.36242903720570041, -162.1342262366031548 ) ) ;
#132093=DIRECTION ( 'NONE',  ( -0.000000000000000000, 1.000000000000000000, 6.982962677686266711E-15 ) ) ;
#132128=DIRECTION ( 'NONE',  ( 0.000000000000000000, -6.938893903907222067E-15, 1.000000000000000000 ) ) ;
#132195=ORIENTED_EDGE ( 'NONE', *, *, #215826, .F. ) ;
#132219=CARTESIAN_POINT ( 'NONE',  ( -20.64999999999999858, 74.07476635515278929, -190.7928639513982318 ) ) ;
#132238=CARTESIAN_POINT ( 'NONE',  ( -20.00857864376270001, 66.65000000001253966, -182.2731074845244166 ) ) ;
#132267=CIRCLE ( 'NONE', #174013, 0.09999999999998898659 ) ;
#132271=CARTESIAN_POINT ( 'NONE',  ( -20.85000000000000142, 77.36242903720570041, -162.1342262366031548 ) ) ;
#132280=DIRECTION ( 'NONE',  ( -1.000000000000000000, -0.000000000000000000, -0.000000000000000000 ) ) ;
#132282=CARTESIAN_POINT ( 'NONE',  ( 20.94999999999999929, 88.41227409416215721, -173.0231074845242745 ) ) ;
#132283=CARTESIAN_POINT ( 'NONE',  ( 20.94999999999999929, 68.87972903831482085, -166.3635444426850825 ) ) ;
#132324=CARTESIAN_POINT ( 'NONE',  ( -23.15000000000000213, 85.00000000001261924, -193.6291383618718385 ) ) ;
#132367=EDGE_CURVE ( 'NONE', #46048, #182093, #79551, .T. ) ;
#132382=AXIS2_PLACEMENT_3D ( 'NONE', #64708, #68569, #125954 ) ;
#132392=DIRECTION ( 'NONE',  ( -1.000000000000000000, 3.265361837132813093E-16, 2.280189983783949500E-30 ) ) ;
#132435=DIRECTION ( 'NONE',  ( 0.000000000000000000, 0.000000000000000000, 1.000000000000000000 ) ) ;
#132441=DIRECTION ( 'NONE',  ( 0.000000000000000000, -6.938893903907222067E-15, 1.000000000000000000 ) ) ;
#132448=ORIENTED_EDGE ( 'NONE', *, *, #33405, .F. ) ;
#132492=EDGE_CURVE ( 'NONE', #95948, #106770, #255905, .T. ) ;
#132502=CARTESIAN_POINT ( 'NONE',  ( -23.15000000000000213, 87.48912529308852015, -173.1231074845242688 ) ) ;
#132516=CARTESIAN_POINT ( 'NONE',  ( -20.64999999999999858, 85.00000000001251976, -179.9170766071767389 ) ) ;
#132519=CIRCLE ( 'NONE', #115965, 0.5000000000000004441 ) ;
#132528=EDGE_LOOP ( 'NONE', ( #218790, #242084, #69199, #230353, #19884, #256606, #9932, #127032, #167303, #167714 ) ) ;
#132570=DIRECTION ( 'NONE',  ( 1.000000000000000000, -0.000000000000000000, 0.000000000000000000 ) ) ;
#132574=VERTEX_POINT ( 'NONE', #120344 ) ;
#132627=PLANE ( 'NONE',  #194939 ) ;
#132663=DIRECTION ( 'NONE',  ( -0.000000000000000000, 0.7397360091702708251, 0.6728971962616883129 ) ) ;
#132690=ORIENTED_EDGE ( 'NONE', *, *, #252022, .T. ) ;
#132737=VECTOR ( 'NONE', #193051, 1000.000000000000114 ) ;
#132739=ORIENTED_EDGE ( 'NONE', *, *, #76889, .F. ) ;
#132746=DIRECTION ( 'NONE',  ( 1.000000000000000000, 0.000000000000000000, 0.000000000000000000 ) ) ;
#132760=VERTEX_POINT ( 'NONE', #242807 ) ;
#132766=DIRECTION ( 'NONE',  ( -0.000000000000000000, -6.982962677686266711E-15, 1.000000000000000000 ) ) ;
#132800=TOROIDAL_SURFACE ( 'NONE', #178601, 0.2000000000000000111, 0.1000000000000000056 ) ;
#132816=DIRECTION ( 'NONE',  ( -1.000000000000000000, 0.000000000000000000, -0.000000000000000000 ) ) ;
#132846=AXIS2_PLACEMENT_3D ( 'NONE', #206457, #27857, #107348 ) ;
#132859=EDGE_CURVE ( 'NONE', #4716, #235019, #179720, .T. ) ;
#132873=EDGE_CURVE ( 'NONE', #129083, #133788, #133910, .T. ) ;
#132891=CARTESIAN_POINT ( 'NONE',  ( 18.49999999999999289, 65.79142135624982757, -178.8731074845244109 ) ) ;
#132895=AXIS2_PLACEMENT_3D ( 'NONE', #56649, #257391, #119244 ) ;
#132915=CARTESIAN_POINT ( 'NONE',  ( 20.85000000000000142, 68.87972903831482085, -166.3635444426850825 ) ) ;
#132948=CARTESIAN_POINT ( 'NONE',  ( 22.39999999999999503, 68.20922040163929978, -203.5231074845243882 ) ) ;
#132951=ADVANCED_FACE ( 'NONE', ( #239953 ), #254841, .F. ) ;
#132954=DIRECTION ( 'NONE',  ( 1.000000000000000000, 0.000000000000000000, 0.000000000000000000 ) ) ;
#132962=CARTESIAN_POINT ( 'NONE',  ( 20.94999999999999574, 77.16270174995064224, -195.4231074845243370 ) ) ;
#132965=CIRCLE ( 'NONE', #166299, 0.2000000000000057288 ) ;
#132969=B_SPLINE_CURVE_WITH_KNOTS ( 'NONE', 3,
 ( #158567, #159845, #239367, #60705, #219787, #200238, #21612, #184510, #202800, #106248 ),
 .UNSPECIFIED., .F., .F.,
 ( 4, 3, 3, 4 ),
 ( 0.000000000000000000, 0.0002000000000008537104, 0.001000000000082977483, 0.001967863649483329782 ),
 .UNSPECIFIED. ) ;
#132985=CARTESIAN_POINT ( 'NONE',  ( 18.50000324121758055, 65.70692517833265356, -164.5644653378304554 ) ) ;
#133043=AXIS2_PLACEMENT_3D ( 'NONE', #150774, #193753, #212048 ) ;
#133072=LINE ( 'NONE', #34005, #132737 ) ;
#133089=DIRECTION ( 'NONE',  ( -1.000000000000000000, 0.000000000000000000, -0.000000000000000000 ) ) ;
#133100=TOROIDAL_SURFACE ( 'NONE', #208126, 0.9750000000000019762, 0.1000000000000000056 ) ;
#133132=TOROIDAL_SURFACE ( 'NONE', #58277, 3.899999999999999467, 0.1000000000000000056 ) ;
#133136=DIRECTION ( 'NONE',  ( 1.000000000000000000, -3.265361837132813093E-16, -2.280189983783949500E-30 ) ) ;
#133146=DIRECTION ( 'NONE',  ( -0.000000000000000000, -6.982962677686266711E-15, 1.000000000000000000 ) ) ;
#133221=EDGE_CURVE ( 'NONE', #41155, #117188, #146721, .T. ) ;
#133227=ORIENTED_EDGE ( 'NONE', *, *, #28187, .T. ) ;
#133232=ORIENTED_EDGE ( 'NONE', *, *, #80833, .F. ) ;
#133242=CARTESIAN_POINT ( 'NONE',  ( 23.14999999999999503, 69.35000000001254250, -182.1731074845243938 ) ) ;
#133278=ORIENTED_EDGE ( 'NONE', *, *, #23770, .F. ) ;
#133285=VERTEX_POINT ( 'NONE', #9030 ) ;
#133288=CARTESIAN_POINT ( 'NONE',  ( 21.09610168723072832, 75.96641049312121652, -209.9020631997491364 ) ) ;
#133291=DIRECTION ( 'NONE',  ( 0.000000000000000000, 6.982962677686266711E-15, -1.000000000000000000 ) ) ;
#133295=SURFACE_STYLE_USAGE ( .BOTH. , #55010 ) ;
#133297=FACE_OUTER_BOUND ( 'NONE', #216757, .T. ) ;
#133309=VERTEX_POINT ( 'NONE', #238336 ) ;
#133320=CARTESIAN_POINT ( 'NONE',  ( -18.50000000000000711, 64.35000000001264198, -196.5083017138704236 ) ) ;
#133330=CARTESIAN_POINT ( 'NONE',  ( -23.25000000000000000, 71.65000000001259650, -191.3731074845243825 ) ) ;
#133346=CARTESIAN_POINT ( 'NONE',  ( -21.05000000000000071, 70.10000000001251408, -180.2422072491807796 ) ) ;
#133391=CARTESIAN_POINT ( 'NONE',  ( 20.95052659398289308, 65.52017563223272134, -195.9478687286588183 ) ) ;
#133392=DIRECTION ( 'NONE',  ( 0.7071067811865127117, 0.7071067811865821007, 0.000000000000000000 ) ) ;
#133415=FACE_OUTER_BOUND ( 'NONE', #1585, .T. ) ;
#133429=CARTESIAN_POINT ( 'NONE',  ( 18.46858270002953262, 85.47420267472320177, -196.4210855498204467 ) ) ;
#133462=EDGE_CURVE ( 'NONE', #60454, #243219, #100911, .T. ) ;
#133470=LINE ( 'NONE', #112627, #257258 ) ;
#133478=AXIS2_PLACEMENT_3D ( 'NONE', #18733, #233930, #156987 ) ;
#133483=CARTESIAN_POINT ( 'NONE',  ( 20.94999999999999574, 87.75000000001264766, -200.6231074845242688 ) ) ;
#133499=CARTESIAN_POINT ( 'NONE',  ( -20.85000000000000142, 76.00000000001244871, -170.0231074845243597 ) ) ;
#133608=CARTESIAN_POINT ( 'NONE',  ( -18.31572283045109018, 85.54843783089823717, -163.1724818334656959 ) ) ;
#133612=VERTEX_POINT ( 'NONE', #166539 ) ;
#133625=VERTEX_POINT ( 'NONE', #106504 ) ;
#133650=ORIENTED_EDGE ( 'NONE', *, *, #150360, .T. ) ;
#133737=EDGE_LOOP ( 'NONE', ( #5260, #180735, #254248, #168204 ) ) ;
#133764=CYLINDRICAL_SURFACE ( 'NONE', #197088, 0.09999999999999939493 ) ;
#133780=CARTESIAN_POINT ( 'NONE',  ( 23.24999999999999645, 76.00000000001267608, -203.5231074845243597 ) ) ;
#133788=VERTEX_POINT ( 'NONE', #99776 ) ;
#133806=ORIENTED_EDGE ( 'NONE', *, *, #25632, .F. ) ;
#133855=EDGE_LOOP ( 'NONE', ( #210102, #184237 ) ) ;
#133863=ADVANCED_FACE ( 'NONE', ( #21567 ), #101090, .T. ) ;
#133879=EDGE_LOOP ( 'NONE', ( #216951, #120338, #100534, #82290 ) ) ;
#133887=FACE_OUTER_BOUND ( 'NONE', #193609, .T. ) ;
#133901=VERTEX_POINT ( 'NONE', #207596 ) ;
#133910=CIRCLE ( 'NONE', #21513, 0.09999999999999939493 ) ;
#133915=EDGE_CURVE ( 'NONE', #218291, #152832, #109514, .T. ) ;
#133930=TOROIDAL_SURFACE ( 'NONE', #125557, 12.97499999999999609, 0.1000000000000000056 ) ;
#133931=VERTEX_POINT ( 'NONE', #92753 ) ;
#133936=ORIENTED_EDGE ( 'NONE', *, *, #93102, .F. ) ;
#133976=DIRECTION ( 'NONE',  ( 1.000000000000000000, 0.000000000000000000, 0.000000000000000000 ) ) ;
#133987=PLANE ( 'NONE',  #18278 ) ;
#134000=DIRECTION ( 'NONE',  ( 1.000000000000000000, 7.304098846218105085E-16, 4.217023435051677501E-16 ) ) ;
#134026=CARTESIAN_POINT ( 'NONE',  ( 18.59999999999999076, 69.55000000001253113, -182.2731074845244166 ) ) ;
#134028=DIRECTION ( 'NONE',  ( 0.000000000000000000, 0.000000000000000000, -1.000000000000000000 ) ) ;
#134048=EDGE_CURVE ( 'NONE', #85698, #27052, #59793, .T. ) ;
#134049=DIRECTION ( 'NONE',  ( 0.000000000000000000, 0.4930308989874980785, 0.8700118002898462599 ) ) ;
#134072=EDGE_LOOP ( 'NONE', ( #10191, #96033, #63979, #160834 ) ) ;
#134117=EDGE_CURVE ( 'NONE', #27358, #71853, #30623, .T. ) ;
#134121=EDGE_CURVE ( 'NONE', #54936, #90288, #215281, .T. ) ;
#134129=AXIS2_PLACEMENT_3D ( 'NONE', #138118, #242367, #22062 ) ;
#134193=CARTESIAN_POINT ( 'NONE',  ( 20.94999999999999929, 76.00000000001246292, -172.0231074845243597 ) ) ;
#134213=EDGE_CURVE ( 'NONE', #257328, #132760, #117517, .T. ) ;
#134236=AXIS2_PLACEMENT_3D ( 'NONE', #222496, #24346, #64730 ) ;
#134293=VECTOR ( 'NONE', #189587, 1000.000000000000000 ) ;
#134296=LINE ( 'NONE', #237278, #182689 ) ;
#134300=ORIENTED_EDGE ( 'NONE', *, *, #197311, .F. ) ;
#134302=ADVANCED_FACE ( 'NONE', ( #84715 ), #147296, .T. ) ;
#134310=DIRECTION ( 'NONE',  ( 1.000000000000000000, 0.000000000000000000, 0.000000000000000000 ) ) ;
#134312=VECTOR ( 'NONE', #230356, 1000.000000000000000 ) ;
#134332=SPHERICAL_SURFACE ( 'NONE', #10409, 0.1000000000000000056 ) ;
#134341=DIRECTION ( 'NONE',  ( -1.000000000000000000, 2.952720810173289112E-16, 2.061873921506763405E-30 ) ) ;
#134356=AXIS2_PLACEMENT_3D ( 'NONE', #169403, #212357, #168125 ) ;
#134357=CARTESIAN_POINT ( 'NONE',  ( 18.59999999999999076, 68.87972903831482085, -166.3635444426850825 ) ) ;
#134377=ORIENTED_EDGE ( 'NONE', *, *, #142683, .F. ) ;
#134408=CARTESIAN_POINT ( 'NONE',  ( 23.14999999999999503, 64.25000000001253397, -182.2731074845244450 ) ) ;
#134419=FACE_OUTER_BOUND ( 'NONE', #226849, .T. ) ;
#134420=ADVANCED_FACE ( 'NONE', ( #228132 ), #33817, .F. ) ;
#134446=CIRCLE ( 'NONE', #171922, 0.1000000000000072220 ) ;
#134463=EDGE_CURVE ( 'NONE', #160017, #43253, #63514, .T. ) ;
#134472=ORIENTED_EDGE ( 'NONE', *, *, #212615, .F. ) ;
#134515=VECTOR ( 'NONE', #179733, 1000.000000000000000 ) ;
#134524=ORIENTED_EDGE ( 'NONE', *, *, #134213, .F. ) ;
#134525=DIRECTION ( 'NONE',  ( -1.000000000000000000, 2.952720810173289112E-16, 2.061873921506763405E-30 ) ) ;
#134529=CARTESIAN_POINT ( 'NONE',  ( -23.15000000000000213, 76.00000000001267608, -203.5231074845243597 ) ) ;
#134576=CARTESIAN_POINT ( 'NONE',  ( 18.39999999999999858, 85.68240343348880117, -163.3662641071115047 ) ) ;
#134611=VECTOR ( 'NONE', #170141, 1000.000000000000000 ) ;
#134634=ORIENTED_EDGE ( 'NONE', *, *, #36201, .F. ) ;
#134643=CARTESIAN_POINT ( 'NONE',  ( -21.05000000000000071, 74.73821383144760944, -195.4366085209788935 ) ) ;
#134657=DIRECTION ( 'NONE',  ( 0.000000000000000000, 0.000000000000000000, 1.000000000000000000 ) ) ;
#134677=AXIS2_PLACEMENT_3D ( 'NONE', #59921, #199478, #178643 ) ;
#134726=CARTESIAN_POINT ( 'NONE',  ( -18.59999999999999787, 77.25000000001263345, -195.5231074845243313 ) ) ;
#134775=VECTOR ( 'NONE', #109725, 1000.000000000000000 ) ;
#134850=DIRECTION ( 'NONE',  ( -0.8660254037843277963, 0.000000000000000000, 0.5000000000001921796 ) ) ;
#134851=CARTESIAN_POINT ( 'NONE',  ( -20.54999999999999716, 71.75000000001259082, -191.2731074845243882 ) ) ;
#134877=EDGE_CURVE ( 'NONE', #31357, #200607, #146891, .T. ) ;
#134892=DIRECTION ( 'NONE',  ( 1.000000000000000000, 0.000000000000000000, 0.000000000000000000 ) ) ;
#134962=DIRECTION ( 'NONE',  ( -4.701977403289178058E-30, -2.433019743745433765E-14, 1.000000000000000000 ) ) ;
#134977=AXIS2_PLACEMENT_3D ( 'NONE', #242983, #5635, #85162 ) ;
#134990=EDGE_LOOP ( 'NONE', ( #181343, #118370, #130132, #68559 ) ) ;
#135027=AXIS2_PLACEMENT_3D ( 'NONE', #13653, #16249, #249699 ) ;
#135030=DIRECTION ( 'NONE',  ( -1.000000000000000000, 0.000000000000000000, 0.000000000000000000 ) ) ;
#135031=FACE_OUTER_BOUND ( 'NONE', #125136, .T. ) ;
#135055=DIRECTION ( 'NONE',  ( 1.000000000000000000, 0.000000000000000000, 0.000000000000000000 ) ) ;
#135066=ORIENTED_EDGE ( 'NONE', *, *, #115913, .F. ) ;
#135086=EDGE_CURVE ( 'NONE', #79128, #241603, #33197, .T. ) ;
#135089=ORIENTED_EDGE ( 'NONE', *, *, #254524, .T. ) ;
#135096=ADVANCED_FACE ( 'NONE', ( #127111 ), #122171, .F. ) ;
#135110=ORIENTED_EDGE ( 'NONE', *, *, #88616, .F. ) ;
#135123=CIRCLE ( 'NONE', #176860, 0.2000000000000057288 ) ;
#135144=ORIENTED_EDGE ( 'NONE', *, *, #88836, .F. ) ;
#135160=DIRECTION ( 'NONE',  ( 0.000000000000000000, 0.000000000000000000, 1.000000000000000000 ) ) ;
#135168=AXIS2_PLACEMENT_3D ( 'NONE', #101381, #57147, #59717 ) ;
#135195=EDGE_LOOP ( 'NONE', ( #238074, #63410, #12982, #191579, #151491 ) ) ;
#135203=VERTEX_POINT ( 'NONE', #173998 ) ;
#135228=VERTEX_POINT ( 'NONE', #175272 ) ;
#135243=FACE_OUTER_BOUND ( 'NONE', #59702, .T. ) ;
#135311=CIRCLE ( 'NONE', #106072, 11.80000000000000426 ) ;
#135313=ORIENTED_EDGE ( 'NONE', *, *, #27402, .F. ) ;
#135321=COLOUR_RGB ( '', 0.66274510, 0.83137255, 0.94901961) ;
#135337=ORIENTED_EDGE ( 'NONE', *, *, #56042, .T. ) ;
#135344=AXIS2_PLACEMENT_3D ( 'NONE', #244184, #241635, #222040 ) ;
#135406=VERTEX_POINT ( 'NONE', #120432 ) ;
#135432=CYLINDRICAL_SURFACE ( 'NONE', #79487, 0.1000000000000046685 ) ;
#135437=DIRECTION ( 'NONE',  ( 1.000000000000000000, -0.000000000000000000, 0.000000000000000000 ) ) ;
#135447=EDGE_CURVE ( 'NONE', #106883, #65528, #31599, .T. ) ;
#135455=CARTESIAN_POINT ( 'NONE',  ( 21.05000000000000071, 65.51540711881831669, -196.0663939139407432 ) ) ;
#135465=CARTESIAN_POINT ( 'NONE',  ( 21.05000000000000071, 87.48912529308852015, -173.0231074845243029 ) ) ;
#135470=ORIENTED_EDGE ( 'NONE', *, *, #150995, .F. ) ;
#135473=EDGE_LOOP ( 'NONE', ( #46329, #155419, #54729, #11283 ) ) ;
#135475=ORIENTED_EDGE ( 'NONE', *, *, #69696, .T. ) ;
#135479=CARTESIAN_POINT ( 'NONE',  ( 20.94999999999999574, 67.07338541492552508, -195.0514244653012952 ) ) ;
#135487=CARTESIAN_POINT ( 'NONE',  ( -23.25000000000000000, 76.00000000001244871, -170.0231074845243597 ) ) ;
#135558=CARTESIAN_POINT ( 'NONE',  ( -23.15000000000000213, 76.00000000001267608, -203.5231074845243597 ) ) ;
#135589=CARTESIAN_POINT ( 'NONE',  ( 20.94999999999997442, 77.26327546522965406, -162.1212428177779543 ) ) ;
#135593=CIRCLE ( 'NONE', #23205, 0.09999999999999939493 ) ;
#135602=EDGE_CURVE ( 'NONE', #64951, #17038, #147291, .T. ) ;
#135608=EDGE_CURVE ( 'NONE', #247011, #66129, #143170, .T. ) ;
#135633=CARTESIAN_POINT ( 'NONE',  ( 23.14999999999999858, 71.00000000001253397, -182.4283735034374843 ) ) ;
#135656=DIRECTION ( 'NONE',  ( 0.000000000000000000, -0.8660254037844420383, 0.4999999999999943379 ) ) ;
#135685=AXIS2_PLACEMENT_3D ( 'NONE', #190142, #91029, #106719 ) ;
#135711=DIRECTION ( 'NONE',  ( -0.000000000000000000, 1.000000000000000000, 6.982962677686266711E-15 ) ) ;
#135715=DIRECTION ( 'NONE',  ( 0.000000000000000000, 0.000000000000000000, 1.000000000000000000 ) ) ;
#135726=ORIENTED_EDGE ( 'NONE', *, *, #105404, .F. ) ;
#135728=ORIENTED_EDGE ( 'NONE', *, *, #215397, .F. ) ;
#135776=AXIS2_PLACEMENT_3D ( 'NONE', #134529, #217915, #197080 ) ;
#135786=ORIENTED_EDGE ( 'NONE', *, *, #151015, .T. ) ;
#135800=AXIS2_PLACEMENT_3D ( 'NONE', #130419, #208702, #53461 ) ;
#135803=VECTOR ( 'NONE', #50838, 1000.000000000000000 ) ;
#135805=ORIENTED_EDGE ( 'NONE', *, *, #132005, .F. ) ;
#135806=EDGE_LOOP ( 'NONE', ( #142768, #194770, #187003, #16893 ) ) ;
#135836=CYLINDRICAL_SURFACE ( 'NONE', #48909, 11.75000000000001066 ) ;
#135860=CARTESIAN_POINT ( 'NONE',  ( -20.64999999999999858, 68.75000000001260503, -191.2731074845244166 ) ) ;
#135882=EDGE_CURVE ( 'NONE', #123921, #239471, #198850, .T. ) ;
#135929=VERTEX_POINT ( 'NONE', #203987 ) ;
#135940=CARTESIAN_POINT ( 'NONE',  ( -23.15000000000000213, 64.25000000001277556, -215.2731074845244450 ) ) ;
#135952=DIRECTION ( 'NONE',  ( 0.000000000000000000, 0.000000000000000000, 1.000000000000000000 ) ) ;
#135964=CARTESIAN_POINT ( 'NONE',  ( 20.85000000000000142, 76.00000000001244871, -170.0231074845243597 ) ) ;
#135976=DIRECTION ( 'NONE',  ( 0.000000000000000000, -7.086529944415886769E-15, 1.000000000000000000 ) ) ;
#135979=DIRECTION ( 'NONE',  ( 0.000000000000000000, -7.109473446599835262E-15, 1.000000000000000000 ) ) ;
#136020=CARTESIAN_POINT ( 'NONE',  ( -18.50000000000000711, 85.42130820975131655, -196.2807442704737753 ) ) ;
#136024=CARTESIAN_POINT ( 'NONE',  ( -21.05000000000000071, 87.65000000001266756, -200.6231074845242688 ) ) ;
#136040=ORIENTED_EDGE ( 'NONE', *, *, #73564, .F. ) ;
#136068=DIRECTION ( 'NONE',  ( 1.000000000000000000, 0.000000000000000000, 0.000000000000000000 ) ) ;
#136080=DIRECTION ( 'NONE',  ( 0.000000000000000000, 6.938893903907222067E-15, -1.000000000000000000 ) ) ;
#136104=DIRECTION ( 'NONE',  ( 0.000000000000000000, 0.000000000000000000, 1.000000000000000000 ) ) ;
#136143=DIRECTION ( 'NONE',  ( 1.000000000000000000, -0.000000000000000000, 0.000000000000000000 ) ) ;
#136156=VERTEX_POINT ( 'NONE', #57392 ) ;
#136168=CARTESIAN_POINT ( 'NONE',  ( -20.64999999999999858, 68.85000000001259934, -191.1731074845243938 ) ) ;
#136175=LINE ( 'NONE', #80048, #228517 ) ;
#136188=CARTESIAN_POINT ( 'NONE',  ( -21.05000000000000071, 87.65000000001269598, -203.5231074845243029 ) ) ;
#136193=ORIENTED_EDGE ( 'NONE', *, *, #50045, .T. ) ;
#136207=ADVANCED_FACE ( 'NONE', ( #205900 ), #43422, .T. ) ;
#136213=ORIENTED_EDGE ( 'NONE', *, *, #247830, .T. ) ;
#136223=VERTEX_POINT ( 'NONE', #125105 ) ;
#136326=DIRECTION ( 'NONE',  ( 1.000000000000000000, 0.000000000000000000, 0.000000000000000000 ) ) ;
#136349=ORIENTED_EDGE ( 'NONE', *, *, #25162, .T. ) ;
#136358=DIRECTION ( 'NONE',  ( -0.000000000000000000, -6.982962677686266711E-15, 1.000000000000000000 ) ) ;
#136359=CARTESIAN_POINT ( 'NONE',  ( 20.94999999999999929, 87.65000000001244018, -170.0231074845242745 ) ) ;
#136391=AXIS2_PLACEMENT_3D ( 'NONE', #190049, #72695, #170540 ) ;
#136394=EDGE_CURVE ( 'NONE', #104211, #150814, #229336, .T. ) ;
#136401=ORIENTED_EDGE ( 'NONE', *, *, #231771, .F. ) ;
#136402=LINE ( 'NONE', #78998, #82533 ) ;
#136454=SPHERICAL_SURFACE ( 'NONE', #168664, 0.1000000000000000056 ) ;
#136459=AXIS2_PLACEMENT_3D ( 'NONE', #140660, #162819, #218903 ) ;
#136483=ADVANCED_FACE ( 'NONE', ( #137901 ), #122740, .T. ) ;
#136507=CIRCLE ( 'NONE', #219716, 0.1000000000000070832 ) ;
#136524=CARTESIAN_POINT ( 'NONE',  ( 20.94999999999999574, 65.37642973952982572, -196.0311622812938879 ) ) ;
#136542=CARTESIAN_POINT ( 'NONE',  ( -23.15000000000000213, 76.00000000001244871, -170.0231074845243597 ) ) ;
#136563=DIRECTION ( 'NONE',  ( -1.000000000000000000, -0.000000000000000000, -0.000000000000000000 ) ) ;
#136587=DIRECTION ( 'NONE',  ( 0.000000000000000000, 7.147358527629766941E-15, -1.000000000000000000 ) ) ;
#136596=CIRCLE ( 'NONE', #174073, 4.049999999999998046 ) ;
#136604=EDGE_CURVE ( 'NONE', #214102, #210483, #231250, .T. ) ;
#136676=FACE_OUTER_BOUND ( 'NONE', #146900, .T. ) ;
#136685=ORIENTED_EDGE ( 'NONE', *, *, #101970, .T. ) ;
#136691=CARTESIAN_POINT ( 'NONE',  ( -21.05000000000000071, 70.15000000001266756, -193.3906102602464330 ) ) ;
#136693=CARTESIAN_POINT ( 'NONE',  ( 20.85000000000000142, 76.00000000001244871, -170.0231074845243597 ) ) ;
#136700=ORIENTED_EDGE ( 'NONE', *, *, #243138, .T. ) ;
#136760=CARTESIAN_POINT ( 'NONE',  ( -20.94999999999999929, 87.48912529308852015, -173.0231074845243029 ) ) ;
#136764=EDGE_LOOP ( 'NONE', ( #222127, #8273, #217687, #221189 ) ) ;
#136800=ORIENTED_EDGE ( 'NONE', *, *, #24095, .T. ) ;
#136807=CARTESIAN_POINT ( 'NONE',  ( 23.14999999999999858, 76.00000000001267608, -203.5231074845243597 ) ) ;
#136815=ORIENTED_EDGE ( 'NONE', *, *, #218319, .T. ) ;
#136867=DIRECTION ( 'NONE',  ( 0.000000000000000000, 0.000000000000000000, -1.000000000000000000 ) ) ;
#136885=CYLINDRICAL_SURFACE ( 'NONE', #112361, 0.09999999999998898659 ) ;
#136890=DIRECTION ( 'NONE',  ( 0.000000000000000000, -1.000000000000000000, -7.272083257015735086E-15 ) ) ;
#136915=AXIS2_PLACEMENT_3D ( 'NONE', #160375, #199494, #61245 ) ;
#136943=ORIENTED_EDGE ( 'NONE', *, *, #26308, .T. ) ;
#136996=DIRECTION ( 'NONE',  ( 0.9880948137434723000, -0.1538461538461484146, -1.074301950413233906E-15 ) ) ;
#137016=CARTESIAN_POINT ( 'NONE',  ( 20.95289811251229750, 67.10683199555401757, -195.0212979906058877 ) ) ;
#137028=CIRCLE ( 'NONE', #78734, 12.97499999999998721 ) ;
#137052=ORIENTED_EDGE ( 'NONE', *, *, #15608, .T. ) ;
#137062=ORIENTED_EDGE ( 'NONE', *, *, #97449, .F. ) ;
#137091=ORIENTED_EDGE ( 'NONE', *, *, #235057, .T. ) ;
#137097=CARTESIAN_POINT ( 'NONE',  ( -22.48660254037843487, 64.35000000001268461, -203.5731074845244279 ) ) ;
#137106=AXIS2_PLACEMENT_3D ( 'NONE', #21077, #13655, #160588 ) ;
#137110=CIRCLE ( 'NONE', #166189, 0.5000000000000004441 ) ;
#137134=ORIENTED_EDGE ( 'NONE', *, *, #55787, .F. ) ;
#137144=ORIENTED_EDGE ( 'NONE', *, *, #100577, .F. ) ;
#137155=DIRECTION ( 'NONE',  ( -1.000000000000000000, -0.000000000000000000, -0.000000000000000000 ) ) ;
#137159=CARTESIAN_POINT ( 'NONE',  ( 18.59999999999999076, 77.14957036958807635, -162.2071950000224092 ) ) ;
#137166=CARTESIAN_POINT ( 'NONE',  ( 18.59999999999999432, 85.48068669529136798, -163.0819923157664562 ) ) ;
#137169=ORIENTED_EDGE ( 'NONE', *, *, #111316, .F. ) ;
#137196=CARTESIAN_POINT ( 'NONE',  ( -20.64999999999999858, 68.85000000001254250, -182.3731074845244109 ) ) ;
#137209=ORIENTED_EDGE ( 'NONE', *, *, #58673, .F. ) ;
#137240=CARTESIAN_POINT ( 'NONE',  ( -21.65000000000000213, 68.29142135624991283, -191.2731074845244166 ) ) ;
#137264=DIRECTION ( 'NONE',  ( 0.000000000000000000, 0.000000000000000000, -1.000000000000000000 ) ) ;
#137279=AXIS2_PLACEMENT_3D ( 'NONE', #216343, #78109, #218900 ) ;
#137298=DIRECTION ( 'NONE',  ( 0.000000000000000000, 0.000000000000000000, 1.000000000000000000 ) ) ;
#137306=DIRECTION ( 'NONE',  ( -1.000000000000000000, 0.000000000000000000, -0.000000000000000000 ) ) ;
#137307=CARTESIAN_POINT ( 'NONE',  ( 18.49999999999999289, 65.79142135624984178, -182.1731074845244223 ) ) ;
#137329=ORIENTED_EDGE ( 'NONE', *, *, #178345, .T. ) ;
#137343=CARTESIAN_POINT ( 'NONE',  ( 23.15000000000000213, 87.65000000001269598, -203.5231074845243029 ) ) ;
#137350=AXIS2_PLACEMENT_3D ( 'NONE', #114360, #16554, #158645 ) ;
#137397=DIRECTION ( 'NONE',  ( 0.000000000000000000, -1.000000000000000000, -6.982962677686266711E-15 ) ) ;
#137399=DIRECTION ( 'NONE',  ( 1.000000000000000000, 0.000000000000000000, 0.000000000000000000 ) ) ;
#137432=CARTESIAN_POINT ( 'NONE',  ( -18.59999999999999787, 68.87972903831482085, -166.3635444426850825 ) ) ;
#137524=CARTESIAN_POINT ( 'NONE',  ( 21.05000000000000071, 85.40000000001252545, -179.9170766071767389 ) ) ;
#137548=DIRECTION ( 'NONE',  ( 0.000000000000000000, -6.982962677686266711E-15, 1.000000000000000000 ) ) ;
#137554=VERTEX_POINT ( 'NONE', #110702 ) ;
#137582=VERTEX_POINT ( 'NONE', #131547 ) ;
#137592=ORIENTED_EDGE ( 'NONE', *, *, #232295, .T. ) ;
#137617=CYLINDRICAL_SURFACE ( 'NONE', #84592, 0.09999999999998898659 ) ;
#137619=CARTESIAN_POINT ( 'NONE',  ( 23.14999999999999858, 64.40000000001248281, -176.9513107147999449 ) ) ;
#137632=ORIENTED_EDGE ( 'NONE', *, *, #63454, .F. ) ;
#137660=VERTEX_POINT ( 'NONE', #19301 ) ;
#137701=CARTESIAN_POINT ( 'NONE',  ( -21.29999999999995808, 76.00000000001270450, -207.5731074845243427 ) ) ;
#137703=DIRECTION ( 'NONE',  ( 0.000000000000000000, 3.469446951953515108E-14, 1.000000000000000000 ) ) ;
#137725=AXIS2_PLACEMENT_3D ( 'NONE', #141895, #40270, #42806 ) ;
#137804=EDGE_LOOP ( 'NONE', ( #148545, #147149, #191617, #67460 ) ) ;
#137808=DIRECTION ( 'NONE',  ( 0.000000000000000000, 0.000000000000000000, -1.000000000000000000 ) ) ;
#137815=AXIS2_PLACEMENT_3D ( 'NONE', #258037, #80709, #181135 ) ;
#137844=CARTESIAN_POINT ( 'NONE',  ( -23.25000000000000000, 76.00000000001267608, -203.5231074845243597 ) ) ;
#137875=AXIS2_PLACEMENT_3D ( 'NONE', #156603, #236095, #57444 ) ;
#137900=ORIENTED_EDGE ( 'NONE', *, *, #146853, .T. ) ;
#137901=FACE_OUTER_BOUND ( 'NONE', #39477, .T. ) ;
#137938=ORIENTED_EDGE ( 'NONE', *, *, #155649, .T. ) ;
#137940=EDGE_LOOP ( 'NONE', ( #26341, #222938, #39084, #98605 ) ) ;
#137947=DIRECTION ( 'NONE',  ( -1.000000000000000000, 0.000000000000000000, 0.000000000000000000 ) ) ;
#137948=VERTEX_POINT ( 'NONE', #209485 ) ;
#137993=CYLINDRICAL_SURFACE ( 'NONE', #220814, 12.87499999999999822 ) ;
#138007=CIRCLE ( 'NONE', #121498, 0.1000000000000033362 ) ;
#138020=DIRECTION ( 'NONE',  ( 0.000000000000000000, 6.982962677686267499E-15, -1.000000000000000000 ) ) ;
#138055=CARTESIAN_POINT ( 'NONE',  ( -23.25000000000000000, 64.25000000001269029, -203.5231074845244166 ) ) ;
#138117=DIRECTION ( 'NONE',  ( 0.000000000000000000, 0.000000000000000000, 1.000000000000000000 ) ) ;
#138118=CARTESIAN_POINT ( 'NONE',  ( -18.39999999999999858, 85.60000000001264198, -196.4910380878246201 ) ) ;
#138127=CARTESIAN_POINT ( 'NONE',  ( 21.14999999999999858, 69.45934304831143891, -203.5231074845243882 ) ) ;
#138128=CARTESIAN_POINT ( 'NONE',  ( 18.59999999999999076, 65.79142135624984178, -182.1731074845244223 ) ) ;
#138130=VECTOR ( 'NONE', #150072, 1000.000000000000000 ) ;
#138155=ADVANCED_FACE ( 'NONE', ( #7113 ), #64531, .T. ) ;
#138188=CYLINDRICAL_SURFACE ( 'NONE', #136915, 4.049999999999998046 ) ;
#138202=LINE ( 'NONE', #82073, #200458 ) ;
#138217=CARTESIAN_POINT ( 'NONE',  ( 18.59999999999999432, 74.36282728704222222, -191.9409541190523498 ) ) ;
#138238=CARTESIAN_POINT ( 'NONE',  ( -21.14999999999999503, 64.25000000001264766, -196.6039602385656337 ) ) ;
#138245=ORIENTED_EDGE ( 'NONE', *, *, #162096, .F. ) ;
#138255=DIRECTION ( 'NONE',  ( 0.000000000000000000, -6.982962677686266711E-15, 1.000000000000000000 ) ) ;
#138288=ORIENTED_EDGE ( 'NONE', *, *, #18008, .F. ) ;
#138306=ORIENTED_EDGE ( 'NONE', *, *, #55691, .T. ) ;
#138354=VERTEX_POINT ( 'NONE', #236441 ) ;
#138368=ADVANCED_FACE ( 'NONE', ( #99476 ), #138755, .F. ) ;
#138380=DIRECTION ( 'NONE',  ( 1.000000000000000000, -0.000000000000000000, 0.000000000000000000 ) ) ;
#138386=ORIENTED_EDGE ( 'NONE', *, *, #78510, .F. ) ;
#138402=AXIS2_PLACEMENT_3D ( 'NONE', #202968, #7338, #4743 ) ;
#138410=CARTESIAN_POINT ( 'NONE',  ( -21.05000000000000071, 69.60000000001261355, -193.5926828544628222 ) ) ;
#138411=DIRECTION ( 'NONE',  ( -1.000000000000000000, 0.000000000000000000, -0.000000000000000000 ) ) ;
#138418=DIRECTION ( 'NONE',  ( 0.000000000000000000, 0.000000000000000000, 1.000000000000000000 ) ) ;
#138500=DIRECTION ( 'NONE',  ( 1.000000000000000000, 0.000000000000000000, 0.000000000000000000 ) ) ;
#138520=CARTESIAN_POINT ( 'NONE',  ( 23.24999999999999289, 71.85000000001268461, -203.5231074845243597 ) ) ;
#138529=VERTEX_POINT ( 'NONE', #221988 ) ;
#138559=ORIENTED_EDGE ( 'NONE', *, *, #112946, .T. ) ;
#138566=DIRECTION ( 'NONE',  ( 0.000000000000000000, 0.000000000000000000, -1.000000000000000000 ) ) ;
#138582=CARTESIAN_POINT ( 'NONE',  ( -18.46093223321778609, 85.48068296828714097, -196.4385569705976025 ) ) ;
#138608=ORIENTED_EDGE ( 'NONE', *, *, #238626, .T. ) ;
#138629=CARTESIAN_POINT ( 'NONE',  ( 21.05000000000000071, 64.25000000001249134, -177.0379132551784096 ) ) ;
#138710=CARTESIAN_POINT ( 'NONE',  ( -18.43634282235122868, 85.67978719994030712, -163.3624555990703300 ) ) ;
#138720=B_SPLINE_CURVE_WITH_KNOTS ( 'NONE', 3,
 ( #125680, #224768, #108691, #8324, #203934, #227346, #27904, #83936, #188229, #183104, #147830, #24038, #46140, #226032, #68289, #167406, #248207, #69582, #48704 ),
 .UNSPECIFIED., .F., .F.,
 ( 4, 3, 3, 3, 3, 3, 4 ),
 ( 0.000000000000000000, 2.646747978908353324E-05, 5.271166642128929112E-05, 9.008788829885582504E-05, 0.0001426648776561122839, 0.0001897378458659801674, 0.0001917382627806533295 ),
 .UNSPECIFIED. ) ;
#138734=ADVANCED_FACE ( 'NONE', ( #23222 ), #161441, .T. ) ;
#138745=CARTESIAN_POINT ( 'NONE',  ( 21.87500000000000355, 66.25000000001253397, -182.3731074845244393 ) ) ;
#138748=AXIS2_PLACEMENT_3D ( 'NONE', #18744, #93139, #253495 ) ;
#138755=TOROIDAL_SURFACE ( 'NONE', #151295, 12.97499999999999787, 0.1000000000000000056 ) ;
#138763=FACE_OUTER_BOUND ( 'NONE', #225287, .T. ) ;
#138768=DIRECTION ( 'NONE',  ( 0.000000000000000000, -7.056502275159890832E-15, 1.000000000000000000 ) ) ;
#138793=AXIS2_PLACEMENT_3D ( 'NONE', #153485, #113024, #192564 ) ;
#138876=AXIS2_PLACEMENT_3D ( 'NONE', #12414, #111493, #214431 ) ;
#138886=EDGE_LOOP ( 'NONE', ( #39621, #157950, #26069, #204389 ) ) ;
#138914=AXIS2_PLACEMENT_3D ( 'NONE', #191822, #190535, #210084 ) ;
#138938=ORIENTED_EDGE ( 'NONE', *, *, #254794, .T. ) ;
#138942=EDGE_LOOP ( 'NONE', ( #49217, #45026, #128295, #242269 ) ) ;
#138947=DIRECTION ( 'NONE',  ( 1.000000000000000000, 0.000000000000000000, 0.000000000000000000 ) ) ;
#138953=DIRECTION ( 'NONE',  ( 1.000000000000000000, -3.265361837132813093E-16, -2.280189983783949500E-30 ) ) ;
#138995=AXIS2_PLACEMENT_3D ( 'NONE', #45579, #204632, #185087 ) ;
#139000=DIRECTION ( 'NONE',  ( -0.000000000000000000, 0.8660254037844377084, 0.5000000000000016653 ) ) ;
#139009=ORIENTED_EDGE ( 'NONE', *, *, #169125, .T. ) ;
#139027=ADVANCED_FACE ( 'NONE', ( #153460 ), #193828, .F. ) ;
#139042=CARTESIAN_POINT ( 'NONE',  ( 23.14999999999999503, 64.35000000001275566, -215.2731074845244450 ) ) ;
#139049=CARTESIAN_POINT ( 'NONE',  ( -23.15000000000000213, 76.00000000001244871, -170.0231074845243597 ) ) ;
#139051=ORIENTED_EDGE ( 'NONE', *, *, #193492, .T. ) ;
#139089=DIRECTION ( 'NONE',  ( 1.000000000000000000, 0.000000000000000000, 0.000000000000000000 ) ) ;
#139121=AXIS2_PLACEMENT_3D ( 'NONE', #108066, #216133, #154919 ) ;
#139125=AXIS2_PLACEMENT_3D ( 'NONE', #152155, #30929, #15195 ) ;
#139131=CARTESIAN_POINT ( 'NONE',  ( -20.54999999999999716, 74.00000000001259082, -190.7984855617622770 ) ) ;
#139134=CIRCLE ( 'NONE', #26772, 0.09999999999999939493 ) ;
#139135=EDGE_CURVE ( 'NONE', #160984, #254122, #22096, .T. ) ;
#139137=DIRECTION ( 'NONE',  ( -1.000000000000000000, 0.000000000000000000, -0.000000000000000000 ) ) ;
#139150=VECTOR ( 'NONE', #146067, 1000.000000000000000 ) ;
#139153=CIRCLE ( 'NONE', #35177, 0.1000000000000043771 ) ;
#139159=CARTESIAN_POINT ( 'NONE',  ( 18.39999999999999858, 85.60000000001264198, -196.4910380878246201 ) ) ;
#139160=APPLICATION_CONTEXT ( 'automotive_design' ) ;
#139162=DIRECTION ( 'NONE',  ( 0.000000000000000000, -0.3738317757008748909, -0.9274965247785733613 ) ) ;
#139178=EDGE_CURVE ( 'NONE', #95308, #141019, #180683, .T. ) ;
#139194=CARTESIAN_POINT ( 'NONE',  ( 20.95512820512820440, 65.37615131630072085, -191.3731074845244393 ) ) ;
#139197=EDGE_LOOP ( 'NONE', ( #21877, #31587, #249319, #180767 ) ) ;
#139255=CIRCLE ( 'NONE', #97556, 0.09999999999998898659 ) ;
#139270=CARTESIAN_POINT ( 'NONE',  ( -20.99780126800916591, 64.39461131213593603, -176.9357549128189362 ) ) ;
#139275=ORIENTED_EDGE ( 'NONE', *, *, #169020, .F. ) ;
#139279=EDGE_CURVE ( 'NONE', #96257, #59994, #122024, .T. ) ;
#139281=ORIENTED_EDGE ( 'NONE', *, *, #231383, .T. ) ;
#139292=DIRECTION ( 'NONE',  ( 0.000000000000000000, -1.000000000000000000, -6.982962677686266711E-15 ) ) ;
#139297=CARTESIAN_POINT ( 'NONE',  ( 20.95512820512820085, 65.37615131630074927, -195.8581939154368285 ) ) ;
#139302=CIRCLE ( 'NONE', #39406, 0.09999999999998712696 ) ;
#139303=VERTEX_POINT ( 'NONE', #717 ) ;
#139310=EDGE_CURVE ( 'NONE', #122787, #241009, #132969, .T. ) ;
#139327=DIRECTION ( 'NONE',  ( 2.952720810173289112E-16, 1.000000000000000000, 6.982962677686266711E-15 ) ) ;
#139330=CARTESIAN_POINT ( 'NONE',  ( -23.25000000000000000, 71.65000000001253966, -182.3731074845244109 ) ) ;
#139346=AXIS2_PLACEMENT_3D ( 'NONE', #247903, #189227, #230934 ) ;
#139381=EDGE_CURVE ( 'NONE', #10156, #4179, #97035, .T. ) ;
#139407=CARTESIAN_POINT ( 'NONE',  ( 18.56308993302918964, 65.61930884468881686, -178.7838848455861580 ) ) ;
#139463=CARTESIAN_POINT ( 'NONE',  ( 23.14999999999998437, 71.95000000001267892, -203.5231074845243597 ) ) ;
#139466=SPHERICAL_SURFACE ( 'NONE', #44411, 0.1000000000000000056 ) ;
#139504=LINE ( 'NONE', #121284, #99518 ) ;
#139506=DIRECTION ( 'NONE',  ( 1.000000000000000000, 0.000000000000000000, 0.000000000000000000 ) ) ;
#139515=CARTESIAN_POINT ( 'NONE',  ( 21.05193202509564543, 65.27606398031542767, -191.3505728811986728 ) ) ;
#139517=LINE ( 'NONE', #40472, #170119 ) ;
#139531=FACE_OUTER_BOUND ( 'NONE', #179898, .T. ) ;
#139576=DIRECTION ( 'NONE',  ( -1.000000000000000000, 0.000000000000000000, -0.000000000000000000 ) ) ;
#139578=VERTEX_POINT ( 'NONE', #174002 ) ;
#139590=EDGE_CURVE ( 'NONE', #115263, #166854, #9773, .T. ) ;
#139621=VERTEX_POINT ( 'NONE', #431 ) ;
#139639=CARTESIAN_POINT ( 'NONE',  ( -23.25000000000000000, 76.00000000001270450, -207.5731074845243427 ) ) ;
#139669=ADVANCED_FACE ( 'NONE', ( #177832 ), #117823, .T. ) ;
#139688=FACE_OUTER_BOUND ( 'NONE', #121165, .T. ) ;
#139692=CIRCLE ( 'NONE', #148093, 0.09999999999998712696 ) ;
#139696=B_SPLINE_CURVE_WITH_KNOTS ( 'NONE', 3,
 ( #250809, #179953, #139515, #23468, #44293, #2569, #224189, #63845, #222904, #202077, #102948, #143373, #162964, #40470, #241213, #182529 ),
 .UNSPECIFIED., .F., .F.,
 ( 4, 3, 3, 3, 3, 4 ),
 ( 0.000000000000000000, 3.357088238235088736E-05, 6.714213034887092689E-05, 0.0001007408646120986739, 0.0001343627955914349754, 0.0001573956632896092792 ),
 .UNSPECIFIED. ) ;
#139697=EDGE_CURVE ( 'NONE', #110167, #207747, #96511, .T. ) ;
#139706=EDGE_CURVE ( 'NONE', #204733, #80372, #234831, .T. ) ;
#139725=EDGE_CURVE ( 'NONE', #246982, #160597, #116116, .T. ) ;
#139750=FACE_OUTER_BOUND ( 'NONE', #46831, .T. ) ;
#139754=DIRECTION ( 'NONE',  ( -1.000000000000000000, 3.265361837132813093E-16, 2.280189983783949500E-30 ) ) ;
#139768=CARTESIAN_POINT ( 'NONE',  ( -22.39999999999999858, 68.20922040163927136, -203.6231074845244109 ) ) ;
#139776=CIRCLE ( 'NONE', #202157, 0.09999999999999939493 ) ;
#139780=CARTESIAN_POINT ( 'NONE',  ( 20.95566103547454517, 65.38175234906556454, -195.8912672915438122 ) ) ;
#139805=FACE_OUTER_BOUND ( 'NONE', #140031, .T. ) ;
#139810=ORIENTED_EDGE ( 'NONE', *, *, #68953, .T. ) ;
#139829=DIRECTION ( 'NONE',  ( -1.000000000000000000, -0.000000000000000000, -0.000000000000000000 ) ) ;
#139883=CARTESIAN_POINT ( 'NONE',  ( -18.54159361262947314, 85.46313213550581622, -196.4739852682315018 ) ) ;
#139894=ORIENTED_EDGE ( 'NONE', *, *, #101523, .F. ) ;
#139907=VERTEX_POINT ( 'NONE', #142437 ) ;
#139957=CARTESIAN_POINT ( 'NONE',  ( 18.59999994388910238, 85.36356618708362021, -196.3419902477231744 ) ) ;
#139962=DIRECTION ( 'NONE',  ( 0.000000000000000000, -6.982962677686266711E-15, 1.000000000000000000 ) ) ;
#139966=DIRECTION ( 'NONE',  ( 0.000000000000000000, -6.938893903907222067E-15, 1.000000000000000000 ) ) ;
#139970=CIRCLE ( 'NONE', #181700, 0.09999999999998898659 ) ;
#139973=TOROIDAL_SURFACE ( 'NONE', #52503, 0.2000000000000000111, 0.1000000000000000056 ) ;
#140002=FACE_OUTER_BOUND ( 'NONE', #21546, .T. ) ;
#140007=DIRECTION ( 'NONE',  ( 0.000000000000000000, 0.000000000000000000, 1.000000000000000000 ) ) ;
#140030=EDGE_CURVE ( 'NONE', #94008, #9660, #251808, .T. ) ;
#140031=EDGE_LOOP ( 'NONE', ( #136815, #13950, #222381, #33576 ) ) ;
#140079=ORIENTED_EDGE ( 'NONE', *, *, #72921, .T. ) ;
#140117=AXIS2_PLACEMENT_3D ( 'NONE', #247750, #110802, #30017 ) ;
#140126=DIRECTION ( 'NONE',  ( 1.000000000000000000, -1.875376730785737719E-16, -1.309568571767809260E-30 ) ) ;
#140150=DIRECTION ( 'NONE',  ( 0.000000000000000000, -6.982962677686266711E-15, 1.000000000000000000 ) ) ;
#140168=CARTESIAN_POINT ( 'NONE',  ( -20.94999999999999574, 64.37928932189385023, -176.8915241368654279 ) ) ;
#140170=DIRECTION ( 'NONE',  ( 0.000000000000000000, -6.853228547068871147E-15, 1.000000000000000000 ) ) ;
#140183=DIRECTION ( 'NONE',  ( 1.000000000000000000, 0.000000000000000000, 0.000000000000000000 ) ) ;
#140185=CARTESIAN_POINT ( 'NONE',  ( 23.14999999999999858, 76.00000000001244871, -170.0231074845243597 ) ) ;
#140200=ORIENTED_EDGE ( 'NONE', *, *, #245879, .T. ) ;
#140208=ORIENTED_EDGE ( 'NONE', *, *, #149701, .T. ) ;
#140219=CARTESIAN_POINT ( 'NONE',  ( 19.99999999738052381, 64.25000000001250555, -178.8359355348915471 ) ) ;
#140241=VECTOR ( 'NONE', #5583, 1000.000000000000000 ) ;
#140246=LINE ( 'NONE', #19036, #219123 ) ;
#140277=AXIS2_PLACEMENT_3D ( 'NONE', #172946, #235423, #35973 ) ;
#140291=AXIS2_PLACEMENT_3D ( 'NONE', #98908, #237180, #93801 ) ;
#140315=EDGE_CURVE ( 'NONE', #139578, #98827, #251566, .T. ) ;
#140322=EDGE_CURVE ( 'NONE', #198203, #133285, #230742, .T. ) ;
#140330=VERTEX_POINT ( 'NONE', #145976 ) ;
#140337=EDGE_LOOP ( 'NONE', ( #107133, #235559, #135313, #219241 ) ) ;
#140360=CYLINDRICAL_SURFACE ( 'NONE', #79010, 0.09999999999998898659 ) ;
#140366=CIRCLE ( 'NONE', #252792, 0.4000000000000114575 ) ;
#140419=LINE ( 'NONE', #157467, #167680 ) ;
#140448=CYLINDRICAL_SURFACE ( 'NONE', #56445, 0.09999999999998898659 ) ;
#140458=DIRECTION ( 'NONE',  ( 0.000000000000000000, -6.982962677686266711E-15, 1.000000000000000000 ) ) ;
#140464=EDGE_CURVE ( 'NONE', #183161, #198203, #139302, .T. ) ;
#140468=CARTESIAN_POINT ( 'NONE',  ( 20.94999999999999929, 87.65000000001244018, -170.0231074845242745 ) ) ;
#140476=CARTESIAN_POINT ( 'NONE',  ( -18.59999999999999787, 76.00000000001267608, -203.5231074845243597 ) ) ;
#140493=DIRECTION ( 'NONE',  ( -1.000000000000000000, 0.000000000000000000, 0.000000000000000000 ) ) ;
#140510=PRODUCT_DEFINITION_FORMATION_WITH_SPECIFIED_SOURCE ( 'ANY', '', #205405, .NOT_KNOWN. ) ;
#140518=ORIENTED_EDGE ( 'NONE', *, *, #71824, .F. ) ;
#140549=EDGE_LOOP ( 'NONE', ( #125090, #238757, #161526 ) ) ;
#140573=AXIS2_PLACEMENT_3D ( 'NONE', #212923, #72143, #133392 ) ;
#140590=VECTOR ( 'NONE', #52936, 1000.000000000000000 ) ;
#140608=ORIENTED_EDGE ( 'NONE', *, *, #191621, .T. ) ;
#140610=ADVANCED_FACE ( 'NONE', ( #46242 ), #216164, .T. ) ;
#140613=EDGE_LOOP ( 'NONE', ( #81921, #24400, #194695, #70669 ) ) ;
#140630=DIRECTION ( 'NONE',  ( 0.000000000000000000, -6.982962677686266711E-15, 1.000000000000000000 ) ) ;
#140660=CARTESIAN_POINT ( 'NONE',  ( -21.05000000000000071, 76.00000000001244871, -170.0231074845243597 ) ) ;
#140667=DIRECTION ( 'NONE',  ( 0.000000000000000000, -1.000000000000000000, 0.000000000000000000 ) ) ;
#140676=LINE ( 'NONE', #41607, #11246 ) ;
#140682=CARTESIAN_POINT ( 'NONE',  ( 23.14999999999999858, 76.00000000001247713, -174.0231074845243882 ) ) ;
#140708=CARTESIAN_POINT ( 'NONE',  ( 18.58143601961851843, 65.56427058491756554, -178.7731074845244166 ) ) ;
#140721=APPLICATION_CONTEXT ( 'automotive_design' ) ;
#140733=DIRECTION ( 'NONE',  ( -1.000000000000000000, -0.000000000000000000, -0.000000000000000000 ) ) ;
#140736=ORIENTED_EDGE ( 'NONE', *, *, #10489, .F. ) ;
#140825=EDGE_LOOP ( 'NONE', ( #117526, #186194, #74839, #159856, #28341 ) ) ;
#140860=CARTESIAN_POINT ( 'NONE',  ( 21.14999999999999858, 67.21339244341248786, -191.1731074845244223 ) ) ;
#140890=CARTESIAN_POINT ( 'NONE',  ( -21.14999999999999858, 64.25000000001263345, -196.7392418215462726 ) ) ;
#140892=ADVANCED_FACE ( 'NONE', ( #22548 ), #196045, .T. ) ;
#140939=ORIENTED_EDGE ( 'NONE', *, *, #88801, .T. ) ;
#140959=ORIENTED_EDGE ( 'NONE', *, *, #39267, .F. ) ;
#140963=CYLINDRICAL_SURFACE ( 'NONE', #7258, 0.09999999999998898659 ) ;
#140970=DIRECTION ( 'NONE',  ( 1.000000000000000000, 0.000000000000000000, 0.000000000000000000 ) ) ;
#140972=VECTOR ( 'NONE', #15730, 1000.000000000000000 ) ;
#141001=ORIENTED_EDGE ( 'NONE', *, *, #110454, .F. ) ;
#141017=CARTESIAN_POINT ( 'NONE',  ( -21.05000000000000071, 64.35000000001268461, -203.4231074845244507 ) ) ;
#141019=VERTEX_POINT ( 'NONE', #225835 ) ;
#141041=FACE_OUTER_BOUND ( 'NONE', #26863, .T. ) ;
#141092=ORIENTED_EDGE ( 'NONE', *, *, #160351, .F. ) ;
#141095=SPHERICAL_SURFACE ( 'NONE', #11815, 0.1000000000000000056 ) ;
#141097=CARTESIAN_POINT ( 'NONE',  ( 21.00000000000000000, 66.25000000001253397, -182.2731074845244450 ) ) ;
#141109=AXIS2_PLACEMENT_3D ( 'NONE', #94900, #72814, #134028 ) ;
#141136=CARTESIAN_POINT ( 'NONE',  ( -21.05000000000000071, 76.00000000001244871, -170.0231074845243597 ) ) ;
#141152=VECTOR ( 'NONE', #72827, 1000.000000000000000 ) ;
#141194=EDGE_CURVE ( 'NONE', #106770, #137660, #11985, .T. ) ;
#141208=DIRECTION ( 'NONE',  ( 0.000000000000000000, 0.8660254037844377084, 0.5000000000000015543 ) ) ;
#141247=EDGE_CURVE ( 'NONE', #120584, #203821, #239659, .T. ) ;
#141262=EDGE_LOOP ( 'NONE', ( #69650, #157334 ) ) ;
#141279=EDGE_CURVE ( 'NONE', #255434, #138354, #57484, .T. ) ;
#141303=ADVANCED_FACE ( 'NONE', ( #3948 ), #146021, .T. ) ;
#141305=DIRECTION ( 'NONE',  ( 0.000000000000000000, 0.4930308989874980785, 0.8700118002898462599 ) ) ;
#141318=AXIS2_PLACEMENT_3D ( 'NONE', #27811, #229826, #207714 ) ;
#141324=CIRCLE ( 'NONE', #53845, 0.1000000000000028644 ) ;
#141370=AXIS2_PLACEMENT_3D ( 'NONE', #147391, #65283, #48288 ) ;
#141382=DIRECTION ( 'NONE',  ( 0.000000000000000000, 0.000000000000000000, 1.000000000000000000 ) ) ;
#141384=EDGE_LOOP ( 'NONE', ( #213992, #31494, #122512, #187499 ) ) ;
#141386=DIRECTION ( 'NONE',  ( 1.000000000000000000, 0.000000000000000000, 0.000000000000000000 ) ) ;
#141422=PLANE ( 'NONE',  #227938 ) ;
#141438=AXIS2_PLACEMENT_3D ( 'NONE', #99372, #79807, #238915 ) ;
#141439=AXIS2_PLACEMENT_3D ( 'NONE', #256847, #254315, #135656 ) ;
#141440=ORIENTED_EDGE ( 'NONE', *, *, #49743, .F. ) ;
#141443=EDGE_CURVE ( 'NONE', #77481, #235211, #235538, .T. ) ;
#141486=FACE_OUTER_BOUND ( 'NONE', #239426, .T. ) ;
#141489=DIRECTION ( 'NONE',  ( 1.000000000000000000, 0.000000000000000000, 0.000000000000000000 ) ) ;
#141514=CARTESIAN_POINT ( 'NONE',  ( 20.97462148592287079, 67.12526242356200612, -191.2684631527934016 ) ) ;
#141530=ADVANCED_FACE ( 'NONE', ( #148611 ), #19065, .T. ) ;
#141533=ORIENTED_EDGE ( 'NONE', *, *, #210598, .T. ) ;
#141582=ORIENTED_EDGE ( 'NONE', *, *, #53712, .F. ) ;
#141587=EDGE_CURVE ( 'NONE', #13339, #108178, #194065, .T. ) ;
#141588=ORIENTED_EDGE ( 'NONE', *, *, #141587, .T. ) ;
#141598=CARTESIAN_POINT ( 'NONE',  ( 22.60000000000000142, 76.00000000001267608, -203.5231074845243597 ) ) ;
#141625=VERTEX_POINT ( 'NONE', #96303 ) ;
#141627=CARTESIAN_POINT ( 'NONE',  ( -23.25000000000000000, 74.00000000001254818, -182.6477294072865050 ) ) ;
#141645=AXIS2_PLACEMENT_3D ( 'NONE', #21098, #215409, #36815 ) ;
#141650=LINE ( 'NONE', #200348, #67798 ) ;
#141714=DIRECTION ( 'NONE',  ( 0.000000000000000000, 0.9999631594459055250, 0.008583690987131395445 ) ) ;
#141730=CARTESIAN_POINT ( 'NONE',  ( -20.94999999999999929, 76.00000000001244871, -170.0231074845243597 ) ) ;
#141772=LINE ( 'NONE', #163924, #45351 ) ;
#141817=ORIENTED_EDGE ( 'NONE', *, *, #7566, .T. ) ;
#141837=VERTEX_POINT ( 'NONE', #183569 ) ;
#141858=EDGE_CURVE ( 'NONE', #84905, #78560, #85669, .T. ) ;
#141876=DIRECTION ( 'NONE',  ( 1.836970198721029934E-16, 1.000000000000000000, 6.982962677686266711E-15 ) ) ;
#141886=AXIS2_PLACEMENT_3D ( 'NONE', #66217, #153504, #94751 ) ;
#141895=CARTESIAN_POINT ( 'NONE',  ( 18.59999999999999432, 77.13501884592258762, -162.3061306010920362 ) ) ;
#141914=DIRECTION ( 'NONE',  ( 0.000000000000000000, -0.9875055080513754913, 0.1575844902526733482 ) ) ;
#141943=CARTESIAN_POINT ( 'NONE',  ( -23.25000000000000000, 64.25000000001253397, -182.1731074845244507 ) ) ;
#141950=EDGE_LOOP ( 'NONE', ( #230966, #14290, #15010, #650 ) ) ;
#141986=CARTESIAN_POINT ( 'NONE',  ( 18.49999999999998224, 65.71984138295536582, -178.7985354133222131 ) ) ;
#141997=ORIENTED_EDGE ( 'NONE', *, *, #148049, .F. ) ;
#142031=DIRECTION ( 'NONE',  ( 0.000000000000000000, 1.000000000000000000, 6.982962677686266711E-15 ) ) ;
#142034=ORIENTED_EDGE ( 'NONE', *, *, #50910, .F. ) ;
#142042=CARTESIAN_POINT ( 'NONE',  ( -21.05000000000000071, 87.48912529308852015, -173.1231074845242688 ) ) ;
#142054=DIRECTION ( 'NONE',  ( 0.000000000000000000, 0.000000000000000000, 1.000000000000000000 ) ) ;
#142129=EDGE_CURVE ( 'NONE', #83659, #229015, #42211, .T. ) ;
#142130=DIRECTION ( 'NONE',  ( 1.000000000000000000, 0.000000000000000000, 0.000000000000000000 ) ) ;
#142132=DIRECTION ( 'NONE',  ( -1.000000000000000000, 0.000000000000000000, 0.000000000000000000 ) ) ;
#142133=ORIENTED_EDGE ( 'NONE', *, *, #32326, .T. ) ;
#142147=AXIS2_PLACEMENT_3D ( 'NONE', #152359, #228015, #110631 ) ;
#142161=FACE_OUTER_BOUND ( 'NONE', #72656, .T. ) ;
#142164=DIRECTION ( 'NONE',  ( 0.000000000000000000, -6.982962677686266711E-15, 1.000000000000000000 ) ) ;
#142218=ORIENTED_EDGE ( 'NONE', *, *, #171295, .F. ) ;
#142239=ORIENTED_EDGE ( 'NONE', *, *, #47224, .F. ) ;
#142244=CARTESIAN_POINT ( 'NONE',  ( 20.94999999999999929, 76.00000000001267608, -203.5231074845243597 ) ) ;
#142259=AXIS2_PLACEMENT_3D ( 'NONE', #39028, #255437, #76845 ) ;
#142294=FACE_OUTER_BOUND ( 'NONE', #118911, .T. ) ;
#142333=VECTOR ( 'NONE', #3469, 1000.000000000000000 ) ;
#142353=TOROIDAL_SURFACE ( 'NONE', #13381, 4.099999999999999645, 0.1000000000000000056 ) ;
#142362=DIRECTION ( 'NONE',  ( 0.000000000000000000, 0.000000000000000000, -1.000000000000000000 ) ) ;
#142364=( BOUNDED_SURFACE ( )  B_SPLINE_SURFACE ( 3, 2, ( 
 ( #143039, #83045, #66089 ),
 ( #68668, #88189, #188598 ),
 ( #45245, #247281, #126046 ),
 ( #166506, #167790, #204301 ) ),
 .UNSPECIFIED., .F., .F., .T. ) 
 B_SPLINE_SURFACE_WITH_KNOTS ( ( 4, 4 ),
 ( 3, 3 ),
 ( 0.04058434257139457990, 0.04256401539001584966 ),
 ( 0.000000000000000000, 1.000000000000000000 ),
 .UNSPECIFIED. ) 
 GEOMETRIC_REPRESENTATION_ITEM ( )  RATIONAL_B_SPLINE_SURFACE ( (
 ( 1.000000000000000000, 0.7103081912007894738, 1.000000000000000000),
 ( 1.000000000000000000, 0.7104998333556562518, 1.000000000000000000),
 ( 1.000000000000000000, 0.7107238315754180746, 1.000000000000000000),
 ( 1.000000000000000000, 0.7110073749539692622, 1.000000000000000000) ) ) 
 REPRESENTATION_ITEM ( '' )  SURFACE ( )  );
#142371=CIRCLE ( 'NONE', #175715, 0.09999999999999489853 ) ;
#142385=EDGE_CURVE ( 'NONE', #230341, #56486, #66154, .T. ) ;
#142414=ADVANCED_FACE ( 'NONE', ( #181370 ), #165184, .F. ) ;
#142437=CARTESIAN_POINT ( 'NONE',  ( -20.85000000000000142, 68.92903212821357783, -166.2765432626560766 ) ) ;
#142447=ORIENTED_EDGE ( 'NONE', *, *, #235535, .T. ) ;
#142504=AXIS2_PLACEMENT_3D ( 'NONE', #181303, #200851, #41800 ) ;
#142532=CARTESIAN_POINT ( 'NONE',  ( 21.09096482362066993, 69.63645563460816845, -203.5625557632985476 ) ) ;
#142544=CARTESIAN_POINT ( 'NONE',  ( -2.995603634470891112E-16, 87.75000000001250555, -178.7731074845242745 ) ) ;
#142548=CARTESIAN_POINT ( 'NONE',  ( 18.59999999999999432, 74.83729825007462466, -195.4231074845243654 ) ) ;
#142572=CARTESIAN_POINT ( 'NONE',  ( -18.59999999999999787, 64.35000000001254250, -182.1731074845244507 ) ) ;
#142574=DIRECTION ( 'NONE',  ( 1.000000000000000000, 0.000000000000000000, 0.000000000000000000 ) ) ;
#142610=CARTESIAN_POINT ( 'NONE',  ( -20.64999999999999858, 76.00000000001267608, -203.5231074845243597 ) ) ;
#142660=CARTESIAN_POINT ( 'NONE',  ( -20.64999999999999858, 68.75000000001260503, -191.2731074845244166 ) ) ;
#142681=DIRECTION ( 'NONE',  ( 0.000000000000000000, -0.4999999999999088507, 0.8660254037844913322 ) ) ;
#142683=EDGE_CURVE ( 'NONE', #71853, #102606, #114643, .T. ) ;
#142689=VERTEX_POINT ( 'NONE', #209912 ) ;
#142757=FACE_OUTER_BOUND ( 'NONE', #22916, .T. ) ;
#142768=ORIENTED_EDGE ( 'NONE', *, *, #232400, .T. ) ;
#142785=CARTESIAN_POINT ( 'NONE',  ( 19.75857864376268935, 64.25000000001250555, -178.7731074845244450 ) ) ;
#142829=CARTESIAN_POINT ( 'NONE',  ( -20.15000000000000568, 66.70857864377528301, -191.1731074845244223 ) ) ;
#142839=ORIENTED_EDGE ( 'NONE', *, *, #162498, .F. ) ;
#142868=ORIENTED_EDGE ( 'NONE', *, *, #6136, .F. ) ;
#142900=EDGE_CURVE ( 'NONE', #131204, #207133, #235862, .T. ) ;
#142915=DIRECTION ( 'NONE',  ( -0.000000000000000000, -1.000000000000000000, -6.982962677686266711E-15 ) ) ;
#142930=ORIENTED_EDGE ( 'NONE', *, *, #181960, .F. ) ;
#142939=EDGE_CURVE ( 'NONE', #165343, #133931, #183608, .T. ) ;
#143013=CARTESIAN_POINT ( 'NONE',  ( 18.59999999999999076, 64.35000000001245724, -170.0231074845244166 ) ) ;
#143031=AXIS2_PLACEMENT_3D ( 'NONE', #43159, #1442, #219206 ) ;
#143032=VERTEX_POINT ( 'NONE', #212163 ) ;
#143038=CARTESIAN_POINT ( 'NONE',  ( -20.64999999999999858, 76.00000000001267608, -203.5231074845243597 ) ) ;
#143039=CARTESIAN_POINT ( 'NONE',  ( -22.39999999999999503, 68.20922040163927136, -203.5231074845244166 ) ) ;
#143043=VECTOR ( 'NONE', #240341, 1000.000000000000000 ) ;
#143051=CARTESIAN_POINT ( 'NONE',  ( 23.14999999999999858, 71.18691588786300883, -181.9646252410481964 ) ) ;
#143061=CARTESIAN_POINT ( 'NONE',  ( 20.85000000000000142, 64.25000000001244871, -170.0231074845244166 ) ) ;
#143087=DIRECTION ( 'NONE',  ( -1.000000000000000000, 0.000000000000000000, -0.000000000000000000 ) ) ;
#143102=FACE_OUTER_BOUND ( 'NONE', #241533, .T. ) ;
#143166=EDGE_LOOP ( 'NONE', ( #76981, #95213, #155703, #220007, #28613 ) ) ;
#143170=CIRCLE ( 'NONE', #43243, 0.09999999999998898659 ) ;
#143186=CARTESIAN_POINT ( 'NONE',  ( 23.25000000000000000, 87.75000000001276135, -215.2731074845242745 ) ) ;
#143234=DIRECTION ( 'NONE',  ( 1.000000000000000000, 0.000000000000000000, 0.000000000000000000 ) ) ;
#143251=DIRECTION ( 'NONE',  ( 0.000000000000000000, 0.000000000000000000, -1.000000000000000000 ) ) ;
#143269=CIRCLE ( 'NONE', #230773, 0.09999999999998898659 ) ;
#143293=CARTESIAN_POINT ( 'NONE',  ( -23.15000000000000213, 76.00000000001270450, -207.5731074845243427 ) ) ;
#143321=LINE ( 'NONE', #225412, #3487 ) ;
#143363=CARTESIAN_POINT ( 'NONE',  ( -20.85000000000000142, 64.25000000001250555, -176.8069731475025321 ) ) ;
#143373=CARTESIAN_POINT ( 'NONE',  ( 21.11701782572532693, 65.27839088400513390, -191.2780700550132167 ) ) ;
#143380=CARTESIAN_POINT ( 'NONE',  ( 21.05000000000000071, 67.18454772081508963, -195.1027149319101568 ) ) ;
#143404=ORIENTED_EDGE ( 'NONE', *, *, #195922, .T. ) ;
#143440=ORIENTED_EDGE ( 'NONE', *, *, #151879, .T. ) ;
#143451=ORIENTED_EDGE ( 'NONE', *, *, #4055, .T. ) ;
#143513=FACE_OUTER_BOUND ( 'NONE', #248357, .T. ) ;
#143524=ORIENTED_EDGE ( 'NONE', *, *, #195901, .F. ) ;
#143536=CARTESIAN_POINT ( 'NONE',  ( 20.85000000000000142, 87.65000000001246860, -172.9231074845242802 ) ) ;
#143542=EDGE_LOOP ( 'NONE', ( #102100, #82608, #180680, #35732 ) ) ;
#143556=CARTESIAN_POINT ( 'NONE',  ( -20.00857864376270001, 66.85000000001254250, -182.2731074845244166 ) ) ;
#143575=DIRECTION ( 'NONE',  ( 2.827886303505249259E-16, 0.8660254037844377084, 0.5000000000000016653 ) ) ;
#143586=CYLINDRICAL_SURFACE ( 'NONE', #78703, 0.09999999999999939493 ) ;
#143639=DIRECTION ( 'NONE',  ( 1.000000000000000000, -0.000000000000000000, 0.000000000000000000 ) ) ;
#143644=CARTESIAN_POINT ( 'NONE',  ( 20.95462737510932882, 65.44321804836889100, -195.9531574279621680 ) ) ;
#143670=B_SPLINE_CURVE_WITH_KNOTS ( 'NONE', 3,
 ( #206169, #147476, #169655, #249162, #70540, #2179, #194336 ),
 .UNSPECIFIED., .F., .F.,
 ( 4, 3, 4 ),
 ( 0.000000000000000000, 0.0009834301579440022593, 0.001767853679402679300 ),
 .UNSPECIFIED. ) ;
#143671=CARTESIAN_POINT ( 'NONE',  ( -23.25000000000000000, 76.00000000001267608, -203.5231074845243597 ) ) ;
#143684=DIRECTION ( 'NONE',  ( 0.000000000000000000, 7.056502275159890832E-15, -1.000000000000000000 ) ) ;
#143689=DIRECTION ( 'NONE',  ( -1.000000000000000000, -0.000000000000000000, -0.000000000000000000 ) ) ;
#143691=DIRECTION ( 'NONE',  ( 0.000000000000000000, 6.982962677686266711E-15, -1.000000000000000000 ) ) ;
#143716=EDGE_CURVE ( 'NONE', #14542, #196907, #53498, .T. ) ;
#143720=CIRCLE ( 'NONE', #210550, 2.000000000000001776 ) ;
#143727=CARTESIAN_POINT ( 'NONE',  ( -18.47690164073607377, 85.46484453802463577, -163.3217265446882323 ) ) ;
#143734=DIRECTION ( 'NONE',  ( 0.000000000000000000, -0.9274965247785555977, 0.3738317757009190223 ) ) ;
#143745=FACE_OUTER_BOUND ( 'NONE', #230632, .T. ) ;
#143777=AXIS2_PLACEMENT_3D ( 'NONE', #21281, #82472, #39567 ) ;
#143778=AXIS2_PLACEMENT_3D ( 'NONE', #112178, #212557, #173475 ) ;
#143779=ORIENTED_EDGE ( 'NONE', *, *, #192235, .T. ) ;
#143780=ADVANCED_FACE ( 'NONE', ( #52060 ), #216277, .F. ) ;
#143814=AXIS2_PLACEMENT_3D ( 'NONE', #220210, #254174, #155130 ) ;
#143881=ORIENTED_EDGE ( 'NONE', *, *, #119206, .F. ) ;
#143882=AXIS2_PLACEMENT_3D ( 'NONE', #132915, #189028, #28717 ) ;
#143899=CIRCLE ( 'NONE', #85602, 0.09999999999998898659 ) ;
#143923=CIRCLE ( 'NONE', #10850, 0.09999999999999939493 ) ;
#143950=VERTEX_POINT ( 'NONE', #28400 ) ;
#143952=CARTESIAN_POINT ( 'NONE',  ( 21.14999999999999858, 76.10000000001276987, -215.1726782920691505 ) ) ;
#143968=DIRECTION ( 'NONE',  ( 0.000000000000000000, -6.982962677686266711E-15, 1.000000000000000000 ) ) ;
#143972=CARTESIAN_POINT ( 'NONE',  ( -20.85000000000000142, 64.35000000001251408, -176.8069731475025321 ) ) ;
#143997=EDGE_CURVE ( 'NONE', #145161, #9837, #236270, .T. ) ;
#144004=LINE ( 'NONE', #164874, #235121 ) ;
#144005=DIRECTION ( 'NONE',  ( 0.000000000000000000, -0.9274965247785504907, -0.3738317757009320674 ) ) ;
#144017=CARTESIAN_POINT ( 'NONE',  ( 21.06280952165520404, 65.37286769941093212, -191.3190535977457785 ) ) ;
#144031=CARTESIAN_POINT ( 'NONE',  ( 23.24999999999999289, 64.35000000001267040, -203.4231074845244507 ) ) ;
#144032=FACE_OUTER_BOUND ( 'NONE', #14907, .T. ) ;
#144066=CARTESIAN_POINT ( 'NONE',  ( -22.60000000000094289, 75.89914163091425792, -215.2726746080137730 ) ) ;
#144074=CARTESIAN_POINT ( 'NONE',  ( 19.81427058490531934, 64.33143601963072911, -178.7731074845244450 ) ) ;
#144079=CARTESIAN_POINT ( 'NONE',  ( 18.59999999999998721, 69.06610602788607878, -166.2374616501508342 ) ) ;
#144095=ADVANCED_FACE ( 'NONE', ( #72643 ), #33542, .T. ) ;
#144129=VERTEX_POINT ( 'NONE', #252524 ) ;
#144167=CARTESIAN_POINT ( 'NONE',  ( 18.50000000000000355, 85.48068669529135377, -163.0819923157664562 ) ) ;
#144170=DIRECTION ( 'NONE',  ( 1.000000000000000000, -2.952720810173289112E-16, -2.061873921506763405E-30 ) ) ;
#144187=CIRCLE ( 'NONE', #252347, 0.09999999999998898659 ) ;
#144206=CARTESIAN_POINT ( 'NONE',  ( 18.49999999999999289, 65.70729864261056719, -164.5657455973725121 ) ) ;
#144215=ORIENTED_EDGE ( 'NONE', *, *, #33252, .F. ) ;
#144248=LINE ( 'NONE', #89423, #6879 ) ;
#144289=VERTEX_POINT ( 'NONE', #198981 ) ;
#144328=DIRECTION ( 'NONE',  ( 0.000000000000000000, -6.982962677686266711E-15, 1.000000000000000000 ) ) ;
#144333=DIRECTION ( 'NONE',  ( 0.000000000000000000, 6.982962677686266711E-15, -1.000000000000000000 ) ) ;
#144340=AXIS2_PLACEMENT_3D ( 'NONE', #168014, #6316, #104123 ) ;
#144346=EDGE_CURVE ( 'NONE', #43445, #13339, #109565, .T. ) ;
#144368=CARTESIAN_POINT ( 'NONE',  ( -22.50000000000000000, 75.90000000001276703, -215.1726782920691505 ) ) ;
#144370=CARTESIAN_POINT ( 'NONE',  ( 21.05000000000000071, 76.00000000001244871, -170.0231074845243597 ) ) ;
#144388=VERTEX_POINT ( 'NONE', #111441 ) ;
#144425=VECTOR ( 'NONE', #220612, 1000.000000000000000 ) ;
#144430=ORIENTED_EDGE ( 'NONE', *, *, #42362, .T. ) ;
#144435=VERTEX_POINT ( 'NONE', #132283 ) ;
#144505=ORIENTED_EDGE ( 'NONE', *, *, #200678, .F. ) ;
#144517=ORIENTED_EDGE ( 'NONE', *, *, #162393, .F. ) ;
#144524=ORIENTED_EDGE ( 'NONE', *, *, #225080, .F. ) ;
#144529=CARTESIAN_POINT ( 'NONE',  ( 18.39999999999999858, 85.60000000001240039, -163.3229180933022633 ) ) ;
#144544=LINE ( 'NONE', #85834, #196671 ) ;
#144547=DIRECTION ( 'NONE',  ( 0.000000000000000000, -1.000000000000000000, -6.982962677686265922E-15 ) ) ;
#144549=CARTESIAN_POINT ( 'NONE',  ( 18.49999999999998934, 65.74999999739348766, -178.8359355348929114 ) ) ;
#144571=DIRECTION ( 'NONE',  ( 1.000000000000000000, -3.265361837132813093E-16, -2.280189983783949500E-30 ) ) ;
#144576=ORIENTED_EDGE ( 'NONE', *, *, #97566, .T. ) ;
#144588=CARTESIAN_POINT ( 'NONE',  ( 21.05000000000000071, 70.10000000001251408, -180.2422072491807796 ) ) ;
#144599=FACE_OUTER_BOUND ( 'NONE', #117772, .T. ) ;
#144641=DIRECTION ( 'NONE',  ( -0.000000000000000000, -6.982962677686266711E-15, 1.000000000000000000 ) ) ;
#144686=AXIS2_PLACEMENT_3D ( 'NONE', #65967, #122098, #5972 ) ;
#144694=CARTESIAN_POINT ( 'NONE',  ( 20.94999999999999929, 87.29603075034775372, -173.0710066441881452 ) ) ;
#144695=ORIENTED_EDGE ( 'NONE', *, *, #149212, .T. ) ;
#144697=ADVANCED_FACE ( 'NONE', ( #102115 ), #245524, .T. ) ;
#144703=LINE ( 'NONE', #147283, #13755 ) ;
#144710=EDGE_CURVE ( 'NONE', #47017, #102497, #219688, .T. ) ;
#144718=CARTESIAN_POINT ( 'NONE',  ( -20.64999999999999858, 74.00000000001254818, -182.7477294072864709 ) ) ;
#144721=FACE_OUTER_BOUND ( 'NONE', #180639, .T. ) ;
#144754=ORIENTED_EDGE ( 'NONE', *, *, #43392, .T. ) ;
#144765=ORIENTED_EDGE ( 'NONE', *, *, #125347, .F. ) ;
#144769=CARTESIAN_POINT ( 'NONE',  ( 18.44444291854884099, 85.49010118095564792, -163.3942035196333507 ) ) ;
#144772=EDGE_CURVE ( 'NONE', #256108, #172693, #174136, .T. ) ;
#144778=CARTESIAN_POINT ( 'NONE',  ( 18.46082813848004278, 85.48074965092008881, -196.4387373818086360 ) ) ;
#144829=DIRECTION ( 'NONE',  ( 0.000000000000000000, 6.982962677686266711E-15, -1.000000000000000000 ) ) ;
#144846=EDGE_CURVE ( 'NONE', #88021, #46518, #153283, .T. ) ;
#144857=DIRECTION ( 'NONE',  ( -1.000000000000000000, 3.265361837132813093E-16, 2.280189983783949500E-30 ) ) ;
#144858=AXIS2_PLACEMENT_3D ( 'NONE', #155135, #96385, #15621 ) ;
#144877=DIRECTION ( 'NONE',  ( -0.000000000000000000, -6.982962677686266711E-15, 1.000000000000000000 ) ) ;
#144889=CARTESIAN_POINT ( 'NONE',  ( -22.50000000000000000, 76.00000000001267608, -203.5231074845243597 ) ) ;
#144894=CIRCLE ( 'NONE', #82518, 0.09999999999999820144 ) ;
#144907=AXIS2_PLACEMENT_3D ( 'NONE', #166444, #162579, #226355 ) ;
#144913=CARTESIAN_POINT ( 'NONE',  ( 23.14999999999999858, 76.00000000001244871, -170.0231074845243597 ) ) ;
#144953=VERTEX_POINT ( 'NONE', #180116 ) ;
#144966=ORIENTED_EDGE ( 'NONE', *, *, #200865, .T. ) ;
#145001=CARTESIAN_POINT ( 'NONE',  ( -18.50000000000000000, 85.40000000001241176, -163.1410656363516125 ) ) ;
#145003=DIRECTION ( 'NONE',  ( 0.000000000000000000, 7.162729191130010591E-15, -1.000000000000000000 ) ) ;
#145017=EDGE_CURVE ( 'NONE', #30910, #38939, #53298, .T. ) ;
#145035=EDGE_LOOP ( 'NONE', ( #69856, #215442, #81323, #44151, #26108 ) ) ;
#145037=ADVANCED_FACE ( 'NONE', ( #43166 ), #211719, .F. ) ;
#145064=ORIENTED_EDGE ( 'NONE', *, *, #112888, .F. ) ;
#145080=VERTEX_POINT ( 'NONE', #161848 ) ;
#145118=DIRECTION ( 'NONE',  ( 0.000000000000000000, -0.4999999999999608646, 0.8660254037844612451 ) ) ;
#145132=VECTOR ( 'NONE', #4761, 1000.000000000000000 ) ;
#145161=VERTEX_POINT ( 'NONE', #149991 ) ;
#145181=CARTESIAN_POINT ( 'NONE',  ( -20.94999999999999929, 77.83534155023700407, -191.9679561919613491 ) ) ;
#145182=DIRECTION ( 'NONE',  ( 1.000000000000000000, 0.000000000000000000, 0.000000000000000000 ) ) ;
#145284=AXIS2_PLACEMENT_3D ( 'NONE', #36111, #94778, #58201 ) ;
#145299=CARTESIAN_POINT ( 'NONE',  ( 21.09551895715278391, 65.37856267284456635, -191.2859828186247171 ) ) ;
#145333=CARTESIAN_POINT ( 'NONE',  ( 20.96937028524355284, 65.37553062838595963, -196.0316813833548508 ) ) ;
#145335=DIRECTION ( 'NONE',  ( -0.000000000000000000, 6.982962677686266711E-15, -1.000000000000000000 ) ) ;
#145342=CIRCLE ( 'NONE', #3894, 0.09999999999999939493 ) ;
#145471=CARTESIAN_POINT ( 'NONE',  ( 21.14999999999999858, 75.90220970870393558, -209.7809220950004772 ) ) ;
#145551=VECTOR ( 'NONE', #213574, 1000.000000000000000 ) ;
#145569=ORIENTED_EDGE ( 'NONE', *, *, #105269, .F. ) ;
#145621=AXIS2_PLACEMENT_3D ( 'NONE', #23814, #55478, #135030 ) ;
#145632=DIRECTION ( 'NONE',  ( 0.000000000000000000, 0.000000000000000000, -1.000000000000000000 ) ) ;
#145636=EDGE_CURVE ( 'NONE', #102120, #100958, #149540, .T. ) ;
#145643=ORIENTED_EDGE ( 'NONE', *, *, #206206, .F. ) ;
#145741=ORIENTED_EDGE ( 'NONE', *, *, #210585, .F. ) ;
#145768=DIRECTION ( 'NONE',  ( -1.000000000000000000, 3.265361837132813093E-16, 2.280189983783949500E-30 ) ) ;
#145822=ORIENTED_EDGE ( 'NONE', *, *, #446, .T. ) ;
#145873=CARTESIAN_POINT ( 'NONE',  ( -18.59999999999999787, 77.63717271298298783, -191.9409541190523214 ) ) ;
#145887=DIRECTION ( 'NONE',  ( 0.000000000000000000, -6.467318590049456648E-15, 1.000000000000000000 ) ) ;
#145894=CIRCLE ( 'NONE', #179247, 0.09999999999999939493 ) ;
#145925=DIRECTION ( 'NONE',  ( 0.000000000000000000, -0.4999999999999088507, -0.8660254037844913322 ) ) ;
#145935=VERTEX_POINT ( 'NONE', #34247 ) ;
#145959=ADVANCED_FACE ( 'NONE', ( #109881 ), #172494, .T. ) ;
#145976=CARTESIAN_POINT ( 'NONE',  ( -21.05000000000000071, 74.63912941282058000, -195.4501095574334215 ) ) ;
#145998=DIRECTION ( 'NONE',  ( 1.000000000000000000, -3.265361837132813093E-16, -2.280189983783949500E-30 ) ) ;
#146021=SPHERICAL_SURFACE ( 'NONE', #81395, 0.1000000000000000056 ) ;
#146032=ORIENTED_EDGE ( 'NONE', *, *, #250051, .F. ) ;
#146063=ORIENTED_EDGE ( 'NONE', *, *, #200680, .F. ) ;
#146067=DIRECTION ( 'NONE',  ( 0.000000000000000000, -7.172728831056617961E-15, 1.000000000000000000 ) ) ;
#146072=CARTESIAN_POINT ( 'NONE',  ( 18.52165635395186172, 85.48115071129494424, -196.4982699016619563 ) ) ;
#146073=CARTESIAN_POINT ( 'NONE',  ( 20.94999999999999929, 76.00000000001244871, -170.0231074845243597 ) ) ;
#146088=CARTESIAN_POINT ( 'NONE',  ( -21.12844524849339223, 64.25000000001264766, -196.6186940136820169 ) ) ;
#146107=EDGE_CURVE ( 'NONE', #144289, #188520, #177610, .T. ) ;
#146111=CIRCLE ( 'NONE', #71116, 4.049999999999998046 ) ;
#146146=CARTESIAN_POINT ( 'NONE',  ( 18.59999999999999076, 74.16465844978819177, -191.9679561919613775 ) ) ;
#146192=EDGE_CURVE ( 'NONE', #236846, #69740, #103881, .T. ) ;
#146203=DIRECTION ( 'NONE',  ( 0.000000000000000000, 0.000000000000000000, -1.000000000000000000 ) ) ;
#146208=CARTESIAN_POINT ( 'NONE',  ( 23.14999999999999503, 64.35000000001258513, -191.3731074845244393 ) ) ;
#146211=EDGE_CURVE ( 'NONE', #44979, #147959, #141324, .T. ) ;
#146214=CARTESIAN_POINT ( 'NONE',  ( -20.94999999999999929, 70.15000000001252545, -180.1556047088023149 ) ) ;
#146219=CIRCLE ( 'NONE', #200397, 0.09999999999998898659 ) ;
#146231=CIRCLE ( 'NONE', #142147, 0.09999999999998898659 ) ;
#146260=EDGE_LOOP ( 'NONE', ( #198856, #69008, #228697, #209197 ) ) ;
#146283=EDGE_CURVE ( 'NONE', #227495, #56183, #248526, .T. ) ;
#146286=EDGE_CURVE ( 'NONE', #97198, #139578, #182702, .T. ) ;
#146304=EDGE_CURVE ( 'NONE', #223652, #163056, #95702, .T. ) ;
#146354=CARTESIAN_POINT ( 'NONE',  ( 23.14999999999999503, 64.35000000001254250, -182.1731074845244507 ) ) ;
#146412=AXIS2_PLACEMENT_3D ( 'NONE', #108351, #6662, #186611 ) ;
#146438=AXIS2_PLACEMENT_3D ( 'NONE', #70014, #107829, #149552 ) ;
#146451=AXIS2_PLACEMENT_3D ( 'NONE', #207467, #152646, #229590 ) ;
#146460=DIRECTION ( 'NONE',  ( -2.812466655313719426E-14, -0.1350103645451835865, -0.9908441862701605762 ) ) ;
#146492=CARTESIAN_POINT ( 'NONE',  ( -2.995603634470891112E-16, 87.75000000001259082, -191.2731074845242745 ) ) ;
#146512=DIRECTION ( 'NONE',  ( 0.000000000000000000, -0.9908441862701420355, -0.1350103645453197554 ) ) ;
#146520=ORIENTED_EDGE ( 'NONE', *, *, #254182, .T. ) ;
#146538=EDGE_LOOP ( 'NONE', ( #48276, #54080, #55593, #208823, #209685, #190185, #78446, #111765 ) ) ;
#146547=CYLINDRICAL_SURFACE ( 'NONE', #149020, 0.09999999999999939493 ) ;
#146562=DIRECTION ( 'NONE',  ( 1.000000000000000000, 0.000000000000000000, 0.000000000000000000 ) ) ;
#146574=CARTESIAN_POINT ( 'NONE',  ( 22.42357213249528769, 68.32706761365277259, -203.6221944485259598 ) ) ;
#146586=DIRECTION ( 'NONE',  ( 0.000000000000000000, -6.769652589177795712E-15, 1.000000000000000000 ) ) ;
#146597=EDGE_CURVE ( 'NONE', #151179, #195444, #87506, .T. ) ;
#146601=CARTESIAN_POINT ( 'NONE',  ( 20.22516295850462598, 66.10063570456237869, -195.6130417724336041 ) ) ;
#146633=CARTESIAN_POINT ( 'NONE',  ( 21.05000005001280172, 67.12872030824237868, -191.3451598962783464 ) ) ;
#146637=AXIS2_PLACEMENT_3D ( 'NONE', #181128, #102829, #182408 ) ;
#146641=DIRECTION ( 'NONE',  ( -1.000000000000000000, 0.000000000000000000, -0.000000000000000000 ) ) ;
#146652=CARTESIAN_POINT ( 'NONE',  ( 20.94999999999999574, 87.48912529308871910, -200.4231074845242802 ) ) ;
#146659=CARTESIAN_POINT ( 'NONE',  ( -22.50000000000000000, 76.00000000001267608, -203.5231074845243597 ) ) ;
#146679=EDGE_CURVE ( 'NONE', #214102, #7443, #225053, .T. ) ;
#146720=FILL_AREA_STYLE_COLOUR ( '', #62366 ) ;
#146721=CIRCLE ( 'NONE', #117534, 0.1999999999999987899 ) ;
#146729=CARTESIAN_POINT ( 'NONE',  ( 18.52326479938723480, 85.64236444492753719, -163.3083500711181273 ) ) ;
#146758=CARTESIAN_POINT ( 'NONE',  ( 18.52130828395272033, 85.48139550263843489, -196.4986007606406986 ) ) ;
#146763=CARTESIAN_POINT ( 'NONE',  ( -18.39999999999999858, 85.51932773110506503, -196.5501311079649724 ) ) ;
#146812=DIRECTION ( 'NONE',  ( 1.000000000000000000, -2.952720810173289112E-16, -2.061873921506763405E-30 ) ) ;
#146827=CIRCLE ( 'NONE', #188538, 0.09999999999998898659 ) ;
#146853=EDGE_CURVE ( 'NONE', #99703, #43253, #237562, .T. ) ;
#146880=ORIENTED_EDGE ( 'NONE', *, *, #140322, .T. ) ;
#146891=CIRCLE ( 'NONE', #5424, 0.09999999999998898659 ) ;
#146900=EDGE_LOOP ( 'NONE', ( #92504, #116775, #212512, #199952 ) ) ;
#146901=VERTEX_POINT ( 'NONE', #205340 ) ;
#146909=CARTESIAN_POINT ( 'NONE',  ( -23.15000000000000213, 76.00000000001244871, -170.0231074845243597 ) ) ;
#146920=EDGE_CURVE ( 'NONE', #165929, #239420, #200140, .T. ) ;
#146997=DIRECTION ( 'NONE',  ( -3.265361837132813093E-16, -1.000000000000000000, 7.445645354460596589E-46 ) ) ;
#147075=VECTOR ( 'NONE', #217973, 1000.000000000000000 ) ;
#147114=DIRECTION ( 'NONE',  ( 0.000000000000000000, 1.000000000000000000, 1.387778780781444413E-14 ) ) ;
#147119=DIRECTION ( 'NONE',  ( 0.000000000000000000, 6.982962677686266711E-15, -1.000000000000000000 ) ) ;
#147123=CARTESIAN_POINT ( 'NONE',  ( -18.50000000000000000, 66.75000000001260503, -191.1731074845244223 ) ) ;
#147127=EDGE_CURVE ( 'NONE', #177471, #55818, #100337, .T. ) ;
#147149=ORIENTED_EDGE ( 'NONE', *, *, #95404, .T. ) ;
#147151=CARTESIAN_POINT ( 'NONE',  ( 20.85000000000000142, 64.35000000001245724, -170.0231074845244166 ) ) ;
#147168=AXIS2_PLACEMENT_3D ( 'NONE', #123012, #463, #25204 ) ;
#147248=DIRECTION ( 'NONE',  ( -0.000000000000000000, 0.1350103645451807555, 0.9908441862701610203 ) ) ;
#147265=CIRCLE ( 'NONE', #34872, 0.4000000000000114575 ) ;
#147283=CARTESIAN_POINT ( 'NONE',  ( 20.94999999999999574, 87.41227409416235616, -200.5231074845242745 ) ) ;
#147291=CIRCLE ( 'NONE', #205717, 0.1999999999999987899 ) ;
#147296=CYLINDRICAL_SURFACE ( 'NONE', #109698, 0.09999999999999939493 ) ;
#147311=ORIENTED_EDGE ( 'NONE', *, *, #18626, .T. ) ;
#147323=EDGE_CURVE ( 'NONE', #90063, #7857, #221645, .T. ) ;
#147330=FACE_OUTER_BOUND ( 'NONE', #200935, .T. ) ;
#147339=CARTESIAN_POINT ( 'NONE',  ( 18.49999999999999289, 69.55000000001253113, -182.3731074845244109 ) ) ;
#147346=EDGE_CURVE ( 'NONE', #193318, #70041, #4488, .T. ) ;
#147356=ORIENTED_EDGE ( 'NONE', *, *, #198815, .F. ) ;
#147375=CARTESIAN_POINT ( 'NONE',  ( -18.59999999999999787, 66.75000000001253397, -182.2731074845244166 ) ) ;
#147384=CARTESIAN_POINT ( 'NONE',  ( -20.94999999999999929, 64.40000000001263913, -196.5949042542488883 ) ) ;
#147387=DIRECTION ( 'NONE',  ( 0.000000000000000000, 7.086529944415886769E-15, -1.000000000000000000 ) ) ;
#147391=CARTESIAN_POINT ( 'NONE',  ( -22.50000000000000000, 76.00000000001271871, -209.7731074845243597 ) ) ;
#147411=DIRECTION ( 'NONE',  ( 1.000000000000000000, 0.000000000000000000, 0.000000000000000000 ) ) ;
#147442=DIRECTION ( 'NONE',  ( 1.000000000000000000, 0.000000000000000000, 0.000000000000000000 ) ) ;
#147450=EDGE_CURVE ( 'NONE', #188235, #41396, #27432, .T. ) ;
#147452=CARTESIAN_POINT ( 'NONE',  ( -18.59999999999999787, 76.00000000001267608, -203.5231074845243597 ) ) ;
#147476=CARTESIAN_POINT ( 'NONE',  ( -22.16821283564876666, 68.44102665923190898, -203.5231074845243882 ) ) ;
#147543=CARTESIAN_POINT ( 'NONE',  ( -22.42253884134832020, 75.99806764887745203, -215.1727131818727798 ) ) ;
#147546=ORIENTED_EDGE ( 'NONE', *, *, #252873, .T. ) ;
#147575=FACE_OUTER_BOUND ( 'NONE', #16464, .T. ) ;
#147638=CARTESIAN_POINT ( 'NONE',  ( -23.15000000000000213, 64.25000000001247713, -173.1231074845244393 ) ) ;
#147655=CIRCLE ( 'NONE', #210030, 0.5000000000000004441 ) ;
#147687=EDGE_CURVE ( 'NONE', #51521, #197466, #81513, .T. ) ;
#147703=CIRCLE ( 'NONE', #93523, 0.09999999999999939493 ) ;
#147717=DIRECTION ( 'NONE',  ( 0.000000000000000000, -7.429790795770644761E-15, 1.000000000000000000 ) ) ;
#147721=AXIS2_PLACEMENT_3D ( 'NONE', #154009, #193092, #215210 ) ;
#147725=DIRECTION ( 'NONE',  ( 1.000000000000000000, 0.000000000000000000, 0.000000000000000000 ) ) ;
#147735=AXIS2_PLACEMENT_3D ( 'NONE', #19872, #173848, #193378 ) ;
#147751=DIRECTION ( 'NONE',  ( 0.000000000000000000, 0.000000000000000000, 1.000000000000000000 ) ) ;
#147790=FACE_OUTER_BOUND ( 'NONE', #114263, .T. ) ;
#147799=DIRECTION ( 'NONE',  ( 0.000000000000000000, 0.1455152366551700771, 0.9893560106964479628 ) ) ;
#147830=CARTESIAN_POINT ( 'NONE',  ( -18.51697539158857353, 65.68434038414410736, -164.4866880726065972 ) ) ;
#147832=DIRECTION ( 'NONE',  ( 0.000000000000000000, -6.982962677686266711E-15, 1.000000000000000000 ) ) ;
#147886=ORIENTED_EDGE ( 'NONE', *, *, #219705, .T. ) ;
#147889=CARTESIAN_POINT ( 'NONE',  ( 20.99780126800950342, 64.39461131213610656, -176.9357549128194194 ) ) ;
#147905=EDGE_LOOP ( 'NONE', ( #11848, #223194, #223731, #248671, #205877, #138608, #13444, #63330, #30821, #165502, #70957, #81585 ) ) ;
#147920=CIRCLE ( 'NONE', #22848, 0.1000000000000072220 ) ;
#147931=CARTESIAN_POINT ( 'NONE',  ( 21.05000000000000426, 76.01759718702115265, -209.9638783781857683 ) ) ;
#147949=EDGE_CURVE ( 'NONE', #235211, #119302, #23327, .T. ) ;
#147959=VERTEX_POINT ( 'NONE', #17692 ) ;
#147968=EDGE_CURVE ( 'NONE', #68342, #117271, #192499, .T. ) ;
#148004=CARTESIAN_POINT ( 'NONE',  ( -20.90851465518106167, 65.67467670974468774, -164.4531731826884879 ) ) ;
#148013=ORIENTED_EDGE ( 'NONE', *, *, #174070, .T. ) ;
#148047=CARTESIAN_POINT ( 'NONE',  ( -21.14999999999999858, 87.75000000001266187, -200.6231074845242688 ) ) ;
#148049=EDGE_CURVE ( 'NONE', #143950, #152244, #139970, .T. ) ;
#148068=CIRCLE ( 'NONE', #39940, 0.4000000000000114575 ) ;
#148071=ORIENTED_EDGE ( 'NONE', *, *, #162717, .T. ) ;
#148091=ORIENTED_EDGE ( 'NONE', *, *, #139706, .F. ) ;
#148093=AXIS2_PLACEMENT_3D ( 'NONE', #110581, #190135, #74061 ) ;
#148112=CARTESIAN_POINT ( 'NONE',  ( -23.25000000000000000, 85.68240343348880117, -163.3662641071115047 ) ) ;
#148167=CARTESIAN_POINT ( 'NONE',  ( -18.50000000000000000, 68.97833521811233481, -166.3895420826271163 ) ) ;
#148199=VERTEX_POINT ( 'NONE', #87925 ) ;
#148204=CARTESIAN_POINT ( 'NONE',  ( -18.59999999999999787, 76.00000000001244871, -170.0231074845243597 ) ) ;
#148236=DIRECTION ( 'NONE',  ( 1.000000000000000000, 0.000000000000000000, 0.000000000000000000 ) ) ;
#148254=FACE_OUTER_BOUND ( 'NONE', #25694, .T. ) ;
#148257=CIRCLE ( 'NONE', #35855, 0.2000000000000057288 ) ;
#148258=ADVANCED_FACE ( 'NONE', ( #110076 ), #187075, .T. ) ;
#148286=CARTESIAN_POINT ( 'NONE',  ( 21.07016717456945187, 69.67905916191242000, -203.5231074845244450 ) ) ;
#148303=ORIENTED_EDGE ( 'NONE', *, *, #250682, .F. ) ;
#148311=DIRECTION ( 'NONE',  ( 0.000000000000000000, -0.4999999999999608646, -0.8660254037844612451 ) ) ;
#148320=ORIENTED_EDGE ( 'NONE', *, *, #246276, .T. ) ;
#148330=ORIENTED_EDGE ( 'NONE', *, *, #247831, .T. ) ;
#148354=ADVANCED_FACE ( 'NONE', ( #236444 ), #252596, .T. ) ;
#148359=FACE_BOUND ( 'NONE', #146538, .T. ) ;
#148394=EDGE_LOOP ( 'NONE', ( #195808, #120407, #37699, #59270 ) ) ;
#148430=CYLINDRICAL_SURFACE ( 'NONE', #29443, 0.09999999999999939493 ) ;
#148457=CARTESIAN_POINT ( 'NONE',  ( 18.49999999999999289, 64.35000000001251408, -178.6731074845244507 ) ) ;
#148461=CIRCLE ( 'NONE', #106736, 0.09999999999998802902 ) ;
#148524=CARTESIAN_POINT ( 'NONE',  ( -18.52139480978221897, 85.48135884507952653, -196.4985509174051970 ) ) ;
#148527=DIRECTION ( 'NONE',  ( 1.000000000000000000, 0.000000000000000000, 0.000000000000000000 ) ) ;
#148542=EDGE_CURVE ( 'NONE', #197466, #21234, #160799, .T. ) ;
#148545=ORIENTED_EDGE ( 'NONE', *, *, #95847, .T. ) ;
#148547=CARTESIAN_POINT ( 'NONE',  ( -18.50000000000000000, 74.65925378207906249, -213.7959699899455472 ) ) ;
#148548=VECTOR ( 'NONE', #48270, 1000.000000000000000 ) ;
#148549=CIRCLE ( 'NONE', #15281, 11.75000000000001066 ) ;
#148582=AXIS2_PLACEMENT_3D ( 'NONE', #107493, #29291, #228748 ) ;
#148595=CARTESIAN_POINT ( 'NONE',  ( -2.995603634470891112E-16, 69.35000000001254250, -182.3731074845244109 ) ) ;
#148611=FACE_OUTER_BOUND ( 'NONE', #214937, .T. ) ;
#148635=DIRECTION ( 'NONE',  ( 0.000000000000000000, 0.9908441862701791170, -0.1350103645450472789 ) ) ;
#148656=ORIENTED_EDGE ( 'NONE', *, *, #68953, .F. ) ;
#148663=ORIENTED_EDGE ( 'NONE', *, *, #236295, .F. ) ;
#148708=DIRECTION ( 'NONE',  ( -1.000000000000000000, 0.000000000000000000, -0.000000000000000000 ) ) ;
#148756=ORIENTED_EDGE ( 'NONE', *, *, #17575, .F. ) ;
#148841=ORIENTED_EDGE ( 'NONE', *, *, #252339, .F. ) ;
#148849=EDGE_CURVE ( 'NONE', #10686, #226489, #161219, .T. ) ;
#148859=DIRECTION ( 'NONE',  ( -0.000000000000000000, 0.9887567792719327286, 0.1495327102803745423 ) ) ;
#148884=CARTESIAN_POINT ( 'NONE',  ( -20.64999999999999858, 76.00000000001244871, -170.0231074845243597 ) ) ;
#149020=AXIS2_PLACEMENT_3D ( 'NONE', #164861, #121888, #83975 ) ;
#149027=DIRECTION ( 'NONE',  ( 1.000000000000000000, 0.000000000000000000, 0.000000000000000000 ) ) ;
#149035=CARTESIAN_POINT ( 'NONE',  ( 23.14999999999999858, 70.10000000001251408, -180.2422072491807796 ) ) ;
#149091=CARTESIAN_POINT ( 'NONE',  ( 20.85000000000000142, 77.13501884592258762, -162.3061306010920362 ) ) ;
#149104=AXIS2_PLACEMENT_3D ( 'NONE', #52771, #209291, #187186 ) ;
#149133=AXIS2_PLACEMENT_3D ( 'NONE', #44726, #99521, #81249 ) ;
#149135=AXIS2_PLACEMENT_3D ( 'NONE', #187486, #169223, #208334 ) ;
#149166=CARTESIAN_POINT ( 'NONE',  ( 22.57320508075687115, 64.25000000001269029, -203.5231074845244166 ) ) ;
#149182=EDGE_LOOP ( 'NONE', ( #255920, #251937, #163242, #201296 ) ) ;
#149212=EDGE_CURVE ( 'NONE', #192399, #87006, #223732, .T. ) ;
#149229=CARTESIAN_POINT ( 'NONE',  ( 21.05000000000000071, 76.00000000001271871, -210.0637644362255685 ) ) ;
#149241=CARTESIAN_POINT ( 'NONE',  ( 19.97071067811864609, 64.27928932189387012, -182.1731074845244507 ) ) ;
#149266=CARTESIAN_POINT ( 'NONE',  ( -18.50000000000000000, 70.05000000001267324, -193.2174051794895320 ) ) ;
#149281=EDGE_LOOP ( 'NONE', ( #222430, #56638, #227334, #210899, #155673, #154773, #249158, #246723 ) ) ;
#149314=VECTOR ( 'NONE', #182023, 1000.000000000000000 ) ;
#149339=FACE_OUTER_BOUND ( 'NONE', #204041, .T. ) ;
#149360=DIRECTION ( 'NONE',  ( 0.000000000000000000, 6.982962677686266711E-15, -1.000000000000000000 ) ) ;
#149363=ORIENTED_EDGE ( 'NONE', *, *, #248684, .F. ) ;
#149411=CARTESIAN_POINT ( 'NONE',  ( 18.59999999999999787, 77.83534155023700407, -191.9679561919613491 ) ) ;
#149419=ORIENTED_EDGE ( 'NONE', *, *, #139381, .T. ) ;
#149421=CARTESIAN_POINT ( 'NONE',  ( -23.25000000000000000, 64.25000000001260503, -191.3731074845244393 ) ) ;
#149429=CARTESIAN_POINT ( 'NONE',  ( 23.24999999999999289, 64.35000000001254250, -182.1731074845244507 ) ) ;
#149445=CARTESIAN_POINT ( 'NONE',  ( -18.59999999999999787, 68.92903212821357783, -166.2765432626560766 ) ) ;
#149480=EDGE_LOOP ( 'NONE', ( #37265, #202495, #61752, #40543 ) ) ;
#149509=DIRECTION ( 'NONE',  ( 0.000000000000000000, 0.000000000000000000, 1.000000000000000000 ) ) ;
#149511=CARTESIAN_POINT ( 'NONE',  ( -18.39999999999999858, 85.60000000001240039, -163.3229180933022633 ) ) ;
#149512=ORIENTED_EDGE ( 'NONE', *, *, #50415, .T. ) ;
#149533=ADVANCED_FACE ( 'NONE', ( #218191 ), #201215, .T. ) ;
#149539=CYLINDRICAL_SURFACE ( 'NONE', #39340, 0.1000000000000118433 ) ;
#149540=CIRCLE ( 'NONE', #37113, 0.09999999999999939493 ) ;
#149541=ADVANCED_FACE ( 'NONE', ( #60415 ), #242908, .T. ) ;
#149542=EDGE_CURVE ( 'NONE', #184002, #32289, #160836, .T. ) ;
#149552=DIRECTION ( 'NONE',  ( 0.000000000000000000, -0.1575844902526687130, -0.9875055080513762684 ) ) ;
#149600=EDGE_LOOP ( 'NONE', ( #58311, #179775, #204727, #11680 ) ) ;
#149635=EDGE_LOOP ( 'NONE', ( #220785, #27774, #117483, #53577 ) ) ;
#149672=ADVANCED_FACE ( 'NONE', ( #70726 ), #30302, .T. ) ;
#149701=EDGE_CURVE ( 'NONE', #104276, #152549, #124181, .T. ) ;
#149702=CARTESIAN_POINT ( 'NONE',  ( -21.14999999999999858, 76.00000000001271871, -210.0637644362255969 ) ) ;
#149709=EDGE_CURVE ( 'NONE', #188810, #120125, #11574, .T. ) ;
#149726=FACE_OUTER_BOUND ( 'NONE', #241598, .T. ) ;
#149765=EDGE_CURVE ( 'NONE', #203961, #236269, #199175, .T. ) ;
#149770=ORIENTED_EDGE ( 'NONE', *, *, #147949, .F. ) ;
#149780=DIRECTION ( 'NONE',  ( 0.000000000000000000, -0.8660254037844445918, -0.4999999999999897304 ) ) ;
#149805=ORIENTED_EDGE ( 'NONE', *, *, #111931, .F. ) ;
#149866=EDGE_LOOP ( 'NONE', ( #225408, #241470, #51522, #55739 ) ) ;
#149871=EDGE_CURVE ( 'NONE', #234461, #144289, #178821, .T. ) ;
#149873=( GEOMETRIC_REPRESENTATION_CONTEXT ( 3 ) GLOBAL_UNCERTAINTY_ASSIGNED_CONTEXT ( ( #131189 ) ) GLOBAL_UNIT_ASSIGNED_CONTEXT ( ( #9804, #188438, #150611 ) ) REPRESENTATION_CONTEXT ( 'NONE', 'WORKASPACE' ) );
#149906=ORIENTED_EDGE ( 'NONE', *, *, #157953, .F. ) ;
#149909=DIRECTION ( 'NONE',  ( 0.000000000000000000, 0.9908441862701791170, -0.1350103645450472789 ) ) ;
#149917=EDGE_CURVE ( 'NONE', #233060, #223851, #232530, .T. ) ;
#149960=EDGE_LOOP ( 'NONE', ( #87133, #115065, #127406, #66441 ) ) ;
#149978=CARTESIAN_POINT ( 'NONE',  ( -21.00250684356849362, 64.25000000001264766, -196.5083017157664358 ) ) ;
#149991=CARTESIAN_POINT ( 'NONE',  ( 21.05000000000000071, 87.65000000001266756, -200.6231074845242688 ) ) ;
#150002=CARTESIAN_POINT ( 'NONE',  ( 20.85000000000000142, 76.32388570108278714, -170.0655178952103768 ) ) ;
#150059=ORIENTED_EDGE ( 'NONE', *, *, #148542, .T. ) ;
#150072=DIRECTION ( 'NONE',  ( 0.000000000000000000, -1.000000000000000000, -6.982962677686266711E-15 ) ) ;
#150135=ORIENTED_EDGE ( 'NONE', *, *, #141443, .T. ) ;
#150179=ORIENTED_EDGE ( 'NONE', *, *, #45193, .T. ) ;
#150184=CIRCLE ( 'NONE', #37765, 0.5999999999999894307 ) ;
#150211=EDGE_LOOP ( 'NONE', ( #209265, #32573, #137938, #116830 ) ) ;
#150265=AXIS2_PLACEMENT_3D ( 'NONE', #23505, #83405, #225488 ) ;
#150272=ORIENTED_EDGE ( 'NONE', *, *, #222541, .F. ) ;
#150314=CARTESIAN_POINT ( 'NONE',  ( -22.50000000000000000, 75.90000000001273861, -211.3138870828977645 ) ) ;
#150341=ORIENTED_EDGE ( 'NONE', *, *, #112888, .T. ) ;
#150342=CARTESIAN_POINT ( 'NONE',  ( 23.14999999999999503, 64.35000000001258513, -191.2731074845244450 ) ) ;
#150356=ORIENTED_EDGE ( 'NONE', *, *, #110454, .T. ) ;
#150360=EDGE_CURVE ( 'NONE', #136156, #18425, #198026, .T. ) ;
#150377=CARTESIAN_POINT ( 'NONE',  ( -20.64999999999999858, 68.75000000001260503, -191.1731074845243938 ) ) ;
#150380=CARTESIAN_POINT ( 'NONE',  ( 20.90851465518106167, 65.67467670974468774, -164.4531731826884879 ) ) ;
#150403=ORIENTED_EDGE ( 'NONE', *, *, #240596, .F. ) ;
#150420=CIRCLE ( 'NONE', #208681, 0.5000000000000004441 ) ;
#150485=B_SPLINE_CURVE_WITH_KNOTS ( 'NONE', 3,
 ( #128337, #146574, #170069, #246977, #29272, #185734, #52628, #69651, #108758, #188287 ),
 .UNSPECIFIED., .F., .F.,
 ( 4, 3, 3, 4 ),
 ( 0.000000000000000000, 0.0002000000000002908468, 0.001000000000045115191, 0.001967863649472108723 ),
 .UNSPECIFIED. ) ;
#150509=ORIENTED_EDGE ( 'NONE', *, *, #69696, .F. ) ;
#150531=CARTESIAN_POINT ( 'NONE',  ( -23.25000000000000000, 76.00000000001239187, -162.1231074845243825 ) ) ;
#150550=DIRECTION ( 'NONE',  ( 0.000000000000000000, -7.124650136758292359E-15, 1.000000000000000000 ) ) ;
#150565=EDGE_CURVE ( 'NONE', #183861, #115598, #153186, .T. ) ;
#150583=ORIENTED_EDGE ( 'NONE', *, *, #116428, .T. ) ;
#150611=( NAMED_UNIT ( * ) SI_UNIT ( $, .STERADIAN. ) SOLID_ANGLE_UNIT ( ) );
#150622=VECTOR ( 'NONE', #77484, 1000.000000000000000 ) ;
#150623=ORIENTED_EDGE ( 'NONE', *, *, #151462, .F. ) ;
#150655=CARTESIAN_POINT ( 'NONE',  ( 23.24999999999999645, 76.00000000001267608, -203.5231074845243597 ) ) ;
#150656=ADVANCED_FACE ( 'NONE', ( #25211 ), #102123, .F. ) ;
#150678=CARTESIAN_POINT ( 'NONE',  ( -23.25000000000000000, 77.73670573947995877, -158.5056848969006182 ) ) ;
#150723=VECTOR ( 'NONE', #85542, 1000.000000000000000 ) ;
#150731=ORIENTED_EDGE ( 'NONE', *, *, #10635, .F. ) ;
#150773=ORIENTED_EDGE ( 'NONE', *, *, #126837, .F. ) ;
#150774=CARTESIAN_POINT ( 'NONE',  ( -23.24999999999999645, 85.60000000001240039, -163.4229180933022576 ) ) ;
#150780=VECTOR ( 'NONE', #144829, 1000.000000000000000 ) ;
#150814=VERTEX_POINT ( 'NONE', #225920 ) ;
#150819=ORIENTED_EDGE ( 'NONE', *, *, #24095, .F. ) ;
#150830=DIRECTION ( 'NONE',  ( 1.000000000000000000, 0.000000000000000000, 0.000000000000000000 ) ) ;
#150869=DIRECTION ( 'NONE',  ( -2.827886303505249259E-16, -0.8660254037844378194, -0.5000000000000016653 ) ) ;
#150879=ORIENTED_EDGE ( 'NONE', *, *, #74636, .T. ) ;
#150890=CARTESIAN_POINT ( 'NONE',  ( -20.85000000000000142, 68.97833521811233481, -166.1895420826271277 ) ) ;
#150896=ORIENTED_EDGE ( 'NONE', *, *, #6118, .T. ) ;
#150903=FACE_OUTER_BOUND ( 'NONE', #143542, .T. ) ;
#150912=EDGE_CURVE ( 'NONE', #252194, #68808, #253320, .T. ) ;
#150915=ORIENTED_EDGE ( 'NONE', *, *, #15424, .T. ) ;
#150916=AXIS2_PLACEMENT_3D ( 'NONE', #91650, #231185, #92917 ) ;
#150921=FACE_OUTER_BOUND ( 'NONE', #30055, .T. ) ;
#150941=DIRECTION ( 'NONE',  ( 0.000000000000000000, -0.8660254037844420383, 0.4999999999999942824 ) ) ;
#150948=AXIS2_PLACEMENT_3D ( 'NONE', #163815, #243330, #5996 ) ;
#150964=VERTEX_POINT ( 'NONE', #175118 ) ;
#150995=EDGE_CURVE ( 'NONE', #222338, #34777, #22436, .T. ) ;
#151015=EDGE_CURVE ( 'NONE', #251509, #185777, #2827, .T. ) ;
#151023=DIRECTION ( 'NONE',  ( 0.000000000000000000, 0.9915357197604862671, -0.1298341882519953583 ) ) ;
#151037=VECTOR ( 'NONE', #73201, 1000.000000000000000 ) ;
#151066=ORIENTED_EDGE ( 'NONE', *, *, #84902, .T. ) ;
#151082=CYLINDRICAL_SURFACE ( 'NONE', #158, 0.09999999999999939493 ) ;
#151094=EDGE_LOOP ( 'NONE', ( #162512, #69546, #201966, #73389 ) ) ;
#151140=AXIS2_PLACEMENT_3D ( 'NONE', #91477, #54894, #35391 ) ;
#151169=EDGE_CURVE ( 'NONE', #65963, #20109, #32611, .T. ) ;
#151179=VERTEX_POINT ( 'NONE', #250439 ) ;
#151231=CARTESIAN_POINT ( 'NONE',  ( -23.25000000000000000, 77.85161776048127535, -158.4199177649206831 ) ) ;
#151279=DIRECTION ( 'NONE',  ( 0.000000000000000000, -6.853228547068871147E-15, 1.000000000000000000 ) ) ;
#151295=AXIS2_PLACEMENT_3D ( 'NONE', #257241, #233880, #158235 ) ;
#151317=DIRECTION ( 'NONE',  ( -6.938893903907222067E-15, -1.000000000000000000, -6.982962677686266711E-15 ) ) ;
#151434=ORIENTED_EDGE ( 'NONE', *, *, #123567, .T. ) ;
#151455=CYLINDRICAL_SURFACE ( 'NONE', #250171, 0.1000000000000070832 ) ;
#151459=DIRECTION ( 'NONE',  ( 0.000000000000000000, -1.616829647512364004E-14, 1.000000000000000000 ) ) ;
#151462=EDGE_CURVE ( 'NONE', #117271, #7443, #24395, .T. ) ;
#151472=DIRECTION ( 'NONE',  ( 0.000000000000000000, 0.000000000000000000, 1.000000000000000000 ) ) ;
#151491=ORIENTED_EDGE ( 'NONE', *, *, #98256, .T. ) ;
#151512=ORIENTED_EDGE ( 'NONE', *, *, #101970, .F. ) ;
#151517=AXIS2_PLACEMENT_3D ( 'NONE', #206324, #167225, #48522 ) ;
#151548=CIRCLE ( 'NONE', #218129, 0.09999999999998898659 ) ;
#151557=ORIENTED_EDGE ( 'NONE', *, *, #204842, .F. ) ;
#151558=EDGE_CURVE ( 'NONE', #85698, #115079, #95293, .T. ) ;
#151569=VERTEX_POINT ( 'NONE', #114477 ) ;
#151574=DIRECTION ( 'NONE',  ( 0.000000000000000000, -0.9654727137038715545, 0.2605042016806676242 ) ) ;
#151586=ORIENTED_EDGE ( 'NONE', *, *, #99036, .F. ) ;
#151606=DIRECTION ( 'NONE',  ( 0.000000000000000000, -1.000000000000000000, -6.982962677686265922E-15 ) ) ;
#151618=FACE_OUTER_BOUND ( 'NONE', #238723, .T. ) ;
#151623=LINE ( 'NONE', #48627, #103833 ) ;
#151626=DIRECTION ( 'NONE',  ( 0.000000000000000000, 0.000000000000000000, -1.000000000000000000 ) ) ;
#151658=CARTESIAN_POINT ( 'NONE',  ( -20.94999999999999929, 87.29603075034795268, -200.4752083248604038 ) ) ;
#151704=EDGE_LOOP ( 'NONE', ( #250983, #236153, #15186, #123129 ) ) ;
#151714=CARTESIAN_POINT ( 'NONE',  ( 22.59999999999999432, 75.89914163091404475, -215.2726746080137445 ) ) ;
#151722=CYLINDRICAL_SURFACE ( 'NONE', #129242, 0.5000000000000004441 ) ;
#151733=DIRECTION ( 'NONE',  ( -0.7071067811865214825, -0.7071067811865735520, 0.000000000000000000 ) ) ;
#151747=DIRECTION ( 'NONE',  ( -1.000000000000000000, 0.000000000000000000, -0.000000000000000000 ) ) ;
#151759=CARTESIAN_POINT ( 'NONE',  ( 21.05000000000000071, 64.25000000001249134, -177.0379132551784096 ) ) ;
#151779=CIRCLE ( 'NONE', #247607, 0.09999999999999939493 ) ;
#151787=AXIS2_PLACEMENT_3D ( 'NONE', #114264, #116832, #257887 ) ;
#151820=TOROIDAL_SURFACE ( 'NONE', #52003, 0.2000000000000000111, 0.1000000000000000056 ) ;
#151837=ORIENTED_EDGE ( 'NONE', *, *, #68076, .F. ) ;
#151840=DIRECTION ( 'NONE',  ( -0.000000000000000000, 6.982962677686266711E-15, -1.000000000000000000 ) ) ;
#151854=DIRECTION ( 'NONE',  ( 0.000000000000000000, -6.982962677686266711E-15, 1.000000000000000000 ) ) ;
#151869=DIRECTION ( 'NONE',  ( -2.252264143451594314E-15, 0.1298341882520054891, 0.9915357197604850459 ) ) ;
#151879=EDGE_CURVE ( 'NONE', #166875, #9660, #157887, .T. ) ;
#151897=DIRECTION ( 'NONE',  ( 1.000000000000000000, 0.000000000000000000, 0.000000000000000000 ) ) ;
#151898=DIRECTION ( 'NONE',  ( 0.000000000000000000, -6.982962677686266711E-15, 1.000000000000000000 ) ) ;
#151912=SURFACE_STYLE_USAGE ( .BOTH. , #248421 ) ;
#151929=CIRCLE ( 'NONE', #2036, 0.09999999999998898659 ) ;
#151955=VERTEX_POINT ( 'NONE', #138520 ) ;
#151972=ORIENTED_EDGE ( 'NONE', *, *, #111141, .F. ) ;
#151982=AXIS2_PLACEMENT_3D ( 'NONE', #182221, #42701, #122246 ) ;
#152005=ORIENTED_EDGE ( 'NONE', *, *, #85585, .T. ) ;
#152022=CARTESIAN_POINT ( 'NONE',  ( -20.94999999999999929, 87.75000000001266187, -200.6231074845242688 ) ) ;
#152023=CIRCLE ( 'NONE', #164480, 0.1000000000000118433 ) ;
#152030=DIRECTION ( 'NONE',  ( 1.000000000000000000, 0.000000000000000000, 0.000000000000000000 ) ) ;
#152063=ORIENTED_EDGE ( 'NONE', *, *, #79553, .T. ) ;
#152106=EDGE_LOOP ( 'NONE', ( #221659, #55500, #1611, #255066 ) ) ;
#152115=ORIENTED_EDGE ( 'NONE', *, *, #232126, .T. ) ;
#152155=CARTESIAN_POINT ( 'NONE',  ( 20.94999999999999929, 70.50000000001253397, -182.4283735034374843 ) ) ;
#152174=CARTESIAN_POINT ( 'NONE',  ( 23.14999999999999858, 76.00000000001243450, -168.0231074845243597 ) ) ;
#152233=CARTESIAN_POINT ( 'NONE',  ( 20.85000000000000142, 77.73670573947995877, -158.5056848969006182 ) ) ;
#152240=VERTEX_POINT ( 'NONE', #250477 ) ;
#152241=ORIENTED_EDGE ( 'NONE', *, *, #166583, .T. ) ;
#152244=VERTEX_POINT ( 'NONE', #11902 ) ;
#152329=CIRCLE ( 'NONE', #235480, 0.09999999999998898659 ) ;
#152344=ORIENTED_EDGE ( 'NONE', *, *, #80419, .T. ) ;
#152357=DIRECTION ( 'NONE',  ( -4.408576920032447972E-17, -0.1350103645451946055, 0.9908441862701591329 ) ) ;
#152359=CARTESIAN_POINT ( 'NONE',  ( -21.14999999999999858, 64.35000000001268461, -203.4231074845244507 ) ) ;
#152414=DIRECTION ( 'NONE',  ( 1.441126678808781001E-14, -0.9876197685951241256, -0.1568667991644932258 ) ) ;
#152426=ADVANCED_FACE ( 'NONE', ( #95262 ), #119996, .T. ) ;
#152486=DIRECTION ( 'NONE',  ( 0.000000000000000000, -6.467318590049456648E-15, 1.000000000000000000 ) ) ;
#152505=ORIENTED_EDGE ( 'NONE', *, *, #182181, .T. ) ;
#152534=VERTEX_POINT ( 'NONE', #243760 ) ;
#152549=VERTEX_POINT ( 'NONE', #46820 ) ;
#152628=EDGE_CURVE ( 'NONE', #155749, #249694, #165522, .T. ) ;
#152646=DIRECTION ( 'NONE',  ( 1.000000000000000000, -0.000000000000000000, 0.000000000000000000 ) ) ;
#152700=DIRECTION ( 'NONE',  ( 1.000000000000000000, 0.000000000000000000, 0.000000000000000000 ) ) ;
#152739=DIRECTION ( 'NONE',  ( 0.000000000000000000, 1.000000000000000000, 6.982962677686266711E-15 ) ) ;
#152819=DIRECTION ( 'NONE',  ( 1.000000000000000000, 0.000000000000000000, 0.000000000000000000 ) ) ;
#152824=VERTEX_POINT ( 'NONE', #40147 ) ;
#152832=VERTEX_POINT ( 'NONE', #239607 ) ;
#152847=ORIENTED_EDGE ( 'NONE', *, *, #180995, .T. ) ;
#152865=FACE_OUTER_BOUND ( 'NONE', #127163, .T. ) ;
#152880=ORIENTED_EDGE ( 'NONE', *, *, #112158, .T. ) ;
#152914=CARTESIAN_POINT ( 'NONE',  ( -20.94999999999999929, 77.16270174995064224, -195.6231074845243540 ) ) ;
#152979=CIRCLE ( 'NONE', #232073, 0.09999999999998898659 ) ;
#152986=FACE_OUTER_BOUND ( 'NONE', #11571, .T. ) ;
#153015=EDGE_CURVE ( 'NONE', #125024, #139303, #183506, .T. ) ;
#153020=DIRECTION ( 'NONE',  ( 1.000000000000000000, 0.000000000000000000, 0.000000000000000000 ) ) ;
#153031=CARTESIAN_POINT ( 'NONE',  ( 18.42555734704285086, 85.49715836194937424, -196.4832769867893205 ) ) ;
#153052=ORIENTED_EDGE ( 'NONE', *, *, #114664, .F. ) ;
#153088=AXIS2_PLACEMENT_3D ( 'NONE', #197197, #235058, #176382 ) ;
#153095=AXIS2_PLACEMENT_3D ( 'NONE', #183667, #205779, #226615 ) ;
#153104=AXIS2_PLACEMENT_3D ( 'NONE', #142544, #3028, #203812 ) ;
#153144=ADVANCED_FACE ( 'NONE', ( #234144 ), #229314, .T. ) ;
#153177=CARTESIAN_POINT ( 'NONE',  ( -22.59999999999999787, 76.00000000001267608, -203.5231074845243597 ) ) ;
#153186=LINE ( 'NONE', #237817, #111494 ) ;
#153233=AXIS2_PLACEMENT_3D ( 'NONE', #74766, #39486, #17330 ) ;
#153252=CARTESIAN_POINT ( 'NONE',  ( -20.94999999999999929, 65.70729864261056719, -164.5657455973725121 ) ) ;
#153278=EDGE_CURVE ( 'NONE', #231047, #202321, #249686, .T. ) ;
#153283=CIRCLE ( 'NONE', #61661, 0.1000000000000033223 ) ;
#153302=CIRCLE ( 'NONE', #74190, 0.1000000000000033362 ) ;
#153311=DIRECTION ( 'NONE',  ( 0.000000000000000000, 0.000000000000000000, 1.000000000000000000 ) ) ;
#153323=CARTESIAN_POINT ( 'NONE',  ( -23.25000000000000000, 77.16412189325360771, -162.1082593989527254 ) ) ;
#153359=ORIENTED_EDGE ( 'NONE', *, *, #154187, .T. ) ;
#153398=CARTESIAN_POINT ( 'NONE',  ( -21.05000000000000071, 76.10000000001272724, -210.0637644362255969 ) ) ;
#153407=EDGE_CURVE ( 'NONE', #72763, #93820, #25482, .T. ) ;
#153426=CIRCLE ( 'NONE', #40980, 0.09999999999999939493 ) ;
#153430=VERTEX_POINT ( 'NONE', #193133 ) ;
#153435=AXIS2_PLACEMENT_3D ( 'NONE', #69480, #49889, #89003 ) ;
#153460=FACE_OUTER_BOUND ( 'NONE', #87411, .T. ) ;
#153485=CARTESIAN_POINT ( 'NONE',  ( -20.94999999999999929, 76.00000000001244871, -170.0231074845243597 ) ) ;
#153489=DIRECTION ( 'NONE',  ( 0.000000000000000000, 0.000000000000000000, -1.000000000000000000 ) ) ;
#153504=DIRECTION ( 'NONE',  ( 1.000000000000000000, 0.000000000000000000, 0.000000000000000000 ) ) ;
#153513=CARTESIAN_POINT ( 'NONE',  ( 0.000000000000000000, 0.000000000000000000, 0.000000000000000000 ) ) ;
#153519=EDGE_LOOP ( 'NONE', ( #254443, #119610, #234457, #144765 ) ) ;
#153579=ORIENTED_EDGE ( 'NONE', *, *, #27146, .T. ) ;
#153595=ADVANCED_FACE ( 'NONE', ( #216530 ), #36649, .T. ) ;
#153621=EDGE_CURVE ( 'NONE', #111659, #182617, #175342, .T. ) ;
#153647=DIRECTION ( 'NONE',  ( 0.000000000000000000, 0.000000000000000000, 1.000000000000000000 ) ) ;
#153667=AXIS2_PLACEMENT_3D ( 'NONE', #193131, #71903, #212693 ) ;
#153674=DIRECTION ( 'NONE',  ( 1.000000000000000000, 0.000000000000000000, 0.000000000000000000 ) ) ;
#153677=EDGE_CURVE ( 'NONE', #116470, #97927, #5157, .T. ) ;
#153680=VERTEX_POINT ( 'NONE', #243800 ) ;
#153687=AXIS2_PLACEMENT_3D ( 'NONE', #149091, #66963, #147799 ) ;
#153701=DIRECTION ( 'NONE',  ( 1.000000000000000000, -2.952720810173289112E-16, -2.061873921506763405E-30 ) ) ;
#153705=FACE_OUTER_BOUND ( 'NONE', #176436, .T. ) ;
#153730=AXIS2_PLACEMENT_3D ( 'NONE', #206719, #230132, #47621 ) ;
#153740=CARTESIAN_POINT ( 'NONE',  ( 21.59780538579341780, 75.90102133041474985, -210.3701980144676043 ) ) ;
#153758=CIRCLE ( 'NONE', #41295, 0.09999999999999080458 ) ;
#153796=ORIENTED_EDGE ( 'NONE', *, *, #179175, .F. ) ;
#153812=CIRCLE ( 'NONE', #41357, 0.09999999999998898659 ) ;
#153817=ORIENTED_EDGE ( 'NONE', *, *, #14613, .F. ) ;
#153846=DIRECTION ( 'NONE',  ( -1.000000000000000000, 0.000000000000000000, -0.000000000000000000 ) ) ;
#153863=ORIENTED_EDGE ( 'NONE', *, *, #134117, .F. ) ;
#153870=CARTESIAN_POINT ( 'NONE',  ( 18.50211644919735221, 65.69792220476372790, -164.5335554128461979 ) ) ;
#153887=DIRECTION ( 'NONE',  ( -3.469446951953515108E-14, -1.000000000000000000, 0.000000000000000000 ) ) ;
#153896=VECTOR ( 'NONE', #187664, 1000.000000000000000 ) ;
#153912=DIRECTION ( 'NONE',  ( 0.000000000000000000, -7.056502275159890832E-15, 1.000000000000000000 ) ) ;
#153916=CIRCLE ( 'NONE', #137279, 0.09999999999998898659 ) ;
#153934=DIRECTION ( 'NONE',  ( 0.000000000000000000, -1.000000000000000000, 0.000000000000000000 ) ) ;
#153951=EDGE_CURVE ( 'NONE', #151179, #10849, #168290, .T. ) ;
#153968=FACE_OUTER_BOUND ( 'NONE', #12471, .T. ) ;
#153978=DIRECTION ( 'NONE',  ( -2.952720810173289112E-16, -1.000000000000000000, -6.982962677686266711E-15 ) ) ;
#153990=DIRECTION ( 'NONE',  ( 0.000000000000000000, 6.982962677686266711E-15, -1.000000000000000000 ) ) ;
#153992=AXIS2_PLACEMENT_3D ( 'NONE', #97037, #193623, #176644 ) ;
#154003=CIRCLE ( 'NONE', #204004, 0.09999999999998898659 ) ;
#154006=ADVANCED_FACE ( 'NONE', ( #136676 ), #37611, .T. ) ;
#154009=CARTESIAN_POINT ( 'NONE',  ( -23.25000000000000000, 77.16412189325360771, -162.1082593989527254 ) ) ;
#154016=VERTEX_POINT ( 'NONE', #18021 ) ;
#154060=CARTESIAN_POINT ( 'NONE',  ( 23.14999999999999503, 64.35000000001254250, -182.1731074845244507 ) ) ;
#154065=DIRECTION ( 'NONE',  ( 0.000000000000000000, 0.000000000000000000, 1.000000000000000000 ) ) ;
#154067=CARTESIAN_POINT ( 'NONE',  ( 18.39999999999999858, 85.60000000001240039, -163.4229180933022576 ) ) ;
#154068=PLANE ( 'NONE',  #188309 ) ;
#154084=AXIS2_PLACEMENT_3D ( 'NONE', #39503, #60298, #135976 ) ;
#154090=AXIS2_PLACEMENT_3D ( 'NONE', #55714, #114452, #15371 ) ;
#154096=DIRECTION ( 'NONE',  ( -1.000000000000000000, 2.952720810173289112E-16, 2.061873921506763405E-30 ) ) ;
#154115=CARTESIAN_POINT ( 'NONE',  ( 21.05000000000000071, 76.00000000001267608, -203.5231074845243597 ) ) ;
#154119=ORIENTED_EDGE ( 'NONE', *, *, #50288, .F. ) ;
#154124=ADVANCED_FACE ( 'NONE', ( #203073 ), #142353, .F. ) ;
#154149=ORIENTED_EDGE ( 'NONE', *, *, #214054, .T. ) ;
#154187=EDGE_CURVE ( 'NONE', #72316, #28626, #158962, .T. ) ;
#154204=LINE ( 'NONE', #35529, #29362 ) ;
#154228=EDGE_CURVE ( 'NONE', #179110, #185777, #184051, .T. ) ;
#154229=ORIENTED_EDGE ( 'NONE', *, *, #67990, .F. ) ;
#154234=CARTESIAN_POINT ( 'NONE',  ( 20.12500000000000355, 66.74195072709531473, -195.1597686473820090 ) ) ;
#154239=DIRECTION ( 'NONE',  ( 1.000000000000000000, 0.000000000000000000, 0.000000000000000000 ) ) ;
#154279=VERTEX_POINT ( 'NONE', #118098 ) ;
#154326=DIRECTION ( 'NONE',  ( -1.000000000000000000, 0.000000000000000000, 0.000000000000000000 ) ) ;
#154345=ORIENTED_EDGE ( 'NONE', *, *, #121745, .F. ) ;
#154357=DIRECTION ( 'NONE',  ( 1.000000000000000000, 0.000000000000000000, 0.000000000000000000 ) ) ;
#154358=AXIS2_PLACEMENT_3D ( 'NONE', #72764, #92280, #91003 ) ;
#154365=DIRECTION ( 'NONE',  ( -1.000000000000000000, 0.000000000000000000, -0.000000000000000000 ) ) ;
#154399=ORIENTED_EDGE ( 'NONE', *, *, #124785, .T. ) ;
#154421=DIRECTION ( 'NONE',  ( 0.000000000000000000, 1.000000000000000000, 1.321694076934707365E-14 ) ) ;
#154437=ORIENTED_EDGE ( 'NONE', *, *, #146211, .F. ) ;
#154455=CARTESIAN_POINT ( 'NONE',  ( -20.54999999999999716, 85.00000000001261924, -193.6291383618718385 ) ) ;
#154524=AXIS2_PLACEMENT_3D ( 'NONE', #109326, #152357, #91068 ) ;
#154576=VERTEX_POINT ( 'NONE', #144206 ) ;
#154617=AXIS2_PLACEMENT_3D ( 'NONE', #85369, #68421, #187103 ) ;
#154621=CIRCLE ( 'NONE', #242062, 0.1000000000000070832 ) ;
#154669=AXIS2_PLACEMENT_3D ( 'NONE', #172771, #78737, #14949 ) ;
#154752=DIRECTION ( 'NONE',  ( -7.304098846218134667E-16, 1.000000000000000000, 6.982962677686266711E-15 ) ) ;
#154773=ORIENTED_EDGE ( 'NONE', *, *, #195603, .T. ) ;
#154782=ORIENTED_EDGE ( 'NONE', *, *, #239702, .F. ) ;
#154787=LINE ( 'NONE', #118200, #87580 ) ;
#154812=DIRECTION ( 'NONE',  ( 0.000000000000000000, -6.547589603894034005E-15, 1.000000000000000000 ) ) ;
#154837=ORIENTED_EDGE ( 'NONE', *, *, #238410, .F. ) ;
#154851=DIRECTION ( 'NONE',  ( 0.000000000000000000, 1.000000000000000000, 6.982962677686266711E-15 ) ) ;
#154888=DIRECTION ( 'NONE',  ( 0.000000000000000000, 6.982962677686266711E-15, -1.000000000000000000 ) ) ;
#154917=DIRECTION ( 'NONE',  ( 1.000000000000000000, -0.000000000000000000, 0.000000000000000000 ) ) ;
#154919=DIRECTION ( 'NONE',  ( 0.000000000000000000, -1.000000000000000000, 0.000000000000000000 ) ) ;
#154923=DIRECTION ( 'NONE',  ( -0.000000000000000000, 1.000000000000000000, 6.352154140967427193E-15 ) ) ;
#154947=CARTESIAN_POINT ( 'NONE',  ( 21.05000000000000071, 67.22371710472020823, -203.5231074845244166 ) ) ;
#155058=ORIENTED_EDGE ( 'NONE', *, *, #255004, .T. ) ;
#155068=CARTESIAN_POINT ( 'NONE',  ( 20.95429693346638800, 65.45669512011706104, -195.9622249462115064 ) ) ;
#155095=EDGE_CURVE ( 'NONE', #51335, #235216, #8892, .T. ) ;
#155112=CARTESIAN_POINT ( 'NONE',  ( 18.59999999999999787, 77.36242903720570041, -162.1342262366031548 ) ) ;
#155130=DIRECTION ( 'NONE',  ( 0.000000000000000000, -7.487053152578134969E-15, 1.000000000000000000 ) ) ;
#155135=CARTESIAN_POINT ( 'NONE',  ( -23.15000000000000213, 76.00000000001270450, -207.6731074845243370 ) ) ;
#155140=LINE ( 'NONE', #54713, #135803 ) ;
#155151=DIRECTION ( 'NONE',  ( 0.000000000000000000, -1.000000000000000000, -6.982962677686266711E-15 ) ) ;
#155162=CARTESIAN_POINT ( 'NONE',  ( 21.07016717457012689, 76.00000000001273293, -209.8440483226252979 ) ) ;
#155174=DIRECTION ( 'NONE',  ( 1.000000000000000000, -0.000000000000000000, 0.000000000000000000 ) ) ;
#155177=AXIS2_PLACEMENT_3D ( 'NONE', #23172, #42708, #243470 ) ;
#155179=CIRCLE ( 'NONE', #200925, 0.09999999999998898659 ) ;
#155181=CIRCLE ( 'NONE', #42702, 12.77500000000000924 ) ;
#155185=CARTESIAN_POINT ( 'NONE',  ( 21.12757541349815682, 69.52661942876123646, -203.5282687003341380 ) ) ;
#155239=DIRECTION ( 'NONE',  ( 4.408576920032447355E-17, 0.1350103645451807555, 0.9908441862701610203 ) ) ;
#155267=( BOUNDED_SURFACE ( )  B_SPLINE_SURFACE ( 3, 2, ( 
 ( #39633, #239087, #450 ),
 ( #119142, #122999, #182974 ),
 ( #142532, #21345, #78699 ),
 ( #1735, #158299, #220798 ),
 ( #60428, #160848, #121722 ),
 ( #180399, #257301, #218204 ) ),
 .UNSPECIFIED., .F., .F., .F. ) 
 B_SPLINE_SURFACE_WITH_KNOTS ( ( 4, 2, 4 ),
 ( 3, 3 ),
 ( 0.0001792624049599534481, 0.0003686986002124527503, 0.0005581347954649519983 ),
 ( 0.000000000000000000, 1.000000000000000000 ),
 .UNSPECIFIED. ) 
 GEOMETRIC_REPRESENTATION_ITEM ( )  RATIONAL_B_SPLINE_SURFACE ( (
 ( 1.000000000000000000, 0.9238795325112854062, 1.000000000000000000),
 ( 1.000000000000000000, 0.9229318695247270554, 1.000000000000000000),
 ( 1.000000000000000000, 0.8926288119218640515, 1.000000000000000000),
 ( 1.000000000000000000, 0.8123777807284088270, 1.000000000000000000),
 ( 1.000000000000000000, 0.7629087100922027354, 1.000000000000000000),
 ( 1.000000000000000000, 0.7071067811865475727, 1.000000000000000000) ) ) 
 REPRESENTATION_ITEM ( '' )  SURFACE ( )  );
#155270=CARTESIAN_POINT ( 'NONE',  ( -21.14999999999999858, 87.65000000001269598, -203.5231074845243029 ) ) ;
#155287=DIRECTION ( 'NONE',  ( 0.000000000000000000, -6.467318590049456648E-15, 1.000000000000000000 ) ) ;
#155297=EDGE_LOOP ( 'NONE', ( #184808, #31063, #169523, #183664 ) ) ;
#155308=EDGE_CURVE ( 'NONE', #94115, #17720, #129853, .T. ) ;
#155338=ORIENTED_EDGE ( 'NONE', *, *, #75007, .T. ) ;
#155366=CARTESIAN_POINT ( 'NONE',  ( 23.24999999999999645, 71.00000000001253397, -182.4283735034374843 ) ) ;
#155379=CARTESIAN_POINT ( 'NONE',  ( 18.52928932188133970, 65.72071067813116940, -178.7731074845244450 ) ) ;
#155382=AXIS2_PLACEMENT_3D ( 'NONE', #120726, #181966, #58129 ) ;
#155396=VECTOR ( 'NONE', #250920, 1000.000000000000000 ) ;
#155419=ORIENTED_EDGE ( 'NONE', *, *, #91997, .F. ) ;
#155442=DIRECTION ( 'NONE',  ( 0.000000000000000000, -7.272083257015735086E-15, 1.000000000000000000 ) ) ;
#155458=EDGE_LOOP ( 'NONE', ( #23853, #93975, #137052, #114532 ) ) ;
#155480=DIRECTION ( 'NONE',  ( 0.000000000000000000, -6.982962677686266711E-15, 1.000000000000000000 ) ) ;
#155499=ORIENTED_EDGE ( 'NONE', *, *, #145017, .T. ) ;
#155527=DIRECTION ( 'NONE',  ( 1.000000000000000000, 0.000000000000000000, 0.000000000000000000 ) ) ;
#155539=EDGE_CURVE ( 'NONE', #42440, #242161, #212594, .T. ) ;
#155546=CARTESIAN_POINT ( 'NONE',  ( 20.94999999999999574, 74.25000000001259082, -191.8535959266227451 ) ) ;
#155549=CARTESIAN_POINT ( 'NONE',  ( 23.24999999999999645, 78.10000000001245724, -170.0231074845243313 ) ) ;
#155576=AXIS2_PLACEMENT_3D ( 'NONE', #197358, #57832, #199953 ) ;
#155602=ORIENTED_EDGE ( 'NONE', *, *, #95597, .T. ) ;
#155609=ORIENTED_EDGE ( 'NONE', *, *, #1103, .T. ) ;
#155649=EDGE_CURVE ( 'NONE', #246982, #3356, #40401, .T. ) ;
#155665=DIRECTION ( 'NONE',  ( -1.000000000000000000, 0.000000000000000000, -0.000000000000000000 ) ) ;
#155673=ORIENTED_EDGE ( 'NONE', *, *, #113320, .T. ) ;
#155703=ORIENTED_EDGE ( 'NONE', *, *, #232165, .F. ) ;
#155710=EDGE_CURVE ( 'NONE', #227674, #100958, #168052, .T. ) ;
#155726=EDGE_CURVE ( 'NONE', #239043, #247011, #105427, .T. ) ;
#155749=VERTEX_POINT ( 'NONE', #185008 ) ;
#155757=CIRCLE ( 'NONE', #214003, 0.09999999999999939493 ) ;
#155789=FACE_OUTER_BOUND ( 'NONE', #54367, .T. ) ;
#155805=CARTESIAN_POINT ( 'NONE',  ( -21.05000000000000071, 76.10000000001276987, -215.1726782920691505 ) ) ;
#155806=DIRECTION ( 'NONE',  ( 1.000000000000000000, 0.000000000000000000, 0.000000000000000000 ) ) ;
#155808=DIRECTION ( 'NONE',  ( 0.000000000000000000, 7.026728003956695223E-15, -1.000000000000000000 ) ) ;
#155833=AXIS2_PLACEMENT_3D ( 'NONE', #70135, #113085, #90943 ) ;
#155901=EDGE_LOOP ( 'NONE', ( #227206, #251895, #228587, #133227 ) ) ;
#155902=CARTESIAN_POINT ( 'NONE',  ( 21.03670563405601968, 65.37517631068435264, -191.1975605983152775 ) ) ;
#155911=AXIS2_PLACEMENT_3D ( 'NONE', #944, #41418, #238302 ) ;
#155993=EDGE_CURVE ( 'NONE', #225819, #33564, #140419, .T. ) ;
#155998=ORIENTED_EDGE ( 'NONE', *, *, #166110, .F. ) ;
#156008=ADVANCED_FACE ( 'NONE', ( #58304 ), #96149, .F. ) ;
#156037=EDGE_CURVE ( 'NONE', #125487, #72763, #9428, .T. ) ;
#156046=ORIENTED_EDGE ( 'NONE', *, *, #226378, .T. ) ;
#156110=VERTEX_POINT ( 'NONE', #223806 ) ;
#156136=VERTEX_POINT ( 'NONE', #183419 ) ;
#156142=DIRECTION ( 'NONE',  ( 0.000000000000000000, -0.8660254037844377084, -0.5000000000000016653 ) ) ;
#156150=DIRECTION ( 'NONE',  ( 0.000000000000000000, -0.8660254037844377084, -0.5000000000000016653 ) ) ;
#156151=VECTOR ( 'NONE', #177568, 1000.000000000000000 ) ;
#156153=CIRCLE ( 'NONE', #68642, 0.09999999999999971412 ) ;
#156162=ADVANCED_FACE ( 'NONE', ( #68606 ), #6039, .F. ) ;
#156165=CYLINDRICAL_SURFACE ( 'NONE', #93978, 0.09999999999999939493 ) ;
#156209=VECTOR ( 'NONE', #157566, 1000.000000000000000 ) ;
#156239=CARTESIAN_POINT ( 'NONE',  ( -18.59999999999999787, 70.10000000001267040, -193.3040077198679967 ) ) ;
#156325=AXIS2_PLACEMENT_3D ( 'NONE', #193064, #36583, #253014 ) ;
#156340=EDGE_LOOP ( 'NONE', ( #154149, #115172, #250667, #156946 ) ) ;
#156384=ORIENTED_EDGE ( 'NONE', *, *, #213375, .T. ) ;
#156386=CARTESIAN_POINT ( 'NONE',  ( -23.15000000000000213, 76.00000000001244871, -170.0231074845243597 ) ) ;
#156423=AXIS2_PLACEMENT_3D ( 'NONE', #187412, #203108, #27073 ) ;
#156426=ORIENTED_EDGE ( 'NONE', *, *, #198285, .F. ) ;
#156456=EDGE_LOOP ( 'NONE', ( #41661, #177117, #164053, #150341 ) ) ;
#156470=PLANE ( 'NONE',  #19679 ) ;
#156480=AXIS2_PLACEMENT_3D ( 'NONE', #98197, #37011, #116528 ) ;
#156517=DIRECTION ( 'NONE',  ( 0.000000000000000000, -1.000000000000000000, -6.982962677686265922E-15 ) ) ;
#156530=AXIS2_PLACEMENT_3D ( 'NONE', #193966, #154851, #17868 ) ;
#156579=CARTESIAN_POINT ( 'NONE',  ( 22.49544290803804003, 64.25012976215469962, -203.5884194437818451 ) ) ;
#156587=ORIENTED_EDGE ( 'NONE', *, *, #122134, .T. ) ;
#156603=CARTESIAN_POINT ( 'NONE',  ( 23.15000000000000213, 87.75000000001259082, -191.3731074845242688 ) ) ;
#156608=DIRECTION ( 'NONE',  ( -6.938893903907222067E-15, -1.000000000000000000, -7.272083257015735086E-15 ) ) ;
#156609=AXIS2_PLACEMENT_3D ( 'NONE', #19023, #178124, #99812 ) ;
#156620=VERTEX_POINT ( 'NONE', #170977 ) ;
#156625=VECTOR ( 'NONE', #100073, 1000.000000000000000 ) ;
#156628=AXIS2_PLACEMENT_3D ( 'NONE', #87372, #246463, #226897 ) ;
#156638=TOROIDAL_SURFACE ( 'NONE', #44182, 12.77500000000000036, 0.1000000000000000056 ) ;
#156698=ADVANCED_FACE ( 'NONE', ( #237323 ), #221576, .T. ) ;
#156719=CARTESIAN_POINT ( 'NONE',  ( -20.94999999999999929, 87.65000000001266756, -200.6231074845242688 ) ) ;
#156733=CARTESIAN_POINT ( 'NONE',  ( 21.14999999999999858, 76.00000000001271871, -210.0637644362255969 ) ) ;
#156736=DIRECTION ( 'NONE',  ( 2.694716079187273439E-16, 1.000000000000000000, 6.467318590049456648E-15 ) ) ;
#156782=LINE ( 'NONE', #133346, #157048 ) ;
#156795=SPHERICAL_SURFACE ( 'NONE', #241585, 0.1000000000000000056 ) ;
#156927=CARTESIAN_POINT ( 'NONE',  ( -18.41799967126735282, 85.50000000001263345, -196.4910376712677476 ) ) ;
#156946=ORIENTED_EDGE ( 'NONE', *, *, #223149, .F. ) ;
#156949=CARTESIAN_POINT ( 'NONE',  ( 23.15000000000000213, 85.00000000001261924, -193.6291383618718385 ) ) ;
#156965=CARTESIAN_POINT ( 'NONE',  ( -21.05000000000000071, 74.73821383144760944, -195.4366085209788935 ) ) ;
#156968=CIRCLE ( 'NONE', #107042, 0.09999999999999646672 ) ;
#156977=ORIENTED_EDGE ( 'NONE', *, *, #206290, .F. ) ;
#156980=ORIENTED_EDGE ( 'NONE', *, *, #178345, .F. ) ;
#156987=DIRECTION ( 'NONE',  ( 0.000000000000000000, -6.454785026890489601E-15, 1.000000000000000000 ) ) ;
#156993=EDGE_CURVE ( 'NONE', #32434, #172249, #126984, .T. ) ;
#156997=DIRECTION ( 'NONE',  ( -1.000000000000000000, 0.000000000000000000, 0.000000000000000000 ) ) ;
#157007=CARTESIAN_POINT ( 'NONE',  ( -23.15000000000000213, 85.60000000001262777, -193.6291383618718385 ) ) ;
#157012=CIRCLE ( 'NONE', #177857, 0.5999999999999894307 ) ;
#157014=ADVANCED_FACE ( 'NONE', ( #253989 ), #206278, .T. ) ;
#157031=DIRECTION ( 'NONE',  ( -1.000000000000000000, 0.000000000000000000, -0.000000000000000000 ) ) ;
#157033=FACE_OUTER_BOUND ( 'NONE', #123561, .T. ) ;
#157047=CARTESIAN_POINT ( 'NONE',  ( -18.41817142474042157, 85.49870306661448183, -163.4191419968870491 ) ) ;
#157048=VECTOR ( 'NONE', #132055, 999.9999999999998863 ) ;
#157070=DIRECTION ( 'NONE',  ( 0.000000000000000000, 0.000000000000000000, -1.000000000000000000 ) ) ;
#157085=LINE ( 'NONE', #1825, #185585 ) ;
#157113=CARTESIAN_POINT ( 'NONE',  ( 20.94999999999999929, 76.00000000001243450, -168.0231074845243597 ) ) ;
#157131=CYLINDRICAL_SURFACE ( 'NONE', #3303, 0.1000000000000028644 ) ;
#157132=ORIENTED_EDGE ( 'NONE', *, *, #234694, .F. ) ;
#157133=CARTESIAN_POINT ( 'NONE',  ( -18.59999999999999787, 77.85161776048127535, -158.4199177649206831 ) ) ;
#157134=LINE ( 'NONE', #142660, #77588 ) ;
#157149=DIRECTION ( 'NONE',  ( 0.000000000000000000, -6.982962677686266711E-15, 1.000000000000000000 ) ) ;
#157195=DIRECTION ( 'NONE',  ( 0.000000000000000000, -1.000000000000000000, 0.000000000000000000 ) ) ;
#157264=DIRECTION ( 'NONE',  ( 0.000000000000000000, 0.000000000000000000, -1.000000000000000000 ) ) ;
#157278=AXIS2_PLACEMENT_3D ( 'NONE', #28799, #33938, #208691 ) ;
#157291=AXIS2_PLACEMENT_3D ( 'NONE', #32055, #91990, #34615 ) ;
#157292=CARTESIAN_POINT ( 'NONE',  ( -21.07928932188134041, 76.00000000001267608, -203.5231074845243597 ) ) ;
#157334=ORIENTED_EDGE ( 'NONE', *, *, #220438, .T. ) ;
#157404=CARTESIAN_POINT ( 'NONE',  ( 22.45301702632625762, 75.98478912030257959, -215.1728997087847404 ) ) ;
#157432=DIRECTION ( 'NONE',  ( 0.000000000000000000, -7.034366652768095332E-15, 1.000000000000000000 ) ) ;
#157442=AXIS2_PLACEMENT_3D ( 'NONE', #56656, #18847, #219606 ) ;
#157446=EDGE_LOOP ( 'NONE', ( #256297, #62231, #142868, #54106 ) ) ;
#157463=AXIS2_PLACEMENT_3D ( 'NONE', #192920, #71703, #11732 ) ;
#157467=CARTESIAN_POINT ( 'NONE',  ( -23.25000000000000000, 76.10085836911147794, -215.2726746080137445 ) ) ;
#157471=ORIENTED_EDGE ( 'NONE', *, *, #122134, .F. ) ;
#157480=CIRCLE ( 'NONE', #78323, 0.09999999999999939493 ) ;
#157484=ORIENTED_EDGE ( 'NONE', *, *, #22755, .T. ) ;
#157529=EDGE_CURVE ( 'NONE', #99797, #80905, #95885, .T. ) ;
#157558=CARTESIAN_POINT ( 'NONE',  ( 23.15000000000000213, 85.60000000001251408, -179.9170766071767389 ) ) ;
#157566=DIRECTION ( 'NONE',  ( 0.000000000000000000, -1.000000000000000000, -8.717686153663073805E-15 ) ) ;
#157567=AXIS2_PLACEMENT_3D ( 'NONE', #163229, #104495, #43275 ) ;
#157572=AXIS2_PLACEMENT_3D ( 'NONE', #103109, #125271, #126551 ) ;
#157586=CARTESIAN_POINT ( 'NONE',  ( -21.07928932188134041, 75.90110485435833709, -209.8516241409176644 ) ) ;
#157592=CARTESIAN_POINT ( 'NONE',  ( -22.48660254037843131, 64.35000000001267040, -203.5731074845244279 ) ) ;
#157618=DIRECTION ( 'NONE',  ( 1.000000000000000000, 0.000000000000000000, 0.000000000000000000 ) ) ;
#157619=EDGE_CURVE ( 'NONE', #196072, #239511, #167087, .T. ) ;
#157631=ORIENTED_EDGE ( 'NONE', *, *, #159405, .T. ) ;
#157646=CARTESIAN_POINT ( 'NONE',  ( 21.05000000000000071, 65.37127968600826478, -195.8581939154368570 ) ) ;
#157653=EDGE_CURVE ( 'NONE', #251965, #200607, #160312, .T. ) ;
#157717=EDGE_CURVE ( 'NONE', #233060, #27358, #222604, .T. ) ;
#157723=TOROIDAL_SURFACE ( 'NONE', #191012, 0.2000000000000000111, 0.1000000000000000056 ) ;
#157731=EDGE_CURVE ( 'NONE', #36049, #119237, #144004, .T. ) ;
#157762=DIRECTION ( 'NONE',  ( -1.000000000000000000, -0.000000000000000000, -0.000000000000000000 ) ) ;
#157775=EDGE_CURVE ( 'NONE', #25370, #161777, #151929, .T. ) ;
#157783=LINE ( 'NONE', #79455, #29777 ) ;
#157808=DIRECTION ( 'NONE',  ( 0.000000000000000000, 0.000000000000000000, -1.000000000000000000 ) ) ;
#157822=DIRECTION ( 'NONE',  ( 0.000000000000000000, 6.982962677686266711E-15, -1.000000000000000000 ) ) ;
#157838=VECTOR ( 'NONE', #191033, 1000.000000000000000 ) ;
#157879=VECTOR ( 'NONE', #146641, 1000.000000000000000 ) ;
#157887=CIRCLE ( 'NONE', #182972, 0.09999999999998898659 ) ;
#157891=CARTESIAN_POINT ( 'NONE',  ( 22.39999999999999503, 68.20922040163929978, -203.5231074845243882 ) ) ;
#157907=ORIENTED_EDGE ( 'NONE', *, *, #56331, .F. ) ;
#157908=CIRCLE ( 'NONE', #107966, 0.09999999999999939493 ) ;
#157912=VECTOR ( 'NONE', #93835, 1000.000000000000000 ) ;
#157932=LINE ( 'NONE', #122632, #32787 ) ;
#157950=ORIENTED_EDGE ( 'NONE', *, *, #34479, .T. ) ;
#157953=EDGE_CURVE ( 'NONE', #180782, #107411, #246519, .T. ) ;
#157978=CARTESIAN_POINT ( 'NONE',  ( 20.93284271247462414, 64.25000000001249134, -177.0379132551784380 ) ) ;
#157986=DIRECTION ( 'NONE',  ( 0.000000000000000000, 1.000000000000000000, 6.982962677686266711E-15 ) ) ;
#157992=ORIENTED_EDGE ( 'NONE', *, *, #171223, .F. ) ;
#158014=CARTESIAN_POINT ( 'NONE',  ( -18.59999999999999787, 77.16270174995064224, -195.4231074845243370 ) ) ;
#158035=EDGE_CURVE ( 'NONE', #255434, #32289, #247761, .T. ) ;
#158041=SPHERICAL_SURFACE ( 'NONE', #13994, 0.1000000000000000056 ) ;
#158055=DIRECTION ( 'NONE',  ( 1.000000000000000000, 0.000000000000000000, 0.000000000000000000 ) ) ;
#158056=DIRECTION ( 'NONE',  ( 0.000000000000000000, 0.000000000000000000, -1.000000000000000000 ) ) ;
#158074=ORIENTED_EDGE ( 'NONE', *, *, #117105, .F. ) ;
#158078=CARTESIAN_POINT ( 'NONE',  ( -23.25000000000000000, 77.25000000001239187, -162.2226267301092548 ) ) ;
#158129=FACE_OUTER_BOUND ( 'NONE', #110278, .T. ) ;
#158143=CYLINDRICAL_SURFACE ( 'NONE', #43044, 2.000000000000001776 ) ;
#158147=DIRECTION ( 'NONE',  ( 1.000000000000000000, 0.000000000000000000, 0.000000000000000000 ) ) ;
#158148=ORIENTED_EDGE ( 'NONE', *, *, #65070, .F. ) ;
#158158=DIRECTION ( 'NONE',  ( -1.000000000000000000, -0.000000000000000000, -0.000000000000000000 ) ) ;
#158193=DIRECTION ( 'NONE',  ( 1.000000000000000000, -1.836970198721029934E-16, -1.282749433769087582E-30 ) ) ;
#158202=EDGE_CURVE ( 'NONE', #152240, #235216, #214803, .T. ) ;
#158205=DIRECTION ( 'NONE',  ( 0.000000000000000000, 1.000000000000000000, 6.982962677686266711E-15 ) ) ;
#158226=CARTESIAN_POINT ( 'NONE',  ( -18.42609945526432824, 85.49999971050360159, -196.5237449942749777 ) ) ;
#158229=DIRECTION ( 'NONE',  ( 1.000000000000000000, 0.000000000000000000, -0.000000000000000000 ) ) ;
#158235=DIRECTION ( 'NONE',  ( 0.000000000000000000, -7.429790795770644761E-15, 1.000000000000000000 ) ) ;
#158258=AXIS2_PLACEMENT_3D ( 'NONE', #13691, #93224, #208068 ) ;
#158274=ORIENTED_EDGE ( 'NONE', *, *, #180929, .T. ) ;
#158299=CARTESIAN_POINT ( 'NONE',  ( 21.05000000000047677, 69.55891531154155416, -203.5053880512165279 ) ) ;
#158316=EDGE_CURVE ( 'NONE', #144289, #136156, #139776, .T. ) ;
#158397=CARTESIAN_POINT ( 'NONE',  ( -22.59999999999999432, 64.25012875563618309, -203.5885370755380848 ) ) ;
#158407=EDGE_CURVE ( 'NONE', #93820, #72763, #31502, .T. ) ;
#158411=EDGE_CURVE ( 'NONE', #30084, #144435, #60662, .T. ) ;
#158432=EDGE_CURVE ( 'NONE', #3727, #24355, #2402, .T. ) ;
#158447=VECTOR ( 'NONE', #117828, 1000.000000000000000 ) ;
#158488=AXIS2_PLACEMENT_3D ( 'NONE', #170502, #164687, #218528 ) ;
#158500=DIRECTION ( 'NONE',  ( -1.000000000000000000, 0.000000000000000000, 0.000000000000000000 ) ) ;
#158501=CARTESIAN_POINT ( 'NONE',  ( 21.30000000000002558, 76.00000000001267608, -203.5231074845243597 ) ) ;
#158542=CARTESIAN_POINT ( 'NONE',  ( 23.14999999999999858, 76.00000000001244871, -170.0231074845243597 ) ) ;
#158546=LINE ( 'NONE', #180658, #32445 ) ;
#158555=FACE_OUTER_BOUND ( 'NONE', #155297, .T. ) ;
#158567=CARTESIAN_POINT ( 'NONE',  ( -21.07928932188134041, 69.67148334361938566, -203.6220026301787982 ) ) ;
#158570=AXIS2_PLACEMENT_3D ( 'NONE', #26239, #7958, #163181 ) ;
#158609=AXIS2_PLACEMENT_3D ( 'NONE', #5021, #102839, #6321 ) ;
#158637=EDGE_LOOP ( 'NONE', ( #156980, #69353, #237155, #219353 ) ) ;
#158645=DIRECTION ( 'NONE',  ( 1.000000000000000000, 0.000000000000000000, 0.000000000000000000 ) ) ;
#158651=CARTESIAN_POINT ( 'NONE',  ( 18.41832399655379504, 85.68240326668673390, -163.3662638644972844 ) ) ;
#158664=VERTEX_POINT ( 'NONE', #45352 ) ;
#158679=EDGE_CURVE ( 'NONE', #141625, #221154, #1061, .T. ) ;
#158711=LINE ( 'NONE', #238203, #80113 ) ;
#158740=ORIENTED_EDGE ( 'NONE', *, *, #109341, .T. ) ;
#158752=DIRECTION ( 'NONE',  ( 0.000000000000000000, 0.000000000000000000, 1.000000000000000000 ) ) ;
#158786=CARTESIAN_POINT ( 'NONE',  ( -18.59999999999999787, 64.35000000001264198, -196.5083017138704236 ) ) ;
#158819=PLANE ( 'NONE',  #220587 ) ;
#158820=DIRECTION ( 'NONE',  ( 0.000000000000000000, 0.000000000000000000, 1.000000000000000000 ) ) ;
#158879=DIRECTION ( 'NONE',  ( 1.000000000000000000, 0.000000000000000000, 0.000000000000000000 ) ) ;
#158925=ORIENTED_EDGE ( 'NONE', *, *, #141194, .F. ) ;
#158962=CIRCLE ( 'NONE', #42402, 0.09999999999998898659 ) ;
#159002=ADVANCED_FACE ( 'NONE', ( #114308 ), #240673, .T. ) ;
#159004=ORIENTED_EDGE ( 'NONE', *, *, #109038, .T. ) ;
#159044=CARTESIAN_POINT ( 'NONE',  ( -21.14999999999999858, 87.65000000001269598, -203.5231074845243029 ) ) ;
#159057=DIRECTION ( 'NONE',  ( 0.000000000000000000, -6.938893903907222067E-15, 1.000000000000000000 ) ) ;
#159087=CARTESIAN_POINT ( 'NONE',  ( -23.15000000000000213, 64.35000000001249987, -177.0379132551783812 ) ) ;
#159088=DIRECTION ( 'NONE',  ( 1.000000000000000000, 0.000000000000000000, 0.000000000000000000 ) ) ;
#159089=EDGE_CURVE ( 'NONE', #203821, #238502, #52658, .T. ) ;
#159126=FACE_OUTER_BOUND ( 'NONE', #227894, .T. ) ;
#159129=CARTESIAN_POINT ( 'NONE',  ( 21.05000000000000071, 69.65000000001262492, -193.6792853948412869 ) ) ;
#159140=ADVANCED_FACE ( 'NONE', ( #110150 ), #206689, .F. ) ;
#159174=CARTESIAN_POINT ( 'NONE',  ( -18.59999999999999787, 76.00000000001267608, -203.5231074845243597 ) ) ;
#159203=ORIENTED_EDGE ( 'NONE', *, *, #2280, .F. ) ;
#159211=EDGE_LOOP ( 'NONE', ( #191548, #1777, #200734, #85008 ) ) ;
#159231=AXIS2_PLACEMENT_3D ( 'NONE', #175591, #71362, #214692 ) ;
#159246=DIRECTION ( 'NONE',  ( 0.000000000000000000, 0.000000000000000000, -1.000000000000000000 ) ) ;
#159249=EDGE_CURVE ( 'NONE', #163131, #105444, #148549, .T. ) ;
#159371=CARTESIAN_POINT ( 'NONE',  ( 19.92426406871192412, 64.25000000001250555, -178.6731074845244507 ) ) ;
#159373=DIRECTION ( 'NONE',  ( 0.000000000000000000, 1.000000000000000000, 6.982962677686266711E-15 ) ) ;
#159405=EDGE_CURVE ( 'NONE', #78560, #13712, #22633, .T. ) ;
#159429=CARTESIAN_POINT ( 'NONE',  ( 23.25000000000000000, 87.65000000001275282, -215.2731074845242745 ) ) ;
#159431=CYLINDRICAL_SURFACE ( 'NONE', #159715, 0.1000000000000028644 ) ;
#159448=CARTESIAN_POINT ( 'NONE',  ( 21.05000000000000071, 84.73084112150795022, -193.9250327655399531 ) ) ;
#159488=ORIENTED_EDGE ( 'NONE', *, *, #149765, .F. ) ;
#159493=AXIS2_PLACEMENT_3D ( 'NONE', #76272, #22760, #141386 ) ;
#159546=CARTESIAN_POINT ( 'NONE',  ( 22.60000000000000142, 75.95218160930798490, -215.2731299035715722 ) ) ;
#159556=CARTESIAN_POINT ( 'NONE',  ( 18.48536876927988715, 85.46352724988010152, -196.4744892194416650 ) ) ;
#159594=ORIENTED_EDGE ( 'NONE', *, *, #59003, .F. ) ;
#159596=DIRECTION ( 'NONE',  ( 0.000000000000000000, -1.000000000000000000, -6.982962677686265922E-15 ) ) ;
#159598=DIRECTION ( 'NONE',  ( -1.000000000000000000, 0.000000000000000000, 0.000000000000000000 ) ) ;
#159634=DIRECTION ( 'NONE',  ( 2.952720810173289112E-16, 1.000000000000000000, 6.982962677686266711E-15 ) ) ;
#159662=DIRECTION ( 'NONE',  ( 0.000000000000000000, 1.000000000000000000, 8.717686153663073805E-15 ) ) ;
#159715=AXIS2_PLACEMENT_3D ( 'NONE', #215528, #135979, #175177 ) ;
#159779=AXIS2_PLACEMENT_3D ( 'NONE', #220852, #194901, #185589 ) ;
#159783=CARTESIAN_POINT ( 'NONE',  ( -20.54999999999999716, 84.66355140188167638, -179.5472086025916099 ) ) ;
#159787=CARTESIAN_POINT ( 'NONE',  ( -20.64999999999999858, 74.05981308412469843, -182.8522266955776843 ) ) ;
#159797=DIRECTION ( 'NONE',  ( 0.000000000000000000, 0.8700118002898356018, -0.4930308989875170078 ) ) ;
#159806=EDGE_CURVE ( 'NONE', #144388, #4003, #115576, .T. ) ;
#159808=ADVANCED_FACE ( 'NONE', ( #171803 ), #241325, .F. ) ;
#159823=ADVANCED_FACE ( 'NONE', ( #89645, #150921 ), #111800, .F. ) ;
#159825=CARTESIAN_POINT ( 'NONE',  ( 19.86930884467575353, 64.31308993304160992, -178.7838848455857317 ) ) ;
#159830=DIRECTION ( 'NONE',  ( -1.000000000000000000, 2.952720810173289112E-16, 2.061873921506763405E-30 ) ) ;
#159832=ORIENTED_EDGE ( 'NONE', *, *, #25219, .T. ) ;
#159845=CARTESIAN_POINT ( 'NONE',  ( -21.12642695952773764, 69.62434007797752145, -203.6220107677137605 ) ) ;
#159856=ORIENTED_EDGE ( 'NONE', *, *, #7065, .T. ) ;
#159863=EDGE_CURVE ( 'NONE', #117188, #92906, #190449, .T. ) ;
#159865=AXIS2_PLACEMENT_3D ( 'NONE', #185824, #128425, #48881 ) ;
#159873=ADVANCED_FACE ( 'NONE', ( #110499 ), #248742, .F. ) ;
#159912=ORIENTED_EDGE ( 'NONE', *, *, #175092, .F. ) ;
#159955=CARTESIAN_POINT ( 'NONE',  ( 22.49806830649814060, 75.92253568368725780, -215.1729971393634457 ) ) ;
#159971=DIRECTION ( 'NONE',  ( -3.265361837132813093E-16, -1.000000000000000000, -6.982962677686266711E-15 ) ) ;
#159974=VECTOR ( 'NONE', #99725, 1000.000000000000000 ) ;
#159987=DIRECTION ( 'NONE',  ( -1.000000000000000000, 0.000000000000000000, -0.000000000000000000 ) ) ;
#160005=CARTESIAN_POINT ( 'NONE',  ( -18.50000000000000000, 85.50000000001263345, -195.4231074845242802 ) ) ;
#160017=VERTEX_POINT ( 'NONE', #43810 ) ;
#160024=ADVANCED_FACE ( 'NONE', ( #82891 ), #94725, .T. ) ;
#160039=DIRECTION ( 'NONE',  ( -1.000000000000000000, 0.000000000000000000, -0.000000000000000000 ) ) ;
#160130=DIRECTION ( 'NONE',  ( 0.000000000000000000, -6.982962677686266711E-15, 1.000000000000000000 ) ) ;
#160143=DIRECTION ( 'NONE',  ( 1.000000000000000000, 0.000000000000000000, 0.000000000000000000 ) ) ;
#160151=DIRECTION ( 'NONE',  ( 0.000000000000000000, -1.000000000000000000, -6.982962677686265922E-15 ) ) ;
#160162=ORIENTED_EDGE ( 'NONE', *, *, #231325, .F. ) ;
#160171=AXIS2_PLACEMENT_3D ( 'NONE', #33492, #175550, #210801 ) ;
#160174=CARTESIAN_POINT ( 'NONE',  ( -20.87155475150660777, 64.25000000001250555, -176.9275209553668162 ) ) ;
#160181=EDGE_CURVE ( 'NONE', #42935, #60608, #103276, .T. ) ;
#160182=EDGE_LOOP ( 'NONE', ( #170567, #205804, #87324, #221743, #119129 ) ) ;
#160206=VECTOR ( 'NONE', #143575, 1000.000000000000000 ) ;
#160217=AXIS2_PLACEMENT_3D ( 'NONE', #132324, #31972, #68514 ) ;
#160231=CARTESIAN_POINT ( 'NONE',  ( -20.64999999999999858, 73.50000000001254818, -183.2477294072864709 ) ) ;
#160253=DIRECTION ( 'NONE',  ( 0.000000000000000000, -1.000000000000000000, 0.000000000000000000 ) ) ;
#160262=CARTESIAN_POINT ( 'NONE',  ( -23.15000000000000213, 85.60000000001276987, -215.2731074845242745 ) ) ;
#160277=CARTESIAN_POINT ( 'NONE',  ( 21.05000000000000071, 87.65000000001246860, -173.0231074845243029 ) ) ;
#160287=FACE_OUTER_BOUND ( 'NONE', #70410, .T. ) ;
#160309=FACE_OUTER_BOUND ( 'NONE', #7912, .T. ) ;
#160312=CIRCLE ( 'NONE', #47823, 1.900000000000012790 ) ;
#160315=( GEOMETRIC_REPRESENTATION_CONTEXT ( 3 ) GLOBAL_UNCERTAINTY_ASSIGNED_CONTEXT ( ( #94628 ) ) GLOBAL_UNIT_ASSIGNED_CONTEXT ( ( #172462, #171181, #91597 ) ) REPRESENTATION_CONTEXT ( 'NONE', 'WORKASPACE' ) );
#160351=EDGE_CURVE ( 'NONE', #60608, #42935, #128245, .T. ) ;
#160362=CARTESIAN_POINT ( 'NONE',  ( 22.50000000000000000, 64.35042919246788529, -203.6231074845244393 ) ) ;
#160375=CARTESIAN_POINT ( 'NONE',  ( -23.25000000000000000, 76.00000000001267608, -203.5231074845243597 ) ) ;
#160385=EDGE_CURVE ( 'NONE', #57380, #228673, #136596, .T. ) ;
#160397=AXIS2_PLACEMENT_3D ( 'NONE', #196142, #102141, #61766 ) ;
#160419=VERTEX_POINT ( 'NONE', #1786 ) ;
#160423=AXIS2_PLACEMENT_3D ( 'NONE', #34018, #116092, #195641 ) ;
#160453=ORIENTED_EDGE ( 'NONE', *, *, #63454, .T. ) ;
#160480=CARTESIAN_POINT ( 'NONE',  ( -21.05000000000000071, 64.35000000001264198, -196.7392418215462726 ) ) ;
#160497=DIRECTION ( 'NONE',  ( 0.000000000000000000, 8.896017825522085641E-15, -1.000000000000000000 ) ) ;
#160501=DIRECTION ( 'NONE',  ( 1.000000000000000000, 0.000000000000000000, 0.000000000000000000 ) ) ;
#160507=CIRCLE ( 'NONE', #252062, 12.97499999999998721 ) ;
#160526=CARTESIAN_POINT ( 'NONE',  ( -22.48660254037843487, 64.35000000001268461, -203.5731074845244279 ) ) ;
#160539=AXIS2_PLACEMENT_3D ( 'NONE', #109654, #66699, #71851 ) ;
#160545=ORIENTED_EDGE ( 'NONE', *, *, #246973, .T. ) ;
#160546=DIRECTION ( 'NONE',  ( -0.000000000000000000, 0.8700118002898356018, -0.4930308989875170078 ) ) ;
#160548=ORIENTED_EDGE ( 'NONE', *, *, #61257, .T. ) ;
#160562=FACE_OUTER_BOUND ( 'NONE', #111192, .T. ) ;
#160588=DIRECTION ( 'NONE',  ( -1.000000000000000000, 0.000000000000000000, 0.000000000000000000 ) ) ;
#160592=DIRECTION ( 'NONE',  ( 0.000000000000000000, -0.9908441862701610203, 0.1350103645451807555 ) ) ;
#160597=VERTEX_POINT ( 'NONE', #205117 ) ;
#160598=CARTESIAN_POINT ( 'NONE',  ( 20.85000000000000142, 77.14957036958807635, -162.2071950000224092 ) ) ;
#160602=AXIS2_PLACEMENT_3D ( 'NONE', #84745, #136068, #233911 ) ;
#160631=AXIS2_PLACEMENT_3D ( 'NONE', #142572, #26513, #183018 ) ;
#160635=CARTESIAN_POINT ( 'NONE',  ( -20.94999999999999929, 70.10000000001251408, -180.2422072491807796 ) ) ;
#160657=AXIS2_PLACEMENT_3D ( 'NONE', #227975, #49331, #44214 ) ;
#160678=AXIS2_PLACEMENT_3D ( 'NONE', #36711, #56219, #96618 ) ;
#160696=ORIENTED_EDGE ( 'NONE', *, *, #56143, .F. ) ;
#160751=DIRECTION ( 'NONE',  ( 0.000000000000000000, -7.189901751995743170E-15, 1.000000000000000000 ) ) ;
#160754=AXIS2_PLACEMENT_3D ( 'NONE', #147638, #169813, #227169 ) ;
#160799=LINE ( 'NONE', #61666, #40452 ) ;
#160819=CARTESIAN_POINT ( 'NONE',  ( 21.05000000000000071, 77.25000000001263345, -195.6231074845243540 ) ) ;
#160832=ORIENTED_EDGE ( 'NONE', *, *, #96387, .T. ) ;
#160834=ORIENTED_EDGE ( 'NONE', *, *, #110004, .F. ) ;
#160836=LINE ( 'NONE', #102089, #186536 ) ;
#160848=CARTESIAN_POINT ( 'NONE',  ( 21.04999999999999716, 69.50331341424610798, -203.5084513660146968 ) ) ;
#160854=EDGE_CURVE ( 'NONE', #229203, #126474, #132519, .T. ) ;
#160859=DIRECTION ( 'NONE',  ( 1.000000000000000000, 0.000000000000000000, 0.000000000000000000 ) ) ;
#160870=FACE_OUTER_BOUND ( 'NONE', #55693, .T. ) ;
#160874=CARTESIAN_POINT ( 'NONE',  ( 20.04142135623730070, 64.35000000001254250, -182.1731074845244507 ) ) ;
#160894=FACE_OUTER_BOUND ( 'NONE', #149866, .T. ) ;
#160922=LINE ( 'NONE', #102176, #150622 ) ;
#160956=DIRECTION ( 'NONE',  ( 0.000000000000000000, -0.9908441862701791170, 0.1350103645450472789 ) ) ;
#160967=FACE_OUTER_BOUND ( 'NONE', #131581, .T. ) ;
#160978=ORIENTED_EDGE ( 'NONE', *, *, #157653, .T. ) ;
#160984=VERTEX_POINT ( 'NONE', #37782 ) ;
#160989=DIRECTION ( 'NONE',  ( 0.000000000000000000, -8.556632174375010717E-15, 1.000000000000000000 ) ) ;
#160996=TOROIDAL_SURFACE ( 'NONE', #52822, 12.77499999999999858, 0.1000000000000000056 ) ;
#161006=ORIENTED_EDGE ( 'NONE', *, *, #127289, .F. ) ;
#161012=EDGE_CURVE ( 'NONE', #233248, #87397, #220194, .T. ) ;
#161032=VERTEX_POINT ( 'NONE', #96427 ) ;
#161054=DIRECTION ( 'NONE',  ( 0.000000000000000000, -0.1298341882519953583, -0.9915357197604861561 ) ) ;
#161068=CARTESIAN_POINT ( 'NONE',  ( 20.30466543256828160, 66.69576306075845196, -195.2694448331317005 ) ) ;
#161071=CARTESIAN_POINT ( 'NONE',  ( -21.45000000000000284, 68.29142135624984178, -182.3731074845244109 ) ) ;
#161095=ORIENTED_EDGE ( 'NONE', *, *, #250623, .F. ) ;
#161105=CARTESIAN_POINT ( 'NONE',  ( 20.04142135391667168, 64.25000000001250555, -178.8206006188949289 ) ) ;
#161106=AXIS2_PLACEMENT_3D ( 'NONE', #4354, #205116, #223400 ) ;
#161118=ORIENTED_EDGE ( 'NONE', *, *, #868, .T. ) ;
#161129=ORIENTED_EDGE ( 'NONE', *, *, #151558, .F. ) ;
#161132=CARTESIAN_POINT ( 'NONE',  ( 21.05000000000000071, 75.96513199699965924, -209.7931933482134923 ) ) ;
#161219=CIRCLE ( 'NONE', #32063, 0.1000000000000026007 ) ;
#161233=DIRECTION ( 'NONE',  ( 0.000000000000000000, 0.000000000000000000, 1.000000000000000000 ) ) ;
#161234=CARTESIAN_POINT ( 'NONE',  ( -23.15000000000000213, 76.00000000001244871, -170.0231074845243597 ) ) ;
#161294=DIRECTION ( 'NONE',  ( 0.000000000000000000, 0.000000000000000000, 1.000000000000000000 ) ) ;
#161376=VECTOR ( 'NONE', #122146, 1000.000000000000114 ) ;
#161402=DIRECTION ( 'NONE',  ( 1.000000000000000000, 7.304098846218133681E-16, 5.100424963727255128E-30 ) ) ;
#161407=EDGE_CURVE ( 'NONE', #18425, #205739, #41334, .T. ) ;
#161412=ORIENTED_EDGE ( 'NONE', *, *, #131989, .F. ) ;
#161425=EDGE_CURVE ( 'NONE', #65312, #89282, #182969, .T. ) ;
#161441=CYLINDRICAL_SURFACE ( 'NONE', #172355, 0.09999999999999939493 ) ;
#161452=ORIENTED_EDGE ( 'NONE', *, *, #10635, .T. ) ;
#161484=ORIENTED_EDGE ( 'NONE', *, *, #96471, .F. ) ;
#161512=DIRECTION ( 'NONE',  ( 1.000000000000000000, 0.000000000000000000, 0.000000000000000000 ) ) ;
#161526=ORIENTED_EDGE ( 'NONE', *, *, #80765, .F. ) ;
#161527=DIRECTION ( 'NONE',  ( 1.000000000000000000, 0.000000000000000000, 0.000000000000000000 ) ) ;
#161564=CARTESIAN_POINT ( 'NONE',  ( -21.04999999999998650, 75.90156250001273008, -209.8223383946112222 ) ) ;
#161565=CARTESIAN_POINT ( 'NONE',  ( 21.05000000000000071, 65.57661458509971908, -196.0310555606543517 ) ) ;
#161580=DIRECTION ( 'NONE',  ( 1.000000000000000000, 0.000000000000000000, 0.000000000000000000 ) ) ;
#161588=TOROIDAL_SURFACE ( 'NONE', #57482, 0.4000000000000003553, 0.1000000000000000056 ) ;
#161635=CARTESIAN_POINT ( 'NONE',  ( -21.05000000000000071, 87.48912529308871910, -200.4231074845242802 ) ) ;
#161650=EDGE_CURVE ( 'NONE', #68241, #137554, #143321, .T. ) ;
#161651=ORIENTED_EDGE ( 'NONE', *, *, #700, .F. ) ;
#161656=AXIS2_PLACEMENT_3D ( 'NONE', #80981, #138380, #18459 ) ;
#161673=ORIENTED_EDGE ( 'NONE', *, *, #132873, .T. ) ;
#161691=ORIENTED_EDGE ( 'NONE', *, *, #125347, .T. ) ;
#161698=CARTESIAN_POINT ( 'NONE',  ( 22.50000000000000000, 68.20922040163929978, -203.6231074845244109 ) ) ;
#161702=EDGE_CURVE ( 'NONE', #230341, #236908, #157480, .T. ) ;
#161708=AXIS2_PLACEMENT_3D ( 'NONE', #65887, #206685, #187143 ) ;
#161745=DIRECTION ( 'NONE',  ( 0.000000000000000000, -0.6728971962617862346, 0.7397360091701815632 ) ) ;
#161767=CARTESIAN_POINT ( 'NONE',  ( 21.14999999999999858, 64.35000000001258513, -191.3731074845244393 ) ) ;
#161775=ORIENTED_EDGE ( 'NONE', *, *, #99794, .T. ) ;
#161777=VERTEX_POINT ( 'NONE', #166780 ) ;
#161826=ORIENTED_EDGE ( 'NONE', *, *, #69419, .F. ) ;
#161827=VECTOR ( 'NONE', #132028, 1000.000000000000000 ) ;
#161829=VERTEX_POINT ( 'NONE', #89760 ) ;
#161848=CARTESIAN_POINT ( 'NONE',  ( 23.15000000000000213, 87.65000000001246860, -173.0231074845243029 ) ) ;
#161872=EDGE_CURVE ( 'NONE', #145080, #178265, #211622, .T. ) ;
#161891=CARTESIAN_POINT ( 'NONE',  ( -18.59999999999999787, 85.48068669529138219, -163.0819923157664562 ) ) ;
#161893=CIRCLE ( 'NONE', #16138, 0.1000000000000072220 ) ;
#161922=VERTEX_POINT ( 'NONE', #77899 ) ;
#161931=CIRCLE ( 'NONE', #3671, 0.2000000000000057288 ) ;
#162026=CIRCLE ( 'NONE', #241135, 0.09999999999998900047 ) ;
#162032=CARTESIAN_POINT ( 'NONE',  ( 20.94999999999999574, 74.83729825007462466, -195.4231074845243654 ) ) ;
#162096=EDGE_CURVE ( 'NONE', #99738, #99483, #43917, .T. ) ;
#162110=ORIENTED_EDGE ( 'NONE', *, *, #241721, .F. ) ;
#162124=VERTEX_POINT ( 'NONE', #110306 ) ;
#162130=FACE_OUTER_BOUND ( 'NONE', #187636, .T. ) ;
#162153=CIRCLE ( 'NONE', #199585, 0.1000000000000046685 ) ;
#162168=VECTOR ( 'NONE', #42316, 1000.000000000000000 ) ;
#162186=DIRECTION ( 'NONE',  ( 0.000000000000000000, -6.853228547068871147E-15, 1.000000000000000000 ) ) ;
#162221=EDGE_CURVE ( 'NONE', #215277, #53042, #95272, .T. ) ;
#162236=VECTOR ( 'NONE', #132816, 1000.000000000000000 ) ;
#162269=AXIS2_PLACEMENT_3D ( 'NONE', #89711, #46736, #123728 ) ;
#162307=EDGE_CURVE ( 'NONE', #211067, #24355, #161931, .T. ) ;
#162322=EDGE_CURVE ( 'NONE', #161829, #233373, #73783, .T. ) ;
#162356=ADVANCED_FACE ( 'NONE', ( #6733 ), #184086, .T. ) ;
#162375=DIRECTION ( 'NONE',  ( 0.000000000000000000, 0.000000000000000000, 1.000000000000000000 ) ) ;
#162385=CARTESIAN_POINT ( 'NONE',  ( -22.39999999999999858, 76.00000000001276135, -215.1726782920691505 ) ) ;
#162393=EDGE_CURVE ( 'NONE', #204559, #162455, #49662, .T. ) ;
#162401=CARTESIAN_POINT ( 'NONE',  ( -21.05000000000000071, 87.48912529308871910, -200.6231074845242688 ) ) ;
#162403=VECTOR ( 'NONE', #50356, 1000.000000000000000 ) ;
#162409=EDGE_CURVE ( 'NONE', #85479, #42935, #91175, .T. ) ;
#162424=CIRCLE ( 'NONE', #45888, 2.000000000000001776 ) ;
#162429=AXIS2_PLACEMENT_3D ( 'NONE', #166395, #51512, #46393 ) ;
#162435=FACE_OUTER_BOUND ( 'NONE', #171831, .T. ) ;
#162455=VERTEX_POINT ( 'NONE', #64148 ) ;
#162470=ORIENTED_EDGE ( 'NONE', *, *, #174879, .T. ) ;
#162485=EDGE_LOOP ( 'NONE', ( #150135, #92223, #61879, #249088, #164627, #115994, #143451 ) ) ;
#162493=DIRECTION ( 'NONE',  ( -1.000000000000000000, -0.000000000000000000, -0.000000000000000000 ) ) ;
#162498=EDGE_CURVE ( 'NONE', #37447, #119237, #28869, .T. ) ;
#162512=ORIENTED_EDGE ( 'NONE', *, *, #99537, .F. ) ;
#162513=ADVANCED_FACE ( 'NONE', ( #11898 ), #95449, .F. ) ;
#162521=DIRECTION ( 'NONE',  ( 1.000000000000000000, 0.000000000000000000, 0.000000000000000000 ) ) ;
#162529=DIRECTION ( 'NONE',  ( 0.000000000000000000, -0.9876197685951265681, -0.1568667991644790149 ) ) ;
#162554=DIRECTION ( 'NONE',  ( -1.000000000000000000, -0.000000000000000000, -0.000000000000000000 ) ) ;
#162571=EDGE_LOOP ( 'NONE', ( #204113, #112586, #36996, #119963 ) ) ;
#162576=CARTESIAN_POINT ( 'NONE',  ( 18.59999999999999076, 64.25000000001277556, -215.2731074845244450 ) ) ;
#162579=DIRECTION ( 'NONE',  ( 1.000000000000000000, -7.304098846218134667E-16, -5.100424963727255829E-30 ) ) ;
#162580=AXIS2_PLACEMENT_3D ( 'NONE', #23684, #103167, #104442 ) ;
#162585=CYLINDRICAL_SURFACE ( 'NONE', #193006, 0.09999999999998898659 ) ;
#162604=TOROIDAL_SURFACE ( 'NONE', #191674, 0.2000000000000000111, 0.1000000000000000056 ) ;
#162606=DIRECTION ( 'NONE',  ( 0.000000000000000000, -0.4930308989874980785, -0.8700118002898462599 ) ) ;
#162615=EDGE_CURVE ( 'NONE', #53042, #34471, #37205, .T. ) ;
#162630=ADVANCED_FACE ( 'NONE', ( #93964 ), #228746, .T. ) ;
#162646=CYLINDRICAL_SURFACE ( 'NONE', #247834, 0.09999999999998898659 ) ;
#162689=FACE_OUTER_BOUND ( 'NONE', #149281, .T. ) ;
#162691=VECTOR ( 'NONE', #48024, 1000.000000000000000 ) ;
#162693=VECTOR ( 'NONE', #170585, 1000.000000000000000 ) ;
#162699=EDGE_CURVE ( 'NONE', #109083, #42440, #139504, .T. ) ;
#162717=EDGE_CURVE ( 'NONE', #77018, #252194, #41317, .T. ) ;
#162735=AXIS2_PLACEMENT_3D ( 'NONE', #94394, #253464, #154421 ) ;
#162746=ORIENTED_EDGE ( 'NONE', *, *, #43392, .F. ) ;
#162748=DIRECTION ( 'NONE',  ( 0.000000000000000000, -6.982962677686266711E-15, 1.000000000000000000 ) ) ;
#162749=FACE_OUTER_BOUND ( 'NONE', #140825, .T. ) ;
#162771=AXIS2_PLACEMENT_3D ( 'NONE', #144370, #160143, #100114 ) ;
#162773=DIRECTION ( 'NONE',  ( 1.000000000000000000, 0.000000000000000000, 0.000000000000000000 ) ) ;
#162790=ORIENTED_EDGE ( 'NONE', *, *, #105404, .T. ) ;
#162795=EDGE_CURVE ( 'NONE', #200485, #91017, #194865, .T. ) ;
#162803=VECTOR ( 'NONE', #37172, 1000.000000000000000 ) ;
#162804=PLANE ( 'NONE',  #85041 ) ;
#162807=EDGE_CURVE ( 'NONE', #670, #244528, #233021, .T. ) ;
#162819=DIRECTION ( 'NONE',  ( -1.000000000000000000, 0.000000000000000000, -0.000000000000000000 ) ) ;
#162823=EDGE_CURVE ( 'NONE', #165929, #66231, #253827, .T. ) ;
#162872=FACE_OUTER_BOUND ( 'NONE', #74026, .T. ) ;
#162875=DIRECTION ( 'NONE',  ( -1.836970198721029934E-16, -1.000000000000000000, -6.982962677686266711E-15 ) ) ;
#162889=ADVANCED_FACE ( 'NONE', ( #126373 ), #95625, .F. ) ;
#162914=LINE ( 'NONE', #119944, #59176 ) ;
#162928=DIRECTION ( 'NONE',  ( 0.000000000000000000, -7.056502275159890832E-15, 1.000000000000000000 ) ) ;
#162942=ORIENTED_EDGE ( 'NONE', *, *, #147346, .F. ) ;
#162943=ADVANCED_FACE ( 'NONE', ( #23458 ), #20641, .F. ) ;
#162952=VERTEX_POINT ( 'NONE', #131502 ) ;
#162956=DIRECTION ( 'NONE',  ( -1.000000000000000000, 0.000000000000000000, -0.000000000000000000 ) ) ;
#162964=CARTESIAN_POINT ( 'NONE',  ( 21.12769345151713196, 65.28071232307203786, -191.2756271383269393 ) ) ;
#162982=DIRECTION ( 'NONE',  ( 1.000000000000000000, 0.000000000000000000, 0.000000000000000000 ) ) ;
#162990=CARTESIAN_POINT ( 'NONE',  ( 21.05000000000000071, 76.00000000001267608, -203.4231074845243654 ) ) ;
#162993=ORIENTED_EDGE ( 'NONE', *, *, #30509, .F. ) ;
#163002=CARTESIAN_POINT ( 'NONE',  ( 23.25000000000000000, 87.65000000001269598, -203.5231074845243029 ) ) ;
#163028=AXIS2_PLACEMENT_3D ( 'NONE', #47403, #126960, #227336 ) ;
#163056=VERTEX_POINT ( 'NONE', #115797 ) ;
#163070=VERTEX_POINT ( 'NONE', #235728 ) ;
#163098=CARTESIAN_POINT ( 'NONE',  ( -18.59999999999999787, 74.73821383144760944, -195.4366085209788935 ) ) ;
#163131=VERTEX_POINT ( 'NONE', #177078 ) ;
#163143=CYLINDRICAL_SURFACE ( 'NONE', #9133, 0.09999999999999939493 ) ;
#163167=CARTESIAN_POINT ( 'NONE',  ( -18.47140463609787986, 85.67147468523329223, -163.3503470262502617 ) ) ;
#163181=DIRECTION ( 'NONE',  ( 0.000000000000000000, 0.000000000000000000, -1.000000000000000000 ) ) ;
#163198=DIRECTION ( 'NONE',  ( 1.000000000000000000, 0.000000000000000000, 0.000000000000000000 ) ) ;
#163229=CARTESIAN_POINT ( 'NONE',  ( -23.15000000000000213, 74.00000000001259082, -190.2984855617622770 ) ) ;
#163242=ORIENTED_EDGE ( 'NONE', *, *, #10597, .F. ) ;
#163259=DIRECTION ( 'NONE',  ( -1.000000000000000000, -0.000000000000000000, -0.000000000000000000 ) ) ;
#163277=DIRECTION ( 'NONE',  ( -7.304098846218134667E-16, -1.000000000000000000, -6.982962677686267499E-15 ) ) ;
#163381=AXIS2_PLACEMENT_3D ( 'NONE', #133242, #157986, #116260 ) ;
#163515=CARTESIAN_POINT ( 'NONE',  ( -23.15000000000000213, 76.00000000001244871, -170.0231074845243597 ) ) ;
#163529=DIRECTION ( 'NONE',  ( 0.000000000000000000, 0.000000000000000000, 1.000000000000000000 ) ) ;
#163572=ORIENTED_EDGE ( 'NONE', *, *, #212170, .F. ) ;
#163578=ORIENTED_EDGE ( 'NONE', *, *, #96116, .T. ) ;
#163586=AXIS2_PLACEMENT_3D ( 'NONE', #65208, #246426, #86025 ) ;
#163590=CARTESIAN_POINT ( 'NONE',  ( -20.54999999999999716, 76.00000000001244871, -170.0231074845243597 ) ) ;
#163704=ORIENTED_EDGE ( 'NONE', *, *, #100263, .F. ) ;
#163707=( BOUNDED_CURVE ( )  B_SPLINE_CURVE ( 3, ( #234796, #138238, #36629, #212674 ),
 .UNSPECIFIED., .F., .T. ) 
 B_SPLINE_CURVE_WITH_KNOTS ( ( 4, 4 ),
 ( 1.570796326794895448, 3.141592653589791784 ),
 .UNSPECIFIED. ) 
 CURVE ( )  GEOMETRIC_REPRESENTATION_ITEM ( )  RATIONAL_B_SPLINE_CURVE ( ( 1.000000000000000000, 0.8047378541243650485, 0.8047378541243650485, 1.000000000000000000 ) ) 
 REPRESENTATION_ITEM ( '' )  );
#163712=FACE_OUTER_BOUND ( 'NONE', #94193, .T. ) ;
#163730=DIRECTION ( 'NONE',  ( 0.000000000000000000, -6.938893903907222067E-15, 1.000000000000000000 ) ) ;
#163731=CIRCLE ( 'NONE', #51270, 4.000000000000003553 ) ;
#163783=DIRECTION ( 'NONE',  ( 0.000000000000000000, -1.000000000000000000, -6.982962677686265922E-15 ) ) ;
#163814=CARTESIAN_POINT ( 'NONE',  ( 21.10320863425824811, 69.59972261355351009, -203.5481297357515302 ) ) ;
#163815=CARTESIAN_POINT ( 'NONE',  ( 20.94999999999999574, 76.00000000001267608, -203.5231074845243597 ) ) ;
#163864=CARTESIAN_POINT ( 'NONE',  ( 23.15000000000000213, 85.50000000001261924, -193.6291383618718385 ) ) ;
#163871=VECTOR ( 'NONE', #149360, 1000.000000000000000 ) ;
#163891=EDGE_LOOP ( 'NONE', ( #139275, #55041, #89305, #132690 ) ) ;
#163924=CARTESIAN_POINT ( 'NONE',  ( -20.54999999999999716, 73.50000000001254818, -183.2477294072864709 ) ) ;
#163925=FACE_OUTER_BOUND ( 'NONE', #225334, .T. ) ;
#163941=ORIENTED_EDGE ( 'NONE', *, *, #247830, .F. ) ;
#163952=ADVANCED_FACE ( 'NONE', ( #202427 ), #96164, .T. ) ;
#163973=AXIS2_PLACEMENT_3D ( 'NONE', #158542, #61991, #221041 ) ;
#163975=DIRECTION ( 'NONE',  ( 1.000000000000000000, 0.000000000000000000, 0.000000000000000000 ) ) ;
#164022=CARTESIAN_POINT ( 'NONE',  ( -20.94999999999999929, 87.75000000001266187, -200.4231074845242802 ) ) ;
#164053=ORIENTED_EDGE ( 'NONE', *, *, #239702, .T. ) ;
#164117=CARTESIAN_POINT ( 'NONE',  ( -21.05000000000000071, 74.75000000001261924, -195.5231074845243597 ) ) ;
#164135=AXIS2_PLACEMENT_3D ( 'NONE', #243686, #144571, #33340 ) ;
#164138=CARTESIAN_POINT ( 'NONE',  ( 22.59999999999999432, 75.90000000001276703, -215.1726782920691505 ) ) ;
#164171=ADVANCED_FACE ( 'NONE', ( #175836 ), #2284, .T. ) ;
#164190=CARTESIAN_POINT ( 'NONE',  ( 20.85000000000000142, 64.35000000001249987, -176.8069731475025321 ) ) ;
#164231=CARTESIAN_POINT ( 'NONE',  ( -20.94999999999999929, 76.00000000001244871, -170.0231074845243597 ) ) ;
#164247=VERTEX_POINT ( 'NONE', #67413 ) ;
#164250=EDGE_LOOP ( 'NONE', ( #3895, #128728, #200372, #161006 ) ) ;
#164251=DIRECTION ( 'NONE',  ( -0.8660254037844653530, 0.000000000000000000, -0.4999999999999539257 ) ) ;
#164256=CARTESIAN_POINT ( 'NONE',  ( 20.94999999999999929, 87.65000000001246860, -172.9231074845242802 ) ) ;
#164297=CARTESIAN_POINT ( 'NONE',  ( -20.54999999999999716, 74.00000000001254818, -182.8477294072864652 ) ) ;
#164300=CARTESIAN_POINT ( 'NONE',  ( 18.59999999999999076, 69.35000000001254250, -182.3731074845244109 ) ) ;
#164304=ADVANCED_FACE ( 'NONE', ( #183517 ), #45286, .F. ) ;
#164331=VERTEX_POINT ( 'NONE', #247328 ) ;
#164344=CARTESIAN_POINT ( 'NONE',  ( 21.05000000000000071, 67.12338541492552224, -195.1380270056797599 ) ) ;
#164368=CARTESIAN_POINT ( 'NONE',  ( 18.50000000000000711, 85.41907808086196496, -163.1931821343160323 ) ) ;
#164370=ORIENTED_EDGE ( 'NONE', *, *, #158316, .T. ) ;
#164400=EDGE_CURVE ( 'NONE', #165343, #105902, #100436, .T. ) ;
#164408=ORIENTED_EDGE ( 'NONE', *, *, #57861, .T. ) ;
#164454=( BOUNDED_CURVE ( )  B_SPLINE_CURVE ( 3, ( #204275, #8658, #225113, #46482 ),
 .UNSPECIFIED., .F., .F. ) 
 B_SPLINE_CURVE_WITH_KNOTS ( ( 4, 4 ),
 ( 4.712388980384689674, 6.283185307179586232 ),
 .UNSPECIFIED. ) 
 CURVE ( )  GEOMETRIC_REPRESENTATION_ITEM ( )  RATIONAL_B_SPLINE_CURVE ( ( 1.000000000000000000, 0.8047378541243649375, 0.8047378541243649375, 1.000000000000000000 ) ) 
 REPRESENTATION_ITEM ( '' )  );
#164462=DIRECTION ( 'NONE',  ( 0.000000000000000000, -6.982962677686266711E-15, 1.000000000000000000 ) ) ;
#164464=CARTESIAN_POINT ( 'NONE',  ( -20.54999999999999716, 73.60000000001251408, -179.9170766071768242 ) ) ;
#164472=ORIENTED_EDGE ( 'NONE', *, *, #155726, .T. ) ;
#164480=AXIS2_PLACEMENT_3D ( 'NONE', #137432, #98283, #141305 ) ;
#164500=DIRECTION ( 'NONE',  ( 1.000000000000000000, 0.000000000000000000, 0.000000000000000000 ) ) ;
#164501=CARTESIAN_POINT ( 'NONE',  ( 18.59999999999999432, 77.83585931145600512, -158.5186683157258187 ) ) ;
#164557=CARTESIAN_POINT ( 'NONE',  ( -21.14999999999999858, 76.10000000001272724, -209.7731074845243597 ) ) ;
#164560=DIRECTION ( 'NONE',  ( 0.000000000000000000, -0.9999631594459053030, -0.008583690987162452199 ) ) ;
#164600=DIRECTION ( 'NONE',  ( 0.000000000000000000, -0.3738317757008748909, -0.9274965247785733613 ) ) ;
#164627=ORIENTED_EDGE ( 'NONE', *, *, #63600, .T. ) ;
#164632=EDGE_CURVE ( 'NONE', #116802, #75446, #196312, .T. ) ;
#164651=CARTESIAN_POINT ( 'NONE',  ( -21.05000000000046967, 69.55922910635128176, -203.5055102975169348 ) ) ;
#164660=AXIS2_PLACEMENT_3D ( 'NONE', #17226, #176306, #255773 ) ;
#164687=DIRECTION ( 'NONE',  ( 1.000000000000000000, 0.000000000000000000, 0.000000000000000000 ) ) ;
#164700=LINE ( 'NONE', #99550, #226432 ) ;
#164719=DIRECTION ( 'NONE',  ( 1.000000000000000000, 0.000000000000000000, 0.000000000000000000 ) ) ;
#164731=DIRECTION ( 'NONE',  ( -0.000000000000000000, -0.8660254037844377084, -0.5000000000000016653 ) ) ;
#164774=DIRECTION ( 'NONE',  ( 0.000000000000000000, -7.116814260417660624E-15, 1.000000000000000000 ) ) ;
#164795=CIRCLE ( 'NONE', #202397, 0.09999999999999939493 ) ;
#164803=FACE_OUTER_BOUND ( 'NONE', #474, .T. ) ;
#164814=CARTESIAN_POINT ( 'NONE',  ( 21.14999999999999858, 76.00000000001260503, -191.3731074845243540 ) ) ;
#164835=AXIS2_PLACEMENT_3D ( 'NONE', #170781, #228144, #88598 ) ;
#164861=CARTESIAN_POINT ( 'NONE',  ( 23.15000000000000213, 87.65000000001275282, -215.2731074845242745 ) ) ;
#164874=CARTESIAN_POINT ( 'NONE',  ( -21.14999999999999858, 87.75000000001267608, -203.5231074845243029 ) ) ;
#164886=VECTOR ( 'NONE', #46187, 1000.000000000000000 ) ;
#164908=CARTESIAN_POINT ( 'NONE',  ( 20.54374330479327426, 65.49498968578961922, -195.7974238496363455 ) ) ;
#164918=CARTESIAN_POINT ( 'NONE',  ( 21.11825140030062897, 75.99279637937966925, -209.9685150499435906 ) ) ;
#164919=DIRECTION ( 'NONE',  ( 0.000000000000000000, -0.4930308989874980785, -0.8700118002898462599 ) ) ;
#164934=CARTESIAN_POINT ( 'NONE',  ( -22.45437739390952814, 76.00000000001276135, -215.1726782961185620 ) ) ;
#164970=CIRCLE ( 'NONE', #15136, 6.329289321881370611 ) ;
#165009=AXIS2_PLACEMENT_3D ( 'NONE', #25001, #245314, #207481 ) ;
#165017=DIRECTION ( 'NONE',  ( 0.000000000000000000, 0.000000000000000000, -1.000000000000000000 ) ) ;
#165027=EDGE_CURVE ( 'NONE', #105902, #41142, #31432, .T. ) ;
#165037=CARTESIAN_POINT ( 'NONE',  ( 18.60000000000000142, 85.48068669529135377, -163.0819923157664562 ) ) ;
#165045=ORIENTED_EDGE ( 'NONE', *, *, #131979, .T. ) ;
#165093=VERTEX_POINT ( 'NONE', #139463 ) ;
#165158=CARTESIAN_POINT ( 'NONE',  ( 18.52928932188133970, 65.72071067813116940, -178.8731074845244109 ) ) ;
#165184=TOROIDAL_SURFACE ( 'NONE', #52745, 0.2000000000000000111, 0.1000000000000000056 ) ;
#165186=VERTEX_POINT ( 'NONE', #36568 ) ;
#165229=CARTESIAN_POINT ( 'NONE',  ( -21.09813707148783735, 75.96864850048329743, -209.9081695902610534 ) ) ;
#165230=ORIENTED_EDGE ( 'NONE', *, *, #212802, .T. ) ;
#165265=ORIENTED_EDGE ( 'NONE', *, *, #77061, .F. ) ;
#165284=ORIENTED_EDGE ( 'NONE', *, *, #44046, .T. ) ;
#165319=ORIENTED_EDGE ( 'NONE', *, *, #185100, .T. ) ;
#165329=ORIENTED_EDGE ( 'NONE', *, *, #139697, .F. ) ;
#165343=VERTEX_POINT ( 'NONE', #77086 ) ;
#165380=VERTEX_POINT ( 'NONE', #219153 ) ;
#165387=CARTESIAN_POINT ( 'NONE',  ( -18.50000000000000000, 66.65000000001253966, -182.3731074845244393 ) ) ;
#165448=DIRECTION ( 'NONE',  ( -0.000000000000000000, -0.8700118002898356018, 0.4930308989875170078 ) ) ;
#165454=DIRECTION ( 'NONE',  ( 0.000000000000000000, -6.982962677686266711E-15, 1.000000000000000000 ) ) ;
#165486=DIRECTION ( 'NONE',  ( 0.000000000000000000, -0.8660254037844377084, -0.5000000000000016653 ) ) ;
#165502=ORIENTED_EDGE ( 'NONE', *, *, #204550, .T. ) ;
#165506=ORIENTED_EDGE ( 'NONE', *, *, #146286, .F. ) ;
#165507=DIRECTION ( 'NONE',  ( 1.000000000000000000, 0.000000000000000000, 0.000000000000000000 ) ) ;
#165522=LINE ( 'NONE', #126378, #174997 ) ;
#165529=ORIENTED_EDGE ( 'NONE', *, *, #253996, .F. ) ;
#165530=CARTESIAN_POINT ( 'NONE',  ( -23.15000000000000213, 87.65000000001246860, -173.1231074845242688 ) ) ;
#165600=CARTESIAN_POINT ( 'NONE',  ( 20.94999999999999929, 64.35000000001249987, -176.8069731475025321 ) ) ;
#165606=ORIENTED_EDGE ( 'NONE', *, *, #92770, .T. ) ;
#165620=CARTESIAN_POINT ( 'NONE',  ( 18.59999999999999432, 77.16270174995064224, -195.4231074845243370 ) ) ;
#165694=VERTEX_POINT ( 'NONE', #1068 ) ;
#165705=CIRCLE ( 'NONE', #61627, 0.2000000000000057288 ) ;
#165712=CARTESIAN_POINT ( 'NONE',  ( 18.50000000000000000, 85.40000000001263913, -196.5238218066854472 ) ) ;
#165724=CIRCLE ( 'NONE', #53281, 0.09999999999999939493 ) ;
#165726=DIRECTION ( 'NONE',  ( -1.000000000000000000, -0.000000000000000000, -0.000000000000000000 ) ) ;
#165734=CARTESIAN_POINT ( 'NONE',  ( 20.85000000000000142, 87.75000000001246292, -172.9231074845242802 ) ) ;
#165806=CARTESIAN_POINT ( 'NONE',  ( -18.59999999999999787, 77.83534155023700407, -191.9679561919613491 ) ) ;
#165833=DIRECTION ( 'NONE',  ( 0.000000000000000000, -8.338584948901395817E-15, 1.000000000000000000 ) ) ;
#165835=DIRECTION ( 'NONE',  ( 1.000000000000000000, 0.000000000000000000, 0.000000000000000000 ) ) ;
#165860=ORIENTED_EDGE ( 'NONE', *, *, #198572, .F. ) ;
#165892=( BOUNDED_CURVE ( )  B_SPLINE_CURVE ( 3, ( #129861, #109012, #251088, #167747 ),
 .UNSPECIFIED., .F., .F. ) 
 B_SPLINE_CURVE_WITH_KNOTS ( ( 4, 4 ),
 ( 3.141592653589793116, 4.712388980384689674 ),
 .UNSPECIFIED. ) 
 CURVE ( )  GEOMETRIC_REPRESENTATION_ITEM ( )  RATIONAL_B_SPLINE_CURVE ( ( 1.000000000000000000, 0.8047378541243649375, 0.8047378541243649375, 1.000000000000000000 ) ) 
 REPRESENTATION_ITEM ( '' )  );
#165929=VERTEX_POINT ( 'NONE', #35770 ) ;
#165960=ADVANCED_FACE ( 'NONE', ( #192268 ), #13619, .F. ) ;
#165971=EDGE_CURVE ( 'NONE', #100336, #62026, #130414, .T. ) ;
#166001=EDGE_CURVE ( 'NONE', #144129, #257328, #117839, .T. ) ;
#166018=ORIENTED_EDGE ( 'NONE', *, *, #115913, .T. ) ;
#166024=FACE_OUTER_BOUND ( 'NONE', #47173, .T. ) ;
#166039=CARTESIAN_POINT ( 'NONE',  ( 18.59999999999998366, 76.00000000001244871, -170.0231074845243597 ) ) ;
#166051=ADVANCED_FACE ( 'NONE', ( #162130 ), #155267, .T. ) ;
#166110=EDGE_CURVE ( 'NONE', #255597, #184002, #223353, .T. ) ;
#166128=DIRECTION ( 'NONE',  ( -1.836970198721029934E-16, -1.000000000000000000, -6.982962677686266711E-15 ) ) ;
#166150=ORIENTED_EDGE ( 'NONE', *, *, #100793, .F. ) ;
#166159=DIRECTION ( 'NONE',  ( 1.000000000000000000, 0.000000000000000000, 0.000000000000000000 ) ) ;
#166189=AXIS2_PLACEMENT_3D ( 'NONE', #64073, #185308, #241441 ) ;
#166213=DIRECTION ( 'NONE',  ( 2.952720810173289112E-16, 1.000000000000000000, -6.088138035986627436E-46 ) ) ;
#166249=ORIENTED_EDGE ( 'NONE', *, *, #162322, .T. ) ;
#166262=AXIS2_PLACEMENT_3D ( 'NONE', #114363, #208350, #188756 ) ;
#166268=CYLINDRICAL_SURFACE ( 'NONE', #23156, 0.5000000000000004441 ) ;
#166299=AXIS2_PLACEMENT_3D ( 'NONE', #3509, #83021, #21813 ) ;
#166360=CARTESIAN_POINT ( 'NONE',  ( 18.59999996954842771, 85.52320413787099085, -163.1400657726075565 ) ) ;
#166370=CARTESIAN_POINT ( 'NONE',  ( -20.94999999999999929, 77.83585931145600512, -158.5186683157258187 ) ) ;
#166395=CARTESIAN_POINT ( 'NONE',  ( 20.94999999999999574, 77.83534155023700407, -191.9679561919613491 ) ) ;
#166413=CARTESIAN_POINT ( 'NONE',  ( -23.15000000000000213, 76.00000000001264766, -199.4731074845243484 ) ) ;
#166415=EDGE_CURVE ( 'NONE', #162455, #15440, #30103, .T. ) ;
#166434=CIRCLE ( 'NONE', #170557, 11.80000000000000426 ) ;
#166436=FACE_OUTER_BOUND ( 'NONE', #178089, .T. ) ;
#166444=CARTESIAN_POINT ( 'NONE',  ( -1.739115166359751801E-14, 64.35000000001255671, -182.1731074845244507 ) ) ;
#166470=CARTESIAN_POINT ( 'NONE',  ( 18.52928932188134326, 65.72071067813118361, -178.8145288407617386 ) ) ;
#166476=CARTESIAN_POINT ( 'NONE',  ( -23.15000000000000213, 85.50000000001261924, -193.6291383618718385 ) ) ;
#166501=EDGE_CURVE ( 'NONE', #108178, #91017, #237499, .T. ) ;
#166504=CARTESIAN_POINT ( 'NONE',  ( 18.59999999999999787, 87.75000000001251976, -182.1731074845242802 ) ) ;
#166506=CARTESIAN_POINT ( 'NONE',  ( -21.00023020733438628, 69.60913075474496736, -203.5231074845244166 ) ) ;
#166536=CIRCLE ( 'NONE', #70678, 0.2000000000000057288 ) ;
#166539=CARTESIAN_POINT ( 'NONE',  ( 20.94999999999999929, 85.00000000001251976, -179.5170766071767332 ) ) ;
#166545=CARTESIAN_POINT ( 'NONE',  ( -21.08884785362073089, 75.95021690494600364, -209.8803008519499826 ) ) ;
#166546=ORIENTED_EDGE ( 'NONE', *, *, #189330, .F. ) ;
#166551=FACE_OUTER_BOUND ( 'NONE', #14942, .T. ) ;
#166583=EDGE_CURVE ( 'NONE', #195224, #155749, #30278, .T. ) ;
#166594=CARTESIAN_POINT ( 'NONE',  ( 22.39999999999999147, 68.20922040163929978, -203.5231074845244166 ) ) ;
#166602=ORIENTED_EDGE ( 'NONE', *, *, #49607, .F. ) ;
#166628=VERTEX_POINT ( 'NONE', #225600 ) ;
#166632=DIRECTION ( 'NONE',  ( 0.000000000000000000, 3.469446951953514729E-13, -1.000000000000000000 ) ) ;
#166636=AXIS2_PLACEMENT_3D ( 'NONE', #94472, #224689, #140007 ) ;
#166644=VERTEX_POINT ( 'NONE', #86086 ) ;
#166669=LINE ( 'NONE', #124951, #239199 ) ;
#166674=CARTESIAN_POINT ( 'NONE',  ( 21.05000000000000071, 71.00000000001253397, -182.0283735034374786 ) ) ;
#166681=SPHERICAL_SURFACE ( 'NONE', #94968, 0.1000000000000000056 ) ;
#166689=TOROIDAL_SURFACE ( 'NONE', #162580, 7.800000000000000711, 0.1000000000000000056 ) ;
#166695=CARTESIAN_POINT ( 'NONE',  ( -18.59999999999999787, 64.25000000001254818, -182.1731074845244507 ) ) ;
#166710=CARTESIAN_POINT ( 'NONE',  ( -21.04999999999999716, 75.98514436511885606, -209.8674665265682791 ) ) ;
#166711=DIRECTION ( 'NONE',  ( -1.000000000000000000, -0.000000000000000000, -0.000000000000000000 ) ) ;
#166730=LINE ( 'NONE', #147123, #162691 ) ;
#166766=EDGE_CURVE ( 'NONE', #203688, #217036, #38634, .T. ) ;
#166780=CARTESIAN_POINT ( 'NONE',  ( 18.49999999999999289, 65.50857864377520912, -178.6731074845244223 ) ) ;
#166794=EDGE_LOOP ( 'NONE', ( #136943, #101394, #105885, #109748 ) ) ;
#166814=CARTESIAN_POINT ( 'NONE',  ( -20.64999999999999858, 85.00000000001261924, -193.6291383618718385 ) ) ;
#166835=DIRECTION ( 'NONE',  ( 1.000000000000000000, 0.000000000000000000, 0.000000000000000000 ) ) ;
#166849=DIRECTION ( 'NONE',  ( -0.000000000000000000, -6.982962677686266711E-15, 1.000000000000000000 ) ) ;
#166854=VERTEX_POINT ( 'NONE', #212511 ) ;
#166858=EDGE_LOOP ( 'NONE', ( #156426, #208790, #171816, #216548, #236662, #250641 ) ) ;
#166865=EDGE_CURVE ( 'NONE', #160419, #28788, #46808, .T. ) ;
#166875=VERTEX_POINT ( 'NONE', #70453 ) ;
#166912=VERTEX_POINT ( 'NONE', #181084 ) ;
#166921=EDGE_CURVE ( 'NONE', #81149, #183114, #98926, .T. ) ;
#166929=EDGE_LOOP ( 'NONE', ( #151434, #116926, #133650, #184282 ) ) ;
#166981=AXIS2_PLACEMENT_3D ( 'NONE', #94005, #95304, #146586 ) ;
#166983=CARTESIAN_POINT ( 'NONE',  ( 20.94999999999999574, 77.36087058720467269, -195.4501095574333931 ) ) ;
#167029=DIRECTION ( 'NONE',  ( 0.000000000000000000, 0.000000000000000000, 1.000000000000000000 ) ) ;
#167050=ADVANCED_FACE ( 'NONE', ( #46669 ), #89170, .T. ) ;
#167056=CIRCLE ( 'NONE', #200339, 11.89999999999999325 ) ;
#167068=ADVANCED_FACE ( 'NONE', ( #247451, #106635, #148359 ), #162804, .F. ) ;
#167087=B_SPLINE_CURVE_WITH_KNOTS ( 'NONE', 3,
 ( #180579, #38505, #155902, #18922, #1914, #78879 ),
 .UNSPECIFIED., .F., .F.,
 ( 4, 2, 4 ),
 ( 0.000000000000000000, 0.0001497467027049226784, 0.0002994934054098453567 ),
 .UNSPECIFIED. ) ;
#167107=EDGE_CURVE ( 'NONE', #34471, #132760, #166669, .T. ) ;
#167141=CARTESIAN_POINT ( 'NONE',  ( -22.44366136229477249, 75.99065843052669322, -215.1728260419982917 ) ) ;
#167157=VECTOR ( 'NONE', #201264, 1000.000000000000000 ) ;
#167173=EDGE_CURVE ( 'NONE', #154279, #152534, #255722, .T. ) ;
#167175=DIRECTION ( 'NONE',  ( 0.000000000000000000, -0.1568667991644355497, -0.9876197685951332295 ) ) ;
#167204=CARTESIAN_POINT ( 'NONE',  ( 21.14999999999999503, 64.35000000001267040, -203.4231074845244507 ) ) ;
#167218=AXIS2_PLACEMENT_3D ( 'NONE', #64378, #103474, #205144 ) ;
#167225=DIRECTION ( 'NONE',  ( 2.952720810173289112E-16, 1.000000000000000000, 6.982962677686266711E-15 ) ) ;
#167232=ORIENTED_EDGE ( 'NONE', *, *, #231383, .F. ) ;
#167282=DIRECTION ( 'NONE',  ( 0.000000000000000000, 7.056502275159890832E-15, -1.000000000000000000 ) ) ;
#167288=CARTESIAN_POINT ( 'NONE',  ( -18.50000000000000711, 85.41920341803927386, -196.2753216740956077 ) ) ;
#167292=CARTESIAN_POINT ( 'NONE',  ( -23.25000000000000000, 68.97833521811233481, -166.1895420826271277 ) ) ;
#167303=ORIENTED_EDGE ( 'NONE', *, *, #187633, .T. ) ;
#167355=CIRCLE ( 'NONE', #233960, 7.899999999999990585 ) ;
#167406=CARTESIAN_POINT ( 'NONE',  ( -18.50000972452446035, 65.70673848567030007, -164.5638252334829303 ) ) ;
#167408=CARTESIAN_POINT ( 'NONE',  ( 23.14999999999999503, 64.35000000001275566, -215.2731074845244450 ) ) ;
#167437=EDGE_CURVE ( 'NONE', #68342, #102259, #9483, .T. ) ;
#167471=CARTESIAN_POINT ( 'NONE',  ( 20.99749315643150638, 64.25000000001249134, -177.0379132532823974 ) ) ;
#167484=DIRECTION ( 'NONE',  ( 1.000000000000000000, -7.304098846218134667E-16, -5.100424963727256530E-30 ) ) ;
#167497=CIRCLE ( 'NONE', #88318, 0.09999999999999134581 ) ;
#167511=ORIENTED_EDGE ( 'NONE', *, *, #238565, .T. ) ;
#167548=CARTESIAN_POINT ( 'NONE',  ( -23.15000000000000213, 71.75000000001259082, -191.2731074845243882 ) ) ;
#167559=DIRECTION ( 'NONE',  ( 0.000000000000000000, 0.000000000000000000, 1.000000000000000000 ) ) ;
#167602=AXIS2_PLACEMENT_3D ( 'NONE', #247684, #78019, #58438 ) ;
#167624=CARTESIAN_POINT ( 'NONE',  ( 18.50000000000000000, 85.50000000001263345, -196.4910380878246201 ) ) ;
#167630=FACE_OUTER_BOUND ( 'NONE', #3707, .T. ) ;
#167631=CARTESIAN_POINT ( 'NONE',  ( -20.54999999999999716, 76.00000000001267608, -203.5231074845243597 ) ) ;
#167638=DIRECTION ( 'NONE',  ( 0.000000000000000000, -1.000000000000000000, -6.352154140967427193E-15 ) ) ;
#167648=AXIS2_PLACEMENT_3D ( 'NONE', #159448, #2910, #79866 ) ;
#167680=VECTOR ( 'NONE', #136563, 1000.000000000000000 ) ;
#167702=CIRCLE ( 'NONE', #163586, 0.2000000000000057288 ) ;
#167713=CARTESIAN_POINT ( 'NONE',  ( 23.14999999999999147, 76.00000000001267608, -203.5231074845243597 ) ) ;
#167714=ORIENTED_EDGE ( 'NONE', *, *, #77061, .T. ) ;
#167722=AXIS2_PLACEMENT_3D ( 'NONE', #215533, #116450, #17352 ) ;
#167747=CARTESIAN_POINT ( 'NONE',  ( -21.05000000000000071, 64.35000000001264198, -196.7392418215462726 ) ) ;
#167753=EDGE_CURVE ( 'NONE', #152240, #84905, #167355, .T. ) ;
#167755=DIRECTION ( 'NONE',  ( -3.265361837132813093E-16, -1.000000000000000000, -6.982962677686266711E-15 ) ) ;
#167757=ADVANCED_FACE ( 'NONE', ( #249112 ), #87434, .F. ) ;
#167790=CARTESIAN_POINT ( 'NONE',  ( -21.07016717456945898, 69.67905916191242000, -203.5231074845244450 ) ) ;
#167796=LINE ( 'NONE', #52942, #162403 ) ;
#167806=DIRECTION ( 'NONE',  ( 1.000000000000000000, 0.000000000000000000, 0.000000000000000000 ) ) ;
#167809=DIRECTION ( 'NONE',  ( 1.000000000000000000, -3.265361837132813093E-16, -2.280189983783949500E-30 ) ) ;
#167824=ORIENTED_EDGE ( 'NONE', *, *, #45193, .F. ) ;
#167831=ORIENTED_EDGE ( 'NONE', *, *, #155993, .F. ) ;
#167850=CARTESIAN_POINT ( 'NONE',  ( -21.05000000000000071, 74.83729825007462466, -195.4231074845243654 ) ) ;
#167854=FACE_OUTER_BOUND ( 'NONE', #252886, .T. ) ;
#167862=EDGE_CURVE ( 'NONE', #198292, #109096, #121584, .T. ) ;
#167863=DIRECTION ( 'NONE',  ( 0.000000000000000000, -1.000000000000000000, -6.860497997771531562E-15 ) ) ;
#167877=VERTEX_POINT ( 'NONE', #6619 ) ;
#167905=B_SPLINE_CURVE_WITH_KNOTS ( 'NONE', 3,
 ( #21335, #159546, #18738, #180391, #1727, #257291 ),
 .UNSPECIFIED., .F., .F.,
 ( 4, 2, 4 ),
 ( 0.000000000000000000, 0.0001569047307838623796, 0.0003138094615677247592 ),
 .UNSPECIFIED. ) ;
#167913=CYLINDRICAL_SURFACE ( 'NONE', #141886, 0.09999999999998898659 ) ;
#167914=ORIENTED_EDGE ( 'NONE', *, *, #216392, .F. ) ;
#167920=ORIENTED_EDGE ( 'NONE', *, *, #48442, .T. ) ;
#167972=AXIS2_PLACEMENT_3D ( 'NONE', #214592, #76358, #33443 ) ;
#167997=CARTESIAN_POINT ( 'NONE',  ( -21.04999999999999716, 76.01465611852667337, -210.0197940702928463 ) ) ;
#168000=PRODUCT_DEFINITION ( 'UNKNOWN', '', #140510, #81763 ) ;
#168014=CARTESIAN_POINT ( 'NONE',  ( 21.05000000000000071, 85.40000000001252545, -179.9170766071767389 ) ) ;
#168021=AXIS2_PLACEMENT_3D ( 'NONE', #221679, #66481, #43071 ) ;
#168029=DIRECTION ( 'NONE',  ( 1.000000000000000000, -0.000000000000000000, -0.000000000000000000 ) ) ;
#168052=LINE ( 'NONE', #183731, #121704 ) ;
#168064=ORIENTED_EDGE ( 'NONE', *, *, #56276, .T. ) ;
#168067=AXIS2_PLACEMENT_3D ( 'NONE', #175911, #71669, #211161 ) ;
#168108=ADVANCED_FACE ( 'NONE', ( #2454 ), #39051, .T. ) ;
#168125=DIRECTION ( 'NONE',  ( 0.000000000000000000, -5.551115123125777653E-14, 1.000000000000000000 ) ) ;
#168186=EDGE_LOOP ( 'NONE', ( #45156, #68287, #52088, #12006 ) ) ;
#168193=DIRECTION ( 'NONE',  ( 1.000000000000000000, 0.000000000000000000, 0.000000000000000000 ) ) ;
#168204=ORIENTED_EDGE ( 'NONE', *, *, #3641, .F. ) ;
#168290=B_SPLINE_CURVE_WITH_KNOTS ( 'NONE', 3,
 ( #238351, #41466, #235781, #178416, #177131, #195410, #174598, #36329, #79259, #157586 ),
 .UNSPECIFIED., .F., .F.,
 ( 4, 3, 3, 4 ),
 ( 0.000000000000000000, 0.0002000000000002785953, 0.001000000000045107602, 0.001967863649472123035 ),
 .UNSPECIFIED. ) ;
#168303=EDGE_CURVE ( 'NONE', #164247, #250604, #169288, .T. ) ;
#168337=DIRECTION ( 'NONE',  ( 1.000000000000000000, -7.304098846218134667E-16, -5.100424963727256530E-30 ) ) ;
#168344=AXIS2_PLACEMENT_3D ( 'NONE', #234658, #53457, #175994 ) ;
#168348=B_SPLINE_CURVE_WITH_KNOTS ( 'NONE', 3,
 ( #247616, #65121, #225462, #148524, #222906, #203361, #228059, #29883 ),
 .UNSPECIFIED., .F., .F.,
 ( 4, 2, 2, 4 ),
 ( 0.000000000000000000, 0.0001049670497869897433, 0.0002099340995739794867, 0.0004198681991479769711 ),
 .UNSPECIFIED. ) ;
#168356=AXIS2_PLACEMENT_3D ( 'NONE', #232929, #252447, #128680 ) ;
#168430=VECTOR ( 'NONE', #242013, 1000.000000000000000 ) ;
#168452=DIRECTION ( 'NONE',  ( 1.000000000000000000, 0.000000000000000000, 0.000000000000000000 ) ) ;
#168454=CARTESIAN_POINT ( 'NONE',  ( -20.54999999999999716, 74.05981308412474107, -190.6939882734710636 ) ) ;
#168472=ORIENTED_EDGE ( 'NONE', *, *, #133462, .F. ) ;
#168479=ORIENTED_EDGE ( 'NONE', *, *, #176462, .F. ) ;
#168485=ORIENTED_EDGE ( 'NONE', *, *, #254286, .F. ) ;
#168489=VECTOR ( 'NONE', #132093, 1000.000000000000000 ) ;
#168506=DIRECTION ( 'NONE',  ( 0.000000000000000000, -6.467318590049456648E-15, 1.000000000000000000 ) ) ;
#168539=TOROIDAL_SURFACE ( 'NONE', #235130, 0.9750000000000019762, 0.1000000000000000056 ) ;
#168577=VECTOR ( 'NONE', #236078, 1000.000000000000000 ) ;
#168618=EDGE_CURVE ( 'NONE', #160597, #14542, #80165, .T. ) ;
#168637=LINE ( 'NONE', #225947, #212319 ) ;
#168656=ADVANCED_FACE ( 'NONE', ( #65985 ), #184255, .F. ) ;
#168664=AXIS2_PLACEMENT_3D ( 'NONE', #21677, #77769, #215999 ) ;
#168670=DIRECTION ( 'NONE',  ( 2.715809747126117987E-16, 1.000000000000000000, 6.517943393102682774E-15 ) ) ;
#168672=EDGE_LOOP ( 'NONE', ( #116890, #220174, #92680, #104371 ) ) ;
#168704=LINE ( 'NONE', #129529, #168489 ) ;
#168724=FACE_OUTER_BOUND ( 'NONE', #7873, .T. ) ;
#168792=CARTESIAN_POINT ( 'NONE',  ( 21.05000000000000071, 85.50000000001251976, -179.9170766071767389 ) ) ;
#168809=CARTESIAN_POINT ( 'NONE',  ( 20.50589344625199217, 65.51681206853709227, -195.9501125058534114 ) ) ;
#168810=FACE_OUTER_BOUND ( 'NONE', #1087, .T. ) ;
#168827=ORIENTED_EDGE ( 'NONE', *, *, #212074, .T. ) ;
#168844=FACE_OUTER_BOUND ( 'NONE', #187929, .T. ) ;
#168851=FACE_OUTER_BOUND ( 'NONE', #27650, .T. ) ;
#168875=AXIS2_PLACEMENT_3D ( 'NONE', #180060, #220476, #117512 ) ;
#168903=CARTESIAN_POINT ( 'NONE',  ( 18.59999999999999432, 74.27191306321832087, -216.6386724793566145 ) ) ;
#168909=EDGE_CURVE ( 'NONE', #105444, #41155, #205228, .T. ) ;
#168931=FILL_AREA_STYLE ('',( #146720 ) ) ;
#168950=EDGE_CURVE ( 'NONE', #165929, #241281, #217743, .T. ) ;
#168974=CARTESIAN_POINT ( 'NONE',  ( 23.24999999999999645, 73.90000000001244018, -170.0231074845244166 ) ) ;
#169011=FACE_OUTER_BOUND ( 'NONE', #16696, .T. ) ;
#169020=EDGE_CURVE ( 'NONE', #210276, #38825, #105292, .T. ) ;
#169056=CIRCLE ( 'NONE', #239757, 4.000000000000003553 ) ;
#169103=DIRECTION ( 'NONE',  ( -3.265361837132813093E-16, -1.000000000000000000, 7.445645354460596589E-46 ) ) ;
#169125=EDGE_CURVE ( 'NONE', #166628, #98827, #55894, .T. ) ;
#169148=CARTESIAN_POINT ( 'NONE',  ( 18.59999999999999432, 74.83729825007462466, -195.4231074845243654 ) ) ;
#169219=DIRECTION ( 'NONE',  ( 1.000000000000000000, 0.000000000000000000, 0.000000000000000000 ) ) ;
#169220=CARTESIAN_POINT ( 'NONE',  ( -22.50000000000000000, 75.90000000001268177, -203.5231074845243597 ) ) ;
#169223=DIRECTION ( 'NONE',  ( -1.000000000000000000, -0.000000000000000000, -0.000000000000000000 ) ) ;
#169236=DIRECTION ( 'NONE',  ( 1.000000000000000000, 0.000000000000000000, 0.000000000000000000 ) ) ;
#169256=FACE_OUTER_BOUND ( 'NONE', #22258, .T. ) ;
#169277=EDGE_LOOP ( 'NONE', ( #252281, #107371, #83215 ) ) ;
#169288=LINE ( 'NONE', #207100, #55056 ) ;
#169302=CYLINDRICAL_SURFACE ( 'NONE', #117576, 2.000000000000001776 ) ;
#169309=FACE_OUTER_BOUND ( 'NONE', #149600, .T. ) ;
#169311=DIRECTION ( 'NONE',  ( 0.000000000000000000, 0.000000000000000000, -1.000000000000000000 ) ) ;
#169333=EDGE_CURVE ( 'NONE', #18724, #43445, #176459, .T. ) ;
#169374=TOROIDAL_SURFACE ( 'NONE', #131736, 11.70000000000000462, 0.1000000000000000056 ) ;
#169386=EDGE_CURVE ( 'NONE', #44979, #96501, #8790, .T. ) ;
#169392=CIRCLE ( 'NONE', #252534, 0.8750000000000007772 ) ;
#169403=CARTESIAN_POINT ( 'NONE',  ( -23.15000000000000213, 85.00000000001251976, -179.9170766071767389 ) ) ;
#169463=EDGE_CURVE ( 'NONE', #230071, #184335, #51734, .T. ) ;
#169488=EDGE_CURVE ( 'NONE', #239176, #25217, #251230, .T. ) ;
#169523=ORIENTED_EDGE ( 'NONE', *, *, #198285, .T. ) ;
#169564=CARTESIAN_POINT ( 'NONE',  ( -21.05000000000000071, 64.36312671090855986, -196.7013482711997199 ) ) ;
#169578=DIRECTION ( 'NONE',  ( 0.000000000000000000, 0.000000000000000000, 1.000000000000000000 ) ) ;
#169615=ORIENTED_EDGE ( 'NONE', *, *, #203519, .F. ) ;
#169646=AXIS2_PLACEMENT_3D ( 'NONE', #233848, #158205, #137298 ) ;
#169651=ORIENTED_EDGE ( 'NONE', *, *, #119205, .F. ) ;
#169655=CARTESIAN_POINT ( 'NONE',  ( -21.93642651522410247, 68.67283376068687062, -203.5231074845243882 ) ) ;
#169659=CARTESIAN_POINT ( 'NONE',  ( -21.05000000000000071, 76.00000000001263345, -195.6231074845243540 ) ) ;
#169668=DIRECTION ( 'NONE',  ( 0.000000000000000000, -6.982962677686266711E-15, 1.000000000000000000 ) ) ;
#169673=AXIS2_PLACEMENT_3D ( 'NONE', #2729, #120172, #185240 ) ;
#169682=CARTESIAN_POINT ( 'NONE',  ( 23.15000000000000213, 87.65000000001246860, -173.1231074845242688 ) ) ;
#169685=AXIS2_PLACEMENT_3D ( 'NONE', #29674, #84428, #126156 ) ;
#169695=AXIS2_PLACEMENT_3D ( 'NONE', #122970, #121696, #1711 ) ;
#169738=DIRECTION ( 'NONE',  ( 0.000000000000000000, 0.000000000000000000, 1.000000000000000000 ) ) ;
#169746=CIRCLE ( 'NONE', #82187, 0.09999999999998898659 ) ;
#169813=DIRECTION ( 'NONE',  ( 0.000000000000000000, -1.000000000000000000, -6.982962677686266711E-15 ) ) ;
#169819=CIRCLE ( 'NONE', #107417, 0.09999999999998898659 ) ;
#169823=CARTESIAN_POINT ( 'NONE',  ( -21.11825140030087411, 69.55459243459324625, -203.5303111051574945 ) ) ;
#169826=EDGE_LOOP ( 'NONE', ( #32533, #7352, #189261, #110995 ) ) ;
#169851=ORIENTED_EDGE ( 'NONE', *, *, #13196, .F. ) ;
#169856=AXIS2_PLACEMENT_3D ( 'NONE', #160262, #242326, #199376 ) ;
#169880=DIRECTION ( 'NONE',  ( 0.000000000000000000, 0.000000000000000000, 1.000000000000000000 ) ) ;
#169904=ORIENTED_EDGE ( 'NONE', *, *, #189330, .T. ) ;
#169916=DIRECTION ( 'NONE',  ( 0.000000000000000000, -1.000000000000000000, -6.982962677686265922E-15 ) ) ;
#169928=AXIS2_PLACEMENT_3D ( 'NONE', #37473, #196521, #156150 ) ;
#169943=ORIENTED_EDGE ( 'NONE', *, *, #162307, .T. ) ;
#169985=DIRECTION ( 'NONE',  ( 0.000000000000000000, 6.982962677686266711E-15, -1.000000000000000000 ) ) ;
#169988=CARTESIAN_POINT ( 'NONE',  ( 18.49999999999999289, 65.79142135624982757, -178.8731074845244109 ) ) ;
#169995=DIRECTION ( 'NONE',  ( -1.000000000000000000, 0.000000000000000000, 0.000000000000000000 ) ) ;
#170005=CARTESIAN_POINT ( 'NONE',  ( -20.94999999999999929, 74.16465844978819177, -191.9679561919613775 ) ) ;
#170008=ORIENTED_EDGE ( 'NONE', *, *, #14964, .T. ) ;
#170020=DIRECTION ( 'NONE',  ( 1.000000000000000000, 0.000000000000000000, 0.000000000000000000 ) ) ;
#170069=CARTESIAN_POINT ( 'NONE',  ( 22.37643362114956247, 68.37421000605431232, -203.6221888582057886 ) ) ;
#170086=ORIENTED_EDGE ( 'NONE', *, *, #219934, .F. ) ;
#170119=VECTOR ( 'NONE', #80817, 1000.000000000000114 ) ;
#170141=DIRECTION ( 'NONE',  ( 1.000000000000000000, 0.000000000000000000, 0.000000000000000000 ) ) ;
#170157=EDGE_CURVE ( 'NONE', #144289, #3432, #122656, .T. ) ;
#170161=VECTOR ( 'NONE', #72595, 999.9999999999998863 ) ;
#170213=EDGE_CURVE ( 'NONE', #255434, #188196, #22703, .T. ) ;
#170248=DIRECTION ( 'NONE',  ( -1.000000000000000000, 0.000000000000000000, -0.000000000000000000 ) ) ;
#170275=CARTESIAN_POINT ( 'NONE',  ( 21.05000000000000071, 77.83534155023701828, -191.9679561919613491 ) ) ;
#170282=LINE ( 'NONE', #69875, #28888 ) ;
#170320=CARTESIAN_POINT ( 'NONE',  ( 23.15000000000000213, 87.65000000001246860, -173.1231074845242688 ) ) ;
#170335=AXIS2_PLACEMENT_3D ( 'NONE', #102133, #223381, #85135 ) ;
#170373=AXIS2_PLACEMENT_3D ( 'NONE', #111137, #250633, #88984 ) ;
#170422=EDGE_CURVE ( 'NONE', #87397, #72158, #251810, .T. ) ;
#170445=CARTESIAN_POINT ( 'NONE',  ( -18.39999999999999858, 85.68240343348880117, -163.3662641071115047 ) ) ;
#170448=DIRECTION ( 'NONE',  ( 0.000000000000000000, -1.000000000000000000, -6.982962677686265922E-15 ) ) ;
#170449=DIRECTION ( 'NONE',  ( -1.000000000000000000, -9.012599976027990443E-15, -6.882867235861669241E-14 ) ) ;
#170452=VERTEX_POINT ( 'NONE', #224350 ) ;
#170502=CARTESIAN_POINT ( 'NONE',  ( -23.15000000000000213, 85.00000000001251976, -179.9170766071767389 ) ) ;
#170525=ORIENTED_EDGE ( 'NONE', *, *, #67990, .T. ) ;
#170540=DIRECTION ( 'NONE',  ( 0.000000000000000000, 0.000000000000000000, -1.000000000000000000 ) ) ;
#170541=CARTESIAN_POINT ( 'NONE',  ( -21.05000000000000071, 87.48912529308852015, -172.9231074845242802 ) ) ;
#170557=AXIS2_PLACEMENT_3D ( 'NONE', #254220, #157762, #153912 ) ;
#170567=ORIENTED_EDGE ( 'NONE', *, *, #201177, .T. ) ;
#170585=DIRECTION ( 'NONE',  ( 0.000000000000000000, -0.8660254037844377084, -0.5000000000000016653 ) ) ;
#170593=CARTESIAN_POINT ( 'NONE',  ( 22.50000000000000000, 75.90000000001273861, -211.3138870828977360 ) ) ;
#170597=CYLINDRICAL_SURFACE ( 'NONE', #115430, 11.75000000000001066 ) ;
#170617=DIRECTION ( 'NONE',  ( -1.000000000000000000, -0.000000000000000000, -0.000000000000000000 ) ) ;
#170626=DIRECTION ( 'NONE',  ( -1.000000000000000000, 2.952720810173289112E-16, 2.061873921506763405E-30 ) ) ;
#170651=CARTESIAN_POINT ( 'NONE',  ( 21.14999999999999858, 64.25000000001269029, -203.4231074845244507 ) ) ;
#170679=EDGE_LOOP ( 'NONE', ( #78989, #229168, #39614, #249652 ) ) ;
#170695=ADVANCED_FACE ( 'NONE', ( #115636 ), #136454, .T. ) ;
#170701=DIRECTION ( 'NONE',  ( 1.000000000000000000, 0.000000000000000000, 0.000000000000000000 ) ) ;
#170706=EDGE_LOOP ( 'NONE', ( #76986, #253907, #102164, #27959 ) ) ;
#170738=AXIS2_PLACEMENT_3D ( 'NONE', #128865, #147119, #87141 ) ;
#170759=CIRCLE ( 'NONE', #87297, 0.09999999999998898659 ) ;
#170770=DIRECTION ( 'NONE',  ( 0.000000000000000000, 0.9908441862701791170, -0.1350103645450472789 ) ) ;
#170781=CARTESIAN_POINT ( 'NONE',  ( 20.85000000000000142, 68.97833521811233481, -166.1895420826271277 ) ) ;
#170817=ORIENTED_EDGE ( 'NONE', *, *, #82261, .F. ) ;
#170860=EDGE_LOOP ( 'NONE', ( #255953, #230381 ) ) ;
#170864=EDGE_CURVE ( 'NONE', #58850, #152824, #6277, .T. ) ;
#170875=CARTESIAN_POINT ( 'NONE',  ( -23.25000000000000000, 76.00000000001244871, -167.9231074845243938 ) ) ;
#170960=CARTESIAN_POINT ( 'NONE',  ( 23.15000000000000213, 85.50000000001251976, -179.9170766071767389 ) ) ;
#170964=DIRECTION ( 'NONE',  ( 0.000000000000000000, -0.008583690987135041833, 0.9999631594459055250 ) ) ;
#170973=CARTESIAN_POINT ( 'NONE',  ( -23.25000000000000000, 73.40000000001259650, -190.2984855617622770 ) ) ;
#170977=CARTESIAN_POINT ( 'NONE',  ( 20.94999999999999574, 87.75000000001264766, -200.4231074845242802 ) ) ;
#171054=ORIENTED_EDGE ( 'NONE', *, *, #246787, .T. ) ;
#171055=DIRECTION ( 'NONE',  ( 0.000000000000000000, 0.000000000000000000, -1.000000000000000000 ) ) ;
#171088=AXIS2_PLACEMENT_3D ( 'NONE', #132066, #101894, #19841 ) ;
#171096=AXIS2_PLACEMENT_3D ( 'NONE', #62244, #42674, #21838 ) ;
#171100=DIRECTION ( 'NONE',  ( 2.952720810173289112E-16, 1.000000000000000000, -6.088138035986627436E-46 ) ) ;
#171151=ORIENTED_EDGE ( 'NONE', *, *, #251186, .F. ) ;
#171181=( NAMED_UNIT ( * ) PLANE_ANGLE_UNIT ( ) SI_UNIT ( $, .RADIAN. ) );
#171223=EDGE_CURVE ( 'NONE', #33906, #146901, #98198, .T. ) ;
#171226=EDGE_LOOP ( 'NONE', ( #113648, #153579, #215343, #210418 ) ) ;
#171243=CARTESIAN_POINT ( 'NONE',  ( 23.24999999999999645, 76.00000000001244871, -170.0231074845243597 ) ) ;
#171252=ORIENTED_EDGE ( 'NONE', *, *, #243405, .F. ) ;
#171265=CARTESIAN_POINT ( 'NONE',  ( 20.88420186297724257, 65.66974365629718591, -164.4360145562605453 ) ) ;
#171269=AXIS2_PLACEMENT_3D ( 'NONE', #64489, #81443, #223534 ) ;
#171273=CARTESIAN_POINT ( 'NONE',  ( 19.75857864376268935, 64.35000000001251408, -178.7731074845244450 ) ) ;
#171295=EDGE_CURVE ( 'NONE', #180641, #104754, #23256, .T. ) ;
#171296=CARTESIAN_POINT ( 'NONE',  ( 22.49999999999996803, 75.89914163091405896, -215.2726746080137445 ) ) ;
#171297=ORIENTED_EDGE ( 'NONE', *, *, #57593, .F. ) ;
#171305=DIRECTION ( 'NONE',  ( 1.000000000000000000, 0.000000000000000000, 0.000000000000000000 ) ) ;
#171324=CARTESIAN_POINT ( 'NONE',  ( 18.41356215285961895, 85.50000000001266187, -196.4910380878247054 ) ) ;
#171329=DIRECTION ( 'NONE',  ( -1.000000000000000000, -0.000000000000000000, -0.000000000000000000 ) ) ;
#171374=DIRECTION ( 'NONE',  ( -1.000000000000000000, 0.000000000000000000, 0.000000000000000000 ) ) ;
#171376=VERTEX_POINT ( 'NONE', #149035 ) ;
#171432=ORIENTED_EDGE ( 'NONE', *, *, #17272, .T. ) ;
#171445=CARTESIAN_POINT ( 'NONE',  ( -21.55000000000000071, 68.65000000001261071, -191.2731074845244166 ) ) ;
#171458=CARTESIAN_POINT ( 'NONE',  ( 20.02499999999999858, 66.25000000001253397, -182.2731074845244450 ) ) ;
#171472=DIRECTION ( 'NONE',  ( -1.000000000000000000, 7.304098846218163263E-16, -4.217023435051627211E-16 ) ) ;
#171486=EDGE_CURVE ( 'NONE', #41259, #53690, #214131, .T. ) ;
#171509=EDGE_CURVE ( 'NONE', #177211, #142689, #257051, .T. ) ;
#171540=ORIENTED_EDGE ( 'NONE', *, *, #62639, .F. ) ;
#171561=ADVANCED_FACE ( 'NONE', ( #203 ), #215404, .T. ) ;
#171564=EDGE_CURVE ( 'NONE', #201210, #96287, #198413, .T. ) ;
#171624=EDGE_CURVE ( 'NONE', #121003, #210954, #84847, .T. ) ;
#171629=ORIENTED_EDGE ( 'NONE', *, *, #162409, .F. ) ;
#171638=CIRCLE ( 'NONE', #117455, 0.09999999999998898659 ) ;
#171689=CARTESIAN_POINT ( 'NONE',  ( -20.64999999999999858, 73.60000000001254250, -183.2477294072864709 ) ) ;
#171705=ORIENTED_EDGE ( 'NONE', *, *, #226538, .F. ) ;
#171781=EDGE_LOOP ( 'NONE', ( #94367, #243125, #213747, #66265 ) ) ;
#171803=FACE_OUTER_BOUND ( 'NONE', #243133, .T. ) ;
#171804=DIRECTION ( 'NONE',  ( 0.000000000000000000, 0.000000000000000000, 1.000000000000000000 ) ) ;
#171816=ORIENTED_EDGE ( 'NONE', *, *, #203886, .T. ) ;
#171831=EDGE_LOOP ( 'NONE', ( #104240, #36524, #39000, #42524 ) ) ;
#171850=CARTESIAN_POINT ( 'NONE',  ( -21.05000000000000071, 76.10000000001274145, -210.0637644362255969 ) ) ;
#171852=EDGE_CURVE ( 'NONE', #109261, #144129, #31376, .T. ) ;
#171862=CARTESIAN_POINT ( 'NONE',  ( 22.39999999999999858, 76.00000000001267608, -203.5231074845243597 ) ) ;
#171872=CARTESIAN_POINT ( 'NONE',  ( 23.14999999999999503, 64.35000000001254250, -182.1731074845244507 ) ) ;
#171922=AXIS2_PLACEMENT_3D ( 'NONE', #184659, #6015, #26911 ) ;
#171925=DIRECTION ( 'NONE',  ( 0.000000000000000000, 0.8660254037844378194, 0.5000000000000016653 ) ) ;
#171933=LINE ( 'NONE', #194044, #85364 ) ;
#171951=LINE ( 'NONE', #53248, #180576 ) ;
#171992=CARTESIAN_POINT ( 'NONE',  ( -20.94999999999999929, 74.16465844978819177, -191.9679561919613775 ) ) ;
#171997=LINE ( 'NONE', #126400, #118775 ) ;
#172015=EDGE_LOOP ( 'NONE', ( #188704, #242500, #77863, #249617 ) ) ;
#172045=FACE_OUTER_BOUND ( 'NONE', #4088, .T. ) ;
#172056=DIRECTION ( 'NONE',  ( 0.000000000000000000, 0.5000000000000128786, 0.8660254037844311581 ) ) ;
#172075=ORIENTED_EDGE ( 'NONE', *, *, #127272, .F. ) ;
#172086=DIRECTION ( 'NONE',  ( 0.000000000000000000, -6.982962677686266711E-15, 1.000000000000000000 ) ) ;
#172096=ORIENTED_EDGE ( 'NONE', *, *, #146283, .T. ) ;
#172190=DIRECTION ( 'NONE',  ( -1.000000000000000000, -0.000000000000000000, -0.000000000000000000 ) ) ;
#172241=DIRECTION ( 'NONE',  ( -0.000000000000000000, -0.1350103645451945777, 0.9908441862701590219 ) ) ;
#172249=VERTEX_POINT ( 'NONE', #170593 ) ;
#172281=DIRECTION ( 'NONE',  ( 0.000000000000000000, 0.8068669527897506244, 0.5907332058516622242 ) ) ;
#172312=ADVANCED_FACE ( 'NONE', ( #116983 ), #248625, .F. ) ;
#172320=PLANE ( 'NONE',  #180776 ) ;
#172321=ADVANCED_FACE ( 'NONE', ( #135243 ), #93563, .T. ) ;
#172322=PLANE ( 'NONE',  #249476 ) ;
#172344=CARTESIAN_POINT ( 'NONE',  ( -23.25000000000000000, 77.83585931145600512, -158.5186683157258187 ) ) ;
#172355=AXIS2_PLACEMENT_3D ( 'NONE', #38921, #81840, #158879 ) ;
#172360=ORIENTED_EDGE ( 'NONE', *, *, #226378, .F. ) ;
#172399=ORIENTED_EDGE ( 'NONE', *, *, #202443, .F. ) ;
#172411=DIRECTION ( 'NONE',  ( 1.000000000000000000, 0.000000000000000000, 0.000000000000000000 ) ) ;
#172436=CARTESIAN_POINT ( 'NONE',  ( -21.05000000000000071, 76.00000000001253397, -181.8231074845243711 ) ) ;
#172462=( LENGTH_UNIT ( ) NAMED_UNIT ( * ) SI_UNIT ( .MILLI., .METRE. ) );
#172465=CIRCLE ( 'NONE', #109858, 11.75000000000001066 ) ;
#172494=CYLINDRICAL_SURFACE ( 'NONE', #62220, 0.1000000000000028644 ) ;
#172497=CARTESIAN_POINT ( 'NONE',  ( 18.58719872626880942, 85.56664439761105712, -163.2006292881272884 ) ) ;
#172527=CYLINDRICAL_SURFACE ( 'NONE', #254339, 0.09999999999999939493 ) ;
#172558=CARTESIAN_POINT ( 'NONE',  ( -18.50000000000000000, 64.35000000001245724, -170.0231074845244166 ) ) ;
#172568=EDGE_CURVE ( 'NONE', #133901, #153430, #194491, .T. ) ;
#172569=ADVANCED_FACE ( 'NONE', ( #112514 ), #182001, .T. ) ;
#172608=DIRECTION ( 'NONE',  ( 0.000000000000000000, -6.938893903907222067E-15, 1.000000000000000000 ) ) ;
#172665=TOROIDAL_SURFACE ( 'NONE', #51787, 11.65000000000000036, 0.1000000000000000056 ) ;
#172693=VERTEX_POINT ( 'NONE', #17266 ) ;
#172763=DIRECTION ( 'NONE',  ( 0.000000000000000000, 1.000000000000000000, 0.000000000000000000 ) ) ;
#172767=EDGE_CURVE ( 'NONE', #6746, #166854, #155140, .T. ) ;
#172771=CARTESIAN_POINT ( 'NONE',  ( -23.15000000000000213, 87.65000000001269598, -203.5231074845243029 ) ) ;
#172803=VERTEX_POINT ( 'NONE', #190401 ) ;
#172847=CARTESIAN_POINT ( 'NONE',  ( -18.50000000000000000, 74.36282728704223643, -191.9409541190523498 ) ) ;
#172849=ORIENTED_EDGE ( 'NONE', *, *, #63600, .F. ) ;
#172857=DIRECTION ( 'NONE',  ( 1.000000000000000000, 0.000000000000000000, 0.000000000000000000 ) ) ;
#172871=DIRECTION ( 'NONE',  ( -1.000000000000000000, 0.000000000000000000, 0.000000000000000000 ) ) ;
#172898=VERTEX_POINT ( 'NONE', #170875 ) ;
#172944=FACE_OUTER_BOUND ( 'NONE', #153519, .T. ) ;
#172946=CARTESIAN_POINT ( 'NONE',  ( 23.14999999999999858, 73.90000000001244018, -170.0231074845243882 ) ) ;
#173022=CARTESIAN_POINT ( 'NONE',  ( -18.59999999999999787, 64.25000000001277556, -215.2731074845244450 ) ) ;
#173040=EDGE_CURVE ( 'NONE', #59053, #55818, #102649, .T. ) ;
#173049=ADVANCED_FACE ( 'NONE', ( #119850 ), #169374, .F. ) ;
#173061=CARTESIAN_POINT ( 'NONE',  ( -18.59999999999999787, 77.16412189325360771, -162.3082593989527425 ) ) ;
#173085=ORIENTED_EDGE ( 'NONE', *, *, #212065, .F. ) ;
#173087=CIRCLE ( 'NONE', #223101, 0.1999999999999987899 ) ;
#173096=ORIENTED_EDGE ( 'NONE', *, *, #248160, .F. ) ;
#173111=CARTESIAN_POINT ( 'NONE',  ( 23.14999999999999503, 64.35000000001254250, -182.2731074845244450 ) ) ;
#173114=EDGE_LOOP ( 'NONE', ( #98934, #108422, #218862, #99880 ) ) ;
#173182=DIRECTION ( 'NONE',  ( 1.000000000000000000, 0.000000000000000000, 0.000000000000000000 ) ) ;
#173207=DIRECTION ( 'NONE',  ( 1.000000000000000000, -2.952720810173289112E-16, -2.061873921506763405E-30 ) ) ;
#173209=ORIENTED_EDGE ( 'NONE', *, *, #218066, .F. ) ;
#173244=DIRECTION ( 'NONE',  ( 0.000000000000000000, 0.000000000000000000, 1.000000000000000000 ) ) ;
#173255=AXIS2_PLACEMENT_3D ( 'NONE', #158014, #117555, #19760 ) ;
#173363=CARTESIAN_POINT ( 'NONE',  ( 20.94999999999999929, 76.00000000001244871, -170.0231074845243597 ) ) ;
#173367=DIRECTION ( 'NONE',  ( 0.000000000000000000, -1.000000000000000000, -6.982962677686266711E-15 ) ) ;
#173375=ORIENTED_EDGE ( 'NONE', *, *, #50910, .T. ) ;
#173376=CIRCLE ( 'NONE', #235853, 2.000000000000001776 ) ;
#173381=CIRCLE ( 'NONE', #60891, 0.09999999999998898659 ) ;
#173402=FACE_BOUND ( 'NONE', #213903, .T. ) ;
#173427=DIRECTION ( 'NONE',  ( -2.940209281316621016E-16, -1.000000000000000000, -7.056502275159890832E-15 ) ) ;
#173442=ADVANCED_FACE ( 'NONE', ( #23009 ), #46372, .T. ) ;
#173453=DIRECTION ( 'NONE',  ( -0.000000000000000000, 6.982962677686266711E-15, -1.000000000000000000 ) ) ;
#173461=ORIENTED_EDGE ( 'NONE', *, *, #169020, .T. ) ;
#173462=ORIENTED_EDGE ( 'NONE', *, *, #67050, .F. ) ;
#173475=DIRECTION ( 'NONE',  ( -1.000000000000000000, 1.836970198721029934E-16, 1.282749433769087757E-30 ) ) ;
#173477=DIRECTION ( 'NONE',  ( 1.000000000000000000, 0.000000000000000000, 0.000000000000000000 ) ) ;
#173542=CARTESIAN_POINT ( 'NONE',  ( -18.59999999999999787, 85.48068669529138219, -163.0819923157664562 ) ) ;
#173554=ORIENTED_EDGE ( 'NONE', *, *, #106997, .T. ) ;
#173556=VECTOR ( 'NONE', #90375, 1000.000000000000000 ) ;
#173563=EDGE_CURVE ( 'NONE', #230071, #199924, #252277, .T. ) ;
#173595=FACE_OUTER_BOUND ( 'NONE', #16656, .T. ) ;
#173609=CARTESIAN_POINT ( 'NONE',  ( 22.16821283564876666, 68.44102665923192319, -203.5231074845243882 ) ) ;
#173628=DIRECTION ( 'NONE',  ( 0.000000000000000000, 1.000000000000000000, 7.116814260417668513E-15 ) ) ;
#173634=ORIENTED_EDGE ( 'NONE', *, *, #199661, .F. ) ;
#173645=EDGE_LOOP ( 'NONE', ( #156587, #211213, #180024, #29965 ) ) ;
#173649=DIRECTION ( 'NONE',  ( -1.000000000000000000, -0.000000000000000000, -0.000000000000000000 ) ) ;
#173675=ORIENTED_EDGE ( 'NONE', *, *, #41970, .T. ) ;
#173679=ORIENTED_EDGE ( 'NONE', *, *, #167437, .T. ) ;
#173763=ORIENTED_EDGE ( 'NONE', *, *, #73889, .T. ) ;
#173774=CARTESIAN_POINT ( 'NONE',  ( -21.05000000000000071, 69.70000000001266471, -203.4231074845244223 ) ) ;
#173786=CARTESIAN_POINT ( 'NONE',  ( 18.60000000000000142, 85.52394631233008226, -163.1410794891860974 ) ) ;
#173787=LINE ( 'NONE', #13380, #243321 ) ;
#173794=ADVANCED_FACE ( 'NONE', ( #174761 ), #156470, .F. ) ;
#173797=TOROIDAL_SURFACE ( 'NONE', #15543, 0.2000000000000000111, 0.1000000000000000056 ) ;
#173830=CARTESIAN_POINT ( 'NONE',  ( -20.15000000000000568, 66.70857864377528301, -191.2731074845244166 ) ) ;
#173832=CARTESIAN_POINT ( 'NONE',  ( 20.87600722750343252, 65.66887361445387228, -164.4329845918269939 ) ) ;
#173847=EDGE_LOOP ( 'NONE', ( #4443, #145643, #195917, #248437 ) ) ;
#173848=DIRECTION ( 'NONE',  ( 0.000000000000000000, -1.000000000000000000, -6.982962677686265922E-15 ) ) ;
#173853=VERTEX_POINT ( 'NONE', #75634 ) ;
#173854=CARTESIAN_POINT ( 'NONE',  ( 23.25000000000000355, 98.45632476063556737, -196.7292090367925823 ) ) ;
#173886=CARTESIAN_POINT ( 'NONE',  ( 18.50000000000000000, 85.40000000001263913, -196.2258477248609836 ) ) ;
#173895=ORIENTED_EDGE ( 'NONE', *, *, #249887, .T. ) ;
#173941=EDGE_CURVE ( 'NONE', #94115, #197918, #152979, .T. ) ;
#173944=ADVANCED_FACE ( 'NONE', ( #160309 ), #81989, .F. ) ;
#173998=CARTESIAN_POINT ( 'NONE',  ( 21.05000000000000071, 87.29603075034795268, -200.4752083248604038 ) ) ;
#174002=CARTESIAN_POINT ( 'NONE',  ( 20.95512820512820440, 65.37615131630076348, -195.8581939154368285 ) ) ;
#174013=AXIS2_PLACEMENT_3D ( 'NONE', #98688, #77870, #177020 ) ;
#174042=ORIENTED_EDGE ( 'NONE', *, *, #234524, .F. ) ;
#174070=EDGE_CURVE ( 'NONE', #207953, #144953, #236324, .T. ) ;
#174073=AXIS2_PLACEMENT_3D ( 'NONE', #103448, #3066, #162186 ) ;
#174079=CARTESIAN_POINT ( 'NONE',  ( -20.07928932188135107, 66.77928932189388433, -182.3731074845244393 ) ) ;
#174131=AXIS2_PLACEMENT_3D ( 'NONE', #250036, #150941, #27175 ) ;
#174136=CIRCLE ( 'NONE', #203328, 11.80000000000000426 ) ;
#174151=VERTEX_POINT ( 'NONE', #225370 ) ;
#174202=EDGE_LOOP ( 'NONE', ( #29653, #140079, #222415, #201133, #4556 ) ) ;
#174239=DIRECTION ( 'NONE',  ( 1.000000000000000000, 0.000000000000000000, 0.000000000000000000 ) ) ;
#174248=DIRECTION ( 'NONE',  ( 0.000000000000000000, 1.000000000000000000, 6.982962677686266711E-15 ) ) ;
#174268=DIRECTION ( 'NONE',  ( -1.000000000000000000, -0.000000000000000000, -0.000000000000000000 ) ) ;
#174281=ORIENTED_EDGE ( 'NONE', *, *, #226337, .F. ) ;
#174286=CIRCLE ( 'NONE', #203468, 0.09999999999998898659 ) ;
#174296=LINE ( 'NONE', #115542, #56064 ) ;
#174305=DIRECTION ( 'NONE',  ( -1.000000000000000000, -0.000000000000000000, -0.000000000000000000 ) ) ;
#174341=ADVANCED_FACE ( 'NONE', ( #56986 ), #38748, .F. ) ;
#174353=ORIENTED_EDGE ( 'NONE', *, *, #95387, .T. ) ;
#174369=DIRECTION ( 'NONE',  ( 1.000000000000000000, 0.000000000000000000, 0.000000000000000000 ) ) ;
#174404=VECTOR ( 'NONE', #119862, 1000.000000000000000 ) ;
#174411=ORIENTED_EDGE ( 'NONE', *, *, #18277, .T. ) ;
#174417=LINE ( 'NONE', #196480, #84298 ) ;
#174432=CIRCLE ( 'NONE', #99336, 1.900000000000012790 ) ;
#174448=ORIENTED_EDGE ( 'NONE', *, *, #42060, .T. ) ;
#174462=DIRECTION ( 'NONE',  ( -0.000000000000000000, 6.982962677686266711E-15, -1.000000000000000000 ) ) ;
#174497=AXIS2_PLACEMENT_3D ( 'NONE', #125815, #187110, #87954 ) ;
#174506=EDGE_CURVE ( 'NONE', #227495, #81505, #128545, .T. ) ;
#174512=DIRECTION ( 'NONE',  ( 1.000000000000000000, 0.000000000000000000, 0.000000000000000000 ) ) ;
#174514=DIRECTION ( 'NONE',  ( 0.000000000000000000, 1.000000000000000000, 6.982962677686266711E-15 ) ) ;
#174535=DIRECTION ( 'NONE',  ( 0.000000000000000000, -0.6728971962617102953, -0.7397360091702507301 ) ) ;
#174548=CYLINDRICAL_SURFACE ( 'NONE', #184728, 0.1000000000000028644 ) ;
#174565=ADVANCED_FACE ( 'NONE', ( #205500 ), #223777, .T. ) ;
#174588=CARTESIAN_POINT ( 'NONE',  ( -18.59999999999999787, 64.35000000001264198, -196.5083017138704236 ) ) ;
#174598=CARTESIAN_POINT ( 'NONE',  ( -21.76363531954647357, 75.90099812571328641, -210.5360440323960916 ) ) ;
#174622=AXIS2_PLACEMENT_3D ( 'NONE', #83662, #227058, #245360 ) ;
#174640=FACE_OUTER_BOUND ( 'NONE', #61387, .T. ) ;
#174654=CARTESIAN_POINT ( 'NONE',  ( 21.05000000000000071, 65.39167043205863195, -195.9314224712280748 ) ) ;
#174660=TOROIDAL_SURFACE ( 'NONE', #207943, 0.2000000000000000111, 0.1000000000000000056 ) ;
#174700=DIRECTION ( 'NONE',  ( 0.000000000000000000, 1.000000000000000000, 0.000000000000000000 ) ) ;
#174722=ORIENTED_EDGE ( 'NONE', *, *, #255749, .F. ) ;
#174729=EDGE_CURVE ( 'NONE', #35701, #109083, #75016, .T. ) ;
#174753=DIRECTION ( 'NONE',  ( -0.7070776581709311559, 4.937903618720164857E-15, -0.7071359030027479786 ) ) ;
#174761=FACE_OUTER_BOUND ( 'NONE', #253013, .T. ) ;
#174803=AXIS2_PLACEMENT_3D ( 'NONE', #207708, #34226, #29101 ) ;
#174835=EDGE_CURVE ( 'NONE', #138529, #257629, #120553, .T. ) ;
#174840=CARTESIAN_POINT ( 'NONE',  ( -21.05000000000000071, 87.29603075034775372, -173.0710066441881452 ) ) ;
#174846=ORIENTED_EDGE ( 'NONE', *, *, #5805, .F. ) ;
#174849=DIRECTION ( 'NONE',  ( 1.000000000000000000, -3.265361837132813093E-16, -2.280189983783949500E-30 ) ) ;
#174859=EDGE_LOOP ( 'NONE', ( #237954, #145064, #184950, #151557 ) ) ;
#174874=CARTESIAN_POINT ( 'NONE',  ( 22.49999999999999645, 64.35012909624849442, -203.6056273753973187 ) ) ;
#174879=EDGE_CURVE ( 'NONE', #246415, #22816, #182552, .T. ) ;
#174915=DIRECTION ( 'NONE',  ( -0.000000000000000000, -6.982962677686266711E-15, 1.000000000000000000 ) ) ;
#174919=PLANE ( 'NONE',  #151140 ) ;
#174934=EDGE_LOOP ( 'NONE', ( #106888, #251264, #61413, #257692 ) ) ;
#174972=ORIENTED_EDGE ( 'NONE', *, *, #146597, .F. ) ;
#174997=VECTOR ( 'NONE', #205910, 1000.000000000000000 ) ;
#175010=DIRECTION ( 'NONE',  ( 0.000000000000000000, -0.5000000000000016653, 0.8660254037844377084 ) ) ;
#175024=CIRCLE ( 'NONE', #75048, 0.2000000000000057288 ) ;
#175029=ORIENTED_EDGE ( 'NONE', *, *, #204015, .F. ) ;
#175038=ORIENTED_EDGE ( 'NONE', *, *, #241854, .F. ) ;
#175067=AXIS2_PLACEMENT_3D ( 'NONE', #222798, #46733, #67593 ) ;
#175070=ADVANCED_FACE ( 'NONE', ( #49974 ), #249479, .F. ) ;
#175088=DIRECTION ( 'NONE',  ( 1.000000000000000000, 0.000000000000000000, 0.000000000000000000 ) ) ;
#175092=EDGE_CURVE ( 'NONE', #81149, #135406, #125036, .T. ) ;
#175103=ORIENTED_EDGE ( 'NONE', *, *, #250771, .F. ) ;
#175118=CARTESIAN_POINT ( 'NONE',  ( -23.25000000000000000, 76.00000000001260503, -190.7481074845243256 ) ) ;
#175130=DIRECTION ( 'NONE',  ( 0.000000000000000000, 0.000000000000000000, 1.000000000000000000 ) ) ;
#175145=CIRCLE ( 'NONE', #187584, 0.09999999999998898659 ) ;
#175170=CARTESIAN_POINT ( 'NONE',  ( 18.44364597020195973, 85.49048731717491023, -196.4651295948403913 ) ) ;
#175177=DIRECTION ( 'NONE',  ( 0.000000000000000000, -1.000000000000000000, 0.000000000000000000 ) ) ;
#175228=CARTESIAN_POINT ( 'NONE',  ( -18.43473496883410334, 85.49495241101196541, -196.4772359122960665 ) ) ;
#175230=FACE_OUTER_BOUND ( 'NONE', #206676, .T. ) ;
#175239=ORIENTED_EDGE ( 'NONE', *, *, #146107, .F. ) ;
#175251=ORIENTED_EDGE ( 'NONE', *, *, #157653, .F. ) ;
#175260=CARTESIAN_POINT ( 'NONE',  ( -18.59999999999999787, 76.00000000001244871, -170.0231074845243597 ) ) ;
#175261=LINE ( 'NONE', #52688, #103254 ) ;
#175272=CARTESIAN_POINT ( 'NONE',  ( -18.50000000000000000, 69.15387683765983695, -166.2853812176745691 ) ) ;
#175276=ORIENTED_EDGE ( 'NONE', *, *, #247831, .F. ) ;
#175292=DIRECTION ( 'NONE',  ( 0.000000000000000000, 6.982962677686267499E-15, -1.000000000000000000 ) ) ;
#175324=EDGE_CURVE ( 'NONE', #37214, #95308, #187912, .T. ) ;
#175328=VERTEX_POINT ( 'NONE', #252676 ) ;
#175342=CIRCLE ( 'NONE', #237682, 0.09999999999998898659 ) ;
#175373=ORIENTED_EDGE ( 'NONE', *, *, #64122, .T. ) ;
#175446=DIRECTION ( 'NONE',  ( -0.000000000000000000, 7.272083257015735086E-15, -1.000000000000000000 ) ) ;
#175475=EDGE_LOOP ( 'NONE', ( #132739, #6704, #118045, #194589 ) ) ;
#175491=ORIENTED_EDGE ( 'NONE', *, *, #55179, .F. ) ;
#175495=DIRECTION ( 'NONE',  ( 1.000000000000000000, 0.000000000000000000, 0.000000000000000000 ) ) ;
#175540=DIRECTION ( 'NONE',  ( 1.000000000000000000, 0.000000000000000000, 0.000000000000000000 ) ) ;
#175550=DIRECTION ( 'NONE',  ( 0.000000000000000000, -0.4930308989875170078, -0.8700118002898356018 ) ) ;
#175591=CARTESIAN_POINT ( 'NONE',  ( -18.59999999999999787, 74.13328508995527955, -191.7704322382423641 ) ) ;
#175636=CARTESIAN_POINT ( 'NONE',  ( 18.46932045258653332, 85.67068520027807210, -163.3492471115275464 ) ) ;
#175644=ORIENTED_EDGE ( 'NONE', *, *, #141587, .F. ) ;
#175701=AXIS2_PLACEMENT_3D ( 'NONE', #248154, #44819, #86479 ) ;
#175709=ORIENTED_EDGE ( 'NONE', *, *, #40577, .T. ) ;
#175710=VECTOR ( 'NONE', #193993, 1000.000000000000000 ) ;
#175715=AXIS2_PLACEMENT_3D ( 'NONE', #64209, #143734, #164600 ) ;
#175719=CARTESIAN_POINT ( 'NONE',  ( -20.85000000000000142, 87.65000000001245439, -170.0231074845242745 ) ) ;
#175740=ADVANCED_FACE ( 'NONE', ( #200114 ), #18898, .F. ) ;
#175816=AXIS2_PLACEMENT_3D ( 'NONE', #170005, #249510, #70891 ) ;
#175834=ORIENTED_EDGE ( 'NONE', *, *, #27402, .T. ) ;
#175836=FACE_OUTER_BOUND ( 'NONE', #212789, .T. ) ;
#175841=EDGE_CURVE ( 'NONE', #92780, #124945, #258048, .T. ) ;
#175845=ORIENTED_EDGE ( 'NONE', *, *, #42362, .F. ) ;
#175880=ORIENTED_EDGE ( 'NONE', *, *, #28187, .F. ) ;
#175911=CARTESIAN_POINT ( 'NONE',  ( -18.59999999999999787, 64.35000000001254250, -182.1731074845244507 ) ) ;
#175942=EDGE_CURVE ( 'NONE', #140330, #141837, #166536, .T. ) ;
#175983=DIRECTION ( 'NONE',  ( 1.000000000000000000, 0.000000000000000000, 0.000000000000000000 ) ) ;
#175994=DIRECTION ( 'NONE',  ( 0.000000000000000000, 0.000000000000000000, -1.000000000000000000 ) ) ;
#175995=TOROIDAL_SURFACE ( 'NONE', #117696, 3.899999999999999467, 0.1000000000000000056 ) ;
#176015=CARTESIAN_POINT ( 'NONE',  ( -21.05000000000000071, 76.10000000001276987, -215.1731074845243654 ) ) ;
#176021=CARTESIAN_POINT ( 'NONE',  ( 21.07928932188134397, 69.67148334361938566, -203.6220026301787982 ) ) ;
#176047=FACE_OUTER_BOUND ( 'NONE', #179502, .T. ) ;
#176065=VERTEX_POINT ( 'NONE', #51274 ) ;
#176093=ORIENTED_EDGE ( 'NONE', *, *, #111949, .T. ) ;
#176104=CARTESIAN_POINT ( 'NONE',  ( 21.05000000000000071, 61.95000000001248708, -175.5368025552853624 ) ) ;
#176142=CARTESIAN_POINT ( 'NONE',  ( -21.05000000000000071, 74.83729825007462466, -195.5231074845243597 ) ) ;
#176161=ORIENTED_EDGE ( 'NONE', *, *, #43213, .F. ) ;
#176179=EDGE_LOOP ( 'NONE', ( #171054, #152344, #64233 ) ) ;
#176300=CARTESIAN_POINT ( 'NONE',  ( -22.39999999999999858, 68.20922040163927136, -203.6231074845244109 ) ) ;
#176306=DIRECTION ( 'NONE',  ( -1.000000000000000000, -0.000000000000000000, -0.000000000000000000 ) ) ;
#176307=DIRECTION ( 'NONE',  ( 0.000000000000000000, 0.000000000000000000, 1.000000000000000000 ) ) ;
#176311=DIRECTION ( 'NONE',  ( 0.000000000000000000, 6.982962677686266711E-15, -1.000000000000000000 ) ) ;
#176317=CARTESIAN_POINT ( 'NONE',  ( 21.05000000000000071, 76.00000000001244871, -170.0231074845243597 ) ) ;
#176320=CARTESIAN_POINT ( 'NONE',  ( 18.52351027002947959, 85.64216290470756121, -163.3080605340145439 ) ) ;
#176338=CARTESIAN_POINT ( 'NONE',  ( -18.59999999999999787, 66.75000000001260503, -191.1731074845244223 ) ) ;
#176342=CARTESIAN_POINT ( 'NONE',  ( -21.14999999999999858, 64.25000000001269029, -203.4231074845244507 ) ) ;
#176355=AXIS2_PLACEMENT_3D ( 'NONE', #179015, #143691, #21217 ) ;
#176360=AXIS2_PLACEMENT_3D ( 'NONE', #145471, #26851, #127207 ) ;
#176382=DIRECTION ( 'NONE',  ( 0.000000000000000000, -6.608470384673536035E-15, 1.000000000000000000 ) ) ;
#176391=CARTESIAN_POINT ( 'NONE',  ( 18.59999999999999787, 74.14897176987174987, -191.8691942151018850 ) ) ;
#176400=CARTESIAN_POINT ( 'NONE',  ( 22.50046968639222200, 75.95483015287750561, -215.2731526389931105 ) ) ;
#176436=EDGE_LOOP ( 'NONE', ( #106059, #90228, #225746, #45003 ) ) ;
#176454=DIRECTION ( 'NONE',  ( -4.408576920032448588E-17, -0.1350103645451807555, -0.9908441862701609093 ) ) ;
#176459=CIRCLE ( 'NONE', #138793, 11.64999999999999325 ) ;
#176462=EDGE_CURVE ( 'NONE', #207133, #133625, #124623, .T. ) ;
#176502=VERTEX_POINT ( 'NONE', #22982 ) ;
#176516=VECTOR ( 'NONE', #222667, 999.9999999999998863 ) ;
#176521=LINE ( 'NONE', #156965, #78322 ) ;
#176527=CIRCLE ( 'NONE', #218175, 0.5000000000000004441 ) ;
#176557=DIRECTION ( 'NONE',  ( 0.000000000000000000, -6.982962677686266711E-15, 1.000000000000000000 ) ) ;
#176595=CARTESIAN_POINT ( 'NONE',  ( 21.05000000000000071, 65.27628289530511552, -195.8581939154368285 ) ) ;
#176616=CARTESIAN_POINT ( 'NONE',  ( -18.43459694179556152, 85.49421012501045425, -163.4061022818634683 ) ) ;
#176636=ADVANCED_FACE ( 'NONE', ( #139688 ), #163143, .T. ) ;
#176644=DIRECTION ( 'NONE',  ( 0.000000000000000000, -6.938893903907222067E-15, 1.000000000000000000 ) ) ;
#176679=LINE ( 'NONE', #240483, #46269 ) ;
#176682=DIRECTION ( 'NONE',  ( 1.000000000000000000, 0.000000000000000000, 0.000000000000000000 ) ) ;
#176696=AXIS2_PLACEMENT_3D ( 'NONE', #113579, #133146, #216526 ) ;
#176704=CARTESIAN_POINT ( 'NONE',  ( -23.15000000000000213, 71.65000000001253966, -182.3731074845244109 ) ) ;
#176718=AXIS2_PLACEMENT_3D ( 'NONE', #118448, #76727, #235802 ) ;
#176750=CIRCLE ( 'NONE', #89235, 0.09999999999998898659 ) ;
#176775=DIRECTION ( 'NONE',  ( 0.000000000000000000, 0.000000000000000000, 1.000000000000000000 ) ) ;
#176799=AXIS2_PLACEMENT_3D ( 'NONE', #41547, #87033, #204427 ) ;
#176807=ORIENTED_EDGE ( 'NONE', *, *, #251298, .T. ) ;
#176839=EDGE_CURVE ( 'NONE', #143032, #71381, #228248, .T. ) ;
#176842=AXIS2_PLACEMENT_3D ( 'NONE', #256232, #77647, #135055 ) ;
#176845=CARTESIAN_POINT ( 'NONE',  ( 21.14999999999999858, 87.75000000001259082, -191.2731074845242745 ) ) ;
#176860=AXIS2_PLACEMENT_3D ( 'NONE', #254920, #215835, #76324 ) ;
#176898=AXIS2_PLACEMENT_3D ( 'NONE', #71919, #206280, #130581 ) ;
#176905=ORIENTED_EDGE ( 'NONE', *, *, #61213, .T. ) ;
#176934=ORIENTED_EDGE ( 'NONE', *, *, #162221, .F. ) ;
#176935=ORIENTED_EDGE ( 'NONE', *, *, #54911, .T. ) ;
#176964=DIRECTION ( 'NONE',  ( 0.000000000000000000, 0.000000000000000000, 1.000000000000000000 ) ) ;
#176969=LINE ( 'NONE', #24305, #8306 ) ;
#176983=EDGE_LOOP ( 'NONE', ( #209487, #4208, #78933, #244787 ) ) ;
#176984=ORIENTED_EDGE ( 'NONE', *, *, #131418, .F. ) ;
#176991=CIRCLE ( 'NONE', #31428, 0.09999999999999939493 ) ;
#177020=DIRECTION ( 'NONE',  ( 0.000000000000000000, 0.000000000000000000, 1.000000000000000000 ) ) ;
#177065=ADVANCED_FACE ( 'NONE', ( #179834 ), #88396, .T. ) ;
#177072=AXIS2_PLACEMENT_3D ( 'NONE', #83179, #4927, #222709 ) ;
#177078=CARTESIAN_POINT ( 'NONE',  ( -22.59999999999999787, 75.89914163091405896, -215.2726746080137445 ) ) ;
#177087=CARTESIAN_POINT ( 'NONE',  ( 21.00000000000000000, 66.25000000001253397, -182.2731074845244450 ) ) ;
#177097=ORIENTED_EDGE ( 'NONE', *, *, #214054, .F. ) ;
#177117=ORIENTED_EDGE ( 'NONE', *, *, #167862, .T. ) ;
#177130=AXIS2_PLACEMENT_3D ( 'NONE', #21588, #81509, #157264 ) ;
#177131=CARTESIAN_POINT ( 'NONE',  ( -22.14074124539699540, 75.90094710416866519, -210.9131853355681301 ) ) ;
#177147=FACE_OUTER_BOUND ( 'NONE', #63910, .T. ) ;
#177161=ADVANCED_FACE ( 'NONE', ( #25893 ), #180022, .T. ) ;
#177175=FACE_OUTER_BOUND ( 'NONE', #38042, .T. ) ;
#177205=ORIENTED_EDGE ( 'NONE', *, *, #124761, .F. ) ;
#177211=VERTEX_POINT ( 'NONE', #188795 ) ;
#177234=VERTEX_POINT ( 'NONE', #149702 ) ;
#177245=AXIS2_PLACEMENT_3D ( 'NONE', #173363, #129059, #113337 ) ;
#177262=CARTESIAN_POINT ( 'NONE',  ( -20.54999999999999716, 68.85000000001259934, -191.2731074845244166 ) ) ;
#177267=VERTEX_POINT ( 'NONE', #114399 ) ;
#177279=ORIENTED_EDGE ( 'NONE', *, *, #153278, .T. ) ;
#177281=CARTESIAN_POINT ( 'NONE',  ( -21.14999999999999858, 76.00000000001267608, -203.5231074845243597 ) ) ;
#177284=VERTEX_POINT ( 'NONE', #12757 ) ;
#177286=CARTESIAN_POINT ( 'NONE',  ( -20.64999999999999858, 74.00000000001254818, -183.2477294072864709 ) ) ;
#177377=FACE_OUTER_BOUND ( 'NONE', #46053, .T. ) ;
#177402=CARTESIAN_POINT ( 'NONE',  ( -20.54999999999999716, 74.00000000001259082, -190.2984855617622770 ) ) ;
#177417=EDGE_CURVE ( 'NONE', #239144, #104754, #116968, .T. ) ;
#177421=CARTESIAN_POINT ( 'NONE',  ( 22.59066674512274986, 64.25000000001267608, -203.5536116081545970 ) ) ;
#177471=VERTEX_POINT ( 'NONE', #168974 ) ;
#177475=TOROIDAL_SURFACE ( 'NONE', #210753, 11.70000000000000639, 0.1000000000000000056 ) ;
#177484=LINE ( 'NONE', #79, #68340 ) ;
#177504=AXIS2_PLACEMENT_3D ( 'NONE', #41470, #6148, #85661 ) ;
#177532=TOROIDAL_SURFACE ( 'NONE', #165009, 11.65000000000000036, 0.1000000000000000056 ) ;
#177544=AXIS2_PLACEMENT_3D ( 'NONE', #118491, #139292, #179741 ) ;
#177552=CARTESIAN_POINT ( 'NONE',  ( -21.05000000000000071, 76.10000000001272724, -210.0637644362255969 ) ) ;
#177568=DIRECTION ( 'NONE',  ( 1.000000000000000000, 0.000000000000000000, 0.000000000000000000 ) ) ;
#177572=FACE_OUTER_BOUND ( 'NONE', #55777, .T. ) ;
#177581=ORIENTED_EDGE ( 'NONE', *, *, #201790, .F. ) ;
#177610=LINE ( 'NONE', #135860, #41392 ) ;
#177674=LINE ( 'NONE', #182795, #202391 ) ;
#177689=ORIENTED_EDGE ( 'NONE', *, *, #255406, .F. ) ;
#177708=AXIS2_PLACEMENT_3D ( 'NONE', #146073, #130359, #28759 ) ;
#177722=CARTESIAN_POINT ( 'NONE',  ( -18.59999999999999787, 66.85000000001254250, -182.3731074845244393 ) ) ;
#177729=FACE_OUTER_BOUND ( 'NONE', #5030, .T. ) ;
#177738=CIRCLE ( 'NONE', #144340, 0.09999999999999939493 ) ;
#177757=ORIENTED_EDGE ( 'NONE', *, *, #80032, .F. ) ;
#177761=DIRECTION ( 'NONE',  ( -0.000000000000000000, 0.1298341882519953583, 0.9915357197604862671 ) ) ;
#177772=CARTESIAN_POINT ( 'NONE',  ( -18.51555513499479844, 85.35265705451605811, -196.3279375888288030 ) ) ;
#177779=AXIS2_PLACEMENT_3D ( 'NONE', #16738, #79235, #17992 ) ;
#177832=FACE_OUTER_BOUND ( 'NONE', #155458, .T. ) ;
#177857=AXIS2_PLACEMENT_3D ( 'NONE', #113106, #130090, #90969 ) ;
#177872=SPHERICAL_SURFACE ( 'NONE', #45668, 0.1000000000000000056 ) ;
#177886=EDGE_CURVE ( 'NONE', #8263, #135203, #61028, .T. ) ;
#177891=DIRECTION ( 'NONE',  ( 0.000000000000000000, -6.982962677686266711E-15, 1.000000000000000000 ) ) ;
#177906=CYLINDRICAL_SURFACE ( 'NONE', #127556, 12.87499999999999822 ) ;
#177920=CYLINDRICAL_SURFACE ( 'NONE', #228104, 0.09999999999998898659 ) ;
#178005=DIRECTION ( 'NONE',  ( 1.000000000000000000, 0.000000000000000000, 0.000000000000000000 ) ) ;
#178025=DIRECTION ( 'NONE',  ( 0.000000000000000000, -0.1350103645451807555, -0.9908441862701610203 ) ) ;
#178039=EDGE_CURVE ( 'NONE', #210147, #161922, #248486, .T. ) ;
#178089=EDGE_LOOP ( 'NONE', ( #237864, #68853, #72686, #106869 ) ) ;
#178114=DIRECTION ( 'NONE',  ( 0.000000000000000000, -0.1350103645451835865, -0.9908441862701605762 ) ) ;
#178124=DIRECTION ( 'NONE',  ( -1.000000000000000000, 0.000000000000000000, -0.000000000000000000 ) ) ;
#178136=DIRECTION ( 'NONE',  ( 0.000000000000000000, 6.577889128801576950E-15, -1.000000000000000000 ) ) ;
#178208=CIRCLE ( 'NONE', #253185, 0.09999999999998898659 ) ;
#178214=CARTESIAN_POINT ( 'NONE',  ( 18.39999999999999858, 85.50000000001240608, -163.4229180933022576 ) ) ;
#178221=ORIENTED_EDGE ( 'NONE', *, *, #22934, .F. ) ;
#178265=VERTEX_POINT ( 'NONE', #10220 ) ;
#178297=DIRECTION ( 'NONE',  ( 0.000000000000000000, 1.096314854800262720E-14, -1.000000000000000000 ) ) ;
#178328=CARTESIAN_POINT ( 'NONE',  ( 21.13461538461538325, 65.38541703798705385, -191.1731074845244223 ) ) ;
#178334=DIRECTION ( 'NONE',  ( 0.000000000000000000, 0.000000000000000000, 1.000000000000000000 ) ) ;
#178345=EDGE_CURVE ( 'NONE', #147959, #214102, #230545, .T. ) ;
#178394=VERTEX_POINT ( 'NONE', #32372 ) ;
#178395=EDGE_CURVE ( 'NONE', #211067, #197295, #34938, .T. ) ;
#178411=DIRECTION ( 'NONE',  ( 0.000000000000000000, -1.000000000000000000, 0.000000000000000000 ) ) ;
#178416=CARTESIAN_POINT ( 'NONE',  ( -22.32929514600008503, 75.90092432189882743, -211.1017550499008735 ) ) ;
#178418=CARTESIAN_POINT ( 'NONE',  ( -20.85000000000000142, 77.83585931145600512, -158.5186683157258187 ) ) ;
#178455=EDGE_CURVE ( 'NONE', #7443, #154279, #60870, .T. ) ;
#178472=CIRCLE ( 'NONE', #124479, 0.1000000000000046685 ) ;
#178484=EDGE_LOOP ( 'NONE', ( #61759, #187593, #87116, #196730, #184277 ) ) ;
#178490=CARTESIAN_POINT ( 'NONE',  ( -18.39999999999999858, 85.50000000001242029, -163.4229180933022576 ) ) ;
#178491=ORIENTED_EDGE ( 'NONE', *, *, #185825, .T. ) ;
#178500=ORIENTED_EDGE ( 'NONE', *, *, #33761, .T. ) ;
#178530=ORIENTED_EDGE ( 'NONE', *, *, #8665, .F. ) ;
#178576=EDGE_LOOP ( 'NONE', ( #32383, #225319, #136401, #82464 ) ) ;
#178591=CARTESIAN_POINT ( 'NONE',  ( 18.49999999999999289, 65.50857864377520912, -178.6731074845244223 ) ) ;
#178601=AXIS2_PLACEMENT_3D ( 'NONE', #235981, #78188, #136890 ) ;
#178606=DIRECTION ( 'NONE',  ( -0.000000000000000000, 6.982962677686266711E-15, -1.000000000000000000 ) ) ;
#178614=DIRECTION ( 'NONE',  ( -1.000000000000000000, 0.000000000000000000, -0.000000000000000000 ) ) ;
#178628=ORIENTED_EDGE ( 'NONE', *, *, #75288, .F. ) ;
#178639=CARTESIAN_POINT ( 'NONE',  ( -20.64999999999999858, 71.65000000001259650, -191.2731074845243882 ) ) ;
#178643=DIRECTION ( 'NONE',  ( 1.000000000000000000, 0.000000000000000000, 0.000000000000000000 ) ) ;
#178661=CARTESIAN_POINT ( 'NONE',  ( 21.08832698747859169, 67.22463560659538473, -191.2943900180602554 ) ) ;
#178667=ADVANCED_FACE ( 'NONE', ( #166436 ), #44665, .T. ) ;
#178668=VERTEX_POINT ( 'NONE', #228949 ) ;
#178670=FACE_OUTER_BOUND ( 'NONE', #112999, .T. ) ;
#178697=DIRECTION ( 'NONE',  ( -7.304098846218134667E-16, 1.000000000000000000, 6.982962677686267499E-15 ) ) ;
#178698=ORIENTED_EDGE ( 'NONE', *, *, #194612, .F. ) ;
#178753=ORIENTED_EDGE ( 'NONE', *, *, #103012, .F. ) ;
#178774=ADVANCED_FACE ( 'NONE', ( #16335 ), #52859, .T. ) ;
#178799=ORIENTED_EDGE ( 'NONE', *, *, #183040, .F. ) ;
#178821=LINE ( 'NONE', #63974, #15471 ) ;
#178825=ORIENTED_EDGE ( 'NONE', *, *, #238410, .T. ) ;
#178865=AXIS2_PLACEMENT_3D ( 'NONE', #92876, #216686, #53761 ) ;
#178870=ADVANCED_FACE ( 'NONE', ( #63125 ), #157131, .F. ) ;
#178895=ORIENTED_EDGE ( 'NONE', *, *, #144772, .F. ) ;
#178911=LINE ( 'NONE', #237571, #147075 ) ;
#178939=DIRECTION ( 'NONE',  ( 0.000000000000000000, -1.000000000000000000, 2.771150684185008344E-14 ) ) ;
#178946=DIRECTION ( 'NONE',  ( 1.000000000000000000, 0.000000000000000000, 0.000000000000000000 ) ) ;
#178954=ADVANCED_FACE ( 'NONE', ( #29207 ), #8327, .T. ) ;
#178969=CARTESIAN_POINT ( 'NONE',  ( 20.95035502843362707, 65.52236167323616201, -195.9468077757880451 ) ) ;
#178970=DIRECTION ( 'NONE',  ( 1.000000000000000000, 0.000000000000000000, 0.000000000000000000 ) ) ;
#178974=ADVANCED_FACE ( 'NONE', ( #47416 ), #68291, .F. ) ;
#178986=ORIENTED_EDGE ( 'NONE', *, *, #133462, .T. ) ;
#178993=AXIS2_PLACEMENT_3D ( 'NONE', #68488, #171472, #172763 ) ;
#179015=CARTESIAN_POINT ( 'NONE',  ( -20.64999999999999858, 73.60000000001259934, -190.2984855617622770 ) ) ;
#179035=ADVANCED_FACE ( 'NONE', ( #104800 ), #124414, .F. ) ;
#179038=CARTESIAN_POINT ( 'NONE',  ( 21.04386569057619027, 64.25000000001250555, -176.8802701327446698 ) ) ;
#179091=CARTESIAN_POINT ( 'NONE',  ( 23.15000000000000213, 87.75000000001259082, -191.2731074845242745 ) ) ;
#179110=VERTEX_POINT ( 'NONE', #254595 ) ;
#179118=CARTESIAN_POINT ( 'NONE',  ( -23.25000000000000000, 76.00000000001267608, -203.5231074845243597 ) ) ;
#179122=ORIENTED_EDGE ( 'NONE', *, *, #186067, .T. ) ;
#179133=AXIS2_PLACEMENT_3D ( 'NONE', #99181, #20987, #63935 ) ;
#179157=ORIENTED_EDGE ( 'NONE', *, *, #209584, .T. ) ;
#179175=EDGE_CURVE ( 'NONE', #51105, #19454, #90794, .T. ) ;
#179207=AXIS2_PLACEMENT_3D ( 'NONE', #149411, #132392, #12462 ) ;
#179242=ORIENTED_EDGE ( 'NONE', *, *, #178395, .F. ) ;
#179247=AXIS2_PLACEMENT_3D ( 'NONE', #143013, #140458, #85590 ) ;
#179259=ADVANCED_FACE ( 'NONE', ( #21181 ), #28510, .T. ) ;
#179307=ORIENTED_EDGE ( 'NONE', *, *, #132367, .T. ) ;
#179329=TOROIDAL_SURFACE ( 'NONE', #158488, 0.6000000000000004219, 0.1000000000000000056 ) ;
#179352=DIRECTION ( 'NONE',  ( 0.000000000000000000, 1.000000000000000000, 6.688090509790097607E-15 ) ) ;
#179360=VECTOR ( 'NONE', #65014, 1000.000000000000000 ) ;
#179376=EDGE_CURVE ( 'NONE', #34176, #41259, #56403, .T. ) ;
#179395=DIRECTION ( 'NONE',  ( -1.000000000000000000, 0.000000000000000000, -0.000000000000000000 ) ) ;
#179427=ORIENTED_EDGE ( 'NONE', *, *, #162307, .F. ) ;
#179483=CARTESIAN_POINT ( 'NONE',  ( 21.00000000000000000, 66.25000000001260503, -191.1731074845244223 ) ) ;
#179490=CARTESIAN_POINT ( 'NONE',  ( 18.31572054635728009, 85.54847543579103331, -163.1725373197758415 ) ) ;
#179501=CARTESIAN_POINT ( 'NONE',  ( 21.05000000000000071, 87.29603075034775372, -173.0710066441881452 ) ) ;
#179502=EDGE_LOOP ( 'NONE', ( #199088, #103931, #134634, #230122 ) ) ;
#179516=CARTESIAN_POINT ( 'NONE',  ( 22.41477678272288188, 75.99917613424982221, -215.1726927690397702 ) ) ;
#179526=ORIENTED_EDGE ( 'NONE', *, *, #117088, .T. ) ;
#179528=ORIENTED_EDGE ( 'NONE', *, *, #240402, .T. ) ;
#179555=CIRCLE ( 'NONE', #92037, 0.2000000000000057288 ) ;
#179578=DIRECTION ( 'NONE',  ( 0.000000000000000000, 0.000000000000000000, 1.000000000000000000 ) ) ;
#179607=LINE ( 'NONE', #114478, #145551 ) ;
#179629=ORIENTED_EDGE ( 'NONE', *, *, #188983, .F. ) ;
#179641=CYLINDRICAL_SURFACE ( 'NONE', #155911, 0.1000000000000033362 ) ;
#179650=CARTESIAN_POINT ( 'NONE',  ( 20.95512840106816199, 65.37615130623927939, -191.3206282637256663 ) ) ;
#179654=FACE_OUTER_BOUND ( 'NONE', #188577, .T. ) ;
#179693=VECTOR ( 'NONE', #153978, 1000.000000000000000 ) ;
#179720=CIRCLE ( 'NONE', #100569, 0.09999999999998898659 ) ;
#179733=DIRECTION ( 'NONE',  ( 1.000000000000000000, 0.000000000000000000, 0.000000000000000000 ) ) ;
#179741=DIRECTION ( 'NONE',  ( 0.000000000000000000, 0.000000000000000000, -1.000000000000000000 ) ) ;
#179775=ORIENTED_EDGE ( 'NONE', *, *, #148849, .T. ) ;
#179780=ORIENTED_EDGE ( 'NONE', *, *, #157529, .F. ) ;
#179784=DIRECTION ( 'NONE',  ( -1.000000000000000000, -0.000000000000000000, -0.000000000000000000 ) ) ;
#179804=LINE ( 'NONE', #257986, #197228 ) ;
#179814=ORIENTED_EDGE ( 'NONE', *, *, #158202, .T. ) ;
#179821=ORIENTED_EDGE ( 'NONE', *, *, #34479, .F. ) ;
#179834=FACE_OUTER_BOUND ( 'NONE', #214036, .T. ) ;
#179852=CARTESIAN_POINT ( 'NONE',  ( -21.14999999999999858, 76.10000000001276987, -215.1726782920691505 ) ) ;
#179898=EDGE_LOOP ( 'NONE', ( #8149, #130632, #69721, #113752, #231346, #207041, #226699 ) ) ;
#179938=EDGE_LOOP ( 'NONE', ( #36422, #96787, #246247, #127268, #9293, #149512, #174722 ) ) ;
#179943=DIRECTION ( 'NONE',  ( 1.000000000000000000, -0.000000000000000000, 0.000000000000000000 ) ) ;
#179953=CARTESIAN_POINT ( 'NONE',  ( 21.05000000000000071, 65.27628289530507288, -191.3619171903970084 ) ) ;
#179973=ADVANCED_FACE ( 'NONE', ( #129737 ), #193572, .T. ) ;
#180022=TOROIDAL_SURFACE ( 'NONE', #42626, 3.899999999999999467, 0.1000000000000000056 ) ;
#180024=ORIENTED_EDGE ( 'NONE', *, *, #253272, .T. ) ;
#180037=ORIENTED_EDGE ( 'NONE', *, *, #224787, .F. ) ;
#180060=CARTESIAN_POINT ( 'NONE',  ( 20.94999999999999574, 69.65000000001262492, -193.6792853948412869 ) ) ;
#180065=CARTESIAN_POINT ( 'NONE',  ( -21.05000000000000071, 62.00000000001249134, -175.4502000149069261 ) ) ;
#180070=ORIENTED_EDGE ( 'NONE', *, *, #226546, .T. ) ;
#180071=ORIENTED_EDGE ( 'NONE', *, *, #211019, .T. ) ;
#180096=CYLINDRICAL_SURFACE ( 'NONE', #236018, 0.09999999999998898659 ) ;
#180116=CARTESIAN_POINT ( 'NONE',  ( -23.15000000000000213, 87.65000000001246860, -173.0231074845243029 ) ) ;
#180131=CARTESIAN_POINT ( 'NONE',  ( -23.25000000000000000, 76.00000000001267608, -203.5231074845243597 ) ) ;
#180154=DIRECTION ( 'NONE',  ( -0.000000000000000000, 1.000000000000000000, 6.982962677686266711E-15 ) ) ;
#180158=ADVANCED_FACE ( 'NONE', ( #166024 ), #121754, .F. ) ;
#180199=DIRECTION ( 'NONE',  ( 0.000000000000000000, 0.000000000000000000, 1.000000000000000000 ) ) ;
#180227=CARTESIAN_POINT ( 'NONE',  ( 20.95568717954149562, 65.39800594612081852, -195.9205991162557723 ) ) ;
#180256=EDGE_LOOP ( 'NONE', ( #119585, #117797, #39921, #8404 ) ) ;
#180284=EDGE_CURVE ( 'NONE', #248091, #247920, #31657, .T. ) ;
#180295=CARTESIAN_POINT ( 'NONE',  ( -18.45140287520618472, 85.48607773954195466, -163.3825843578381978 ) ) ;
#180296=EDGE_CURVE ( 'NONE', #72158, #163070, #91374, .T. ) ;
#180320=CARTESIAN_POINT ( 'NONE',  ( -18.49719636458550553, 85.44636535924099974, -196.4514936146412367 ) ) ;
#180331=AXIS2_PLACEMENT_3D ( 'NONE', #231231, #215491, #19880 ) ;
#180350=FACE_OUTER_BOUND ( 'NONE', #168186, .T. ) ;
#180352=ORIENTED_EDGE ( 'NONE', *, *, #187402, .F. ) ;
#180361=( BOUNDED_SURFACE ( )  B_SPLINE_SURFACE ( 3, 2, ( 
 ( #203231, #161564, #205797 ),
 ( #27202, #106679, #7600 ),
 ( #87123, #166710, #200674 ),
 ( #22047, #181124, #92260 ),
 ( #208391, #167997, #51838 ),
 ( #31056, #252617, #171850 ) ),
 .UNSPECIFIED., .F., .F., .F. ) 
 B_SPLINE_SURFACE_WITH_KNOTS ( ( 4, 2, 4 ),
 ( 3, 3 ),
 ( 0.0001792624049599621759, 0.0003686986002124819695, 0.0005581347954650017632 ),
 ( 0.000000000000000000, 1.000000000000000000 ),
 .UNSPECIFIED. ) 
 GEOMETRIC_REPRESENTATION_ITEM ( )  RATIONAL_B_SPLINE_SURFACE ( (
 ( 1.000000000000000000, 0.9238795325112516554, 1.000000000000000000),
 ( 1.000000000000000000, 0.9229318695242004766, 1.000000000000000000),
 ( 1.000000000000000000, 0.8926288119226696294, 1.000000000000000000),
 ( 1.000000000000000000, 0.8123777807275355256, 1.000000000000000000),
 ( 1.000000000000000000, 0.7629087100928401144, 1.000000000000000000),
 ( 1.000000000000000000, 0.7071067811865352493, 1.000000000000000000) ) ) 
 REPRESENTATION_ITEM ( '' )  SURFACE ( )  );
#180374=ORIENTED_EDGE ( 'NONE', *, *, #235679, .T. ) ;
#180391=CARTESIAN_POINT ( 'NONE',  ( 22.50497660315937765, 76.07871793023828388, -215.2729029894197197 ) ) ;
#180399=CARTESIAN_POINT ( 'NONE',  ( 21.14999999999999858, 69.45934304831143891, -203.5231074845243882 ) ) ;
#180400=CARTESIAN_POINT ( 'NONE',  ( 18.43473516226069364, 85.49494228277087871, -196.4772088011747826 ) ) ;
#180418=ORIENTED_EDGE ( 'NONE', *, *, #205661, .T. ) ;
#180425=AXIS2_PLACEMENT_3D ( 'NONE', #146652, #188372, #29342 ) ;
#180440=SPHERICAL_SURFACE ( 'NONE', #199933, 0.1000000000000000056 ) ;
#180488=ORIENTED_EDGE ( 'NONE', *, *, #98909, .F. ) ;
#180558=ORIENTED_EDGE ( 'NONE', *, *, #80833, .T. ) ;
#180566=CARTESIAN_POINT ( 'NONE',  ( 18.50000000000000000, 85.50000000001276135, -215.2731074845243029 ) ) ;
#180576=VECTOR ( 'NONE', #231904, 1000.000000000000000 ) ;
#180579=CARTESIAN_POINT ( 'NONE',  ( 21.13461538461538325, 65.38541703798705385, -191.1731074845244223 ) ) ;
#180589=EDGE_CURVE ( 'NONE', #221704, #199924, #181432, .T. ) ;
#180625=CARTESIAN_POINT ( 'NONE',  ( 20.75572585718184015, 67.11768327161523473, -195.0258490858114158 ) ) ;
#180630=ORIENTED_EDGE ( 'NONE', *, *, #206377, .T. ) ;
#180639=EDGE_LOOP ( 'NONE', ( #6313, #165606, #28735, #23955 ) ) ;
#180641=VERTEX_POINT ( 'NONE', #189117 ) ;
#180656=EDGE_CURVE ( 'NONE', #143950, #177267, #246512, .T. ) ;
#180658=CARTESIAN_POINT ( 'NONE',  ( 18.59999999999999076, 69.45000000001252261, -182.2731074845244166 ) ) ;
#180661=CARTESIAN_POINT ( 'NONE',  ( 19.87657994472028378, 64.25000000001250555, -178.7573193598975649 ) ) ;
#180680=ORIENTED_EDGE ( 'NONE', *, *, #95847, .F. ) ;
#180683=LINE ( 'NONE', #97239, #10184 ) ;
#180696=CARTESIAN_POINT ( 'NONE',  ( 18.59999999999999787, 76.00000000001267608, -203.5231074845243597 ) ) ;
#180726=EDGE_LOOP ( 'NONE', ( #51364, #127548, #94769, #113355 ) ) ;
#180735=ORIENTED_EDGE ( 'NONE', *, *, #122048, .F. ) ;
#180760=CARTESIAN_POINT ( 'NONE',  ( 18.47135592147665406, 85.47108861327795637, -163.3395125446803320 ) ) ;
#180765=CIRCLE ( 'NONE', #210001, 0.1000000000000028644 ) ;
#180767=ORIENTED_EDGE ( 'NONE', *, *, #169488, .T. ) ;
#180776=AXIS2_PLACEMENT_3D ( 'NONE', #251803, #152739, #138255 ) ;
#180782=VERTEX_POINT ( 'NONE', #116015 ) ;
#180806=ORIENTED_EDGE ( 'NONE', *, *, #230488, .F. ) ;
#180826=ADVANCED_FACE ( 'NONE', ( #213814 ), #117151, .F. ) ;
#180849=ORIENTED_EDGE ( 'NONE', *, *, #50257, .F. ) ;
#180867=VERTEX_POINT ( 'NONE', #144529 ) ;
#180929=EDGE_CURVE ( 'NONE', #125507, #98827, #81968, .T. ) ;
#180982=ADVANCED_FACE ( 'NONE', ( #107990 ), #62513, .T. ) ;
#180995=EDGE_CURVE ( 'NONE', #178394, #176, #237670, .T. ) ;
#181053=ORIENTED_EDGE ( 'NONE', *, *, #180995, .F. ) ;
#181066=ADVANCED_FACE ( 'NONE', ( #71451 ), #125059, .T. ) ;
#181084=CARTESIAN_POINT ( 'NONE',  ( -23.25000000000000000, 74.08971962618080909, -190.8917396293254285 ) ) ;
#181105=ORIENTED_EDGE ( 'NONE', *, *, #178039, .F. ) ;
#181111=FACE_OUTER_BOUND ( 'NONE', #246566, .T. ) ;
#181124=CARTESIAN_POINT ( 'NONE',  ( -21.04999999999999716, 76.01771943332158799, -209.9641921729950127 ) ) ;
#181128=CARTESIAN_POINT ( 'NONE',  ( -18.50000000000000000, 64.35000000001259934, -191.3731074845244393 ) ) ;
#181135=DIRECTION ( 'NONE',  ( -1.000000000000000000, 0.000000000000000000, 0.000000000000000000 ) ) ;
#181157=CARTESIAN_POINT ( 'NONE',  ( -20.00857864376270001, 66.75000000001260503, -191.1731074845244223 ) ) ;
#181159=DIRECTION ( 'NONE',  ( 0.000000000000000000, 6.997203936713175802E-15, -1.000000000000000000 ) ) ;
#181221=AXIS2_PLACEMENT_3D ( 'NONE', #128701, #163975, #243494 ) ;
#181246=ORIENTED_EDGE ( 'NONE', *, *, #13200, .T. ) ;
#181249=ORIENTED_EDGE ( 'NONE', *, *, #182375, .T. ) ;
#181282=ORIENTED_EDGE ( 'NONE', *, *, #1651, .T. ) ;
#181288=ORIENTED_EDGE ( 'NONE', *, *, #1103, .F. ) ;
#181303=CARTESIAN_POINT ( 'NONE',  ( -18.59999999999999787, 77.16270174995064224, -195.4231074845243370 ) ) ;
#181316=DIRECTION ( 'NONE',  ( 0.000000000000000000, 1.000000000000000000, 6.982962677686266711E-15 ) ) ;
#181326=AXIS2_PLACEMENT_3D ( 'NONE', #171243, #250719, #132065 ) ;
#181343=ORIENTED_EDGE ( 'NONE', *, *, #56331, .T. ) ;
#181359=VERTEX_POINT ( 'NONE', #90340 ) ;
#181368=ORIENTED_EDGE ( 'NONE', *, *, #175942, .F. ) ;
#181370=FACE_OUTER_BOUND ( 'NONE', #108401, .T. ) ;
#181426=AXIS2_PLACEMENT_3D ( 'NONE', #128517, #244599, #225021 ) ;
#181431=CARTESIAN_POINT ( 'NONE',  ( 20.85000000000000142, 77.75000000001236344, -158.4041574459020865 ) ) ;
#181432=LINE ( 'NONE', #185264, #183306 ) ;
#181440=DIRECTION ( 'NONE',  ( 2.952720810173289112E-16, 1.000000000000000000, 6.982962677686266711E-15 ) ) ;
#181442=VERTEX_POINT ( 'NONE', #150342 ) ;
#181448=CARTESIAN_POINT ( 'NONE',  ( -18.43707690579160641, 85.68240343348881538, -163.3662641071115615 ) ) ;
#181530=CARTESIAN_POINT ( 'NONE',  ( -18.59999999999999787, 64.35000000001276987, -215.2731074845244450 ) ) ;
#181534=ORIENTED_EDGE ( 'NONE', *, *, #42060, .F. ) ;
#181559=AXIS2_PLACEMENT_3D ( 'NONE', #113027, #29669, #153489 ) ;
#181617=ADVANCED_FACE ( 'NONE', ( #65343 ), #186601, .F. ) ;
#181692=DIRECTION ( 'NONE',  ( -1.000000000000000000, -0.000000000000000000, -0.000000000000000000 ) ) ;
#181700=AXIS2_PLACEMENT_3D ( 'NONE', #20294, #82772, #60666 ) ;
#181742=EDGE_LOOP ( 'NONE', ( #81586, #101146, #218906, #173679 ) ) ;
#181746=ORIENTED_EDGE ( 'NONE', *, *, #251038, .T. ) ;
#181796=DIRECTION ( 'NONE',  ( 1.000000000000000000, -0.000000000000000000, 0.000000000000000000 ) ) ;
#181829=EDGE_CURVE ( 'NONE', #173853, #216782, #83848, .T. ) ;
#181833=EDGE_CURVE ( 'NONE', #239511, #166628, #112947, .T. ) ;
#181845=DIRECTION ( 'NONE',  ( 0.000000000000000000, -6.982962677686266711E-15, 1.000000000000000000 ) ) ;
#181860=AXIS2_PLACEMENT_3D ( 'NONE', #153323, #236659, #253645 ) ;
#181862=EDGE_CURVE ( 'NONE', #188520, #111659, #157783, .T. ) ;
#181886=ORIENTED_EDGE ( 'NONE', *, *, #54389, .F. ) ;
#181925=CARTESIAN_POINT ( 'NONE',  ( 21.14999999999999858, 69.45934304831143891, -203.4231074845244223 ) ) ;
#181926=ORIENTED_EDGE ( 'NONE', *, *, #23463, .F. ) ;
#181944=CARTESIAN_POINT ( 'NONE',  ( 20.00000000000000355, 64.25000000001250555, -178.8731074845244393 ) ) ;
#181960=EDGE_CURVE ( 'NONE', #121283, #138529, #183864, .T. ) ;
#181966=DIRECTION ( 'NONE',  ( -0.000000000000000000, 0.4791956752371484551, 0.8777080977375184556 ) ) ;
#181981=VECTOR ( 'NONE', #144877, 1000.000000000000000 ) ;
#181984=VECTOR ( 'NONE', #170248, 1000.000000000000000 ) ;
#182001=TOROIDAL_SURFACE ( 'NONE', #69590, 0.2000000000000000111, 0.1000000000000000056 ) ;
#182010=DIRECTION ( 'NONE',  ( 0.000000000000000000, 0.000000000000000000, -1.000000000000000000 ) ) ;
#182023=DIRECTION ( 'NONE',  ( -0.000000000000000000, -6.982962677686266711E-15, 1.000000000000000000 ) ) ;
#182037=ORIENTED_EDGE ( 'NONE', *, *, #67234, .F. ) ;
#182056=CARTESIAN_POINT ( 'NONE',  ( 22.39999999999999503, 76.00000000001273293, -211.3138870828977360 ) ) ;
#182064=EDGE_LOOP ( 'NONE', ( #2999, #150403, #243690, #1870 ) ) ;
#182069=CARTESIAN_POINT ( 'NONE',  ( 22.49999999999999645, 75.91119002362582080, -215.1728704025562706 ) ) ;
#182093=VERTEX_POINT ( 'NONE', #11511 ) ;
#182131=VECTOR ( 'NONE', #162773, 1000.000000000000000 ) ;
#182163=EDGE_CURVE ( 'NONE', #124908, #54825, #25829, .T. ) ;
#182165=DIRECTION ( 'NONE',  ( 0.000000000000000000, -0.8700118002898357128, 0.4930308989875170633 ) ) ;
#182176=EDGE_CURVE ( 'NONE', #172898, #105425, #96536, .T. ) ;
#182181=EDGE_CURVE ( 'NONE', #152824, #165380, #238195, .T. ) ;
#182193=CARTESIAN_POINT ( 'NONE',  ( 20.94999999999999574, 74.16465844978819177, -191.9679561919613775 ) ) ;
#182199=FACE_OUTER_BOUND ( 'NONE', #25764, .T. ) ;
#182203=CARTESIAN_POINT ( 'NONE',  ( -23.15000000000000213, 74.08971962618075224, -182.6544753397233194 ) ) ;
#182213=CARTESIAN_POINT ( 'NONE',  ( 23.14999999999999503, 64.35000000001249987, -176.9379132551783869 ) ) ;
#182221=CARTESIAN_POINT ( 'NONE',  ( 22.39999999999999858, 68.20922040163929978, -203.6231074845244109 ) ) ;
#182261=CIRCLE ( 'NONE', #107228, 0.09999999999998898659 ) ;
#182277=DIRECTION ( 'NONE',  ( 0.000000000000000000, -7.487053152578134969E-15, 1.000000000000000000 ) ) ;
#182285=FACE_OUTER_BOUND ( 'NONE', #72847, .T. ) ;
#182288=EDGE_CURVE ( 'NONE', #166875, #51521, #115730, .T. ) ;
#182289=AXIS2_PLACEMENT_3D ( 'NONE', #40964, #72711, #131367 ) ;
#182308=DIRECTION ( 'NONE',  ( -0.000000000000000000, 1.000000000000000000, 6.982962677686266711E-15 ) ) ;
#182310=CARTESIAN_POINT ( 'NONE',  ( -20.54999999999999716, 73.60000000001259934, -190.2984855617622770 ) ) ;
#182374=DIRECTION ( 'NONE',  ( 0.000000000000000000, -1.000000000000000000, -6.982962677686266711E-15 ) ) ;
#182375=EDGE_CURVE ( 'NONE', #202321, #18724, #119601, .T. ) ;
#182408=DIRECTION ( 'NONE',  ( 0.000000000000000000, -1.000000000000000000, 0.000000000000000000 ) ) ;
#182420=CARTESIAN_POINT ( 'NONE',  ( 20.12500000000000000, 66.25000000001253397, -182.2731074845244450 ) ) ;
#182423=DIRECTION ( 'NONE',  ( 0.000000000000000000, -0.008583690987162452199, -0.9999631594459053030 ) ) ;
#182426=CARTESIAN_POINT ( 'NONE',  ( 18.49999999999997868, 65.62657994473291012, -178.7573193598993555 ) ) ;
#182440=EDGE_CURVE ( 'NONE', #50587, #230108, #239532, .T. ) ;
#182452=AXIS2_PLACEMENT_3D ( 'NONE', #229396, #126426, #108157 ) ;
#182496=CARTESIAN_POINT ( 'NONE',  ( 21.09706851349341861, 67.22415748653919820, -191.2875412681247838 ) ) ;
#182523=AXIS2_PLACEMENT_3D ( 'NONE', #204614, #88502, #145925 ) ;
#182529=CARTESIAN_POINT ( 'NONE',  ( 21.14999999999999858, 65.28660755661270798, -191.2731074845244166 ) ) ;
#182541=FACE_OUTER_BOUND ( 'NONE', #38553, .T. ) ;
#182543=PLANE ( 'NONE',  #231415 ) ;
#182552=CIRCLE ( 'NONE', #219944, 0.1000000000000033362 ) ;
#182596=VERTEX_POINT ( 'NONE', #9891 ) ;
#182617=VERTEX_POINT ( 'NONE', #88119 ) ;
#182648=AXIS2_PLACEMENT_3D ( 'NONE', #78507, #95514, #75960 ) ;
#182664=VECTOR ( 'NONE', #70360, 1000.000000000000000 ) ;
#182676=DIRECTION ( 'NONE',  ( 1.000000000000000000, 0.000000000000000000, 0.000000000000000000 ) ) ;
#182678=FACE_OUTER_BOUND ( 'NONE', #156340, .T. ) ;
#182689=VECTOR ( 'NONE', #76901, 1000.000000000000000 ) ;
#182701=LINE ( 'NONE', #165712, #82731 ) ;
#182702=( BOUNDED_CURVE ( )  B_SPLINE_CURVE ( 3, ( #103156, #26225, #125317, #185287 ),
 .UNSPECIFIED., .F., .F. ) 
 B_SPLINE_CURVE_WITH_KNOTS ( ( 4, 4 ),
 ( 4.712388980384689674, 6.231880751915386263 ),
 .UNSPECIFIED. ) 
 CURVE ( )  GEOMETRIC_REPRESENTATION_ITEM ( )  RATIONAL_B_SPLINE_CURVE ( ( 1.000000000000000000, 0.8166740347213228279, 0.8166740347213228279, 1.000000000000000000 ) ) 
 REPRESENTATION_ITEM ( '' )  );
#182723=CARTESIAN_POINT ( 'NONE',  ( 23.24999999999999289, 69.45000000001252261, -182.1731074845243938 ) ) ;
#182766=EDGE_LOOP ( 'NONE', ( #226877, #13052, #7477, #63856, #88991, #113682 ) ) ;
#182786=CARTESIAN_POINT ( 'NONE',  ( -20.54999999999999716, 76.00000000001243450, -168.0231074845243597 ) ) ;
#182795=CARTESIAN_POINT ( 'NONE',  ( 23.14999999999999503, 64.25000000001276135, -215.2731074845244450 ) ) ;
#182819=CIRCLE ( 'NONE', #70396, 2.000000000000001776 ) ;
#182845=CARTESIAN_POINT ( 'NONE',  ( -22.46246831459151494, 75.97808783307333158, -215.1729720457343262 ) ) ;
#182896=ORIENTED_EDGE ( 'NONE', *, *, #210598, .F. ) ;
#182901=CARTESIAN_POINT ( 'NONE',  ( -23.15000000000000213, 64.35000000001249987, -177.0379132551783812 ) ) ;
#182908=TOROIDAL_SURFACE ( 'NONE', #153730, 0.6000000000000004219, 0.1000000000000000056 ) ;
#182955=AXIS2_PLACEMENT_3D ( 'NONE', #13165, #90104, #10598 ) ;
#182969=CIRCLE ( 'NONE', #82958, 3.900000000000000799 ) ;
#182972=AXIS2_PLACEMENT_3D ( 'NONE', #189552, #153020, #253356 ) ;
#182974=CARTESIAN_POINT ( 'NONE',  ( 21.05000000000000071, 69.74115287693359733, -203.5548658375798823 ) ) ;
#183015=CARTESIAN_POINT ( 'NONE',  ( 23.14999999999999858, 70.40000000001253966, -182.4283735034374843 ) ) ;
#183018=DIRECTION ( 'NONE',  ( 0.000000000000000000, 0.000000000000000000, -1.000000000000000000 ) ) ;
#183022=ORIENTED_EDGE ( 'NONE', *, *, #26073, .F. ) ;
#183040=EDGE_CURVE ( 'NONE', #249694, #246415, #236015, .T. ) ;
#183049=AXIS2_PLACEMENT_3D ( 'NONE', #196134, #254770, #76169 ) ;
#183076=LINE ( 'NONE', #22732, #228142 ) ;
#183083=CARTESIAN_POINT ( 'NONE',  ( 20.97239005616516394, 67.12515615866247742, -191.2729546823712496 ) ) ;
#183089=AXIS2_PLACEMENT_3D ( 'NONE', #98957, #116007, #153887 ) ;
#183095=DIRECTION ( 'NONE',  ( -1.000000000000000000, 0.000000000000000000, 0.000000000000000000 ) ) ;
#183104=CARTESIAN_POINT ( 'NONE',  ( -18.52643265882458579, 65.68026841930954163, -164.4725740131889893 ) ) ;
#183106=CARTESIAN_POINT ( 'NONE',  ( 20.94999999999999929, 85.00000000001251976, -179.9170766071767389 ) ) ;
#183114=VERTEX_POINT ( 'NONE', #199486 ) ;
#183129=EDGE_CURVE ( 'NONE', #104276, #210147, #183671, .T. ) ;
#183136=ORIENTED_EDGE ( 'NONE', *, *, #1734, .T. ) ;
#183150=DIRECTION ( 'NONE',  ( -0.000000000000000000, -6.982962677686266711E-15, 1.000000000000000000 ) ) ;
#183155=AXIS2_PLACEMENT_3D ( 'NONE', #47101, #126662, #206202 ) ;
#183158=DIRECTION ( 'NONE',  ( -1.000000000000000000, -0.000000000000000000, -0.000000000000000000 ) ) ;
#183159=DIRECTION ( 'NONE',  ( 0.000000000000000000, 0.3738317757009942399, -0.9274965247785252886 ) ) ;
#183161=VERTEX_POINT ( 'NONE', #220323 ) ;
#183175=AXIS2_PLACEMENT_3D ( 'NONE', #212367, #130227, #31187 ) ;
#183186=CARTESIAN_POINT ( 'NONE',  ( -20.94999999999999929, 64.35000000001251408, -176.8069731475025321 ) ) ;
#183197=DIRECTION ( 'NONE',  ( 0.000000000000000000, 0.000000000000000000, 1.000000000000000000 ) ) ;
#183224=CARTESIAN_POINT ( 'NONE',  ( 21.13461538461538680, 67.11458296203814200, -191.1731074845244223 ) ) ;
#183266=ORIENTED_EDGE ( 'NONE', *, *, #69166, .T. ) ;
#183288=EDGE_CURVE ( 'NONE', #177211, #235019, #146231, .T. ) ;
#183306=VECTOR ( 'NONE', #5306, 1000.000000000000000 ) ;
#183359=FACE_OUTER_BOUND ( 'NONE', #256278, .T. ) ;
#183371=CARTESIAN_POINT ( 'NONE',  ( 21.56666275994540172, 76.00000000001271871, -210.4804758914176830 ) ) ;
#183419=CARTESIAN_POINT ( 'NONE',  ( 20.94999999999999929, 77.83585931145600512, -158.5186683157258187 ) ) ;
#183506=CIRCLE ( 'NONE', #200075, 0.2000000000000057288 ) ;
#183517=FACE_OUTER_BOUND ( 'NONE', #242414, .T. ) ;
#183563=VECTOR ( 'NONE', #9080, 1000.000000000000000 ) ;
#183569=CARTESIAN_POINT ( 'NONE',  ( -21.05000000000000071, 74.83729825007462466, -195.6231074845243540 ) ) ;
#183594=VERTEX_POINT ( 'NONE', #34160 ) ;
#183602=DIRECTION ( 'NONE',  ( -1.000000000000000000, -0.000000000000000000, -0.000000000000000000 ) ) ;
#183608=LINE ( 'NONE', #67498, #182131 ) ;
#183610=ORIENTED_EDGE ( 'NONE', *, *, #219705, .F. ) ;
#183625=LINE ( 'NONE', #138055, #27869 ) ;
#183664=ORIENTED_EDGE ( 'NONE', *, *, #1258, .T. ) ;
#183667=CARTESIAN_POINT ( 'NONE',  ( -18.50000000000000000, 74.16465844978819177, -191.9679561919613775 ) ) ;
#183671=CIRCLE ( 'NONE', #104517, 11.80000000000000426 ) ;
#183675=ORIENTED_EDGE ( 'NONE', *, *, #185181, .T. ) ;
#183707=ORIENTED_EDGE ( 'NONE', *, *, #69166, .F. ) ;
#183718=ORIENTED_EDGE ( 'NONE', *, *, #6057, .T. ) ;
#183731=CARTESIAN_POINT ( 'NONE',  ( -23.25000000000000000, 87.75000000001246292, -170.0231074845242745 ) ) ;
#183758=EDGE_LOOP ( 'NONE', ( #226138, #168827, #63620, #86141 ) ) ;
#183782=EDGE_CURVE ( 'NONE', #144953, #131204, #87349, .T. ) ;
#183806=DIRECTION ( 'NONE',  ( 0.000000000000000000, -6.308085367188367561E-15, 1.000000000000000000 ) ) ;
#183838=VERTEX_POINT ( 'NONE', #147339 ) ;
#183861=VERTEX_POINT ( 'NONE', #70414 ) ;
#183864=CIRCLE ( 'NONE', #71458, 11.89999999999999325 ) ;
#183945=DIRECTION ( 'NONE',  ( -1.000000000000000000, -0.000000000000000000, -0.000000000000000000 ) ) ;
#183960=AXIS2_PLACEMENT_3D ( 'NONE', #193706, #186337, #35929 ) ;
#183994=DIRECTION ( 'NONE',  ( 2.952720810173289112E-16, 1.000000000000000000, 6.982962677686266711E-15 ) ) ;
#184002=VERTEX_POINT ( 'NONE', #135465 ) ;
#184006=CARTESIAN_POINT ( 'NONE',  ( 18.49999999999999645, 77.16270174995064224, -195.4231074845243370 ) ) ;
#184027=DIRECTION ( 'NONE',  ( 1.000000000000000000, 0.000000000000000000, 0.000000000000000000 ) ) ;
#184031=CARTESIAN_POINT ( 'NONE',  ( 19.75857864376268935, 64.35000000001251408, -178.6731074845244507 ) ) ;
#184051=CIRCLE ( 'NONE', #146438, 0.09999999999999459321 ) ;
#184056=CARTESIAN_POINT ( 'NONE',  ( 20.95378194480896639, 65.46508800846984855, -195.9580533363765937 ) ) ;
#184086=CYLINDRICAL_SURFACE ( 'NONE', #174622, 0.09999999999999939493 ) ;
#184091=DIRECTION ( 'NONE',  ( -1.000000000000000000, 0.000000000000000000, -0.000000000000000000 ) ) ;
#184186=AXIS2_PLACEMENT_3D ( 'NONE', #53714, #212804, #253192 ) ;
#184233=CIRCLE ( 'NONE', #130249, 0.6000000000000033085 ) ;
#184237=ORIENTED_EDGE ( 'NONE', *, *, #197533, .T. ) ;
#184239=DIRECTION ( 'NONE',  ( 0.000000000000000000, -1.000000000000000000, -8.609265936414504429E-15 ) ) ;
#184250=DIRECTION ( 'NONE',  ( 0.000000000000000000, 0.000000000000000000, -1.000000000000000000 ) ) ;
#184254=ORIENTED_EDGE ( 'NONE', *, *, #147346, .T. ) ;
#184255=TOROIDAL_SURFACE ( 'NONE', #150948, 11.70000000000000462, 0.1000000000000000056 ) ;
#184259=ORIENTED_EDGE ( 'NONE', *, *, #74480, .F. ) ;
#184277=ORIENTED_EDGE ( 'NONE', *, *, #8450, .F. ) ;
#184282=ORIENTED_EDGE ( 'NONE', *, *, #233697, .T. ) ;
#184320=ORIENTED_EDGE ( 'NONE', *, *, #180284, .T. ) ;
#184323=ORIENTED_EDGE ( 'NONE', *, *, #166001, .F. ) ;
#184335=VERTEX_POINT ( 'NONE', #74904 ) ;
#184352=DIRECTION ( 'NONE',  ( -0.000000000000000000, -1.000000000000000000, -6.982962677686266711E-15 ) ) ;
#184426=ORIENTED_EDGE ( 'NONE', *, *, #239629, .T. ) ;
#184462=CARTESIAN_POINT ( 'NONE',  ( 20.41140022480505323, 65.58956915761099538, -195.9081061808921902 ) ) ;
#184485=CARTESIAN_POINT ( 'NONE',  ( -22.50000000000094147, 75.89914163091414423, -215.2726746080137730 ) ) ;
#184510=CARTESIAN_POINT ( 'NONE',  ( -22.01447462590972748, 68.73619979878276354, -203.6221444845839699 ) ) ;
#184548=EDGE_CURVE ( 'NONE', #199384, #38969, #56947, .T. ) ;
#184561=AXIS2_PLACEMENT_3D ( 'NONE', #9712, #46265, #107529 ) ;
#184593=CARTESIAN_POINT ( 'NONE',  ( -21.07946286933445279, 69.67096268100499401, -203.5997913277808493 ) ) ;
#184601=VECTOR ( 'NONE', #174512, 1000.000000000000000 ) ;
#184602=AXIS2_PLACEMENT_3D ( 'NONE', #230691, #250240, #256252 ) ;
#184622=DIRECTION ( 'NONE',  ( 0.000000000000000000, 0.000000000000000000, 1.000000000000000000 ) ) ;
#184646=ORIENTED_EDGE ( 'NONE', *, *, #128372, .T. ) ;
#184652=CARTESIAN_POINT ( 'NONE',  ( -23.15000000000000213, 74.00000000001254818, -183.2477294072864709 ) ) ;
#184659=CARTESIAN_POINT ( 'NONE',  ( 21.05000000000000071, 70.15000000001252545, -180.1556047088023149 ) ) ;
#184672=CYLINDRICAL_SURFACE ( 'NONE', #51190, 0.1000000000000070832 ) ;
#184698=CIRCLE ( 'NONE', #138876, 7.900000000000003908 ) ;
#184705=CIRCLE ( 'NONE', #89027, 12.87499999999999822 ) ;
#184711=CIRCLE ( 'NONE', #34926, 3.899999999999987033 ) ;
#184728=AXIS2_PLACEMENT_3D ( 'NONE', #92375, #216168, #194076 ) ;
#184759=ADVANCED_FACE ( 'NONE', ( #152865 ), #255244, .T. ) ;
#184769=AXIS2_PLACEMENT_3D ( 'NONE', #93898, #74383, #153934 ) ;
#184787=CARTESIAN_POINT ( 'NONE',  ( -21.08198257630413508, 75.92735667622814333, -209.8597042185394059 ) ) ;
#184799=EDGE_LOOP ( 'NONE', ( #135089, #33526, #31120, #222626, #112960 ) ) ;
#184808=ORIENTED_EDGE ( 'NONE', *, *, #46420, .F. ) ;
#184810=CARTESIAN_POINT ( 'NONE',  ( -23.15000000000000213, 64.25000000001249134, -177.0379132551784096 ) ) ;
#184811=DIRECTION ( 'NONE',  ( 1.000000000000000000, 0.000000000000000000, 0.000000000000000000 ) ) ;
#184822=VECTOR ( 'NONE', #224201, 1000.000000000000000 ) ;
#184838=CIRCLE ( 'NONE', #205681, 11.89999999999999325 ) ;
#184839=EDGE_LOOP ( 'NONE', ( #178500, #34526, #202675, #191927, #181053 ) ) ;
#184852=VECTOR ( 'NONE', #236686, 1000.000000000000000 ) ;
#184873=AXIS2_PLACEMENT_3D ( 'NONE', #167631, #7233, #68516 ) ;
#184877=CIRCLE ( 'NONE', #26698, 0.1000000000000028644 ) ;
#184909=EDGE_CURVE ( 'NONE', #99703, #72316, #68050, .T. ) ;
#184914=ORIENTED_EDGE ( 'NONE', *, *, #253996, .T. ) ;
#184950=ORIENTED_EDGE ( 'NONE', *, *, #11377, .T. ) ;
#184984=ORIENTED_EDGE ( 'NONE', *, *, #135086, .T. ) ;
#185008=CARTESIAN_POINT ( 'NONE',  ( 20.94999999999999574, 77.26178616857765746, -195.4366085209788935 ) ) ;
#185057=ADVANCED_FACE ( 'NONE', ( #182678 ), #247090, .T. ) ;
#185078=VERTEX_POINT ( 'NONE', #35187 ) ;
#185087=DIRECTION ( 'NONE',  ( 1.000000000000000000, 0.000000000000000000, 0.000000000000000000 ) ) ;
#185100=EDGE_CURVE ( 'NONE', #57467, #46518, #113840, .T. ) ;
#185116=CARTESIAN_POINT ( 'NONE',  ( 20.94999999999999929, 65.27628289530511552, -195.8581939154368285 ) ) ;
#185136=ORIENTED_EDGE ( 'NONE', *, *, #17479, .F. ) ;
#185143=DIRECTION ( 'NONE',  ( -1.000000000000000000, 0.000000000000000000, 0.000000000000000000 ) ) ;
#185165=DIRECTION ( 'NONE',  ( 0.7071067811865474617, -0.7071067811865474617, -4.937700262164531476E-15 ) ) ;
#185181=EDGE_CURVE ( 'NONE', #4003, #68241, #179804, .T. ) ;
#185230=CARTESIAN_POINT ( 'NONE',  ( -21.00448002041592233, 64.25000000001263345, -196.6747666222132125 ) ) ;
#185234=ADVANCED_FACE ( 'NONE', ( #81926 ), #1122, .F. ) ;
#185240=DIRECTION ( 'NONE',  ( -0.7071067811865127117, -0.7071067811865821007, 0.000000000000000000 ) ) ;
#185261=LINE ( 'NONE', #6614, #62786 ) ;
#185264=CARTESIAN_POINT ( 'NONE',  ( -23.15000000000000213, 85.50000000001261924, -193.6291383618718385 ) ) ;
#185278=AXIS2_PLACEMENT_3D ( 'NONE', #98503, #178114, #2002 ) ;
#185287=CARTESIAN_POINT ( 'NONE',  ( 20.95512820512820440, 65.37615131630076348, -195.8581939154368285 ) ) ;
#185301=ORIENTED_EDGE ( 'NONE', *, *, #249878, .F. ) ;
#185308=DIRECTION ( 'NONE',  ( -1.000000000000000000, -0.000000000000000000, -0.000000000000000000 ) ) ;
#185323=DIRECTION ( 'NONE',  ( 0.000000000000000000, 0.000000000000000000, -1.000000000000000000 ) ) ;
#185337=DIRECTION ( 'NONE',  ( 0.000000000000000000, 0.000000000000000000, 1.000000000000000000 ) ) ;
#185339=CARTESIAN_POINT ( 'NONE',  ( -20.94999999999999929, 77.84915357198842401, -158.4171408647273154 ) ) ;
#185354=CARTESIAN_POINT ( 'NONE',  ( -21.05000000000000071, 77.85102823015347440, -191.8691942151018566 ) ) ;
#185365=EDGE_LOOP ( 'NONE', ( #115022, #1465, #231609, #207826 ) ) ;
#185380=CARTESIAN_POINT ( 'NONE',  ( 20.04142135623730070, 64.35000000001254250, -182.1731074845244507 ) ) ;
#185437=EDGE_LOOP ( 'NONE', ( #236414, #107435, #175029, #209822 ) ) ;
#185447=EDGE_LOOP ( 'NONE', ( #119022, #116894, #208628, #44367 ) ) ;
#185491=CARTESIAN_POINT ( 'NONE',  ( -21.13435531349799135, 69.50627893642020183, -203.5231074845243882 ) ) ;
#185507=ORIENTED_EDGE ( 'NONE', *, *, #221868, .F. ) ;
#185585=VECTOR ( 'NONE', #220880, 1000.000000000000000 ) ;
#185589=DIRECTION ( 'NONE',  ( -0.7071067811865127117, -0.7071067811865821007, 0.000000000000000000 ) ) ;
#185606=DIRECTION ( 'NONE',  ( 1.301042606982683734E-14, 0.8660254037844367092, -0.5000000000000037748 ) ) ;
#185648=DIRECTION ( 'NONE',  ( 0.000000000000000000, 0.000000000000000000, -1.000000000000000000 ) ) ;
#185713=DIRECTION ( 'NONE',  ( 0.000000000000000000, -0.7397360091702647189, -0.6728971962616949742 ) ) ;
#185717=EDGE_CURVE ( 'NONE', #24355, #138354, #64316, .T. ) ;
#185732=ADVANCED_FACE ( 'NONE', ( #235588 ), #130952, .T. ) ;
#185734=CARTESIAN_POINT ( 'NONE',  ( 21.95218792049437795, 68.79849243876603282, -203.6221359243243114 ) ) ;
#185754=CARTESIAN_POINT ( 'NONE',  ( 18.59999999999999076, 77.85161776048127535, -158.4199177649206831 ) ) ;
#185756=CARTESIAN_POINT ( 'NONE',  ( 20.74897398619119215, 65.40430697834617035, -195.8437960282675192 ) ) ;
#185777=VERTEX_POINT ( 'NONE', #166370 ) ;
#185815=CARTESIAN_POINT ( 'NONE',  ( -23.15000000000000213, 71.75000000001253397, -182.2731074845243882 ) ) ;
#185824=CARTESIAN_POINT ( 'NONE',  ( -21.05000000000000071, 74.25000000001259082, -191.8535959266227451 ) ) ;
#185825=EDGE_CURVE ( 'NONE', #161777, #204733, #204157, .T. ) ;
#185834=CARTESIAN_POINT ( 'NONE',  ( 18.59999999999999787, 77.85102823015347440, -191.8691942151018566 ) ) ;
#185910=CYLINDRICAL_SURFACE ( 'NONE', #144686, 11.80000000000000426 ) ;
#185918=ORIENTED_EDGE ( 'NONE', *, *, #177417, .F. ) ;
#185972=FACE_OUTER_BOUND ( 'NONE', #191545, .T. ) ;
#185974=ORIENTED_EDGE ( 'NONE', *, *, #202522, .T. ) ;
#185993=CARTESIAN_POINT ( 'NONE',  ( 22.50000000000000000, 75.90000000001276703, -215.2731074845243597 ) ) ;
#186007=CYLINDRICAL_SURFACE ( 'NONE', #69054, 0.09999999999999939493 ) ;
#186033=ADVANCED_FACE ( 'NONE', ( #51487 ), #71103, .T. ) ;
#186058=CARTESIAN_POINT ( 'NONE',  ( -23.15000000000000213, 76.00000000001267608, -203.5231074845243597 ) ) ;
#186067=EDGE_CURVE ( 'NONE', #96287, #92780, #240119, .T. ) ;
#186081=DIRECTION ( 'NONE',  ( 1.000000000000000000, 0.000000000000000000, 0.000000000000000000 ) ) ;
#186107=CARTESIAN_POINT ( 'NONE',  ( -22.59999999999999787, 76.00000000001267608, -203.5231074845243597 ) ) ;
#186146=DIRECTION ( 'NONE',  ( -0.000000000000000000, 6.982962677686266711E-15, -1.000000000000000000 ) ) ;
#186194=ORIENTED_EDGE ( 'NONE', *, *, #41597, .T. ) ;
#186203=DIRECTION ( 'NONE',  ( 0.000000000000000000, -1.000000000000000000, 0.000000000000000000 ) ) ;
#186247=AXIS2_PLACEMENT_3D ( 'NONE', #134026, #94898, #131472 ) ;
#186277=AXIS2_PLACEMENT_3D ( 'NONE', #40375, #162875, #239830 ) ;
#186294=VECTOR ( 'NONE', #165486, 1000.000000000000000 ) ;
#186306=DIRECTION ( 'NONE',  ( 0.000000000000000000, -0.8660254037844468122, -0.4999999999999859557 ) ) ;
#186337=DIRECTION ( 'NONE',  ( -1.000000000000000000, 2.952720810173289112E-16, 2.061873921506763405E-30 ) ) ;
#186355=ADVANCED_FACE ( 'NONE', ( #194290 ), #27308, .T. ) ;
#186369=CARTESIAN_POINT ( 'NONE',  ( -21.44999999999999929, 68.65000000001253966, -182.3731074845244109 ) ) ;
#186378=ORIENTED_EDGE ( 'NONE', *, *, #220465, .T. ) ;
#186383=CIRCLE ( 'NONE', #190669, 0.1000000000000072220 ) ;
#186385=DIRECTION ( 'NONE',  ( 0.000000000000000000, 6.982962677686266711E-15, -1.000000000000000000 ) ) ;
#186386=CARTESIAN_POINT ( 'NONE',  ( -18.50000000000000000, 64.35000000001264198, -196.5083017138704236 ) ) ;
#186459=EDGE_LOOP ( 'NONE', ( #251838, #184259, #241023, #228840 ) ) ;
#186491=VERTEX_POINT ( 'NONE', #209984 ) ;
#186496=ORIENTED_EDGE ( 'NONE', *, *, #220025, .T. ) ;
#186506=CYLINDRICAL_SURFACE ( 'NONE', #177708, 11.80000000000000426 ) ;
#186536=VECTOR ( 'NONE', #22604, 1000.000000000000000 ) ;
#186601=CYLINDRICAL_SURFACE ( 'NONE', #158570, 0.5000000000000004441 ) ;
#186611=DIRECTION ( 'NONE',  ( 0.7071067811865127117, 0.7071067811865821007, 0.000000000000000000 ) ) ;
#186630=FACE_OUTER_BOUND ( 'NONE', #203279, .T. ) ;
#186649=CARTESIAN_POINT ( 'NONE',  ( -21.05000000000000071, 77.36087058720467269, -195.4501095574333931 ) ) ;
#186654=FACE_OUTER_BOUND ( 'NONE', #208633, .T. ) ;
#186673=CARTESIAN_POINT ( 'NONE',  ( -21.05000000000000071, 76.00000000001247713, -174.1231074845243540 ) ) ;
#186676=CARTESIAN_POINT ( 'NONE',  ( 18.59999999999997655, 64.25000000001244871, -170.0231074845244166 ) ) ;
#186685=CARTESIAN_POINT ( 'NONE',  ( -22.48479450179659977, 75.95300841882587406, -215.1731059307759892 ) ) ;
#186689=ORIENTED_EDGE ( 'NONE', *, *, #226665, .T. ) ;
#186702=DIRECTION ( 'NONE',  ( -3.890533409366484652E-14, 0.1298341882520054891, 0.9915357197604850459 ) ) ;
#186717=DIRECTION ( 'NONE',  ( 0.000000000000000000, -0.9876197685951263461, 0.1568667991644794590 ) ) ;
#186723=AXIS2_PLACEMENT_3D ( 'NONE', #233634, #254439, #13298 ) ;
#186758=AXIS2_PLACEMENT_3D ( 'NONE', #52471, #32978, #192028 ) ;
#186763=VERTEX_POINT ( 'NONE', #51846 ) ;
#186905=EDGE_CURVE ( 'NONE', #220964, #115079, #123798, .T. ) ;
#186946=EDGE_LOOP ( 'NONE', ( #159004, #107260, #187672, #2305 ) ) ;
#186949=VECTOR ( 'NONE', #115875, 1000.000000000000000 ) ;
#186954=DIRECTION ( 'NONE',  ( 1.000000000000000000, 0.000000000000000000, 0.000000000000000000 ) ) ;
#186960=FACE_BOUND ( 'NONE', #25186, .T. ) ;
#187003=ORIENTED_EDGE ( 'NONE', *, *, #192235, .F. ) ;
#187021=VECTOR ( 'NONE', #132766, 1000.000000000000000 ) ;
#187070=CARTESIAN_POINT ( 'NONE',  ( 21.05000000000000071, 75.90220970870350925, -209.7809220950058773 ) ) ;
#187075=CYLINDRICAL_SURFACE ( 'NONE', #40255, 0.09999999999998898659 ) ;
#187103=DIRECTION ( 'NONE',  ( 0.000000000000000000, -8.326672684688666480E-14, 1.000000000000000000 ) ) ;
#187110=DIRECTION ( 'NONE',  ( 1.000000000000000000, 0.000000000000000000, 0.000000000000000000 ) ) ;
#187112=ORIENTED_EDGE ( 'NONE', *, *, #179376, .F. ) ;
#187116=AXIS2_PLACEMENT_3D ( 'NONE', #235366, #60576, #198813 ) ;
#187126=FACE_OUTER_BOUND ( 'NONE', #124087, .T. ) ;
#187142=ORIENTED_EDGE ( 'NONE', *, *, #153015, .F. ) ;
#187143=DIRECTION ( 'NONE',  ( 0.000000000000000000, 1.000000000000000000, 6.938893903907222067E-15 ) ) ;
#187151=CARTESIAN_POINT ( 'NONE',  ( -20.94983749550516450, 65.70233904877071041, -164.5487410911968595 ) ) ;
#187182=VERTEX_POINT ( 'NONE', #1703 ) ;
#187186=DIRECTION ( 'NONE',  ( 0.000000000000000000, 6.769652589177795712E-15, -1.000000000000000000 ) ) ;
#187190=AXIS2_PLACEMENT_3D ( 'NONE', #29223, #107426, #142681 ) ;
#187223=CARTESIAN_POINT ( 'NONE',  ( 18.54116936837188234, 85.46356419838508600, -196.4745649936360508 ) ) ;
#187269=AXIS2_PLACEMENT_3D ( 'NONE', #230948, #66720, #88817 ) ;
#187270=ORIENTED_EDGE ( 'NONE', *, *, #3190, .F. ) ;
#187402=EDGE_CURVE ( 'NONE', #152534, #210483, #192088, .T. ) ;
#187412=CARTESIAN_POINT ( 'NONE',  ( -23.25000000000000000, 74.00000000001254818, -183.2477294072864709 ) ) ;
#187486=CARTESIAN_POINT ( 'NONE',  ( 21.05000000000000071, 87.48912529308871910, -200.4231074845242802 ) ) ;
#187498=VECTOR ( 'NONE', #185165, 1000.000000000000114 ) ;
#187499=ORIENTED_EDGE ( 'NONE', *, *, #11377, .F. ) ;
#187521=AXIS2_PLACEMENT_3D ( 'NONE', #124283, #184239, #5576 ) ;
#187549=DIRECTION ( 'NONE',  ( 1.000000000000000000, 0.000000000000000000, 0.000000000000000000 ) ) ;
#187564=CARTESIAN_POINT ( 'NONE',  ( -20.54999999999999716, 76.00000000001244871, -170.0231074845243597 ) ) ;
#187573=DIRECTION ( 'NONE',  ( 0.000000000000000000, 0.000000000000000000, 1.000000000000000000 ) ) ;
#187574=CARTESIAN_POINT ( 'NONE',  ( -23.15000000000000213, 87.65000000001246860, -173.1231074845242688 ) ) ;
#187584=AXIS2_PLACEMENT_3D ( 'NONE', #184031, #243998, #180199 ) ;
#187593=ORIENTED_EDGE ( 'NONE', *, *, #203575, .F. ) ;
#187607=EDGE_LOOP ( 'NONE', ( #82823, #171705, #160696, #92548, #82749 ) ) ;
#187624=ORIENTED_EDGE ( 'NONE', *, *, #98679, .T. ) ;
#187633=EDGE_CURVE ( 'NONE', #62333, #207338, #177674, .T. ) ;
#187636=EDGE_LOOP ( 'NONE', ( #52994, #7869, #237196, #222993 ) ) ;
#187664=DIRECTION ( 'NONE',  ( 1.000000000000000000, 0.000000000000000000, 0.000000000000000000 ) ) ;
#187672=ORIENTED_EDGE ( 'NONE', *, *, #175841, .F. ) ;
#187693=EDGE_CURVE ( 'NONE', #172693, #100865, #189911, .T. ) ;
#187701=CARTESIAN_POINT ( 'NONE',  ( 20.94999999999999929, 71.18691588786307989, -191.5815897280005800 ) ) ;
#187719=LINE ( 'NONE', #207282, #42986 ) ;
#187733=ORIENTED_EDGE ( 'NONE', *, *, #231771, .T. ) ;
#187738=CARTESIAN_POINT ( 'NONE',  ( -18.50000000000000000, 64.25000000001260503, -191.3731074845244393 ) ) ;
#187739=VECTOR ( 'NONE', #33128, 999.9999999999998863 ) ;
#187752=ADVANCED_FACE ( 'NONE', ( #225725 ), #156638, .T. ) ;
#187766=ORIENTED_EDGE ( 'NONE', *, *, #153015, .T. ) ;
#187768=LINE ( 'NONE', #7845, #70174 ) ;
#187771=CARTESIAN_POINT ( 'NONE',  ( 20.94999999999999929, 77.13501884592258762, -162.3061306010920362 ) ) ;
#187815=CARTESIAN_POINT ( 'NONE',  ( -20.94999999999999929, 64.25000000001264766, -196.5083017138704236 ) ) ;
#187817=ORIENTED_EDGE ( 'NONE', *, *, #213375, .F. ) ;
#187850=ORIENTED_EDGE ( 'NONE', *, *, #161425, .F. ) ;
#187854=ORIENTED_EDGE ( 'NONE', *, *, #22755, .F. ) ;
#187905=DIRECTION ( 'NONE',  ( 0.000000000000000000, 1.000000000000000000, 6.982962677686266711E-15 ) ) ;
#187912=LINE ( 'NONE', #33694, #187021 ) ;
#187929=EDGE_LOOP ( 'NONE', ( #47228, #17061, #232406, #164472, #112758, #115908, #183675, #68092, #192645, #88897, #213506, #191550 ) ) ;
#187936=AXIS2_PLACEMENT_3D ( 'NONE', #211004, #173207, #76612 ) ;
#187964=ORIENTED_EDGE ( 'NONE', *, *, #160385, .T. ) ;
#187971=CARTESIAN_POINT ( 'NONE',  ( -21.45000000000000284, 68.29142135624991283, -191.1731074845243938 ) ) ;
#187984=VECTOR ( 'NONE', #142130, 1000.000000000000000 ) ;
#188021=ORIENTED_EDGE ( 'NONE', *, *, #195901, .T. ) ;
#188025=DIRECTION ( 'NONE',  ( 0.000000000000000000, 0.000000000000000000, -1.000000000000000000 ) ) ;
#188065=ORIENTED_EDGE ( 'NONE', *, *, #124429, .F. ) ;
#188102=ORIENTED_EDGE ( 'NONE', *, *, #214860, .T. ) ;
#188138=CARTESIAN_POINT ( 'NONE',  ( 21.05000000000000071, 76.00000000001264766, -199.2231074845243199 ) ) ;
#188139=VECTOR ( 'NONE', #134000, 1000.000000000000000 ) ;
#188146=DIRECTION ( 'NONE',  ( 0.000000000000000000, -1.000000000000000000, -7.105427357601001859E-15 ) ) ;
#188150=SPHERICAL_SURFACE ( 'NONE', #256832, 0.1000000000000000056 ) ;
#188155=CARTESIAN_POINT ( 'NONE',  ( 18.49999999999999289, 68.87972903831482085, -166.3635444426850825 ) ) ;
#188157=LINE ( 'NONE', #190752, #161827 ) ;
#188162=CARTESIAN_POINT ( 'NONE',  ( 20.94999999999999929, 76.00000000001259082, -190.5481074845243654 ) ) ;
#188171=EDGE_CURVE ( 'NONE', #60084, #80905, #127559, .T. ) ;
#188196=VERTEX_POINT ( 'NONE', #128590 ) ;
#188198=DIRECTION ( 'NONE',  ( 0.000000000000000000, 0.000000000000000000, 1.000000000000000000 ) ) ;
#188215=CARTESIAN_POINT ( 'NONE',  ( -23.15000000000000213, 71.85000000001254250, -182.3731074845244109 ) ) ;
#188220=CARTESIAN_POINT ( 'NONE',  ( 18.49999999999999289, 65.50857864377520912, -178.6731074845244223 ) ) ;
#188229=CARTESIAN_POINT ( 'NONE',  ( -18.53317502108577486, 65.67736539654997330, -164.4625116876572406 ) ) ;
#188234=EDGE_CURVE ( 'NONE', #172249, #213320, #9919, .T. ) ;
#188235=VERTEX_POINT ( 'NONE', #67325 ) ;
#188249=CYLINDRICAL_SURFACE ( 'NONE', #12961, 12.87499999999999822 ) ;
#188287=CARTESIAN_POINT ( 'NONE',  ( 21.07928932188134397, 69.67148334361938566, -203.6220026301787982 ) ) ;
#188309=AXIS2_PLACEMENT_3D ( 'NONE', #19653, #256916, #116195 ) ;
#188372=DIRECTION ( 'NONE',  ( 1.000000000000000000, 0.000000000000000000, 0.000000000000000000 ) ) ;
#188405=CARTESIAN_POINT ( 'NONE',  ( -20.87600722750343252, 65.66887361445387228, -164.4329845918269939 ) ) ;
#188438=( NAMED_UNIT ( * ) PLANE_ANGLE_UNIT ( ) SI_UNIT ( $, .RADIAN. ) );
#188455=CARTESIAN_POINT ( 'NONE',  ( -23.25000000000000000, 76.10000000001276987, -215.1726782920691505 ) ) ;
#188489=CARTESIAN_POINT ( 'NONE',  ( 21.14999999999999858, 64.35000000001267040, -203.4231074845244507 ) ) ;
#188491=B_SPLINE_CURVE_WITH_KNOTS ( 'NONE', 3,
 ( #23778, #103253, #6743, #86256, #107123, #101962, #186685, #87548, #83673, #182845, #242778, #167141, #68003, #147543, #245370, #203665 ),
 .UNSPECIFIED., .F., .F.,
 ( 4, 3, 3, 3, 3, 4 ),
 ( 0.000000000000000000, 2.209075297431620268E-05, 5.594258369009776820E-05, 8.979524372341989448E-05, 0.0001236472815274567327, 0.0001574990747609542811 ),
 .UNSPECIFIED. ) ;
#188520=VERTEX_POINT ( 'NONE', #224800 ) ;
#188538=AXIS2_PLACEMENT_3D ( 'NONE', #35023, #118380, #54540 ) ;
#188568=CARTESIAN_POINT ( 'NONE',  ( -18.50000000000000000, 68.87972903831483507, -166.3635444426850825 ) ) ;
#188572=CARTESIAN_POINT ( 'NONE',  ( 21.05000000000000071, 76.00000000001247713, -174.1231074845243540 ) ) ;
#188577=EDGE_LOOP ( 'NONE', ( #4594, #223651 ) ) ;
#188586=AXIS2_PLACEMENT_3D ( 'NONE', #256547, #192794, #158820 ) ;
#188598=CARTESIAN_POINT ( 'NONE',  ( -22.00411653962162362, 68.74655713164246151, -203.6221455902930302 ) ) ;
#188605=EDGE_LOOP ( 'NONE', ( #28180, #150059, #52730, #138288, #61625, #114060, #257424, #3858, #71364, #26910, #217347, #233387, #54488, #180037, #74262, #144505, #168472, #79482, #155499, #254196, #250581, #226242, #53827, #90198, #83904 ) ) ;
#188615=EDGE_CURVE ( 'NONE', #100865, #12967, #152329, .T. ) ;
#188643=ADVANCED_FACE ( 'NONE', ( #215520 ), #57721, .F. ) ;
#188670=ORIENTED_EDGE ( 'NONE', *, *, #47352, .F. ) ;
#188704=ORIENTED_EDGE ( 'NONE', *, *, #180284, .F. ) ;
#188736=CARTESIAN_POINT ( 'NONE',  ( 23.14999999999998437, 76.00000000001267608, -203.5231074845243597 ) ) ;
#188739=CARTESIAN_POINT ( 'NONE',  ( 18.59999999999999076, 64.35000000001251408, -178.6731074845244507 ) ) ;
#188752=FACE_OUTER_BOUND ( 'NONE', #64388, .T. ) ;
#188755=CARTESIAN_POINT ( 'NONE',  ( -21.07094088545368749, 75.90110629746051529, -209.8432747064414912 ) ) ;
#188756=DIRECTION ( 'NONE',  ( 0.000000000000000000, 0.000000000000000000, -1.000000000000000000 ) ) ;
#188785=CARTESIAN_POINT ( 'NONE',  ( 21.05000000000000071, 76.00000000001267608, -203.5231074845243597 ) ) ;
#188795=CARTESIAN_POINT ( 'NONE',  ( -21.05000000000000071, 64.35000000001268461, -203.4231074845244507 ) ) ;
#188800=CIRCLE ( 'NONE', #84709, 0.1000000000000028644 ) ;
#188810=VERTEX_POINT ( 'NONE', #221916 ) ;
#188834=EDGE_CURVE ( 'NONE', #130315, #256678, #223011, .T. ) ;
#188844=LINE ( 'NONE', #89731, #76847 ) ;
#188845=DIRECTION ( 'NONE',  ( 0.000000000000000000, -6.608470384673580212E-15, 1.000000000000000000 ) ) ;
#188848=FACE_OUTER_BOUND ( 'NONE', #179938, .T. ) ;
#188854=PLANE ( 'NONE',  #31182 ) ;
#188892=ORIENTED_EDGE ( 'NONE', *, *, #162409, .T. ) ;
#188962=CARTESIAN_POINT ( 'NONE',  ( 21.40925344232283223, 75.90104981139307938, -210.1816263439147860 ) ) ;
#188974=AXIS2_PLACEMENT_3D ( 'NONE', #159174, #196971, #60024 ) ;
#188983=EDGE_CURVE ( 'NONE', #102606, #59053, #173376, .T. ) ;
#189020=ORIENTED_EDGE ( 'NONE', *, *, #56798, .F. ) ;
#189028=DIRECTION ( 'NONE',  ( 0.000000000000000000, 0.8700118002898393765, -0.4930308989875104575 ) ) ;
#189082=CARTESIAN_POINT ( 'NONE',  ( -21.14999999999999858, 64.25000000001264766, -196.7392418215462726 ) ) ;
#189096=DIRECTION ( 'NONE',  ( -1.000000000000000000, -0.000000000000000000, -0.000000000000000000 ) ) ;
#189105=CYLINDRICAL_SURFACE ( 'NONE', #3580, 0.1000000000000046685 ) ;
#189108=CARTESIAN_POINT ( 'NONE',  ( -20.94999999999999929, 74.83729825007462466, -195.6231074845243540 ) ) ;
#189117=CARTESIAN_POINT ( 'NONE',  ( 22.39999999999999503, 64.35000000001267040, -203.5231074845244166 ) ) ;
#189120=CARTESIAN_POINT ( 'NONE',  ( -23.15000000000000213, 76.00000000001267608, -203.5231074845243597 ) ) ;
#189136=DIRECTION ( 'NONE',  ( 7.304098846218134667E-16, 1.000000000000000000, 6.982962677686266711E-15 ) ) ;
#189142=CIRCLE ( 'NONE', #222410, 0.09999999999998898659 ) ;
#189170=DIRECTION ( 'NONE',  ( 0.7071067811865487940, -4.937700262164522799E-15, 0.7071067811865463515 ) ) ;
#189175=AXIS2_PLACEMENT_3D ( 'NONE', #85927, #204610, #228043 ) ;
#189195=VECTOR ( 'NONE', #160039, 1000.000000000000000 ) ;
#189206=FACE_OUTER_BOUND ( 'NONE', #59972, .T. ) ;
#189227=DIRECTION ( 'NONE',  ( 1.000000000000000000, 0.000000000000000000, 0.000000000000000000 ) ) ;
#189240=AXIS2_PLACEMENT_3D ( 'NONE', #252373, #13786, #257155 ) ;
#189261=ORIENTED_EDGE ( 'NONE', *, *, #242116, .F. ) ;
#189264=ADVANCED_FACE ( 'NONE', ( #159126 ), #139973, .T. ) ;
#189265=CARTESIAN_POINT ( 'NONE',  ( -23.15000000000000213, 74.08971962618080909, -190.8917396293254285 ) ) ;
#189268=TOROIDAL_SURFACE ( 'NONE', #176799, 0.2000000000000000111, 0.1000000000000000056 ) ;
#189330=EDGE_CURVE ( 'NONE', #104211, #234183, #197106, .T. ) ;
#189339=EDGE_LOOP ( 'NONE', ( #121593, #38670, #66037, #184914 ) ) ;
#189340=AXIS2_PLACEMENT_3D ( 'NONE', #15473, #55826, #74181 ) ;
#189345=ADVANCED_FACE ( 'NONE', ( #242472 ), #69007, .T. ) ;
#189371=DIRECTION ( 'NONE',  ( 0.000000000000000000, -1.000000000000000000, -6.982962677686265922E-15 ) ) ;
#189386=CARTESIAN_POINT ( 'NONE',  ( -20.94999999999999929, 76.00000000001244871, -170.0231074845243597 ) ) ;
#189417=ORIENTED_EDGE ( 'NONE', *, *, #79568, .F. ) ;
#189429=DIRECTION ( 'NONE',  ( 0.000000000000000000, 0.000000000000000000, 1.000000000000000000 ) ) ;
#189499=CARTESIAN_POINT ( 'NONE',  ( 20.84999999999998721, 65.66751761918722252, -164.4282609406112670 ) ) ;
#189502=VECTOR ( 'NONE', #98517, 1000.000000000000000 ) ;
#189504=DIRECTION ( 'NONE',  ( 0.000000000000000000, 1.000000000000000000, 0.000000000000000000 ) ) ;
#189552=CARTESIAN_POINT ( 'NONE',  ( -20.94999999999999929, 64.35000000001262777, -196.5083017138704236 ) ) ;
#189559=VERTEX_POINT ( 'NONE', #57090 ) ;
#189569=AXIS2_PLACEMENT_3D ( 'NONE', #18966, #174248, #232921 ) ;
#189587=DIRECTION ( 'NONE',  ( -1.000000000000000000, -0.000000000000000000, -0.000000000000000000 ) ) ;
#189614=ADVANCED_FACE ( 'NONE', ( #223547 ), #592, .F. ) ;
#189624=EDGE_CURVE ( 'NONE', #38825, #152824, #150485, .T. ) ;
#189631=ORIENTED_EDGE ( 'NONE', *, *, #124741, .T. ) ;
#189645=ORIENTED_EDGE ( 'NONE', *, *, #50019, .T. ) ;
#189679=CIRCLE ( 'NONE', #168875, 0.1000000000000072220 ) ;
#189729=TOROIDAL_SURFACE ( 'NONE', #106310, 0.4000000000000005773, 0.1000000000000000056 ) ;
#189741=CARTESIAN_POINT ( 'NONE',  ( -18.58744394320977733, 85.56638515456042171, -163.2002594306475203 ) ) ;
#189756=ORIENTED_EDGE ( 'NONE', *, *, #1473, .T. ) ;
#189787=EDGE_CURVE ( 'NONE', #142689, #28569, #90471, .T. ) ;
#189809=AXIS2_PLACEMENT_3D ( 'NONE', #64174, #121608, #241522 ) ;
#189820=ADVANCED_FACE ( 'NONE', ( #254653, #18647, #77321 ), #36965, .F. ) ;
#189868=DIRECTION ( 'NONE',  ( 0.000000000000000000, -5.214354714482140540E-14, 1.000000000000000000 ) ) ;
#189879=CIRCLE ( 'NONE', #156609, 0.2000000000000057288 ) ;
#189911=CIRCLE ( 'NONE', #123270, 0.09999999999998898659 ) ;
#189951=ORIENTED_EDGE ( 'NONE', *, *, #67234, .T. ) ;
#189952=AXIS2_PLACEMENT_3D ( 'NONE', #234545, #135437, #76752 ) ;
#189960=DIRECTION ( 'NONE',  ( 0.000000000000000000, -7.086529944415886769E-15, 1.000000000000000000 ) ) ;
#189964=CARTESIAN_POINT ( 'NONE',  ( 20.94999999999999929, 65.27628289530501604, -182.2731074845244450 ) ) ;
#189977=CARTESIAN_POINT ( 'NONE',  ( -23.25000000000000000, 65.66751761918722252, -164.4282609406112670 ) ) ;
#190049=CARTESIAN_POINT ( 'NONE',  ( -22.39999999999999858, 76.00000000001267608, -203.6231074845243540 ) ) ;
#190135=DIRECTION ( 'NONE',  ( 0.000000000000000000, 0.7397360091702792628, -0.6728971962616790981 ) ) ;
#190142=CARTESIAN_POINT ( 'NONE',  ( -18.59999999999999787, 77.83534155023700407, -191.9679561919613491 ) ) ;
#190148=CARTESIAN_POINT ( 'NONE',  ( 21.00000000000000000, 66.25000000001253397, -182.2731074845244450 ) ) ;
#190175=CYLINDRICAL_SURFACE ( 'NONE', #207749, 0.1000000000000072220 ) ;
#190180=CARTESIAN_POINT ( 'NONE',  ( -23.15000000000000213, 76.00000000001246292, -172.0231074845243597 ) ) ;
#190185=ORIENTED_EDGE ( 'NONE', *, *, #58673, .T. ) ;
#190268=CIRCLE ( 'NONE', #244210, 0.09999999999998898659 ) ;
#190276=AXIS2_PLACEMENT_3D ( 'NONE', #166039, #245560, #66907 ) ;
#190287=AXIS2_PLACEMENT_3D ( 'NONE', #256041, #198692, #102127 ) ;
#190310=DIRECTION ( 'NONE',  ( 1.000000000000000000, 0.000000000000000000, 0.000000000000000000 ) ) ;
#190336=CARTESIAN_POINT ( 'NONE',  ( -20.94999999999999929, 76.00000000001253397, -181.8231074845243711 ) ) ;
#190337=EDGE_LOOP ( 'NONE', ( #2832, #217005, #70380, #91251 ) ) ;
#190353=EDGE_LOOP ( 'NONE', ( #223693, #102604, #149805 ) ) ;
#190365=EDGE_CURVE ( 'NONE', #255583, #6746, #182261, .T. ) ;
#190367=LINE ( 'NONE', #246465, #252545 ) ;
#190376=CIRCLE ( 'NONE', #77911, 0.09999999999998898659 ) ;
#190401=CARTESIAN_POINT ( 'NONE',  ( -18.59999999999999787, 77.73670573947995877, -158.5056848969006182 ) ) ;
#190411=FACE_OUTER_BOUND ( 'NONE', #156456, .T. ) ;
#190420=EDGE_CURVE ( 'NONE', #51521, #36195, #198994, .T. ) ;
#190449=CIRCLE ( 'NONE', #119692, 0.09999999999998898659 ) ;
#190475=DIRECTION ( 'NONE',  ( 1.000000000000000000, -0.000000000000000000, 0.000000000000000000 ) ) ;
#190535=DIRECTION ( 'NONE',  ( 0.000000000000000000, -1.000000000000000000, -6.982962677686266711E-15 ) ) ;
#190536=DIRECTION ( 'NONE',  ( 0.000000000000000000, 0.000000000000000000, 1.000000000000000000 ) ) ;
#190555=CARTESIAN_POINT ( 'NONE',  ( 21.04999999999999716, 69.69554417806499202, -203.5020720079843102 ) ) ;
#190573=FACE_OUTER_BOUND ( 'NONE', #189339, .T. ) ;
#190590=LINE ( 'NONE', #11956, #16844 ) ;
#190607=CARTESIAN_POINT ( 'NONE',  ( -22.39999999999999503, 68.20922040163927136, -203.6231074845244109 ) ) ;
#190657=FACE_OUTER_BOUND ( 'NONE', #118456, .T. ) ;
#190669=AXIS2_PLACEMENT_3D ( 'NONE', #7297, #25595, #45145 ) ;
#190680=ADVANCED_FACE ( 'NONE', ( #101363 ), #38714, .T. ) ;
#190686=CIRCLE ( 'NONE', #144858, 0.09999999999998898659 ) ;
#190726=FILL_AREA_STYLE ('',( #51151 ) ) ;
#190743=DIRECTION ( 'NONE',  ( 0.000000000000000000, 0.000000000000000000, -1.000000000000000000 ) ) ;
#190750=FACE_OUTER_BOUND ( 'NONE', #208440, .T. ) ;
#190752=CARTESIAN_POINT ( 'NONE',  ( 23.24999999999999289, 64.25000000001259082, -191.3731074845244393 ) ) ;
#190783=CYLINDRICAL_SURFACE ( 'NONE', #150916, 0.1000000000000106914 ) ;
#190811=CARTESIAN_POINT ( 'NONE',  ( 20.94999999999999929, 65.70711192142420032, -164.5651054685122574 ) ) ;
#190868=ORIENTED_EDGE ( 'NONE', *, *, #118562, .F. ) ;
#190968=LINE ( 'NONE', #30606, #17808 ) ;
#190972=DIRECTION ( 'NONE',  ( 0.000000000000000000, 0.000000000000000000, 1.000000000000000000 ) ) ;
#190978=ADVANCED_FACE ( 'NONE', ( #65693 ), #248194, .F. ) ;
#190989=ORIENTED_EDGE ( 'NONE', *, *, #176839, .T. ) ;
#190994=ADVANCED_FACE ( 'NONE', ( #226019, #186960 ), #7005, .F. ) ;
#190998=DIRECTION ( 'NONE',  ( 1.000000000000000000, 0.000000000000000000, 0.000000000000000000 ) ) ;
#191008=CARTESIAN_POINT ( 'NONE',  ( -23.15000000000000213, 76.00000000001244871, -170.0231074845243597 ) ) ;
#191012=AXIS2_PLACEMENT_3D ( 'NONE', #6596, #126554, #106973 ) ;
#191014=( BOUNDED_SURFACE ( )  B_SPLINE_SURFACE ( 3, 2, ( 
 ( #256641, #157646, #139297 ),
 ( #78053, #199307, #220153 ),
 ( #95055, #174654, #41529 ),
 ( #237141, #194183, #155068 ),
 ( #135455, #75522, #15553 ),
 ( #218841, #58474, #40251 ) ),
 .UNSPECIFIED., .F., .F., .F. ) 
 B_SPLINE_SURFACE_WITH_KNOTS ( ( 4, 2, 4 ),
 ( 3, 3 ),
 ( 6.719893378901192380E-05, 0.0002757154632485820170, 0.0004842319927081520695 ),
 ( 0.000000000000000000, 1.000000000000000000 ),
 .UNSPECIFIED. ) 
 GEOMETRIC_REPRESENTATION_ITEM ( )  RATIONAL_B_SPLINE_SURFACE ( (
 ( 1.000000000000000000, 0.7250110520819756932, 1.000000000000000000),
 ( 1.000000000000000000, 0.7277932058358560496, 1.000000000000000000),
 ( 1.000000000000000000, 0.7278452872618367264, 1.000000000000000000),
 ( 1.000000000000000000, 0.7221445671548437639, 1.000000000000000000),
 ( 1.000000000000000000, 0.7163662143779749858, 1.000000000000000000),
 ( 1.000000000000000000, 0.7071067811865475727, 1.000000000000000000) ) ) 
 REPRESENTATION_ITEM ( '' )  SURFACE ( )  );
#191033=DIRECTION ( 'NONE',  ( 1.000000000000000000, 0.000000000000000000, 0.000000000000000000 ) ) ;
#191050=CARTESIAN_POINT ( 'NONE',  ( -18.37151313414632625, 85.57101412579078215, -163.2064445752853601 ) ) ;
#191090=DIRECTION ( 'NONE',  ( 2.715809747126117987E-16, 1.000000000000000000, 8.690591190803577558E-15 ) ) ;
#191155=CARTESIAN_POINT ( 'NONE',  ( -20.94999999999999929, 77.16412189325360771, -162.3082593989527425 ) ) ;
#191216=DIRECTION ( 'NONE',  ( 1.000000000000000000, 0.000000000000000000, 0.000000000000000000 ) ) ;
#191219=ORIENTED_EDGE ( 'NONE', *, *, #199219, .T. ) ;
#191299=ORIENTED_EDGE ( 'NONE', *, *, #209613, .F. ) ;
#191311=EDGE_LOOP ( 'NONE', ( #108111, #155998, #216283, #179242 ) ) ;
#191313=FACE_OUTER_BOUND ( 'NONE', #55605, .T. ) ;
#191333=CYLINDRICAL_SURFACE ( 'NONE', #33747, 0.1000000000000046685 ) ;
#191360=DIRECTION ( 'NONE',  ( 0.000000000000000000, 0.000000000000000000, 1.000000000000000000 ) ) ;
#191380=DIRECTION ( 'NONE',  ( 0.000000000000000000, 0.000000000000000000, 1.000000000000000000 ) ) ;
#191406=FACE_OUTER_BOUND ( 'NONE', #229434, .T. ) ;
#191444=DIRECTION ( 'NONE',  ( 0.000000000000000000, 0.000000000000000000, -1.000000000000000000 ) ) ;
#191469=DIRECTION ( 'NONE',  ( 1.000000000000000000, 0.000000000000000000, 0.000000000000000000 ) ) ;
#191495=DIRECTION ( 'NONE',  ( 0.000000000000000000, -6.661338147750933721E-15, 1.000000000000000000 ) ) ;
#191498=EDGE_CURVE ( 'NONE', #161829, #42440, #162153, .T. ) ;
#191545=EDGE_LOOP ( 'NONE', ( #81925, #177581, #246425, #124302 ) ) ;
#191548=ORIENTED_EDGE ( 'NONE', *, *, #151558, .T. ) ;
#191550=ORIENTED_EDGE ( 'NONE', *, *, #167107, .T. ) ;
#191563=DIRECTION ( 'NONE',  ( 1.000000000000000000, 0.000000000000000000, 0.000000000000000000 ) ) ;
#191579=ORIENTED_EDGE ( 'NONE', *, *, #6666, .T. ) ;
#191607=ORIENTED_EDGE ( 'NONE', *, *, #110318, .T. ) ;
#191610=EDGE_CURVE ( 'NONE', #154016, #224589, #24804, .T. ) ;
#191617=ORIENTED_EDGE ( 'NONE', *, *, #36188, .T. ) ;
#191618=CARTESIAN_POINT ( 'NONE',  ( -23.15000000000000213, 76.00000000001244871, -170.0231074845243597 ) ) ;
#191621=EDGE_CURVE ( 'NONE', #163131, #70073, #112270, .T. ) ;
#191638=ORIENTED_EDGE ( 'NONE', *, *, #169463, .F. ) ;
#191641=LINE ( 'NONE', #12994, #32956 ) ;
#191674=AXIS2_PLACEMENT_3D ( 'NONE', #55027, #75903, #155480 ) ;
#191701=ADVANCED_FACE ( 'NONE', ( #188752 ), #174660, .T. ) ;
#191704=ORIENTED_EDGE ( 'NONE', *, *, #240140, .T. ) ;
#191706=CARTESIAN_POINT ( 'NONE',  ( -20.54999999999999716, 74.07476635515273244, -182.7533510176504876 ) ) ;
#191708=CYLINDRICAL_SURFACE ( 'NONE', #7401, 4.049999999999998046 ) ;
#191752=CARTESIAN_POINT ( 'NONE',  ( -21.05000000000000071, 76.00000000001267608, -203.5231074845243597 ) ) ;
#191816=CIRCLE ( 'NONE', #233499, 0.5000000000000004441 ) ;
#191822=CARTESIAN_POINT ( 'NONE',  ( 18.59999999999999076, 64.35000000001251408, -178.6731074845244507 ) ) ;
#191867=FACE_OUTER_BOUND ( 'NONE', #149480, .T. ) ;
#191878=FACE_OUTER_BOUND ( 'NONE', #101362, .T. ) ;
#191887=CARTESIAN_POINT ( 'NONE',  ( 20.95512820512820440, 67.12384868372450342, -194.9644784893834810 ) ) ;
#191888=VERTEX_POINT ( 'NONE', #195205 ) ;
#191902=EDGE_CURVE ( 'NONE', #254689, #109261, #104022, .T. ) ;
#191927=ORIENTED_EDGE ( 'NONE', *, *, #208223, .F. ) ;
#191938=CIRCLE ( 'NONE', #54330, 0.09999999999999939493 ) ;
#191973=AXIS2_PLACEMENT_3D ( 'NONE', #199060, #38708, #42539 ) ;
#191998=CARTESIAN_POINT ( 'NONE',  ( 21.07946286933444924, 75.92331615675632861, -209.8521448035321555 ) ) ;
#191999=CARTESIAN_POINT ( 'NONE',  ( 20.94999999999999929, 71.00000000001260503, -191.1178414656112921 ) ) ;
#192010=ORIENTED_EDGE ( 'NONE', *, *, #208697, .F. ) ;
#192028=DIRECTION ( 'NONE',  ( 0.000000000000000000, -6.467318590049456648E-15, 1.000000000000000000 ) ) ;
#192075=TOROIDAL_SURFACE ( 'NONE', #100448, 11.65000000000000036, 0.1000000000000000056 ) ;
#192084=MANIFOLD_SOLID_BREP ( 'Stock-MAS-200-1', #203484 ) ;
#192088=LINE ( 'NONE', #155546, #31552 ) ;
#192090=DIRECTION ( 'NONE',  ( 0.000000000000000000, 0.000000000000000000, -1.000000000000000000 ) ) ;
#192103=DIRECTION ( 'NONE',  ( 0.000000000000000000, 0.000000000000000000, -1.000000000000000000 ) ) ;
#192122=CARTESIAN_POINT ( 'NONE',  ( -20.64999999999999858, 76.00000000001244871, -170.0231074845243597 ) ) ;
#192137=EDGE_LOOP ( 'NONE', ( #119838, #226536, #243853, #93971 ) ) ;
#192152=FACE_OUTER_BOUND ( 'NONE', #226641, .T. ) ;
#192173=DIRECTION ( 'NONE',  ( 1.000000000000000000, -0.000000000000000000, 0.000000000000000000 ) ) ;
#192202=ORIENTED_EDGE ( 'NONE', *, *, #147127, .F. ) ;
#192205=ADVANCED_FACE ( 'NONE', ( #140002 ), #180440, .T. ) ;
#192235=EDGE_CURVE ( 'NONE', #52715, #58661, #225010, .T. ) ;
#192255=DIRECTION ( 'NONE',  ( 1.000000000000000000, 0.000000000000000000, 0.000000000000000000 ) ) ;
#192268=FACE_OUTER_BOUND ( 'NONE', #247045, .T. ) ;
#192274=DIRECTION ( 'NONE',  ( 1.000000000000000000, 0.000000000000000000, 0.000000000000000000 ) ) ;
#192282=CIRCLE ( 'NONE', #225557, 0.5000000000000004441 ) ;
#192286=AXIS2_PLACEMENT_3D ( 'NONE', #86131, #126579, #108304 ) ;
#192308=CARTESIAN_POINT ( 'NONE',  ( -20.94999999999999929, 76.00000000001244871, -170.0231074845243597 ) ) ;
#192313=CARTESIAN_POINT ( 'NONE',  ( -18.52309608778521266, 85.64247632006754429, -163.3085111433545933 ) ) ;
#192377=CARTESIAN_POINT ( 'NONE',  ( -20.54999999999999716, 84.73084112150785074, -179.6211822035086243 ) ) ;
#192386=EDGE_CURVE ( 'NONE', #37719, #60608, #216666, .T. ) ;
#192387=TOROIDAL_SURFACE ( 'NONE', #46603, 0.4000000000000017431, 0.1000000000000000056 ) ;
#192393=ADVANCED_FACE ( 'NONE', ( #87736 ), #83359, .T. ) ;
#192399=VERTEX_POINT ( 'NONE', #150314 ) ;
#192422=EDGE_LOOP ( 'NONE', ( #251778, #97583, #232374, #119757 ) ) ;
#192425=CIRCLE ( 'NONE', #859, 0.09999999999999939493 ) ;
#192429=TOROIDAL_SURFACE ( 'NONE', #67339, 0.9750000000000019762, 0.1000000000000000056 ) ;
#192477=AXIS2_PLACEMENT_3D ( 'NONE', #177281, #198091, #237227 ) ;
#192499=LINE ( 'NONE', #16450, #81695 ) ;
#192523=VERTEX_POINT ( 'NONE', #40355 ) ;
#192535=CARTESIAN_POINT ( 'NONE',  ( 18.59999999999999787, 77.83585931145600512, -158.5186683157258187 ) ) ;
#192558=VERTEX_POINT ( 'NONE', #195558 ) ;
#192564=DIRECTION ( 'NONE',  ( 0.000000000000000000, 7.147358527629766941E-15, -1.000000000000000000 ) ) ;
#192575=AXIS2_PLACEMENT_3D ( 'NONE', #166983, #104374, #84800 ) ;
#192616=AXIS2_PLACEMENT_3D ( 'NONE', #133780, #35987, #179352 ) ;
#192619=CARTESIAN_POINT ( 'NONE',  ( -22.47007471830798409, 76.00000000001273293, -211.2438181364508409 ) ) ;
#192645=ORIENTED_EDGE ( 'NONE', *, *, #212427, .F. ) ;
#192650=CARTESIAN_POINT ( 'NONE',  ( -23.25000000000000000, 77.83585931145600512, -158.4186683157258244 ) ) ;
#192665=ORIENTED_EDGE ( 'NONE', *, *, #239629, .F. ) ;
#192670=ADVANCED_FACE ( 'NONE', ( #224066 ), #71118, .T. ) ;
#192674=ADVANCED_FACE ( 'NONE', ( #225342 ), #180361, .T. ) ;
#192699=DIRECTION ( 'NONE',  ( 1.000000000000000000, -3.265361837132813093E-16, -2.280189983783949500E-30 ) ) ;
#192704=DIRECTION ( 'NONE',  ( 0.000000000000000000, 6.982962677686266711E-15, -1.000000000000000000 ) ) ;
#192718=EDGE_CURVE ( 'NONE', #115079, #213491, #90981, .T. ) ;
#192741=CIRCLE ( 'NONE', #80257, 0.09999999999998898659 ) ;
#192752=CARTESIAN_POINT ( 'NONE',  ( -21.05000000000000071, 76.00000000001267608, -203.5231074845243597 ) ) ;
#192768=CIRCLE ( 'NONE', #234248, 12.77500000000000924 ) ;
#192794=DIRECTION ( 'NONE',  ( 1.000000000000000000, 0.000000000000000000, 0.000000000000000000 ) ) ;
#192800=AXIS2_PLACEMENT_3D ( 'NONE', #196182, #197456, #134892 ) ;
#192862=ORIENTED_EDGE ( 'NONE', *, *, #149871, .T. ) ;
#192902=AXIS2_PLACEMENT_3D ( 'NONE', #142548, #222065, #184250 ) ;
#192918=CARTESIAN_POINT ( 'NONE',  ( 18.49999999999998934, 69.45000000001252261, -182.3731074845244109 ) ) ;
#192920=CARTESIAN_POINT ( 'NONE',  ( -22.50000000000000000, 76.00000000001267608, -203.5231074845243597 ) ) ;
#192928=DIRECTION ( 'NONE',  ( 0.000000000000000000, 0.000000000000000000, 1.000000000000000000 ) ) ;
#192978=CARTESIAN_POINT ( 'NONE',  ( 21.53699400385212570, 76.00000000000815703, -210.3108192777586964 ) ) ;
#192998=CIRCLE ( 'NONE', #101335, 0.1000000000000033362 ) ;
#193000=PLANE ( 'NONE',  #98373 ) ;
#193006=AXIS2_PLACEMENT_3D ( 'NONE', #105115, #7340, #221233 ) ;
#193011=CARTESIAN_POINT ( 'NONE',  ( 18.50000000000000000, 85.40000000001262492, -196.2258477248610120 ) ) ;
#193051=DIRECTION ( 'NONE',  ( -0.7071067811865474617, 0.7071067811865474617, 4.937700262164531476E-15 ) ) ;
#193064=CARTESIAN_POINT ( 'NONE',  ( 18.59999999999997655, 76.00000000001244871, -170.0231074845243597 ) ) ;
#193067=DIRECTION ( 'NONE',  ( 2.952720810173289112E-16, 1.000000000000000000, -6.088138035986627436E-46 ) ) ;
#193092=DIRECTION ( 'NONE',  ( 1.000000000000000000, 0.000000000000000000, 0.000000000000000000 ) ) ;
#193105=CARTESIAN_POINT ( 'NONE',  ( -21.05000000000000071, 87.48912529308852015, -173.0231074845243029 ) ) ;
#193107=CIRCLE ( 'NONE', #176360, 0.09999999999998708533 ) ;
#193125=ORIENTED_EDGE ( 'NONE', *, *, #93607, .F. ) ;
#193130=DIRECTION ( 'NONE',  ( 0.000000000000000000, 0.000000000000000000, 1.000000000000000000 ) ) ;
#193131=CARTESIAN_POINT ( 'NONE',  ( 20.94999999999999574, 74.83729825007462466, -195.4231074845243654 ) ) ;
#193133=CARTESIAN_POINT ( 'NONE',  ( 23.24999999999999289, 64.35000000001258513, -191.3731074845244393 ) ) ;
#193138=LINE ( 'NONE', #134408, #91522 ) ;
#193143=EDGE_CURVE ( 'NONE', #55154, #252148, #216458, .T. ) ;
#193152=AXIS2_PLACEMENT_3D ( 'NONE', #2412, #61117, #161527 ) ;
#193157=DIRECTION ( 'NONE',  ( 1.000000000000000000, 0.000000000000000000, 0.000000000000000000 ) ) ;
#193184=CIRCLE ( 'NONE', #114041, 0.09999999999999939493 ) ;
#193233=VERTEX_POINT ( 'NONE', #138745 ) ;
#193278=ORIENTED_EDGE ( 'NONE', *, *, #237302, .T. ) ;
#193301=DIRECTION ( 'NONE',  ( 1.000000000000000000, 7.304098846218105085E-16, 4.217023435051676515E-16 ) ) ;
#193318=VERTEX_POINT ( 'NONE', #239175 ) ;
#193333=CARTESIAN_POINT ( 'NONE',  ( 23.14999999999999503, 64.35000000001258513, -191.3731074845244393 ) ) ;
#193354=FACE_OUTER_BOUND ( 'NONE', #150211, .T. ) ;
#193378=DIRECTION ( 'NONE',  ( 1.000000000000000000, 0.000000000000000000, 0.000000000000000000 ) ) ;
#193397=LINE ( 'NONE', #18593, #71777 ) ;
#193407=DIRECTION ( 'NONE',  ( 0.000000000000000000, -6.467318590049456648E-15, 1.000000000000000000 ) ) ;
#193436=ORIENTED_EDGE ( 'NONE', *, *, #16107, .T. ) ;
#193443=CARTESIAN_POINT ( 'NONE',  ( 21.02374657821565407, 64.39999999919231755, -176.9513107143264108 ) ) ;
#193444=LINE ( 'NONE', #35670, #134293 ) ;
#193479=CARTESIAN_POINT ( 'NONE',  ( 21.05000000000000071, 69.45934304831143891, -203.4231074845244223 ) ) ;
#193492=EDGE_CURVE ( 'NONE', #144388, #11973, #83342, .T. ) ;
#193497=DIRECTION ( 'NONE',  ( -1.000000000000000000, 2.952720810173289112E-16, 2.061873921506763405E-30 ) ) ;
#193515=ORIENTED_EDGE ( 'NONE', *, *, #254107, .F. ) ;
#193566=ADVANCED_FACE ( 'NONE', ( #147790 ), #156795, .F. ) ;
#193572=CYLINDRICAL_SURFACE ( 'NONE', #216246, 0.09999999999999939493 ) ;
#193586=EDGE_LOOP ( 'NONE', ( #109126, #155609, #141997 ) ) ;
#193592=DIRECTION ( 'NONE',  ( -0.000000000000000000, 1.000000000000000000, 6.352154140967427193E-15 ) ) ;
#193609=EDGE_LOOP ( 'NONE', ( #137900, #22905, #171151, #13034 ) ) ;
#193623=DIRECTION ( 'NONE',  ( 1.000000000000000000, 0.000000000000000000, 0.000000000000000000 ) ) ;
#193676=AXIS2_PLACEMENT_3D ( 'NONE', #162032, #175495, #176775 ) ;
#193689=ADVANCED_FACE ( 'NONE', ( #57644 ), #237591, .F. ) ;
#193693=LINE ( 'NONE', #75056, #87125 ) ;
#193706=CARTESIAN_POINT ( 'NONE',  ( 23.14999999999999858, 76.00000000001244871, -170.0231074845243597 ) ) ;
#193715=EDGE_LOOP ( 'NONE', ( #250357, #196814, #94566 ) ) ;
#193728=FACE_OUTER_BOUND ( 'NONE', #40330, .T. ) ;
#193744=UNCERTAINTY_MEASURE_WITH_UNIT (LENGTH_MEASURE( 1.000000000000000082E-05 ), #47303, 'distance_accuracy_value', 'NONE');
#193753=DIRECTION ( 'NONE',  ( 1.000000000000000000, 0.000000000000000000, 0.000000000000000000 ) ) ;
#193760=CARTESIAN_POINT ( 'NONE',  ( -23.15000000000000213, 87.75000000001247713, -173.1231074845242688 ) ) ;
#193765=CARTESIAN_POINT ( 'NONE',  ( -21.45000000000000284, 68.29142135624991283, -191.2731074845244166 ) ) ;
#193768=ORIENTED_EDGE ( 'NONE', *, *, #27036, .T. ) ;
#193772=AXIS2_PLACEMENT_3D ( 'NONE', #7156, #110122, #5869 ) ;
#193792=ORIENTED_EDGE ( 'NONE', *, *, #102336, .T. ) ;
#193828=PLANE ( 'NONE',  #139125 ) ;
#193859=DIRECTION ( 'NONE',  ( 0.000000000000000000, 0.4999999999999608646, -0.8660254037844612451 ) ) ;
#193864=PLANE ( 'NONE',  #121641 ) ;
#193868=DIRECTION ( 'NONE',  ( -0.000000000000000000, 1.000000000000000000, 6.982962677686266711E-15 ) ) ;
#193891=CARTESIAN_POINT ( 'NONE',  ( 18.59999999999999076, 69.45000000001260787, -193.5060803140843859 ) ) ;
#193941=FACE_OUTER_BOUND ( 'NONE', #96095, .T. ) ;
#193966=CARTESIAN_POINT ( 'NONE',  ( -18.59999999999999787, 68.75000000001253397, -182.1731074845244223 ) ) ;
#193975=CARTESIAN_POINT ( 'NONE',  ( 18.59999999999999432, 77.73625713161000306, -191.9544551555068495 ) ) ;
#193993=DIRECTION ( 'NONE',  ( 0.000000000000000000, -1.000000000000000000, -6.352154140967427193E-15 ) ) ;
#193994=CARTESIAN_POINT ( 'NONE',  ( 20.94999999999999929, 76.00000000001247713, -172.9231074845243654 ) ) ;
#194017=VECTOR ( 'NONE', #27343, 1000.000000000000000 ) ;
#194023=FACE_OUTER_BOUND ( 'NONE', #180726, .T. ) ;
#194025=AXIS2_PLACEMENT_3D ( 'NONE', #242255, #8794, #3646 ) ;
#194026=ORIENTED_EDGE ( 'NONE', *, *, #95404, .F. ) ;
#194037=DIRECTION ( 'NONE',  ( 0.000000000000000000, 7.026728003956695223E-15, -1.000000000000000000 ) ) ;
#194044=CARTESIAN_POINT ( 'NONE',  ( 18.59999999999999076, 74.25000000001259082, -191.8535959266227451 ) ) ;
#194065=CIRCLE ( 'NONE', #189952, 11.75000000000001066 ) ;
#194076=DIRECTION ( 'NONE',  ( 0.000000000000000000, 1.000000000000000000, 0.000000000000000000 ) ) ;
#194103=VECTOR ( 'NONE', #88064, 1000.000000000000000 ) ;
#194167=ORIENTED_EDGE ( 'NONE', *, *, #218066, .T. ) ;
#194183=CARTESIAN_POINT ( 'NONE',  ( 21.05000000000000071, 65.45624872451701037, -195.9667196758603893 ) ) ;
#194226=CARTESIAN_POINT ( 'NONE',  ( 23.25000000000000000, 64.25000000001253397, -182.1731074845244507 ) ) ;
#194228=DIRECTION ( 'NONE',  ( -1.000000000000000000, -0.000000000000000000, -0.000000000000000000 ) ) ;
#194255=CARTESIAN_POINT ( 'NONE',  ( 18.54148534481893407, 65.67467670974468774, -164.4531731826884879 ) ) ;
#194281=CARTESIAN_POINT ( 'NONE',  ( 21.93340585900753936, 76.00000000001273293, -210.8472545066313160 ) ) ;
#194284=ORIENTED_EDGE ( 'NONE', *, *, #203182, .T. ) ;
#194290=FACE_OUTER_BOUND ( 'NONE', #103544, .T. ) ;
#194294=DIRECTION ( 'NONE',  ( 0.000000000000000000, 8.783410004945868831E-15, -1.000000000000000000 ) ) ;
#194302=CIRCLE ( 'NONE', #11106, 2.000000000000001776 ) ;
#194336=CARTESIAN_POINT ( 'NONE',  ( -21.14999999999999858, 69.45934304831143891, -203.5231074845243882 ) ) ;
#194346=ADVANCED_FACE ( 'NONE', ( #194978 ), #97093, .F. ) ;
#194366=CARTESIAN_POINT ( 'NONE',  ( -18.50000000000000000, 66.65000000001259650, -191.3731074845244393 ) ) ;
#194420=DIRECTION ( 'NONE',  ( 0.000000000000000000, -6.982962677686266711E-15, 1.000000000000000000 ) ) ;
#194457=ORIENTED_EDGE ( 'NONE', *, *, #139590, .T. ) ;
#194470=DIRECTION ( 'NONE',  ( -0.000000000000000000, -1.000000000000000000, -7.272083257015735086E-15 ) ) ;
#194483=CYLINDRICAL_SURFACE ( 'NONE', #201007, 0.1000000000000118433 ) ;
#194491=CIRCLE ( 'NONE', #36274, 0.09999999999999939493 ) ;
#194557=FACE_OUTER_BOUND ( 'NONE', #207944, .T. ) ;
#194567=ORIENTED_EDGE ( 'NONE', *, *, #231595, .F. ) ;
#194570=AXIS2_PLACEMENT_3D ( 'NONE', #113897, #154357, #196018 ) ;
#194589=ORIENTED_EDGE ( 'NONE', *, *, #122385, .T. ) ;
#194612=EDGE_CURVE ( 'NONE', #97945, #180641, #51874, .T. ) ;
#194616=DIRECTION ( 'NONE',  ( 1.000000000000000000, 0.000000000000000000, 0.000000000000000000 ) ) ;
#194629=DIRECTION ( 'NONE',  ( -0.000000000000000000, 1.000000000000000000, 6.982962677686267499E-15 ) ) ;
#194633=CARTESIAN_POINT ( 'NONE',  ( 20.94999999999999929, 76.00000000001244871, -170.0231074845243597 ) ) ;
#194640=ORIENTED_EDGE ( 'NONE', *, *, #59499, .F. ) ;
#194652=CYLINDRICAL_SURFACE ( 'NONE', #11863, 0.09999999999999939493 ) ;
#194691=EDGE_CURVE ( 'NONE', #209410, #124945, #209006, .T. ) ;
#194695=ORIENTED_EDGE ( 'NONE', *, *, #207512, .F. ) ;
#194699=DIRECTION ( 'NONE',  ( 0.000000000000000000, 0.000000000000000000, 1.000000000000000000 ) ) ;
#194770=ORIENTED_EDGE ( 'NONE', *, *, #209584, .F. ) ;
#194790=EDGE_CURVE ( 'NONE', #160984, #196419, #76586, .T. ) ;
#194824=CIRCLE ( 'NONE', #207294, 0.09999999999999939493 ) ;
#194865=( BOUNDED_CURVE ( )  B_SPLINE_CURVE ( 3, ( #104223, #106797, #243751, #143363 ),
 .UNSPECIFIED., .F., .T. ) 
 B_SPLINE_CURVE_WITH_KNOTS ( ( 4, 4 ),
 ( 3.141592653589791784, 4.712388980384688786 ),
 .UNSPECIFIED. ) 
 CURVE ( )  GEOMETRIC_REPRESENTATION_ITEM ( )  RATIONAL_B_SPLINE_CURVE ( ( 1.000000000000000000, 0.8047378541243649375, 0.8047378541243649375, 1.000000000000000000 ) ) 
 REPRESENTATION_ITEM ( '' )  );
#194901=DIRECTION ( 'NONE',  ( -0.7071067811865475727, 0.7071067811865475727, 4.937700262164531476E-15 ) ) ;
#194938=CARTESIAN_POINT ( 'NONE',  ( -22.59080734064477625, 64.25000000001269029, -203.5538571926214502 ) ) ;
#194939=AXIS2_PLACEMENT_3D ( 'NONE', #213431, #169219, #93485 ) ;
#194941=ORIENTED_EDGE ( 'NONE', *, *, #113348, .F. ) ;
#194963=LINE ( 'NONE', #149421, #24471 ) ;
#194978=FACE_OUTER_BOUND ( 'NONE', #89521, .T. ) ;
#194994=AXIS2_PLACEMENT_3D ( 'NONE', #80805, #61271, #121286 ) ;
#194999=FACE_OUTER_BOUND ( 'NONE', #148394, .T. ) ;
#195046=ADVANCED_FACE ( 'NONE', ( #169011 ), #69890, .T. ) ;
#195101=DIRECTION ( 'NONE',  ( 1.000000000000000000, 0.000000000000000000, 0.000000000000000000 ) ) ;
#195123=ORIENTED_EDGE ( 'NONE', *, *, #128020, .T. ) ;
#195137=EDGE_LOOP ( 'NONE', ( #207028, #42136, #221462, #194284 ) ) ;
#195139=AXIS2_PLACEMENT_3D ( 'NONE', #136168, #215724, #157070 ) ;
#195156=ORIENTED_EDGE ( 'NONE', *, *, #97449, .T. ) ;
#195171=ORIENTED_EDGE ( 'NONE', *, *, #73976, .F. ) ;
#195186=ORIENTED_EDGE ( 'NONE', *, *, #67942, .T. ) ;
#195192=DIRECTION ( 'NONE',  ( 0.000000000000000000, 7.086529944415886769E-15, -1.000000000000000000 ) ) ;
#195205=CARTESIAN_POINT ( 'NONE',  ( -18.50000000000000000, 77.63717271298298783, -191.9409541190523214 ) ) ;
#195224=VERTEX_POINT ( 'NONE', #239210 ) ;
#195255=AXIS2_PLACEMENT_3D ( 'NONE', #102741, #121087, #78062 ) ;
#195276=AXIS2_PLACEMENT_3D ( 'NONE', #105454, #6388, #220317 ) ;
#195297=AXIS2_PLACEMENT_3D ( 'NONE', #189108, #155151, #234649 ) ;
#195299=AXIS2_PLACEMENT_3D ( 'NONE', #71729, #225618, #196778 ) ;
#195305=CARTESIAN_POINT ( 'NONE',  ( -21.05000000000000071, 69.74168394268066606, -203.5888090948464537 ) ) ;
#195347=CARTESIAN_POINT ( 'NONE',  ( -20.85000000000000142, 68.87972903831482085, -166.3635444426850825 ) ) ;
#195382=ADVANCED_FACE ( 'NONE', ( #119278 ), #254857, .F. ) ;
#195386=AXIS2_PLACEMENT_3D ( 'NONE', #119638, #98732, #20541 ) ;
#195410=CARTESIAN_POINT ( 'NONE',  ( -21.95218792049438861, 75.90097156021282387, -210.7246150457710314 ) ) ;
#195415=ORIENTED_EDGE ( 'NONE', *, *, #25997, .F. ) ;
#195428=LINE ( 'NONE', #119732, #126817 ) ;
#195431=CARTESIAN_POINT ( 'NONE',  ( 23.24999999999999289, 64.35000000001275566, -215.2731074845244450 ) ) ;
#195444=VERTEX_POINT ( 'NONE', #244337 ) ;
#195464=AXIS2_PLACEMENT_3D ( 'NONE', #122189, #117050, #199150 ) ;
#195537=CARTESIAN_POINT ( 'NONE',  ( 18.56579813702274961, 65.66974365629718591, -164.4360145562605169 ) ) ;
#195548=CARTESIAN_POINT ( 'NONE',  ( -23.15000000000000213, 85.00000000001251976, -179.4170766071767389 ) ) ;
#195558=CARTESIAN_POINT ( 'NONE',  ( -23.15000000000000213, 76.00000000001253397, -182.8981074845243597 ) ) ;
#195587=EDGE_LOOP ( 'NONE', ( #180071, #78498 ) ) ;
#195603=EDGE_CURVE ( 'NONE', #119237, #225819, #209360, .T. ) ;
#195641=DIRECTION ( 'NONE',  ( -1.000000000000000000, 0.000000000000000000, 0.000000000000000000 ) ) ;
#195668=AXIS2_PLACEMENT_3D ( 'NONE', #33589, #70130, #171804 ) ;
#195738=CARTESIAN_POINT ( 'NONE',  ( -21.14999999999999858, 64.35000000001268461, -203.4231074845244507 ) ) ;
#195798=ADVANCED_FACE ( 'NONE', ( #238916 ), #255284, .T. ) ;
#195808=ORIENTED_EDGE ( 'NONE', *, *, #12581, .T. ) ;
#195815=CARTESIAN_POINT ( 'NONE',  ( -22.48970261584618058, 64.35000000001268461, -203.5784769727418393 ) ) ;
#195868=DIRECTION ( 'NONE',  ( -0.000000000000000000, 1.000000000000000000, 6.982962677686266711E-15 ) ) ;
#195888=DIRECTION ( 'NONE',  ( 0.000000000000000000, 0.1298341882519953583, 0.9915357197604862671 ) ) ;
#195897=CARTESIAN_POINT ( 'NONE',  ( 20.46382478191414833, 67.09862044131001824, -194.9773793896413281 ) ) ;
#195901=EDGE_CURVE ( 'NONE', #19454, #158664, #122073, .T. ) ;
#195903=CARTESIAN_POINT ( 'NONE',  ( 20.94999999999999574, 74.83729825007462466, -195.5231074845243597 ) ) ;
#195917=ORIENTED_EDGE ( 'NONE', *, *, #161872, .F. ) ;
#195922=EDGE_CURVE ( 'NONE', #200926, #180867, #126663, .T. ) ;
#195923=CARTESIAN_POINT ( 'NONE',  ( 22.39999999999999503, 75.90000000001273861, -209.7731074845243597 ) ) ;
#195943=EDGE_LOOP ( 'NONE', ( #15848, #176984, #41336, #26791 ) ) ;
#196018=DIRECTION ( 'NONE',  ( 0.000000000000000000, -6.982962677686266711E-15, 1.000000000000000000 ) ) ;
#196045=CYLINDRICAL_SURFACE ( 'NONE', #143777, 0.09999999999999939493 ) ;
#196064=ORIENTED_EDGE ( 'NONE', *, *, #3310, .F. ) ;
#196071=AXIS2_PLACEMENT_3D ( 'NONE', #173061, #89610, #214698 ) ;
#196072=VERTEX_POINT ( 'NONE', #178328 ) ;
#196134=CARTESIAN_POINT ( 'NONE',  ( 18.39999999999999858, 85.60000000001240039, -163.4229180933022576 ) ) ;
#196142=CARTESIAN_POINT ( 'NONE',  ( 20.94999999999999574, 76.00000000001267608, -203.5231074845243597 ) ) ;
#196155=CARTESIAN_POINT ( 'NONE',  ( -18.40904629823843663, 85.50000000001242029, -163.4229179220422736 ) ) ;
#196166=CARTESIAN_POINT ( 'NONE',  ( 20.94999999999999929, 76.00000000001267608, -203.5231074845243597 ) ) ;
#196182=CARTESIAN_POINT ( 'NONE',  ( -18.59999999999999787, 66.85000000001259934, -191.1731074845244223 ) ) ;
#196189=ORIENTED_EDGE ( 'NONE', *, *, #166501, .F. ) ;
#196197=CARTESIAN_POINT ( 'NONE',  ( 23.24999999999999645, 76.00000000001244871, -170.0231074845243597 ) ) ;
#196240=FACE_OUTER_BOUND ( 'NONE', #34261, .T. ) ;
#196270=CARTESIAN_POINT ( 'NONE',  ( -20.94999999999999929, 76.00000000001242029, -165.9231074845243654 ) ) ;
#196312=CIRCLE ( 'NONE', #38124, 0.09999999999998898659 ) ;
#196355=EDGE_LOOP ( 'NONE', ( #106330, #140959, #116266, #53953 ) ) ;
#196365=CYLINDRICAL_SURFACE ( 'NONE', #114535, 0.5000000000000004441 ) ;
#196370=ORIENTED_EDGE ( 'NONE', *, *, #156037, .F. ) ;
#196400=DIRECTION ( 'NONE',  ( -0.000000000000000000, -0.8660254037844420383, 0.4999999999999943379 ) ) ;
#196419=VERTEX_POINT ( 'NONE', #118015 ) ;
#196480=CARTESIAN_POINT ( 'NONE',  ( 21.87500000000000355, 66.25000000001253397, -182.2731074845244450 ) ) ;
#196503=AXIS2_PLACEMENT_3D ( 'NONE', #96144, #196538, #178297 ) ;
#196506=DIRECTION ( 'NONE',  ( 1.000000000000000000, 0.000000000000000000, 0.000000000000000000 ) ) ;
#196508=ORIENTED_EDGE ( 'NONE', *, *, #222541, .T. ) ;
#196521=DIRECTION ( 'NONE',  ( 0.000000000000000000, -0.5000000000000016653, 0.8660254037844377084 ) ) ;
#196531=DIRECTION ( 'NONE',  ( -1.000000000000000000, 0.000000000000000000, 0.000000000000000000 ) ) ;
#196538=DIRECTION ( 'NONE',  ( 1.000000000000000000, -0.000000000000000000, -0.000000000000000000 ) ) ;
#196544=ORIENTED_EDGE ( 'NONE', *, *, #170422, .T. ) ;
#196557=CARTESIAN_POINT ( 'NONE',  ( -20.94999999999999929, 87.48912529308871910, -200.4231074845242802 ) ) ;
#196562=ORIENTED_EDGE ( 'NONE', *, *, #248684, .T. ) ;
#196577=DIRECTION ( 'NONE',  ( 0.000000000000000000, 1.000000000000000000, 6.982962677686266711E-15 ) ) ;
#196609=CARTESIAN_POINT ( 'NONE',  ( -20.85000000000000142, 77.16412189325360771, -162.2082593989527197 ) ) ;
#196622=ORIENTED_EDGE ( 'NONE', *, *, #110318, .F. ) ;
#196653=DIRECTION ( 'NONE',  ( -1.000000000000000000, -0.000000000000000000, 0.000000000000000000 ) ) ;
#196659=CARTESIAN_POINT ( 'NONE',  ( -22.50000000000000000, 64.35042919246788529, -203.6231074845244393 ) ) ;
#196671=VECTOR ( 'NONE', #248807, 1000.000000000000000 ) ;
#196672=FACE_OUTER_BOUND ( 'NONE', #247994, .T. ) ;
#196673=AXIS2_PLACEMENT_3D ( 'NONE', #164300, #145998, #204678 ) ;
#196694=VERTEX_POINT ( 'NONE', #149166 ) ;
#196718=DIRECTION ( 'NONE',  ( 0.000000000000000000, -0.9908441862701610203, 0.1350103645451807555 ) ) ;
#196719=CIRCLE ( 'NONE', #88564, 0.1000000000000043771 ) ;
#196730=ORIENTED_EDGE ( 'NONE', *, *, #251274, .F. ) ;
#196745=ORIENTED_EDGE ( 'NONE', *, *, #27473, .T. ) ;
#196754=CARTESIAN_POINT ( 'NONE',  ( -22.45305610364635385, 76.10085836911147794, -215.2726746080137161 ) ) ;
#196774=ADVANCED_FACE ( 'NONE', ( #177729 ), #159431, .F. ) ;
#196778=DIRECTION ( 'NONE',  ( 0.000000000000000000, -3.469446951953515108E-14, 1.000000000000000000 ) ) ;
#196784=ORIENTED_EDGE ( 'NONE', *, *, #127465, .T. ) ;
#196814=ORIENTED_EDGE ( 'NONE', *, *, #136604, .T. ) ;
#196842=VECTOR ( 'NONE', #39004, 1000.000000000000000 ) ;
#196907=VERTEX_POINT ( 'NONE', #26333 ) ;
#196938=ORIENTED_EDGE ( 'NONE', *, *, #4902, .F. ) ;
#196946=ORIENTED_EDGE ( 'NONE', *, *, #226546, .F. ) ;
#196956=CARTESIAN_POINT ( 'NONE',  ( -21.44999999999999929, 68.85000000001259934, -191.1731074845243938 ) ) ;
#196968=ORIENTED_EDGE ( 'NONE', *, *, #247165, .T. ) ;
#196971=DIRECTION ( 'NONE',  ( -1.000000000000000000, 0.000000000000000000, -0.000000000000000000 ) ) ;
#196990=CIRCLE ( 'NONE', #84526, 12.87499999999999822 ) ;
#196997=CIRCLE ( 'NONE', #5452, 0.09999999999998712696 ) ;
#197056=ORIENTED_EDGE ( 'NONE', *, *, #151169, .T. ) ;
#197062=AXIS2_PLACEMENT_3D ( 'NONE', #103999, #10065, #129990 ) ;
#197080=DIRECTION ( 'NONE',  ( 0.000000000000000000, -6.530723674265620862E-15, 1.000000000000000000 ) ) ;
#197086=EDGE_CURVE ( 'NONE', #75446, #58850, #215243, .T. ) ;
#197088=AXIS2_PLACEMENT_3D ( 'NONE', #16414, #94635, #158500 ) ;
#197095=ORIENTED_EDGE ( 'NONE', *, *, #170213, .F. ) ;
#197106=B_SPLINE_CURVE_WITH_KNOTS ( 'NONE', 3,
 ( #10313, #85944, #143380, #104235 ),
 .UNSPECIFIED., .F., .F.,
 ( 4, 4 ),
 ( 0.000000000000000000, 0.0002118541922231925311 ),
 .UNSPECIFIED. ) ;
#197197=CARTESIAN_POINT ( 'NONE',  ( 21.05000000000000071, 76.00000000001244871, -170.0231074845243597 ) ) ;
#197217=CIRCLE ( 'NONE', #201305, 0.1000000000000028783 ) ;
#197228=VECTOR ( 'NONE', #97656, 1000.000000000000000 ) ;
#197250=DIRECTION ( 'NONE',  ( 0.000000000000000000, -0.1575844902526687130, -0.9875055080513762684 ) ) ;
#197287=EDGE_LOOP ( 'NONE', ( #11465, #152115, #2739 ) ) ;
#197288=CARTESIAN_POINT ( 'NONE',  ( -18.59999999999999787, 66.65000000001253966, -182.3731074845244393 ) ) ;
#197291=LINE ( 'NONE', #18660, #222887 ) ;
#197295=VERTEX_POINT ( 'NONE', #164256 ) ;
#197311=EDGE_CURVE ( 'NONE', #176, #192558, #1296, .T. ) ;
#197316=EDGE_CURVE ( 'NONE', #218130, #161032, #255702, .T. ) ;
#197358=CARTESIAN_POINT ( 'NONE',  ( -18.59999999999999787, 74.16465844978819177, -191.9679561919613775 ) ) ;
#197359=AXIS2_PLACEMENT_3D ( 'NONE', #220435, #181316, #142164 ) ;
#197361=ORIENTED_EDGE ( 'NONE', *, *, #232295, .F. ) ;
#197364=EDGE_LOOP ( 'NONE', ( #134300, #30607, #95725, #107457 ) ) ;
#197398=EDGE_CURVE ( 'NONE', #121258, #98885, #151548, .T. ) ;
#197438=ORIENTED_EDGE ( 'NONE', *, *, #19922, .F. ) ;
#197456=DIRECTION ( 'NONE',  ( 0.000000000000000000, 6.982962677686266711E-15, -1.000000000000000000 ) ) ;
#197466=VERTEX_POINT ( 'NONE', #186386 ) ;
#197509=DIRECTION ( 'NONE',  ( 0.7071067811865474617, -0.7071067811865474617, -4.937700262164531476E-15 ) ) ;
#197533=EDGE_CURVE ( 'NONE', #227067, #223699, #5919, .T. ) ;
#197590=DIRECTION ( 'NONE',  ( 1.000000000000000000, 0.000000000000000000, 0.000000000000000000 ) ) ;
#197655=CIRCLE ( 'NONE', #219072, 0.5000000000000004441 ) ;
#197661=ORIENTED_EDGE ( 'NONE', *, *, #1651, .F. ) ;
#197674=CIRCLE ( 'NONE', #93639, 0.1000000000000028644 ) ;
#197676=ORIENTED_EDGE ( 'NONE', *, *, #149917, .F. ) ;
#197700=ORIENTED_EDGE ( 'NONE', *, *, #115129, .F. ) ;
#197708=AXIS2_PLACEMENT_3D ( 'NONE', #29275, #192173, #209136 ) ;
#197723=EDGE_LOOP ( 'NONE', ( #108541, #136193, #8167, #214226 ) ) ;
#197725=DIRECTION ( 'NONE',  ( -0.000000000000000000, -6.982962677686266711E-15, 1.000000000000000000 ) ) ;
#197737=EDGE_CURVE ( 'NONE', #129083, #166628, #73528, .T. ) ;
#197744=FACE_OUTER_BOUND ( 'NONE', #116839, .T. ) ;
#197766=VECTOR ( 'NONE', #214018, 1000.000000000000000 ) ;
#197768=DIRECTION ( 'NONE',  ( 1.000000000000000000, 0.000000000000000000, 0.000000000000000000 ) ) ;
#197780=ORIENTED_EDGE ( 'NONE', *, *, #141279, .T. ) ;
#197813=CARTESIAN_POINT ( 'NONE',  ( 21.08489247129321953, 67.12232480914252619, -191.1731074845244507 ) ) ;
#197854=DIRECTION ( 'NONE',  ( -1.000000000000000000, 0.000000000000000000, -0.000000000000000000 ) ) ;
#197862=VECTOR ( 'NONE', #105520, 1000.000000000000000 ) ;
#197911=DIRECTION ( 'NONE',  ( -5.603264701231743991E-32, -7.172728831056617961E-15, 1.000000000000000000 ) ) ;
#197912=CIRCLE ( 'NONE', #189569, 0.09999999999998898659 ) ;
#197918=VERTEX_POINT ( 'NONE', #137307 ) ;
#197942=CARTESIAN_POINT ( 'NONE',  ( -22.59999985501179154, 64.25013020700970401, -203.5887061543241714 ) ) ;
#197958=CIRCLE ( 'NONE', #164660, 0.5000000000000004441 ) ;
#197967=ORIENTED_EDGE ( 'NONE', *, *, #255113, .F. ) ;
#197982=CIRCLE ( 'NONE', #81439, 4.049999999999998046 ) ;
#198017=EDGE_LOOP ( 'NONE', ( #110981, #148756, #97296, #123549 ) ) ;
#198024=VECTOR ( 'NONE', #178606, 1000.000000000000000 ) ;
#198026=LINE ( 'NONE', #257958, #227823 ) ;
#198039=ORIENTED_EDGE ( 'NONE', *, *, #221272, .T. ) ;
#198077=EDGE_LOOP ( 'NONE', ( #160545, #35993, #36857 ) ) ;
#198091=DIRECTION ( 'NONE',  ( 1.000000000000000000, 0.000000000000000000, 0.000000000000000000 ) ) ;
#198179=ORIENTED_EDGE ( 'NONE', *, *, #175942, .T. ) ;
#198183=CARTESIAN_POINT ( 'NONE',  ( 21.07199075132372101, 67.22505500089651775, -191.3095753229115701 ) ) ;
#198197=CARTESIAN_POINT ( 'NONE',  ( -20.94999999999999929, 87.65000000001246860, -173.0231074845243029 ) ) ;
#198198=VECTOR ( 'NONE', #96711, 1000.000000000000000 ) ;
#198203=VERTEX_POINT ( 'NONE', #44207 ) ;
#198232=ORIENTED_EDGE ( 'NONE', *, *, #23743, .F. ) ;
#198239=ORIENTED_EDGE ( 'NONE', *, *, #244378, .F. ) ;
#198269=CARTESIAN_POINT ( 'NONE',  ( -22.39999999999999858, 76.10085836911147794, -215.2726746080137445 ) ) ;
#198285=EDGE_CURVE ( 'NONE', #115127, #252901, #242383, .T. ) ;
#198292=VERTEX_POINT ( 'NONE', #143293 ) ;
#198323=CARTESIAN_POINT ( 'NONE',  ( -22.39999999999999858, 76.10000000001276987, -215.1726782920691505 ) ) ;
#198336=CARTESIAN_POINT ( 'NONE',  ( 20.85000000000000142, 64.25000000001249134, -176.8069731475025321 ) ) ;
#198397=EDGE_CURVE ( 'NONE', #77018, #121003, #20807, .T. ) ;
#198413=LINE ( 'NONE', #138410, #102481 ) ;
#198486=SPHERICAL_SURFACE ( 'NONE', #147735, 0.1000000000000000056 ) ;
#198504=VECTOR ( 'NONE', #4346, 1000.000000000000000 ) ;
#198511=DIRECTION ( 'NONE',  ( 0.000000000000000000, 1.000000000000000000, 0.000000000000000000 ) ) ;
#198529=DIRECTION ( 'NONE',  ( 1.000000000000000000, 0.000000000000000000, 0.000000000000000000 ) ) ;
#198549=EDGE_CURVE ( 'NONE', #147959, #87546, #56538, .T. ) ;
#198572=EDGE_CURVE ( 'NONE', #154016, #205739, #188844, .T. ) ;
#198617=CIRCLE ( 'NONE', #111331, 0.09999999999999939493 ) ;
#198640=EDGE_CURVE ( 'NONE', #58809, #236908, #131434, .T. ) ;
#198652=CARTESIAN_POINT ( 'NONE',  ( 23.24999999999999289, 64.35000000001249987, -177.0379132551783812 ) ) ;
#198666=CARTESIAN_POINT ( 'NONE',  ( 18.49351773456780634, 85.44302569515771495, -196.3377819584974588 ) ) ;
#198692=DIRECTION ( 'NONE',  ( 0.000000000000000000, 0.8660254037844419273, -0.4999999999999942824 ) ) ;
#198705=ADVANCED_FACE ( 'NONE', ( #101240 ), #156165, .F. ) ;
#198728=( BOUNDED_SURFACE ( )  B_SPLINE_SURFACE ( 3, 2, ( 
 ( #78270, #215232, #233527 ),
 ( #15781, #95282, #174874 ),
 ( #177421, #156579, #254334 ),
 ( #75732, #116146, #37901 ) ),
 .UNSPECIFIED., .F., .F., .T. ) 
 B_SPLINE_SURFACE_WITH_KNOTS ( ( 4, 4 ),
 ( 3, 3 ),
 ( 0.0006461284895273780972, 0.0007503702773985888950 ),
 ( 0.000000000000000000, 1.000000000000000000 ),
 .UNSPECIFIED. ) 
 GEOMETRIC_REPRESENTATION_ITEM ( )  RATIONAL_B_SPLINE_SURFACE ( (
 ( 1.000000000000000000, 0.7071067811865483499, 1.000000000000000000),
 ( 1.000000000000000000, 0.7076476444648895914, 1.000000000000000000),
 ( 1.000000000000000000, 0.7075727925191884760, 1.000000000000000000),
 ( 1.000000000000000000, 0.7071067811865966446, 1.000000000000000000) ) ) 
 REPRESENTATION_ITEM ( '' )  SURFACE ( )  );
#198758=AXIS2_PLACEMENT_3D ( 'NONE', #160874, #42200, #121749 ) ;
#198768=CARTESIAN_POINT ( 'NONE',  ( 20.94999999999999574, 87.41227409416235616, -200.6231074845242688 ) ) ;
#198779=CARTESIAN_POINT ( 'NONE',  ( 20.94999999999999574, 87.48912529308871910, -200.5231074845242745 ) ) ;
#198786=ADVANCED_FACE ( 'NONE', ( #249485 ), #33043, .F. ) ;
#198813=DIRECTION ( 'NONE',  ( 0.000000000000000000, 0.000000000000000000, 1.000000000000000000 ) ) ;
#198815=EDGE_CURVE ( 'NONE', #188235, #166644, #168704, .T. ) ;
#198822=VECTOR ( 'NONE', #40319, 1000.000000000000000 ) ;
#198827=ORIENTED_EDGE ( 'NONE', *, *, #178455, .T. ) ;
#198850=LINE ( 'NONE', #20231, #159974 ) ;
#198856=ORIENTED_EDGE ( 'NONE', *, *, #203723, .T. ) ;
#198894=FACE_OUTER_BOUND ( 'NONE', #226825, .T. ) ;
#198903=DIRECTION ( 'NONE',  ( -1.000000000000000000, 2.952720810173289112E-16, 2.061873921506763405E-30 ) ) ;
#198922=ORIENTED_EDGE ( 'NONE', *, *, #44962, .F. ) ;
#198924=DIRECTION ( 'NONE',  ( 1.040834085586049673E-13, 0.7899159663865300551, 0.6132151058540831201 ) ) ;
#198952=ADVANCED_FACE ( 'NONE', ( #121549 ), #203618, .F. ) ;
#198981=CARTESIAN_POINT ( 'NONE',  ( -20.64999999999999858, 68.75000000001253397, -182.3731074845244109 ) ) ;
#198994=CIRCLE ( 'NONE', #182452, 0.09999999999998898659 ) ;
#199037=CARTESIAN_POINT ( 'NONE',  ( 18.39999999999999858, 85.68240343348878696, -163.3662641071115047 ) ) ;
#199046=CARTESIAN_POINT ( 'NONE',  ( 21.14999999999999858, 76.00000000001267608, -203.5231074845243597 ) ) ;
#199060=CARTESIAN_POINT ( 'NONE',  ( -21.64999999999999858, 68.65000000001253966, -182.3731074845244109 ) ) ;
#199061=LINE ( 'NONE', #20440, #236608 ) ;
#199079=EDGE_LOOP ( 'NONE', ( #230088, #248012, #52545, #32857 ) ) ;
#199088=ORIENTED_EDGE ( 'NONE', *, *, #159089, .T. ) ;
#199103=ORIENTED_EDGE ( 'NONE', *, *, #90504, .T. ) ;
#199143=CARTESIAN_POINT ( 'NONE',  ( -18.50000000000000000, 77.83534155023700407, -191.9679561919613491 ) ) ;
#199150=DIRECTION ( 'NONE',  ( 0.000000000000000000, -0.9998779222360104635, -0.01562499999996343723 ) ) ;
#199155=CARTESIAN_POINT ( 'NONE',  ( -18.50000000000000000, 65.70729864261058140, -164.5657455973725121 ) ) ;
#199158=AXIS2_PLACEMENT_3D ( 'NONE', #228736, #246983, #127047 ) ;
#199175=CIRCLE ( 'NONE', #186723, 0.09999999999998898659 ) ;
#199176=EDGE_CURVE ( 'NONE', #163070, #248091, #239346, .T. ) ;
#199202=CARTESIAN_POINT ( 'NONE',  ( 21.05000000000000071, 65.27628289530507288, -191.3731074845244393 ) ) ;
#199219=EDGE_CURVE ( 'NONE', #218429, #9515, #254278, .T. ) ;
#199237=EDGE_LOOP ( 'NONE', ( #174972, #59656, #137632 ) ) ;
#199263=DIRECTION ( 'NONE',  ( 1.000000000000000000, -0.000000000000000000, 0.000000000000000000 ) ) ;
#199295=ADVANCED_FACE ( 'NONE', ( #153968 ), #134332, .F. ) ;
#199297=ORIENTED_EDGE ( 'NONE', *, *, #230488, .T. ) ;
#199307=CARTESIAN_POINT ( 'NONE',  ( 21.04999999999999716, 65.37049252075502181, -195.8951280845284373 ) ) ;
#199341=DIRECTION ( 'NONE',  ( 0.000000000000000000, 0.000000000000000000, 1.000000000000000000 ) ) ;
#199345=CARTESIAN_POINT ( 'NONE',  ( -23.25000000000000000, 77.73670573947995877, -158.5056848969006182 ) ) ;
#199376=DIRECTION ( 'NONE',  ( 0.000000000000000000, 1.000000000000000000, 0.000000000000000000 ) ) ;
#199384=VERTEX_POINT ( 'NONE', #22132 ) ;
#199390=CARTESIAN_POINT ( 'NONE',  ( -23.25000000000000000, 76.00000000001264766, -199.3731074845243540 ) ) ;
#199427=CARTESIAN_POINT ( 'NONE',  ( 18.50000000000002132, 65.50857864377520912, -178.7731074845244166 ) ) ;
#199451=ORIENTED_EDGE ( 'NONE', *, *, #245343, .T. ) ;
#199452=DIRECTION ( 'NONE',  ( 0.000000000000000000, 0.000000000000000000, 1.000000000000000000 ) ) ;
#199455=DIRECTION ( 'NONE',  ( -0.7071067811865389130, 4.937700262164590641E-15, -0.7071067811865561215 ) ) ;
#199465=ORIENTED_EDGE ( 'NONE', *, *, #102304, .T. ) ;
#199467=CARTESIAN_POINT ( 'NONE',  ( -23.25000000000000000, 87.75000000001247713, -173.1231074845242688 ) ) ;
#199478=DIRECTION ( 'NONE',  ( 0.000000000000000000, 6.982962677686267499E-15, -1.000000000000000000 ) ) ;
#199486=CARTESIAN_POINT ( 'NONE',  ( 18.59999999999996945, 65.66751761918722252, -164.4282609406112670 ) ) ;
#199494=DIRECTION ( 'NONE',  ( 1.000000000000000000, 0.000000000000000000, 0.000000000000000000 ) ) ;
#199497=CARTESIAN_POINT ( 'NONE',  ( -23.15000000000000213, 64.35000000001254250, -182.1731074845244507 ) ) ;
#199502=AXIS2_PLACEMENT_3D ( 'NONE', #210844, #92171, #146997 ) ;
#199585=AXIS2_PLACEMENT_3D ( 'NONE', #155112, #98918, #95103 ) ;
#199625=CARTESIAN_POINT ( 'NONE',  ( 21.05000000000000071, 85.00000000001251976, -179.9170766071767389 ) ) ;
#199631=TOROIDAL_SURFACE ( 'NONE', #203872, 0.9750000000000019762, 0.1000000000000000056 ) ;
#199657=CARTESIAN_POINT ( 'NONE',  ( 18.41416235934318735, 85.50000000001242029, -163.4229180933022576 ) ) ;
#199661=EDGE_CURVE ( 'NONE', #87546, #221522, #171933, .T. ) ;
#199666=LINE ( 'NONE', #241351, #90252 ) ;
#199713=LINE ( 'NONE', #181431, #34859 ) ;
#199726=EDGE_LOOP ( 'NONE', ( #210554, #227380, #176905, #193768 ) ) ;
#199729=CYLINDRICAL_SURFACE ( 'NONE', #141645, 0.5000000000000004441 ) ;
#199775=ORIENTED_EDGE ( 'NONE', *, *, #63809, .T. ) ;
#199776=DIRECTION ( 'NONE',  ( -1.000000000000000000, -0.000000000000000000, -0.000000000000000000 ) ) ;
#199778=CARTESIAN_POINT ( 'NONE',  ( -18.50000000000000000, 77.83585931145600512, -158.5186683157258187 ) ) ;
#199794=ORIENTED_EDGE ( 'NONE', *, *, #110435, .F. ) ;
#199799=CARTESIAN_POINT ( 'NONE',  ( 20.95561247346651967, 65.40499263480907643, -195.9293247175427837 ) ) ;
#199842=ADVANCED_FACE ( 'NONE', ( #237005 ), #23104, .T. ) ;
#199873=VECTOR ( 'NONE', #62130, 1000.000000000000114 ) ;
#199894=ORIENTED_EDGE ( 'NONE', *, *, #50415, .F. ) ;
#199898=VECTOR ( 'NONE', #79234, 1000.000000000000000 ) ;
#199906=ADVANCED_FACE ( 'NONE', ( #105136 ), #186007, .T. ) ;
#199924=VERTEX_POINT ( 'NONE', #166476 ) ;
#199933=AXIS2_PLACEMENT_3D ( 'NONE', #3061, #159596, #142574 ) ;
#199948=DIRECTION ( 'NONE',  ( 0.000000000000000000, -6.853228547068871147E-15, 1.000000000000000000 ) ) ;
#199952=ORIENTED_EDGE ( 'NONE', *, *, #142900, .T. ) ;
#199953=DIRECTION ( 'NONE',  ( 0.000000000000000000, 0.000000000000000000, -1.000000000000000000 ) ) ;
#199982=DIRECTION ( 'NONE',  ( 1.000000000000000000, 0.000000000000000000, 0.000000000000000000 ) ) ;
#199997=EDGE_LOOP ( 'NONE', ( #71930, #244438, #236149, #166018 ) ) ;
#199998=CARTESIAN_POINT ( 'NONE',  ( -20.54999999999999716, 76.00000000001244871, -170.0231074845243597 ) ) ;
#200004=CARTESIAN_POINT ( 'NONE',  ( 22.39999999999999503, 64.35000000001267040, -203.4231074845244507 ) ) ;
#200005=ORIENTED_EDGE ( 'NONE', *, *, #207778, .F. ) ;
#200017=CIRCLE ( 'NONE', #162429, 0.09999999999999938105 ) ;
#200020=CARTESIAN_POINT ( 'NONE',  ( 18.59999999999997655, 76.00000000001239187, -162.1231074845243825 ) ) ;
#200025=ORIENTED_EDGE ( 'NONE', *, *, #47657, .T. ) ;
#200067=EDGE_CURVE ( 'NONE', #172693, #121283, #39825, .T. ) ;
#200075=AXIS2_PLACEMENT_3D ( 'NONE', #249866, #68670, #149509 ) ;
#200080=CARTESIAN_POINT ( 'NONE',  ( -21.44999999999999929, 68.65000000001253966, -182.3731074845244109 ) ) ;
#200114=FACE_OUTER_BOUND ( 'NONE', #242252, .T. ) ;
#200140=CIRCLE ( 'NONE', #87687, 0.2000000000000057288 ) ;
#200143=ORIENTED_EDGE ( 'NONE', *, *, #133221, .T. ) ;
#200190=CARTESIAN_POINT ( 'NONE',  ( -21.05000000000000071, 77.16270174995064224, -195.4231074845243370 ) ) ;
#200196=VECTOR ( 'NONE', #126930, 1000.000000000000000 ) ;
#200226=FACE_OUTER_BOUND ( 'NONE', #172015, .T. ) ;
#200229=CARTESIAN_POINT ( 'NONE',  ( 22.59999999999999076, 64.25012875563618309, -203.5885370755381132 ) ) ;
#200238=CARTESIAN_POINT ( 'NONE',  ( -21.59780538579341069, 69.15290947006943156, -203.6220861541223996 ) ) ;
#200244=CYLINDRICAL_SURFACE ( 'NONE', #79669, 2.000000000000001776 ) ;
#200293=EDGE_LOOP ( 'NONE', ( #140208, #216864, #239595, #10763 ) ) ;
#200339=AXIS2_PLACEMENT_3D ( 'NONE', #67201, #208015, #45069 ) ;
#200348=CARTESIAN_POINT ( 'NONE',  ( -21.55000000000000071, 68.85000000001254250, -182.2731074845244166 ) ) ;
#200352=DIRECTION ( 'NONE',  ( 1.000000000000000000, 0.000000000000000000, 0.000000000000000000 ) ) ;
#200358=EDGE_LOOP ( 'NONE', ( #252497, #122040, #150272, #171540 ) ) ;
#200364=EDGE_CURVE ( 'NONE', #203708, #218733, #127469, .T. ) ;
#200372=ORIENTED_EDGE ( 'NONE', *, *, #228388, .T. ) ;
#200378=EDGE_CURVE ( 'NONE', #115263, #255583, #223527, .T. ) ;
#200397=AXIS2_PLACEMENT_3D ( 'NONE', #73117, #95211, #113484 ) ;
#200444=ADVANCED_FACE ( 'NONE', ( #192152 ), #85925, .F. ) ;
#200458=VECTOR ( 'NONE', #97784, 1000.000000000000000 ) ;
#200466=DIRECTION ( 'NONE',  ( -1.000000000000000000, 2.952720810173289112E-16, 2.061873921506763405E-30 ) ) ;
#200485=VERTEX_POINT ( 'NONE', #90444 ) ;
#200551=CARTESIAN_POINT ( 'NONE',  ( -20.99749315643150638, 64.25000000001250555, -177.0379132532823974 ) ) ;
#200560=DIRECTION ( 'NONE',  ( 0.000000000000000000, 1.000000000000000000, 6.938893903907222067E-15 ) ) ;
#200570=LINE ( 'NONE', #84423, #224591 ) ;
#200583=EDGE_CURVE ( 'NONE', #166628, #119302, #139696, .T. ) ;
#200584=CARTESIAN_POINT ( 'NONE',  ( -23.25000000000000000, 71.65000000001253966, -182.1731074845243938 ) ) ;
#200607=VERTEX_POINT ( 'NONE', #3868 ) ;
#200619=ORIENTED_EDGE ( 'NONE', *, *, #83752, .F. ) ;
#200674=CARTESIAN_POINT ( 'NONE',  ( -21.05000000000000071, 76.02110330807143157, -209.8276238137888186 ) ) ;
#200678=EDGE_CURVE ( 'NONE', #243219, #135228, #23644, .T. ) ;
#200680=EDGE_CURVE ( 'NONE', #182596, #223140, #169392, .T. ) ;
#200719=DIRECTION ( 'NONE',  ( 1.000000000000000000, 0.000000000000000000, 0.000000000000000000 ) ) ;
#200734=ORIENTED_EDGE ( 'NONE', *, *, #251731, .F. ) ;
#200756=CARTESIAN_POINT ( 'NONE',  ( 21.06600267594171783, 67.22483393081269298, -191.3188447021496756 ) ) ;
#200776=CARTESIAN_POINT ( 'NONE',  ( 23.14999999999999503, 64.35000000001249987, -177.0379132551783812 ) ) ;
#200827=DIRECTION ( 'NONE',  ( 0.000000000000000000, 6.982962677686266711E-15, -1.000000000000000000 ) ) ;
#200851=DIRECTION ( 'NONE',  ( 0.000000000000000000, 1.000000000000000000, 6.982962677686266711E-15 ) ) ;
#200865=EDGE_CURVE ( 'NONE', #181359, #15440, #28292, .T. ) ;
#200892=DIRECTION ( 'NONE',  ( 0.000000000000000000, 0.000000000000000000, 1.000000000000000000 ) ) ;
#200908=VERTEX_POINT ( 'NONE', #9976 ) ;
#200925=AXIS2_PLACEMENT_3D ( 'NONE', #242751, #221892, #223190 ) ;
#200926=VERTEX_POINT ( 'NONE', #149511 ) ;
#200935=EDGE_LOOP ( 'NONE', ( #127609, #202913, #108410, #169904 ) ) ;
#200970=DIRECTION ( 'NONE',  ( 0.000000000000000000, -1.000000000000000000, 0.000000000000000000 ) ) ;
#200977=AXIS2_PLACEMENT_3D ( 'NONE', #137844, #79155, #38772 ) ;
#201007=AXIS2_PLACEMENT_3D ( 'NONE', #15853, #36702, #116225 ) ;
#201011=EDGE_CURVE ( 'NONE', #205515, #177471, #236163, .T. ) ;
#201060=ADVANCED_FACE ( 'NONE', ( #135031 ), #92072, .F. ) ;
#201068=ORIENTED_EDGE ( 'NONE', *, *, #87418, .F. ) ;
#201076=CIRCLE ( 'NONE', #188586, 0.09999999999998898659 ) ;
#201080=TOROIDAL_SURFACE ( 'NONE', #22030, 12.97499999999999609, 0.1000000000000000056 ) ;
#201083=DIRECTION ( 'NONE',  ( -3.469446951953515108E-14, -1.000000000000000000, 0.000000000000000000 ) ) ;
#201124=EDGE_CURVE ( 'NONE', #47017, #32552, #231907, .T. ) ;
#201133=ORIENTED_EDGE ( 'NONE', *, *, #6521, .F. ) ;
#201177=EDGE_CURVE ( 'NONE', #246161, #246982, #252715, .T. ) ;
#201207=CARTESIAN_POINT ( 'NONE',  ( -21.05000000000000071, 76.00000000001267608, -203.5231074845243597 ) ) ;
#201210=VERTEX_POINT ( 'NONE', #121926 ) ;
#201215=CYLINDRICAL_SURFACE ( 'NONE', #24225, 4.000000000000003553 ) ;
#201235=ADVANCED_FACE ( 'NONE', ( #77621 ), #26695, .T. ) ;
#201249=ORIENTED_EDGE ( 'NONE', *, *, #59003, .T. ) ;
#201264=DIRECTION ( 'NONE',  ( -0.000000000000000000, 6.982962677686266711E-15, -1.000000000000000000 ) ) ;
#201296=ORIENTED_EDGE ( 'NONE', *, *, #228516, .F. ) ;
#201305=AXIS2_PLACEMENT_3D ( 'NONE', #176300, #255769, #77167 ) ;
#201351=CARTESIAN_POINT ( 'NONE',  ( -23.15000000000000213, 64.35000000001258513, -191.3731074845244393 ) ) ;
#201364=CARTESIAN_POINT ( 'NONE',  ( -20.64999999999999858, 85.00000000001261924, -194.1291383618718385 ) ) ;
#201379=CARTESIAN_POINT ( 'NONE',  ( -20.54999999999999716, 76.00000000001244871, -170.0231074845243597 ) ) ;
#201403=ORIENTED_EDGE ( 'NONE', *, *, #87429, .F. ) ;
#201405=LINE ( 'NONE', #41082, #25876 ) ;
#201409=DIRECTION ( 'NONE',  ( 0.000000000000000000, 0.9908441862701420355, 0.1350103645453197554 ) ) ;
#201441=CARTESIAN_POINT ( 'NONE',  ( -21.05000000000000071, 64.40000000001249703, -176.9513107147999449 ) ) ;
#201450=CARTESIAN_POINT ( 'NONE',  ( 23.14999999999999858, 72.00000000001244871, -170.0231074845243882 ) ) ;
#201455=CARTESIAN_POINT ( 'NONE',  ( 20.22483756094572271, 66.49809532114224453, -195.3835683558092171 ) ) ;
#201507=ORIENTED_EDGE ( 'NONE', *, *, #19645, .T. ) ;
#201542=DIRECTION ( 'NONE',  ( -0.7071067811865475727, 0.7071067811865475727, 4.937700262164531476E-15 ) ) ;
#201560=ORIENTED_EDGE ( 'NONE', *, *, #105039, .T. ) ;
#201566=CARTESIAN_POINT ( 'NONE',  ( 18.49999999999999645, 76.00000000001244871, -170.0231074845243597 ) ) ;
#201571=ADVANCED_FACE ( 'NONE', ( #71793 ), #124006, .T. ) ;
#201583=DIRECTION ( 'NONE',  ( 0.000000000000000000, 0.1455152366551700771, 0.9893560106964479628 ) ) ;
#201640=CIRCLE ( 'NONE', #105756, 0.1000000000000021289 ) ;
#201641=CARTESIAN_POINT ( 'NONE',  ( 21.08035267497491105, 69.66829316022966623, -203.6057961093005417 ) ) ;
#201664=DIRECTION ( 'NONE',  ( 0.000000000000000000, -6.938893903907222067E-15, 1.000000000000000000 ) ) ;
#201681=ORIENTED_EDGE ( 'NONE', *, *, #19651, .T. ) ;
#201703=CARTESIAN_POINT ( 'NONE',  ( 18.60000000000000142, 85.32100840337392356, -196.2871692354463846 ) ) ;
#201737=EDGE_LOOP ( 'NONE', ( #144754, #87620 ) ) ;
#201771=ORIENTED_EDGE ( 'NONE', *, *, #247165, .F. ) ;
#201777=ADVANCED_FACE ( 'NONE', ( #113379 ), #35165, .T. ) ;
#201790=EDGE_CURVE ( 'NONE', #7857, #62333, #230776, .T. ) ;
#201791=ORIENTED_EDGE ( 'NONE', *, *, #114847, .T. ) ;
#201866=ORIENTED_EDGE ( 'NONE', *, *, #159806, .F. ) ;
#201873=EDGE_LOOP ( 'NONE', ( #204873, #252242, #66039, #153796 ) ) ;
#201891=EDGE_LOOP ( 'NONE', ( #184254, #123742, #109330, #226668 ) ) ;
#201910=VECTOR ( 'NONE', #8814, 1000.000000000000000 ) ;
#201916=ADVANCED_FACE ( 'NONE', ( #218874, #256683 ), #96356, .T. ) ;
#201946=DIRECTION ( 'NONE',  ( 0.000000000000000000, 0.000000000000000000, -1.000000000000000000 ) ) ;
#201966=ORIENTED_EDGE ( 'NONE', *, *, #174729, .F. ) ;
#201982=DIRECTION ( 'NONE',  ( -0.000000000000000000, 1.000000000000000000, 6.982962677686266711E-15 ) ) ;
#201995=DIRECTION ( 'NONE',  ( 1.000000000000000000, 0.000000000000000000, 0.000000000000000000 ) ) ;
#202049=DIRECTION ( 'NONE',  ( 1.000000000000000000, 0.000000000000000000, 0.000000000000000000 ) ) ;
#202076=CARTESIAN_POINT ( 'NONE',  ( 20.94999999999999929, 70.50000000001260503, -191.1178414656113205 ) ) ;
#202077=CARTESIAN_POINT ( 'NONE',  ( 21.09696443733127325, 65.27599011609412116, -191.2883299574762077 ) ) ;
#202084=EDGE_LOOP ( 'NONE', ( #186689, #141440, #17033, #72684 ) ) ;
#202087=DIRECTION ( 'NONE',  ( 1.000000000000000000, -3.265361837132813093E-16, -2.280189983783949500E-30 ) ) ;
#202099=DIRECTION ( 'NONE',  ( 0.000000000000000000, 0.000000000000000000, 1.000000000000000000 ) ) ;
#202157=AXIS2_PLACEMENT_3D ( 'NONE', #5223, #125211, #87339 ) ;
#202170=ORIENTED_EDGE ( 'NONE', *, *, #119206, .T. ) ;
#202180=CYLINDRICAL_SURFACE ( 'NONE', #95078, 0.5000000000000004441 ) ;
#202231=CARTESIAN_POINT ( 'NONE',  ( 20.94999999999999929, 71.00000000001253397, -182.4283735034374843 ) ) ;
#202234=CARTESIAN_POINT ( 'NONE',  ( 22.39999999999999858, 75.90000000001273861, -211.3138870828977360 ) ) ;
#202245=AXIS2_PLACEMENT_3D ( 'NONE', #242552, #67774, #44377 ) ;
#202260=TOROIDAL_SURFACE ( 'NONE', #31421, 0.2000000000000000111, 0.1000000000000000056 ) ;
#202261=DIRECTION ( 'NONE',  ( -0.000000000000000000, 0.1298341882519953583, 0.9915357197604862671 ) ) ;
#202312=PLANE ( 'NONE',  #254232 ) ;
#202321=VERTEX_POINT ( 'NONE', #238127 ) ;
#202341=LINE ( 'NONE', #103218, #51851 ) ;
#202364=EDGE_CURVE ( 'NONE', #109246, #115263, #120233, .T. ) ;
#202388=CARTESIAN_POINT ( 'NONE',  ( 18.59999999999999076, 77.83585931145600512, -158.5186683157258187 ) ) ;
#202391=VECTOR ( 'NONE', #40736, 1000.000000000000000 ) ;
#202397=AXIS2_PLACEMENT_3D ( 'NONE', #211304, #32713, #245300 ) ;
#202424=CARTESIAN_POINT ( 'NONE',  ( -18.41418431465368499, 85.50000000001263345, -163.4229180933028260 ) ) ;
#202427=FACE_OUTER_BOUND ( 'NONE', #173645, .T. ) ;
#202443=EDGE_CURVE ( 'NONE', #241281, #75576, #50193, .T. ) ;
#202495=ORIENTED_EDGE ( 'NONE', *, *, #234524, .T. ) ;
#202522=EDGE_CURVE ( 'NONE', #47404, #115127, #153758, .T. ) ;
#202538=ADVANCED_FACE ( 'NONE', ( #157033 ), #257334, .T. ) ;
#202546=CIRCLE ( 'NONE', #248336, 4.000000000000003553 ) ;
#202591=VECTOR ( 'NONE', #110393, 1000.000000000000000 ) ;
#202631=CIRCLE ( 'NONE', #19497, 0.09999999999998898659 ) ;
#202666=LINE ( 'NONE', #87835, #207962 ) ;
#202675=ORIENTED_EDGE ( 'NONE', *, *, #252339, .T. ) ;
#202699=B_SPLINE_CURVE_WITH_KNOTS ( 'NONE', 3,
 ( #64303, #8197, #87698, #44751, #47281, #6891, #205076, #124290, #167288, #105969 ),
 .UNSPECIFIED., .F., .F.,
 ( 4, 2, 2, 2, 4 ),
 ( 0.000000000000000000, 3.990160268011731543E-05, 7.980320536023463086E-05, 0.0001596064107204822450, 0.0003192128214409942514 ),
 .UNSPECIFIED. ) ;
#202705=ORIENTED_EDGE ( 'NONE', *, *, #254209, .F. ) ;
#202732=DIRECTION ( 'NONE',  ( 0.000000000000000000, 0.9915357197604982575, -0.1298341882519033486 ) ) ;
#202745=CARTESIAN_POINT ( 'NONE',  ( -21.05000000000000071, 74.16465844978819177, -191.9679561919613775 ) ) ;
#202749=DIRECTION ( 'NONE',  ( 0.000000000000000000, 0.000000000000000000, 1.000000000000000000 ) ) ;
#202759=EDGE_CURVE ( 'NONE', #133788, #239144, #61765, .T. ) ;
#202767=LINE ( 'NONE', #42412, #252280 ) ;
#202776=CARTESIAN_POINT ( 'NONE',  ( 21.14999999999999858, 67.21339244341248786, -191.2731074845244166 ) ) ;
#202790=DIRECTION ( 'NONE',  ( 0.000000000000000000, 0.000000000000000000, -1.000000000000000000 ) ) ;
#202800=CARTESIAN_POINT ( 'NONE',  ( -22.24259225415828567, 68.50806212944726781, -203.6221733679772399 ) ) ;
#202813=CARTESIAN_POINT ( 'NONE',  ( 21.05000000000000426, 75.93429838969065315, -209.7814235418563840 ) ) ;
#202842=CYLINDRICAL_SURFACE ( 'NONE', #11012, 0.1000000000000033362 ) ;
#202844=ORIENTED_EDGE ( 'NONE', *, *, #219451, .F. ) ;
#202847=EDGE_CURVE ( 'NONE', #10056, #99738, #257877, .T. ) ;
#202872=CARTESIAN_POINT ( 'NONE',  ( -21.10257677756356998, 69.60161825747997000, -203.5480582340924229 ) ) ;
#202874=CARTESIAN_POINT ( 'NONE',  ( 18.49362639424878196, 85.44260436790082736, -163.2586665510135049 ) ) ;
#202881=ORIENTED_EDGE ( 'NONE', *, *, #100552, .T. ) ;
#202913=ORIENTED_EDGE ( 'NONE', *, *, #114639, .T. ) ;
#202923=CARTESIAN_POINT ( 'NONE',  ( 21.11927991906888025, 69.55150688152127714, -203.5321911639982773 ) ) ;
#202942=VERTEX_POINT ( 'NONE', #15955 ) ;
#202968=CARTESIAN_POINT ( 'NONE',  ( 21.05000000000000071, 76.00000000001247713, -172.9231074845243654 ) ) ;
#203006=CARTESIAN_POINT ( 'NONE',  ( 23.14999999999999858, 71.22429906543310096, -181.8718755885703615 ) ) ;
#203008=EDGE_CURVE ( 'NONE', #28626, #34288, #224600, .T. ) ;
#203040=CIRCLE ( 'NONE', #78138, 0.09999999999999938105 ) ;
#203054=CIRCLE ( 'NONE', #82228, 0.1999999999999987899 ) ;
#203073=FACE_OUTER_BOUND ( 'NONE', #251705, .T. ) ;
#203084=EDGE_LOOP ( 'NONE', ( #21816, #124568, #162746, #187854 ) ) ;
#203108=DIRECTION ( 'NONE',  ( 1.000000000000000000, 0.000000000000000000, 0.000000000000000000 ) ) ;
#203115=CIRCLE ( 'NONE', #153095, 0.2000000000000057288 ) ;
#203161=ORIENTED_EDGE ( 'NONE', *, *, #55787, .T. ) ;
#203182=EDGE_CURVE ( 'NONE', #215277, #203821, #242664, .T. ) ;
#203209=ORIENTED_EDGE ( 'NONE', *, *, #15092, .T. ) ;
#203231=CARTESIAN_POINT ( 'NONE',  ( -21.07928932188134397, 75.90110485435833709, -209.8516241409176928 ) ) ;
#203232=CARTESIAN_POINT ( 'NONE',  ( 21.05000000000000426, 65.43724016256159359, -196.0662935266058184 ) ) ;
#203256=CIRCLE ( 'NONE', #236393, 11.80000000000000426 ) ;
#203279=EDGE_LOOP ( 'NONE', ( #47523, #203791, #201681, #154229 ) ) ;
#203282=ORIENTED_EDGE ( 'NONE', *, *, #30509, .T. ) ;
#203287=CIRCLE ( 'NONE', #111523, 12.87499999999999822 ) ;
#203314=FACE_OUTER_BOUND ( 'NONE', #42872, .T. ) ;
#203328=AXIS2_PLACEMENT_3D ( 'NONE', #47284, #225912, #43461 ) ;
#203347=ORIENTED_EDGE ( 'NONE', *, *, #102978, .F. ) ;
#203348=DIRECTION ( 'NONE',  ( 0.000000000000000000, 6.853228547068871147E-15, -1.000000000000000000 ) ) ;
#203361=CARTESIAN_POINT ( 'NONE',  ( -18.58671080940899145, 85.40693285883926933, -196.3989530196196256 ) ) ;
#203368=CARTESIAN_POINT ( 'NONE',  ( 23.14999999999999503, 64.25000000001249134, -177.0379132551784096 ) ) ;
#203369=CARTESIAN_POINT ( 'NONE',  ( 18.59999999999996945, 68.97833521811233481, -166.1895420826271277 ) ) ;
#203376=EDGE_CURVE ( 'NONE', #60192, #34777, #245649, .T. ) ;
#203381=CIRCLE ( 'NONE', #74231, 0.09999999999999939493 ) ;
#203408=CARTESIAN_POINT ( 'NONE',  ( -20.94999999999999929, 74.16465844978819177, -191.9679561919613775 ) ) ;
#203415=ADVANCED_FACE ( 'NONE', ( #239485 ), #140360, .F. ) ;
#203416=DIRECTION ( 'NONE',  ( 0.000000000000000000, -6.982962677686266711E-15, 1.000000000000000000 ) ) ;
#203433=CARTESIAN_POINT ( 'NONE',  ( -23.15000000000000213, 73.50000000001254818, -183.2477294072864709 ) ) ;
#203465=AXIS2_PLACEMENT_3D ( 'NONE', #39973, #197725, #174369 ) ;
#203468=AXIS2_PLACEMENT_3D ( 'NONE', #238800, #120173, #122722 ) ;
#203469=EDGE_LOOP ( 'NONE', ( #78511, #144517, #250734, #37385 ) ) ;
#203484=CLOSED_SHELL ( 'NONE', ( #110742, #195798, #215471, #49905, #215411, #220503, #30798, #238943, #227242, #48769, #213229, #256014, #232799, #233090, #252327, #56646, #75434, #12707, #28524, #154124, #177161, #118578, #76877, #49160, #198786, #36373, #242000, #211984, #800, #209576, #173442, #114641, #219768, #128887, #118282, #192393, #228842, #160024, #70283, #200444, #77001, #162889, #80273, #76827, #226934, #164304, #2587, #23641, #107358, #214745, #108179, #167757, #124586, #81794, #81153, #21584, #215681, #2506, #189820, #1921, #106034, #231265, #201916, #159823, #254283, #233765, #64631, #68797, #49189, #127802, #167068, #112315, #109789, #82360, #173944, #85543, #254613, #236347, #245243, #108797, #256203, #30237, #21225, #70007, #106345, #98788, #81959, #106223, #156008, #39656, #118420, #212122, #116622, #119429, #118251, #143780, #119099, #174341, #114518, #93385, #120359, #122343, #173794, #20433, #1080, #130587, #201777, #34788, #74745, #5840, #149533, #117399, #121573, #67468, #178974, #159140, #227740, #74177, #59293, #139027, #9925, #248429, #110585, #181617, #26748, #254768, #226819, #227655, #87083, #66664, #232997, #244754, #17835, #202538, #37923, #154006, #152426, #215693, #139669, #98801, #10599, #190994, #208420, #234549, #87914, #32487, #228362, #61478, #194346, #144697, #109610, #132951, #157014, #163952, #93703, #193566, #94652, #231007, #243701, #215375, #207689, #131181, #30846, #230538, #142414, #252392, #201060, #239633, #238342, #180158, #96807, #193689, #103576, #30898, #121175, #90487, #73795, #9604, #53652, #82660, #246364, #156698, #107454, #27352, #112704, #242186, #79020, #176636, #98892, #172321, #164171, #43829, #72179, #4609, #118400, #58161, #100230, #101867, #8867, #38817, #210320, #221054, #234741, #98985, #70816, #30003, #206443, #122028, #1806, #188643, #171561, #80565, #140892, #134302, #220713, #257951, #159002, #56144, #199842, #89111, #18202, #73849, #254700, #83991, #238088, #199906, #112631, #105787, #55922, #189345, #178667, #217000, #149672, #192670, #185057, #217894, #56934, #105328, #221538, #115562, #35702, #36535, #33909, #149541, #138734, #94982, #36714, #178954, #116337, #234466, #71288, #212936, #106369, #168108, #73994, #138155, #95028, #107320, #111232, #56125, #20117, #115732, #90797, #220645, #64098, #95277, #189614, #216688, #192205, #253668, #133863, #219882, #121653, #156162, #141530, #167050, #222426, #134420, #228230, #153595, #209233, #190978, #250032, #25442, #90147, #28878, #148354, #215074, #7790, #73127, #236326, #1116, #91116, #70420, #50089, #172569, #28739, #27231, #191701, #129425, #220938, #14492, #223166, #120334, #77642, #241238, #153144, #17579, #125905, #136207, #225407, #131514, #175070, #90363, #67299, #37197, #33070, #144095, #148258, #129818, #131796, #175740, #24072, #52791, #204568, #76198, #257300, #122431, #249844, #170695, #218856, #220442, #55331, #150656, #179035, #251652, #88442, #37240, #41231, #181066, #60152, #203415, #228898, #71707, #58112, #123133, #218624, #71275, #87304, #165960, #252355, #178774, #208313, #26390, #89893, #61924, #34163, #120996, #255157, #211257, #201571, #236678, #74639, #90639, #204534, #162630, #254447, #246171, #198952, #185234, #255851, #118249, #173049, #59039, #227359, #220429, #232730, #199295, #55264, #70659, #46110, #168656, #58137, #135096, #88761, #113363, #186355, #118179, #180982, #86029, #58214, #179259, #233032, #4547, #20009, #184759, #4574, #4304, #247711, #162943, #248129, #196774, #91927, #256467, #92623, #105864, #198705, #10593, #5551, #138368, #84435, #25535, #162513, #178870, #58176, #51121, #95216, #246658, #14153, #105473, #218770, #42244, #73619, #136483, #63377, #264, #21970, #30550, #227557, #187752, #3468, #206147, #117639, #177065, #223965, #159873, #51360, #22105, #145037, #227188, #185732, #186033, #166051, #257009, #246204, #24984, #172312, #67233, #195382, #159808, #192674, #68105, #108566, #226501, #70401, #30160, #190680, #189264, #174565, #62683, #162356, #225612, #145959, #127827, #110611, #180826, #140610, #179973, #195046, #95696, #249845, #117863, #32373, #94489, #201235, #89047, #251513, #141303 ) ) ;
#203519=EDGE_CURVE ( 'NONE', #109246, #160984, #3412, .T. ) ;
#203549=CARTESIAN_POINT ( 'NONE',  ( -20.05000000000000426, 66.75000000001260503, -191.1731074845244223 ) ) ;
#203575=EDGE_CURVE ( 'NONE', #127123, #137948, #216414, .T. ) ;
#203580=CARTESIAN_POINT ( 'NONE',  ( -20.85000000000000142, 77.73670573947995877, -158.5056848969006182 ) ) ;
#203618=CYLINDRICAL_SURFACE ( 'NONE', #218470, 0.09999999999998898659 ) ;
#203624=CARTESIAN_POINT ( 'NONE',  ( 20.95512820512820440, 65.37615131630076348, -195.8581939154368285 ) ) ;
#203643=ORIENTED_EDGE ( 'NONE', *, *, #157717, .T. ) ;
#203659=CARTESIAN_POINT ( 'NONE',  ( 18.39999999999999858, 85.40000000001276703, -215.2731074845243029 ) ) ;
#203665=CARTESIAN_POINT ( 'NONE',  ( -22.39999999999999858, 76.00000000001276135, -215.1726782920691505 ) ) ;
#203674=CARTESIAN_POINT ( 'NONE',  ( 22.39999999999999503, 64.35000000001267040, -203.6231074845244393 ) ) ;
#203688=VERTEX_POINT ( 'NONE', #155805 ) ;
#203705=AXIS2_PLACEMENT_3D ( 'NONE', #234609, #93807, #153846 ) ;
#203708=VERTEX_POINT ( 'NONE', #253579 ) ;
#203723=EDGE_CURVE ( 'NONE', #32289, #145080, #136175, .T. ) ;
#203731=CARTESIAN_POINT ( 'NONE',  ( -20.64999999999999858, 85.00000000001251976, -179.9170766071767389 ) ) ;
#203760=ORIENTED_EDGE ( 'NONE', *, *, #36460, .T. ) ;
#203777=ORIENTED_EDGE ( 'NONE', *, *, #188171, .F. ) ;
#203791=ORIENTED_EDGE ( 'NONE', *, *, #21054, .T. ) ;
#203812=DIRECTION ( 'NONE',  ( 1.000000000000000000, 0.000000000000000000, 0.000000000000000000 ) ) ;
#203818=AXIS2_PLACEMENT_3D ( 'NONE', #23295, #121118, #224020 ) ;
#203821=VERTEX_POINT ( 'NONE', #47364 ) ;
#203832=AXIS2_PLACEMENT_3D ( 'NONE', #202234, #62725, #97961 ) ;
#203843=DIRECTION ( 'NONE',  ( -6.938893903907222856E-15, -1.000000000000000000, -6.982962677686266711E-15 ) ) ;
#203852=CIRCLE ( 'NONE', #141318, 12.97499999999998721 ) ;
#203872=AXIS2_PLACEMENT_3D ( 'NONE', #118539, #206707, #161512 ) ;
#203875=DIRECTION ( 'NONE',  ( 1.000000000000000000, 0.000000000000000000, 0.000000000000000000 ) ) ;
#203879=CARTESIAN_POINT ( 'NONE',  ( -20.64999999999999858, 76.00000000001244871, -170.0231074845243597 ) ) ;
#203886=EDGE_CURVE ( 'NONE', #247461, #183161, #91135, .T. ) ;
#203930=CARTESIAN_POINT ( 'NONE',  ( 21.05000000000000071, 70.60000000001259934, -191.1178414656113205 ) ) ;
#203931=EDGE_LOOP ( 'NONE', ( #195156, #60809, #239859, #16148, #175880 ) ) ;
#203934=CARTESIAN_POINT ( 'NONE',  ( -18.56579813702275672, 65.66974365629718591, -164.4360145562605169 ) ) ;
#203961=VERTEX_POINT ( 'NONE', #52502 ) ;
#203975=EDGE_CURVE ( 'NONE', #14901, #218733, #211761, .T. ) ;
#203987=CARTESIAN_POINT ( 'NONE',  ( -23.25000000000000000, 71.85000000001254250, -182.3731074845244109 ) ) ;
#204004=AXIS2_PLACEMENT_3D ( 'NONE', #170541, #250020, #71406 ) ;
#204011=FACE_OUTER_BOUND ( 'NONE', #124207, .T. ) ;
#204015=EDGE_CURVE ( 'NONE', #91470, #164331, #103758, .T. ) ;
#204041=EDGE_LOOP ( 'NONE', ( #85823, #242442, #35182, #133936 ) ) ;
#204045=AXIS2_PLACEMENT_3D ( 'NONE', #176704, #211979, #153311 ) ;
#204113=ORIENTED_EDGE ( 'NONE', *, *, #82498, .T. ) ;
#204157=LINE ( 'NONE', #127209, #168430 ) ;
#204172=AXIS2_PLACEMENT_3D ( 'NONE', #44781, #23953, #102146 ) ;
#204191=EDGE_CURVE ( 'NONE', #236913, #229203, #137110, .T. ) ;
#204194=CARTESIAN_POINT ( 'NONE',  ( 21.98333005346336222, 76.00000000001273293, -210.8971828135810256 ) ) ;
#204198=VECTOR ( 'NONE', #172086, 1000.000000000000000 ) ;
#204245=CIRCLE ( 'NONE', #196071, 0.09999999999998898659 ) ;
#204275=CARTESIAN_POINT ( 'NONE',  ( 20.94999999999999929, 64.35000000001249987, -176.8069731475025321 ) ) ;
#204285=AXIS2_PLACEMENT_3D ( 'NONE', #49660, #129208, #116071 ) ;
#204294=ORIENTED_EDGE ( 'NONE', *, *, #213030, .T. ) ;
#204301=CARTESIAN_POINT ( 'NONE',  ( -21.07094088545304444, 69.67983277809619835, -203.6220011870766200 ) ) ;
#204329=ORIENTED_EDGE ( 'NONE', *, *, #190365, .F. ) ;
#204332=ORIENTED_EDGE ( 'NONE', *, *, #213593, .F. ) ;
#204341=CARTESIAN_POINT ( 'NONE',  ( -21.10320863425827298, 75.97497774878561927, -209.9233848709835684 ) ) ;
#204361=AXIS2_PLACEMENT_3D ( 'NONE', #239512, #162554, #101222 ) ;
#204385=VERTEX_POINT ( 'NONE', #110905 ) ;
#204389=ORIENTED_EDGE ( 'NONE', *, *, #226237, .T. ) ;
#204390=CARTESIAN_POINT ( 'NONE',  ( 22.47007471830798409, 68.27928934808623751, -203.5231074845244450 ) ) ;
#204391=CARTESIAN_POINT ( 'NONE',  ( 20.85000000000000142, 76.00000000001244871, -170.0231074845243597 ) ) ;
#204396=ORIENTED_EDGE ( 'NONE', *, *, #24279, .F. ) ;
#204425=ORIENTED_EDGE ( 'NONE', *, *, #134877, .T. ) ;
#204427=DIRECTION ( 'NONE',  ( 2.952720810173289112E-16, 1.000000000000000000, -6.088138035986627436E-46 ) ) ;
#204465=DIRECTION ( 'NONE',  ( 6.938893903907224433E-15, 1.000000000000000000, 7.272083257015735086E-15 ) ) ;
#204485=CARTESIAN_POINT ( 'NONE',  ( 22.39999999999999503, 64.25000000001269029, -203.6231074845244393 ) ) ;
#204522=DIRECTION ( 'NONE',  ( 0.000000000000000000, 6.938893903907222067E-15, -1.000000000000000000 ) ) ;
#204534=ADVANCED_FACE ( 'NONE', ( #232154 ), #136885, .F. ) ;
#204550=EDGE_CURVE ( 'NONE', #219970, #241382, #116461, .T. ) ;
#204551=DIRECTION ( 'NONE',  ( -1.000000000000000000, 0.000000000000000000, -0.000000000000000000 ) ) ;
#204559=VERTEX_POINT ( 'NONE', #80744 ) ;
#204568=ADVANCED_FACE ( 'NONE', ( #100305 ), #42927, .T. ) ;
#204606=AXIS2_PLACEMENT_3D ( 'NONE', #201566, #60764, #81589 ) ;
#204610=DIRECTION ( 'NONE',  ( 1.000000000000000000, -3.265361837132813093E-16, -2.280189983783949500E-30 ) ) ;
#204614=CARTESIAN_POINT ( 'NONE',  ( -21.05000000000000071, 70.15000000001252545, -180.1556047088023149 ) ) ;
#204632=DIRECTION ( 'NONE',  ( -0.000000000000000000, -6.982962677686266711E-15, 1.000000000000000000 ) ) ;
#204638=AXIS2_PLACEMENT_3D ( 'NONE', #212341, #51934, #173244 ) ;
#204640=FACE_OUTER_BOUND ( 'NONE', #232362, .T. ) ;
#204643=ORIENTED_EDGE ( 'NONE', *, *, #124223, .F. ) ;
#204672=ORIENTED_EDGE ( 'NONE', *, *, #159863, .F. ) ;
#204678=DIRECTION ( 'NONE',  ( -3.265361837132813093E-16, -1.000000000000000000, 7.445645354460596589E-46 ) ) ;
#204688=ORIENTED_EDGE ( 'NONE', *, *, #162807, .F. ) ;
#204716=EDGE_CURVE ( 'NONE', #183161, #182093, #220295, .T. ) ;
#204727=ORIENTED_EDGE ( 'NONE', *, *, #109341, .F. ) ;
#204730=ORIENTED_EDGE ( 'NONE', *, *, #182181, .F. ) ;
#204733=VERTEX_POINT ( 'NONE', #148457 ) ;
#204747=VERTEX_POINT ( 'NONE', #11518 ) ;
#204772=CARTESIAN_POINT ( 'NONE',  ( -21.03922262424653056, 64.37609936600787819, -196.6638994416307753 ) ) ;
#204807=EDGE_LOOP ( 'NONE', ( #173895, #136349, #197780, #240414 ) ) ;
#204837=EDGE_CURVE ( 'NONE', #93986, #58809, #79192, .T. ) ;
#204842=EDGE_CURVE ( 'NONE', #174151, #165186, #58335, .T. ) ;
#204858=CARTESIAN_POINT ( 'NONE',  ( -21.05000000000000071, 76.00000000001264766, -199.2231074845243768 ) ) ;
#204865=TOROIDAL_SURFACE ( 'NONE', #196673, 0.2000000000000000111, 0.1000000000000000056 ) ;
#204873=ORIENTED_EDGE ( 'NONE', *, *, #50045, .F. ) ;
#204907=DIRECTION ( 'NONE',  ( 0.000000000000000000, -6.982962677686266711E-15, 1.000000000000000000 ) ) ;
#204957=EDGE_CURVE ( 'NONE', #240431, #139907, #12598, .T. ) ;
#204965=ORIENTED_EDGE ( 'NONE', *, *, #244203, .F. ) ;
#204987=DIRECTION ( 'NONE',  ( 0.000000000000000000, 0.000000000000000000, 1.000000000000000000 ) ) ;
#205010=ORIENTED_EDGE ( 'NONE', *, *, #115129, .T. ) ;
#205026=EDGE_LOOP ( 'NONE', ( #50072, #5825, #171432, #138559 ) ) ;
#205041=DIRECTION ( 'NONE',  ( -0.000000000000000000, -6.982962677686266711E-15, 1.000000000000000000 ) ) ;
#205076=CARTESIAN_POINT ( 'NONE',  ( -18.47653818581420992, 85.46528038777560710, -196.3971466683844938 ) ) ;
#205085=AXIS2_PLACEMENT_3D ( 'NONE', #186369, #123824, #225458 ) ;
#205106=CARTESIAN_POINT ( 'NONE',  ( 21.14999999999999858, 64.25000000001276135, -215.2731074845244450 ) ) ;
#205116=DIRECTION ( 'NONE',  ( 0.7070776581708965169, 4.937903618720407826E-15, -0.7071359030027827286 ) ) ;
#205117=CARTESIAN_POINT ( 'NONE',  ( 23.14999999999998437, 76.00000000001270450, -207.5731074845243427 ) ) ;
#205124=CARTESIAN_POINT ( 'NONE',  ( -20.64999999999999858, 74.00000000001259082, -190.2984855617622770 ) ) ;
#205130=ORIENTED_EDGE ( 'NONE', *, *, #208750, .F. ) ;
#205144=DIRECTION ( 'NONE',  ( 0.000000000000000000, -6.454785026890489601E-15, 1.000000000000000000 ) ) ;
#205152=DIRECTION ( 'NONE',  ( 0.000000000000000000, -7.545205021724366615E-15, 1.000000000000000000 ) ) ;
#205179=CIRCLE ( 'NONE', #209283, 2.000000000000001776 ) ;
#205185=DIRECTION ( 'NONE',  ( 0.000000000000000000, 0.000000000000000000, -1.000000000000000000 ) ) ;
#205228=B_SPLINE_CURVE_WITH_KNOTS ( 'NONE', 3,
 ( #98338, #158397, #194938, #16306 ),
 .UNSPECIFIED., .F., .F.,
 ( 4, 4 ),
 ( 0.000000000000000000, 0.0001048066582182473756 ),
 .UNSPECIFIED. ) ;
#205254=CIRCLE ( 'NONE', #76082, 7.800000000000001599 ) ;
#205262=ORIENTED_EDGE ( 'NONE', *, *, #171223, .T. ) ;
#205287=DIRECTION ( 'NONE',  ( 0.000000000000000000, -1.000000000000000000, 0.000000000000000000 ) ) ;
#205305=CARTESIAN_POINT ( 'NONE',  ( 21.05000000000000071, 75.96798630682469877, -209.7819502080617156 ) ) ;
#205323=CARTESIAN_POINT ( 'NONE',  ( 21.05000000000000071, 67.22371711014486095, -191.3468923434563465 ) ) ;
#205340=CARTESIAN_POINT ( 'NONE',  ( -18.50000000000000000, 64.35000000001254250, -182.1731074845244507 ) ) ;
#205359=ORIENTED_EDGE ( 'NONE', *, *, #183129, .F. ) ;
#205363=AXIS2_PLACEMENT_3D ( 'NONE', #163515, #243041, #138768 ) ;
#205390=ORIENTED_EDGE ( 'NONE', *, *, #142129, .F. ) ;
#205391=AXIS2_PLACEMENT_3D ( 'NONE', #251625, #234626, #173427 ) ;
#205405=PRODUCT ( 'Injection Molded Chain Links 11', 'Injection Molded Chain Links 11', '', ( #39107 ) ) ;
#205433=CARTESIAN_POINT ( 'NONE',  ( 23.14999999999999858, 71.00000000001260503, -191.1178414656112921 ) ) ;
#205455=EDGE_CURVE ( 'NONE', #6765, #116410, #235338, .T. ) ;
#205477=DIRECTION ( 'NONE',  ( -1.000000000000000000, 0.000000000000000000, 0.000000000000000000 ) ) ;
#205500=FACE_OUTER_BOUND ( 'NONE', #206399, .T. ) ;
#205515=VERTEX_POINT ( 'NONE', #123119 ) ;
#205520=CIRCLE ( 'NONE', #167972, 0.09999999999999939493 ) ;
#205627=ORIENTED_EDGE ( 'NONE', *, *, #41597, .F. ) ;
#205661=EDGE_CURVE ( 'NONE', #4716, #236840, #89117, .T. ) ;
#205681=AXIS2_PLACEMENT_3D ( 'NONE', #119984, #125096, #24732 ) ;
#205694=PLANE ( 'NONE',  #194025 ) ;
#205717=AXIS2_PLACEMENT_3D ( 'NONE', #100165, #138020, #1069 ) ;
#205719=AXIS2_PLACEMENT_3D ( 'NONE', #212670, #78266, #155287 ) ;
#205736=CARTESIAN_POINT ( 'NONE',  ( -20.54999999999999716, 85.00000000001261924, -193.6291383618718385 ) ) ;
#205739=VERTEX_POINT ( 'NONE', #68284 ) ;
#205752=DIRECTION ( 'NONE',  ( -3.265361837132813093E-16, -1.000000000000000000, -7.086529944415894657E-15 ) ) ;
#205759=ORIENTED_EDGE ( 'NONE', *, *, #182163, .F. ) ;
#205778=DIRECTION ( 'NONE',  ( 1.000000000000000000, 0.000000000000000000, 0.000000000000000000 ) ) ;
#205779=DIRECTION ( 'NONE',  ( 1.000000000000000000, -0.000000000000000000, 0.000000000000000000 ) ) ;
#205797=CARTESIAN_POINT ( 'NONE',  ( -21.05000000000000071, 75.90220970870393558, -209.7809220950004772 ) ) ;
#205804=ORIENTED_EDGE ( 'NONE', *, *, #139725, .T. ) ;
#205822=CARTESIAN_POINT ( 'NONE',  ( 22.39999999999999503, 64.25000000001269029, -203.6231074845244393 ) ) ;
#205827=ORIENTED_EDGE ( 'NONE', *, *, #45244, .F. ) ;
#205842=CARTESIAN_POINT ( 'NONE',  ( -20.85000000000000142, 77.83585931145600512, -158.5186683157258187 ) ) ;
#205854=DIRECTION ( 'NONE',  ( 0.000000000000000000, 0.4999999999999088507, -0.8660254037844913322 ) ) ;
#205867=DIRECTION ( 'NONE',  ( 1.000000000000000000, 0.000000000000000000, 0.000000000000000000 ) ) ;
#205877=ORIENTED_EDGE ( 'NONE', *, *, #95977, .F. ) ;
#205879=DIRECTION ( 'NONE',  ( -1.000000000000000000, 3.265361837132813093E-16, 2.280189983783949500E-30 ) ) ;
#205896=B_SPLINE_CURVE_WITH_KNOTS ( 'NONE', 3,
 ( #121262, #66382, #219023, #41698 ),
 .UNSPECIFIED., .F., .F.,
 ( 4, 4 ),
 ( 0.000000000000000000, 0.001767853679387143117 ),
 .UNSPECIFIED. ) ;
#205900=FACE_OUTER_BOUND ( 'NONE', #187607, .T. ) ;
#205903=CARTESIAN_POINT ( 'NONE',  ( 21.30000000000002558, 76.00000000001267608, -203.5231074845243597 ) ) ;
#205909=CARTESIAN_POINT ( 'NONE',  ( -18.59999999999999787, 74.16465844978819177, -191.9679561919613775 ) ) ;
#205910=DIRECTION ( 'NONE',  ( -1.000000000000000000, -0.000000000000000000, -0.000000000000000000 ) ) ;
#205914=DIRECTION ( 'NONE',  ( -0.000000000000000000, -6.982962677686266711E-15, 1.000000000000000000 ) ) ;
#205923=DIRECTION ( 'NONE',  ( -0.4999999999999799050, -6.047423072554995242E-15, 0.8660254037844502539 ) ) ;
#205930=LINE ( 'NONE', #248927, #194017 ) ;
#205940=ORIENTED_EDGE ( 'NONE', *, *, #81642, .T. ) ;
#205960=ORIENTED_EDGE ( 'NONE', *, *, #237213, .T. ) ;
#206023=EDGE_CURVE ( 'NONE', #60454, #30910, #108386, .T. ) ;
#206028=CARTESIAN_POINT ( 'NONE',  ( 21.05000000000000071, 67.12791932463488820, -195.0020600656924614 ) ) ;
#206059=CARTESIAN_POINT ( 'NONE',  ( 18.41789779300686192, 85.50000000001263345, -196.4910378181636190 ) ) ;
#206088=DIRECTION ( 'NONE',  ( 0.000000000000000000, 6.608470384673536035E-15, -1.000000000000000000 ) ) ;
#206104=AXIS2_PLACEMENT_3D ( 'NONE', #139159, #106143, #239582 ) ;
#206124=TOROIDAL_SURFACE ( 'NONE', #56254, 0.6000000000000006439, 0.1000000000000000056 ) ;
#206133=DIRECTION ( 'NONE',  ( 0.000000000000000000, -1.000000000000000000, 0.000000000000000000 ) ) ;
#206147=ADVANCED_FACE ( 'NONE', ( #177377 ), #121935, .T. ) ;
#206164=ORIENTED_EDGE ( 'NONE', *, *, #200364, .T. ) ;
#206165=LINE ( 'NONE', #204858, #84572 ) ;
#206169=CARTESIAN_POINT ( 'NONE',  ( -22.39999999999999858, 68.20922040163927136, -203.5231074845243882 ) ) ;
#206202=DIRECTION ( 'NONE',  ( 0.000000000000000000, 0.000000000000000000, 1.000000000000000000 ) ) ;
#206206=EDGE_CURVE ( 'NONE', #178265, #188196, #74428, .T. ) ;
#206225=DIRECTION ( 'NONE',  ( -1.000000000000000000, 1.836970198721029934E-16, 1.282749433769087582E-30 ) ) ;
#206261=VERTEX_POINT ( 'NONE', #194366 ) ;
#206278=CONICAL_SURFACE ( 'NONE', #222828, 6.250000000000005329, 0.7853981633974431720 ) ;
#206280=DIRECTION ( 'NONE',  ( 1.000000000000000000, 0.000000000000000000, 0.000000000000000000 ) ) ;
#206285=FACE_OUTER_BOUND ( 'NONE', #3522, .T. ) ;
#206290=EDGE_CURVE ( 'NONE', #36195, #94008, #67242, .T. ) ;
#206324=CARTESIAN_POINT ( 'NONE',  ( 23.15000000000000213, 88.41227409416215721, -173.1231074845242688 ) ) ;
#206333=DIRECTION ( 'NONE',  ( 7.589415207398576792E-15, 1.000000000000000000, 6.982962677686266711E-15 ) ) ;
#206344=CARTESIAN_POINT ( 'NONE',  ( -21.05000000000000071, 69.45934304831145312, -203.5231074845243882 ) ) ;
#206353=DIRECTION ( 'NONE',  ( 1.000000000000000000, 0.000000000000000000, 0.000000000000000000 ) ) ;
#206374=ORIENTED_EDGE ( 'NONE', *, *, #44148, .F. ) ;
#206377=EDGE_CURVE ( 'NONE', #177234, #195444, #205896, .T. ) ;
#206399=EDGE_LOOP ( 'NONE', ( #14586, #194026, #56365, #101696 ) ) ;
#206409=LINE ( 'NONE', #207712, #33978 ) ;
#206443=ADVANCED_FACE ( 'NONE', ( #49388 ), #92179, .T. ) ;
#206444=ORIENTED_EDGE ( 'NONE', *, *, #214145, .T. ) ;
#206457=CARTESIAN_POINT ( 'NONE',  ( 21.05000000000000071, 85.00000000001251976, -179.9170766071767389 ) ) ;
#206489=CYLINDRICAL_SURFACE ( 'NONE', #65465, 0.09999999999998898659 ) ;
#206493=CARTESIAN_POINT ( 'NONE',  ( 20.94999999999999929, 67.22371710472005191, -182.2731074845244166 ) ) ;
#206508=ORIENTED_EDGE ( 'NONE', *, *, #38577, .F. ) ;
#206545=ORIENTED_EDGE ( 'NONE', *, *, #91997, .T. ) ;
#206604=CARTESIAN_POINT ( 'NONE',  ( 20.85000000000000142, 87.75000000001246292, -173.0231074845243029 ) ) ;
#206630=AXIS2_PLACEMENT_3D ( 'NONE', #111412, #90546, #190972 ) ;
#206660=DIRECTION ( 'NONE',  ( 0.000000000000000000, 1.000000000000000000, 6.982962677686266711E-15 ) ) ;
#206676=EDGE_LOOP ( 'NONE', ( #187850, #90930, #27135, #234957, #232959 ) ) ;
#206685=DIRECTION ( 'NONE',  ( -1.000000000000000000, 2.952720810173289112E-16, 2.061873921506763405E-30 ) ) ;
#206689=PLANE ( 'NONE',  #98417 ) ;
#206707=DIRECTION ( 'NONE',  ( 0.000000000000000000, 6.982962677686266711E-15, -1.000000000000000000 ) ) ;
#206714=ORIENTED_EDGE ( 'NONE', *, *, #215351, .F. ) ;
#206719=CARTESIAN_POINT ( 'NONE',  ( -23.15000000000000213, 85.00000000001251976, -179.9170766071767389 ) ) ;
#206720=DIRECTION ( 'NONE',  ( 0.000000000000000000, 1.000000000000000000, 6.982962677686266711E-15 ) ) ;
#206768=DIRECTION ( 'NONE',  ( 0.000000000000000000, 0.000000000000000000, 1.000000000000000000 ) ) ;
#206784=DIRECTION ( 'NONE',  ( 0.000000000000000000, 1.000000000000000000, 6.853228547068871147E-15 ) ) ;
#206800=CIRCLE ( 'NONE', #177779, 0.09999999999999939493 ) ;
#206815=DIRECTION ( 'NONE',  ( 0.000000000000000000, 0.9908441862701420355, 0.1350103645453197554 ) ) ;
#206841=DIRECTION ( 'NONE',  ( -0.000000000000000000, 6.982962677686266711E-15, -1.000000000000000000 ) ) ;
#206857=DIRECTION ( 'NONE',  ( 0.000000000000000000, 0.000000000000000000, -1.000000000000000000 ) ) ;
#206861=CARTESIAN_POINT ( 'NONE',  ( -23.25000000000000000, 76.00000000001267608, -203.5231074845243597 ) ) ;
#206896=ORIENTED_EDGE ( 'NONE', *, *, #192386, .T. ) ;
#206922=EDGE_LOOP ( 'NONE', ( #151066, #2558, #101804, #18088 ) ) ;
#207022=EDGE_LOOP ( 'NONE', ( #248918, #6848, #144524, #163941 ) ) ;
#207026=VECTOR ( 'NONE', #233110, 1000.000000000000000 ) ;
#207028=ORIENTED_EDGE ( 'NONE', *, *, #24279, .T. ) ;
#207041=ORIENTED_EDGE ( 'NONE', *, *, #253248, .T. ) ;
#207045=AXIS2_PLACEMENT_3D ( 'NONE', #35782, #237812, #116582 ) ;
#207056=DIRECTION ( 'NONE',  ( 0.000000000000000000, 1.000000000000000000, 6.853228547068871147E-15 ) ) ;
#207066=CIRCLE ( 'NONE', #169695, 0.2000000000000057288 ) ;
#207100=CARTESIAN_POINT ( 'NONE',  ( -18.50000000000000000, 66.85000000001275566, -215.2731074845244166 ) ) ;
#207101=ORIENTED_EDGE ( 'NONE', *, *, #237452, .T. ) ;
#207112=FACE_OUTER_BOUND ( 'NONE', #208516, .T. ) ;
#207133=VERTEX_POINT ( 'NONE', #193105 ) ;
#207156=ORIENTED_EDGE ( 'NONE', *, *, #112829, .F. ) ;
#207168=DIRECTION ( 'NONE',  ( 1.000000000000000000, 0.000000000000000000, 0.000000000000000000 ) ) ;
#207223=LINE ( 'NONE', #50673, #39397 ) ;
#207242=FACE_OUTER_BOUND ( 'NONE', #125532, .T. ) ;
#207282=CARTESIAN_POINT ( 'NONE',  ( 20.95000000000000284, 64.40000000001248281, -176.9513107147999449 ) ) ;
#207294=AXIS2_PLACEMENT_3D ( 'NONE', #216803, #119011, #198529 ) ;
#207338=VERTEX_POINT ( 'NONE', #203368 ) ;
#207354=DIRECTION ( 'NONE',  ( 0.000000000000000000, -0.9915357197604982575, 0.1298341882519033486 ) ) ;
#207357=DIRECTION ( 'NONE',  ( 0.000000000000000000, 1.000000000000000000, 6.982962677686266711E-15 ) ) ;
#207358=CARTESIAN_POINT ( 'NONE',  ( 18.43579564894469414, 85.51932753530516607, -196.5501308406639680 ) ) ;
#207376=CARTESIAN_POINT ( 'NONE',  ( -18.59999999999999787, 76.00000000001244871, -170.0231074845243597 ) ) ;
#207408=CARTESIAN_POINT ( 'NONE',  ( -23.15000000000000213, 87.48912529308852015, -173.1231074845242688 ) ) ;
#207467=CARTESIAN_POINT ( 'NONE',  ( -18.50000000000000000, 76.00000000001244871, -170.0231074845243597 ) ) ;
#207470=CARTESIAN_POINT ( 'NONE',  ( -23.15000000000000213, 71.65000000001259650, -191.2731074845243882 ) ) ;
#207475=LINE ( 'NONE', #211315, #91053 ) ;
#207481=DIRECTION ( 'NONE',  ( 0.000000000000000000, -7.086529944415886769E-15, 1.000000000000000000 ) ) ;
#207484=DIRECTION ( 'NONE',  ( 2.840903330521631775E-16, 0.8700118002898354908, -0.4930308989875170078 ) ) ;
#207512=EDGE_CURVE ( 'NONE', #7857, #63242, #38767, .T. ) ;
#207528=LINE ( 'NONE', #4167, #248861 ) ;
#207557=AXIS2_PLACEMENT_3D ( 'NONE', #98056, #21158, #57664 ) ;
#207561=EDGE_CURVE ( 'NONE', #192523, #201210, #201076, .T. ) ;
#207573=ORIENTED_EDGE ( 'NONE', *, *, #158316, .F. ) ;
#207575=CARTESIAN_POINT ( 'NONE',  ( -18.59999999999999787, 77.68707439010432836, -216.3376804510660065 ) ) ;
#207578=ORIENTED_EDGE ( 'NONE', *, *, #142939, .T. ) ;
#207585=ORIENTED_EDGE ( 'NONE', *, *, #131238, .T. ) ;
#207596=CARTESIAN_POINT ( 'NONE',  ( 23.14999999999999503, 64.25000000001259082, -191.3731074845244393 ) ) ;
#207626=AXIS2_PLACEMENT_3D ( 'NONE', #93246, #37153, #115376 ) ;
#207637=AXIS2_PLACEMENT_3D ( 'NONE', #15230, #150869, #193859 ) ;
#207639=DIRECTION ( 'NONE',  ( 0.000000000000000000, 0.000000000000000000, 1.000000000000000000 ) ) ;
#207689=ADVANCED_FACE ( 'NONE', ( #25702 ), #64815, .T. ) ;
#207693=EDGE_LOOP ( 'NONE', ( #212085, #245385 ) ) ;
#207708=CARTESIAN_POINT ( 'NONE',  ( 20.94999999999999929, 85.00000000001261924, -193.6291383618718385 ) ) ;
#207712=CARTESIAN_POINT ( 'NONE',  ( 22.50000000000000000, 68.25000000001267608, -203.6231074845244109 ) ) ;
#207714=DIRECTION ( 'NONE',  ( 0.000000000000000000, 3.208737065390628822E-15, 1.000000000000000000 ) ) ;
#207747=VERTEX_POINT ( 'NONE', #29583 ) ;
#207748=AXIS2_PLACEMENT_3D ( 'NONE', #112480, #66912, #128179 ) ;
#207749=AXIS2_PLACEMENT_3D ( 'NONE', #92340, #171925, #113193 ) ;
#207776=DIRECTION ( 'NONE',  ( -1.000000000000000000, 0.000000000000000000, 0.000000000000000000 ) ) ;
#207778=EDGE_CURVE ( 'NONE', #24117, #193233, #222066, .T. ) ;
#207826=ORIENTED_EDGE ( 'NONE', *, *, #87017, .T. ) ;
#207832=CIRCLE ( 'NONE', #220284, 0.1999999999999987899 ) ;
#207840=ORIENTED_EDGE ( 'NONE', *, *, #18790, .F. ) ;
#207847=EDGE_CURVE ( 'NONE', #15440, #253585, #80410, .T. ) ;
#207882=CARTESIAN_POINT ( 'NONE',  ( -23.25000000000000000, 64.25000000001249134, -177.0379132551784096 ) ) ;
#207907=DIRECTION ( 'NONE',  ( 0.000000000000000000, -6.982962677686266711E-15, 1.000000000000000000 ) ) ;
#207927=EDGE_LOOP ( 'NONE', ( #43744, #199775, #208173, #142839 ) ) ;
#207943=AXIS2_PLACEMENT_3D ( 'NONE', #208346, #248738, #29718 ) ;
#207944=EDGE_LOOP ( 'NONE', ( #105278, #139810, #169651 ) ) ;
#207947=EDGE_CURVE ( 'NONE', #104211, #107411, #205520, .T. ) ;
#207948=PLANE ( 'NONE',  #184561 ) ;
#207953=VERTEX_POINT ( 'NONE', #193760 ) ;
#207962=VECTOR ( 'NONE', #224784, 1000.000000000000000 ) ;
#208015=DIRECTION ( 'NONE',  ( 1.000000000000000000, 0.000000000000000000, 0.000000000000000000 ) ) ;
#208042=ORIENTED_EDGE ( 'NONE', *, *, #18768, .T. ) ;
#208068=DIRECTION ( 'NONE',  ( 0.000000000000000000, -6.938893903907222067E-15, 1.000000000000000000 ) ) ;
#208084=AXIS2_PLACEMENT_3D ( 'NONE', #200776, #39160, #236048 ) ;
#208086=DIRECTION ( 'NONE',  ( 1.000000000000000000, -2.952720810173289112E-16, -2.061873921506763405E-30 ) ) ;
#208113=CARTESIAN_POINT ( 'NONE',  ( 21.05000000000000071, 67.12338541492553645, -195.1380270056797599 ) ) ;
#208126=AXIS2_PLACEMENT_3D ( 'NONE', #64679, #125926, #81643 ) ;
#208160=DIRECTION ( 'NONE',  ( 0.000000000000000000, 0.8700118002898356018, -0.4930308989875170078 ) ) ;
#208165=EDGE_CURVE ( 'NONE', #27052, #19071, #13232, .T. ) ;
#208173=ORIENTED_EDGE ( 'NONE', *, *, #195603, .F. ) ;
#208216=CIRCLE ( 'NONE', #237430, 0.09999999999999939493 ) ;
#208223=EDGE_CURVE ( 'NONE', #176, #148199, #9894, .T. ) ;
#208232=TOROIDAL_SURFACE ( 'NONE', #233192, 0.6000000000000009770, 0.1000000000000000056 ) ;
#208273=CARTESIAN_POINT ( 'NONE',  ( 21.00023020733438273, 69.60913075474496736, -203.5231074845244166 ) ) ;
#208282=FACE_OUTER_BOUND ( 'NONE', #60640, .T. ) ;
#208285=AXIS2_PLACEMENT_3D ( 'NONE', #39166, #24745, #59961 ) ;
#208313=ADVANCED_FACE ( 'NONE', ( #79581 ), #43227, .T. ) ;
#208318=VECTOR ( 'NONE', #212117, 1000.000000000000000 ) ;
#208334=DIRECTION ( 'NONE',  ( 0.000000000000000000, 0.000000000000000000, 1.000000000000000000 ) ) ;
#208346=CARTESIAN_POINT ( 'NONE',  ( 20.85000000000000142, 77.16412189325360771, -162.1082593989527254 ) ) ;
#208350=DIRECTION ( 'NONE',  ( -1.000000000000000000, -0.000000000000000000, 0.000000000000000000 ) ) ;
#208391=CARTESIAN_POINT ( 'NONE',  ( -21.13422380239133958, 76.00000000001273293, -210.0164339993299620 ) ) ;
#208420=ADVANCED_FACE ( 'NONE', ( #113148 ), #133987, .F. ) ;
#208440=EDGE_LOOP ( 'NONE', ( #229880, #137329, #94946, #55713 ) ) ;
#208444=DIRECTION ( 'NONE',  ( 1.000000000000000000, 0.000000000000000000, 0.000000000000000000 ) ) ;
#208449=EDGE_CURVE ( 'NONE', #45489, #48315, #68163, .T. ) ;
#208460=ORIENTED_EDGE ( 'NONE', *, *, #95597, .F. ) ;
#208506=DIRECTION ( 'NONE',  ( -1.000000000000000000, 0.000000000000000000, -0.000000000000000000 ) ) ;
#208516=EDGE_LOOP ( 'NONE', ( #135470, #213365, #26854, #245412 ) ) ;
#208524=DIRECTION ( 'NONE',  ( 1.000000000000000000, 0.000000000000000000, 0.000000000000000000 ) ) ;
#208571=DIRECTION ( 'NONE',  ( 0.000000000000000000, 0.000000000000000000, 1.000000000000000000 ) ) ;
#208628=ORIENTED_EDGE ( 'NONE', *, *, #73264, .F. ) ;
#208633=EDGE_LOOP ( 'NONE', ( #91257, #120948, #239302, #225490 ) ) ;
#208641=LINE ( 'NONE', #91250, #139150 ) ;
#208681=AXIS2_PLACEMENT_3D ( 'NONE', #229695, #113593, #247957 ) ;
#208688=FACE_OUTER_BOUND ( 'NONE', #121497, .T. ) ;
#208691=DIRECTION ( 'NONE',  ( 0.000000000000000000, -0.4999999999999608646, 0.8660254037844612451 ) ) ;
#208694=CARTESIAN_POINT ( 'NONE',  ( 20.94999999999999929, 70.60000000001251408, -179.9170766071768526 ) ) ;
#208697=EDGE_CURVE ( 'NONE', #41142, #133931, #76708, .T. ) ;
#208702=DIRECTION ( 'NONE',  ( -3.787827842127534447E-15, -0.7397360091702729346, -0.6728971962616859814 ) ) ;
#208715=EDGE_CURVE ( 'NONE', #239420, #240431, #239218, .T. ) ;
#208719=CARTESIAN_POINT ( 'NONE',  ( 23.24999999999999289, 64.25000000001276135, -215.2731074845244450 ) ) ;
#208750=EDGE_CURVE ( 'NONE', #246278, #4741, #243297, .T. ) ;
#208785=AXIS2_PLACEMENT_3D ( 'NONE', #111913, #213552, #153647 ) ;
#208788=ORIENTED_EDGE ( 'NONE', *, *, #30258, .T. ) ;
#208790=ORIENTED_EDGE ( 'NONE', *, *, #222456, .T. ) ;
#208805=EDGE_LOOP ( 'NONE', ( #236155, #196189, #210024, #130756 ) ) ;
#208809=DIRECTION ( 'NONE',  ( 0.000000000000000000, 6.982962677686266711E-15, -1.000000000000000000 ) ) ;
#208822=AXIS2_PLACEMENT_3D ( 'NONE', #123840, #186385, #5129 ) ;
#208823=ORIENTED_EDGE ( 'NONE', *, *, #221324, .T. ) ;
#208827=DIRECTION ( 'NONE',  ( 1.000000000000000000, 0.000000000000000000, 0.000000000000000000 ) ) ;
#208865=DIRECTION ( 'NONE',  ( -1.000000000000000000, -3.469446951953635015E-14, -2.422701857770461054E-28 ) ) ;
#208883=CARTESIAN_POINT ( 'NONE',  ( 21.14999999999999858, 76.00000000001276135, -215.1726782920691505 ) ) ;
#208953=CARTESIAN_POINT ( 'NONE',  ( 18.60000000000000142, 85.40000000001258229, -196.2258477248609836 ) ) ;
#208968=ORIENTED_EDGE ( 'NONE', *, *, #226538, .T. ) ;
#209006=CIRCLE ( 'NONE', #246422, 11.90000000000000746 ) ;
#209012=ORIENTED_EDGE ( 'NONE', *, *, #35193, .T. ) ;
#209036=CARTESIAN_POINT ( 'NONE',  ( 23.24999999999999289, 69.35000000001254250, -182.1731074845243938 ) ) ;
#209091=EDGE_CURVE ( 'NONE', #207953, #117519, #93655, .T. ) ;
#209109=DIRECTION ( 'NONE',  ( 0.000000000000000000, 0.000000000000000000, 1.000000000000000000 ) ) ;
#209116=AXIS2_PLACEMENT_3D ( 'NONE', #94265, #138500, #135952 ) ;
#209128=VECTOR ( 'NONE', #206225, 1000.000000000000000 ) ;
#209136=DIRECTION ( 'NONE',  ( 0.000000000000000000, 7.086529944415886769E-15, -1.000000000000000000 ) ) ;
#209150=DIRECTION ( 'NONE',  ( 1.000000000000000000, 0.000000000000000000, 0.000000000000000000 ) ) ;
#209196=EDGE_CURVE ( 'NONE', #181442, #133901, #72843, .T. ) ;
#209197=ORIENTED_EDGE ( 'NONE', *, *, #149542, .T. ) ;
#209233=ADVANCED_FACE ( 'NONE', ( #256362 ), #168539, .F. ) ;
#209236=CIRCLE ( 'NONE', #250918, 11.80000000000000426 ) ;
#209261=ORIENTED_EDGE ( 'NONE', *, *, #77999, .T. ) ;
#209265=ORIENTED_EDGE ( 'NONE', *, *, #43173, .F. ) ;
#209283=AXIS2_PLACEMENT_3D ( 'NONE', #13730, #172857, #252326 ) ;
#209291=DIRECTION ( 'NONE',  ( 1.000000000000000000, -0.000000000000000000, 0.000000000000000000 ) ) ;
#209292=CARTESIAN_POINT ( 'NONE',  ( 20.94999999999999574, 87.48912529308871910, -200.4231074845242802 ) ) ;
#209294=CARTESIAN_POINT ( 'NONE',  ( -18.50000000000000000, 85.42129027953541254, -163.1992253054984587 ) ) ;
#209296=CARTESIAN_POINT ( 'NONE',  ( -22.50000000000000000, 68.20922040163927136, -203.6231074845244109 ) ) ;
#209360=CIRCLE ( 'NONE', #180331, 11.75000000000001066 ) ;
#209366=CIRCLE ( 'NONE', #51122, 0.09999999999999939493 ) ;
#209387=EDGE_LOOP ( 'NONE', ( #107511, #165529, #244586, #198922 ) ) ;
#209388=ORIENTED_EDGE ( 'NONE', *, *, #142385, .T. ) ;
#209406=DIRECTION ( 'NONE',  ( 0.000000000000000000, 1.000000000000000000, 0.000000000000000000 ) ) ;
#209410=VERTEX_POINT ( 'NONE', #245855 ) ;
#209479=VERTEX_POINT ( 'NONE', #232418 ) ;
#209484=DIRECTION ( 'NONE',  ( 0.000000000000000000, 0.4930308989874980785, 0.8700118002898462599 ) ) ;
#209485=CARTESIAN_POINT ( 'NONE',  ( -23.15000000000000213, 73.50000000001259082, -190.2984855617622770 ) ) ;
#209487=ORIENTED_EDGE ( 'NONE', *, *, #38448, .T. ) ;
#209496=CARTESIAN_POINT ( 'NONE',  ( -20.94999999999999929, 76.00000000001247713, -174.0231074845243882 ) ) ;
#209520=AXIS2_PLACEMENT_3D ( 'NONE', #188736, #110482, #10110 ) ;
#209521=DIRECTION ( 'NONE',  ( 1.000000000000000000, 0.000000000000000000, 0.000000000000000000 ) ) ;
#209526=EDGE_LOOP ( 'NONE', ( #113475, #255041, #75772, #254706 ) ) ;
#209528=AXIS2_PLACEMENT_3D ( 'NONE', #106206, #104903, #164919 ) ;
#209529=ORIENTED_EDGE ( 'NONE', *, *, #173040, .T. ) ;
#209538=VECTOR ( 'NONE', #164462, 1000.000000000000000 ) ;
#209549=VECTOR ( 'NONE', #51732, 1000.000000000000000 ) ;
#209552=CIRCLE ( 'NONE', #184602, 0.2000000000000057288 ) ;
#209557=DIRECTION ( 'NONE',  ( 0.000000000000000000, -7.109473446599835262E-15, 1.000000000000000000 ) ) ;
#209576=ADVANCED_FACE ( 'NONE', ( #133297 ), #158041, .T. ) ;
#209584=EDGE_CURVE ( 'NONE', #58661, #183838, #257041, .T. ) ;
#209610=CARTESIAN_POINT ( 'NONE',  ( -21.00023020733502932, 76.00000000001273293, -209.9139767297926937 ) ) ;
#209611=CYLINDRICAL_SURFACE ( 'NONE', #195668, 0.09999999999998898659 ) ;
#209613=EDGE_CURVE ( 'NONE', #242161, #35701, #199713, .T. ) ;
#209626=FACE_OUTER_BOUND ( 'NONE', #12083, .T. ) ;
#209662=CARTESIAN_POINT ( 'NONE',  ( 20.04142135623730070, 64.25000000001253397, -182.1731074845244507 ) ) ;
#209685=ORIENTED_EDGE ( 'NONE', *, *, #63070, .T. ) ;
#209753=EDGE_CURVE ( 'NONE', #13712, #42440, #180765, .T. ) ;
#209758=CARTESIAN_POINT ( 'NONE',  ( -23.15000000000000213, 71.65000000001259650, -191.1731074845243654 ) ) ;
#209801=DIRECTION ( 'NONE',  ( 0.000000000000000000, 0.1350103645451807555, 0.9908441862701609093 ) ) ;
#209813=CARTESIAN_POINT ( 'NONE',  ( 21.07928932188134397, 75.90110485435833709, -209.8516241409176928 ) ) ;
#209822=ORIENTED_EDGE ( 'NONE', *, *, #78839, .T. ) ;
#209851=CARTESIAN_POINT ( 'NONE',  ( 20.94999999999999929, 70.15000000001266756, -193.3906102602464330 ) ) ;
#209885=CARTESIAN_POINT ( 'NONE',  ( 20.94999999999999929, 76.00000000001244871, -170.0231074845243597 ) ) ;
#209898=DIRECTION ( 'NONE',  ( -0.000000000000000000, -6.982962677686266711E-15, 1.000000000000000000 ) ) ;
#209912=CARTESIAN_POINT ( 'NONE',  ( -21.05000000000000071, 69.45934304831143891, -203.4231074845244223 ) ) ;
#209931=EDGE_CURVE ( 'NONE', #30344, #228338, #89169, .T. ) ;
#209940=CARTESIAN_POINT ( 'NONE',  ( -21.14999999999999858, 76.10000000001276987, -215.1726782920691505 ) ) ;
#209968=CARTESIAN_POINT ( 'NONE',  ( -20.85000000000000142, 77.83585931145600512, -158.5186683157258187 ) ) ;
#209980=EDGE_LOOP ( 'NONE', ( #148303, #137209, #110616, #12710 ) ) ;
#209984=CARTESIAN_POINT ( 'NONE',  ( 23.15000000000000213, 85.00000000001251976, -179.4170766071767389 ) ) ;
#210001=AXIS2_PLACEMENT_3D ( 'NONE', #1475, #121467, #200970 ) ;
#210024=ORIENTED_EDGE ( 'NONE', *, *, #230952, .F. ) ;
#210030=AXIS2_PLACEMENT_3D ( 'NONE', #205124, #107326, #147751 ) ;
#210063=CARTESIAN_POINT ( 'NONE',  ( -18.50000000000000000, 102.4393534156134962, -185.3815988770167280 ) ) ;
#210081=AXIS2_PLACEMENT_3D ( 'NONE', #179501, #238154, #256382 ) ;
#210084=DIRECTION ( 'NONE',  ( 0.000000000000000000, 0.000000000000000000, -1.000000000000000000 ) ) ;
#210102=ORIENTED_EDGE ( 'NONE', *, *, #46101, .T. ) ;
#210147=VERTEX_POINT ( 'NONE', #78134 ) ;
#210148=CYLINDRICAL_SURFACE ( 'NONE', #103711, 0.09999999999999939493 ) ;
#210170=ORIENTED_EDGE ( 'NONE', *, *, #191610, .T. ) ;
#210255=FACE_OUTER_BOUND ( 'NONE', #219298, .T. ) ;
#210276=VERTEX_POINT ( 'NONE', #244923 ) ;
#210305=ORIENTED_EDGE ( 'NONE', *, *, #200378, .F. ) ;
#210320=ADVANCED_FACE ( 'NONE', ( #191406 ), #234338, .T. ) ;
#210344=ORIENTED_EDGE ( 'NONE', *, *, #1645, .F. ) ;
#210349=CARTESIAN_POINT ( 'NONE',  ( 20.93975676684922504, 65.68895814178293335, -164.5026557862138645 ) ) ;
#210350=PLANE ( 'NONE',  #98744 ) ;
#210361=DIRECTION ( 'NONE',  ( 0.000000000000000000, -1.000000000000000000, -6.982962677686266711E-15 ) ) ;
#210391=EDGE_CURVE ( 'NONE', #120125, #64517, #239494, .T. ) ;
#210397=CARTESIAN_POINT ( 'NONE',  ( 20.95512820512820440, 65.37615131630072085, -191.3731074845244393 ) ) ;
#210418=ORIENTED_EDGE ( 'NONE', *, *, #57913, .F. ) ;
#210441=AXIS2_PLACEMENT_3D ( 'NONE', #78949, #99795, #175540 ) ;
#210456=CIRCLE ( 'NONE', #73108, 0.09999999999998898659 ) ;
#210483=VERTEX_POINT ( 'NONE', #4699 ) ;
#210513=EDGE_LOOP ( 'NONE', ( #5227, #16526, #146520, #62869, #35169, #5168, #86863, #54602, #51964, #40238 ) ) ;
#210550=AXIS2_PLACEMENT_3D ( 'NONE', #214651, #174305, #115554 ) ;
#210554=ORIENTED_EDGE ( 'NONE', *, *, #116198, .F. ) ;
#210564=CYLINDRICAL_SURFACE ( 'NONE', #29147, 11.80000000000000426 ) ;
#210581=DIRECTION ( 'NONE',  ( 0.000000000000000000, 1.000000000000000000, 0.000000000000000000 ) ) ;
#210585=EDGE_CURVE ( 'NONE', #65541, #183861, #23171, .T. ) ;
#210598=EDGE_CURVE ( 'NONE', #220769, #239144, #27031, .T. ) ;
#210610=CARTESIAN_POINT ( 'NONE',  ( 18.59999999999999787, 77.83534155023700407, -191.8679561919613832 ) ) ;
#210620=AXIS2_PLACEMENT_3D ( 'NONE', #156719, #80979, #1449 ) ;
#210623=VECTOR ( 'NONE', #142915, 1000.000000000000000 ) ;
#210632=ORIENTED_EDGE ( 'NONE', *, *, #66275, .T. ) ;
#210729=VERTEX_POINT ( 'NONE', #119238 ) ;
#210748=DIRECTION ( 'NONE',  ( 0.000000000000000000, 0.000000000000000000, 1.000000000000000000 ) ) ;
#210753=AXIS2_PLACEMENT_3D ( 'NONE', #213099, #192274, #211833 ) ;
#210771=EDGE_CURVE ( 'NONE', #91470, #203708, #157085, .T. ) ;
#210782=AXIS2_PLACEMENT_3D ( 'NONE', #166674, #231763, #17821 ) ;
#210801=DIRECTION ( 'NONE',  ( 0.000000000000000000, 0.8700118002898356018, -0.4930308989875170078 ) ) ;
#210802=AXIS2_PLACEMENT_3D ( 'NONE', #203930, #49997, #169995 ) ;
#210804=AXIS2_PLACEMENT_3D ( 'NONE', #251727, #250435, #71823 ) ;
#210815=DIRECTION ( 'NONE',  ( 0.000000000000000000, 0.1350103645451974088, -0.9908441862701587999 ) ) ;
#210839=EDGE_CURVE ( 'NONE', #218130, #227674, #5667, .T. ) ;
#210844=CARTESIAN_POINT ( 'NONE',  ( 18.59999999999998366, 68.97833521811233481, -166.1895420826271277 ) ) ;
#210890=DIRECTION ( 'NONE',  ( 0.000000000000000000, 0.000000000000000000, -1.000000000000000000 ) ) ;
#210899=ORIENTED_EDGE ( 'NONE', *, *, #207847, .T. ) ;
#210903=ORIENTED_EDGE ( 'NONE', *, *, #208750, .T. ) ;
#210906=CARTESIAN_POINT ( 'NONE',  ( 23.24999999999999645, 72.10000000001244302, -170.0231074845243882 ) ) ;
#210909=CARTESIAN_POINT ( 'NONE',  ( -18.59999999999999787, 85.50000000001259082, -191.3731074845242972 ) ) ;
#210954=VERTEX_POINT ( 'NONE', #209036 ) ;
#210963=DIRECTION ( 'NONE',  ( 0.000000000000000000, 6.982962677686266711E-15, -1.000000000000000000 ) ) ;
#210974=DIRECTION ( 'NONE',  ( -1.000000000000000000, 0.000000000000000000, -0.000000000000000000 ) ) ;
#210990=DIRECTION ( 'NONE',  ( -1.000000000000000000, 0.000000000000000000, -0.000000000000000000 ) ) ;
#211004=CARTESIAN_POINT ( 'NONE',  ( 23.15000000000000213, 85.00000000001261924, -193.6291383618718385 ) ) ;
#211015=CYLINDRICAL_SURFACE ( 'NONE', #186247, 0.09999999999999939493 ) ;
#211019=EDGE_CURVE ( 'NONE', #55818, #177471, #243839, .T. ) ;
#211048=ORIENTED_EDGE ( 'NONE', *, *, #111400, .F. ) ;
#211067=VERTEX_POINT ( 'NONE', #24669 ) ;
#211070=LINE ( 'NONE', #15451, #217160 ) ;
#211075=DIRECTION ( 'NONE',  ( -1.000000000000000000, 0.000000000000000000, -0.000000000000000000 ) ) ;
#211154=DIRECTION ( 'NONE',  ( -1.000000000000000000, 0.000000000000000000, 0.000000000000000000 ) ) ;
#211157=DIRECTION ( 'NONE',  ( -1.000000000000000000, -0.000000000000000000, -0.000000000000000000 ) ) ;
#211161=DIRECTION ( 'NONE',  ( 0.000000000000000000, 0.000000000000000000, 1.000000000000000000 ) ) ;
#211182=ORIENTED_EDGE ( 'NONE', *, *, #252491, .T. ) ;
#211213=ORIENTED_EDGE ( 'NONE', *, *, #153951, .T. ) ;
#211235=EDGE_CURVE ( 'NONE', #152832, #42819, #169056, .T. ) ;
#211257=ADVANCED_FACE ( 'NONE', ( #130143 ), #244019, .T. ) ;
#211263=ORIENTED_EDGE ( 'NONE', *, *, #150912, .F. ) ;
#211304=CARTESIAN_POINT ( 'NONE',  ( -21.14999999999999858, 64.35000000001268461, -203.4231074845244507 ) ) ;
#211312=AXIS2_PLACEMENT_3D ( 'NONE', #46728, #126267, #227949 ) ;
#211315=CARTESIAN_POINT ( 'NONE',  ( 21.05000000000000071, 76.00000000001260503, -191.3731074845243540 ) ) ;
#211394=ORIENTED_EDGE ( 'NONE', *, *, #54389, .T. ) ;
#211412=CARTESIAN_POINT ( 'NONE',  ( 20.12500000000000000, 66.25000000001257661, -182.3731074845244393 ) ) ;
#211420=ORIENTED_EDGE ( 'NONE', *, *, #128190, .F. ) ;
#211427=ORIENTED_EDGE ( 'NONE', *, *, #3190, .T. ) ;
#211444=CARTESIAN_POINT ( 'NONE',  ( 23.14999999999999858, 87.75000000001276135, -215.2731074845242745 ) ) ;
#211506=CIRCLE ( 'NONE', #32476, 12.87499999999999822 ) ;
#211539=ORIENTED_EDGE ( 'NONE', *, *, #155095, .F. ) ;
#211559=EDGE_CURVE ( 'NONE', #10849, #217568, #227274, .T. ) ;
#211560=CARTESIAN_POINT ( 'NONE',  ( -20.54999999999999716, 85.00000000001251976, -179.9170766071767389 ) ) ;
#211610=CARTESIAN_POINT ( 'NONE',  ( -18.59999999999999787, 77.16412189325360771, -162.1082593989527254 ) ) ;
#211622=CIRCLE ( 'NONE', #45015, 0.09999999999999939493 ) ;
#211641=DIRECTION ( 'NONE',  ( -0.000000000000000000, 0.1298341882520054891, 0.9915357197604850459 ) ) ;
#211653=EDGE_CURVE ( 'NONE', #205739, #3432, #144248, .T. ) ;
#211655=CYLINDRICAL_SURFACE ( 'NONE', #7486, 0.09999999999998898659 ) ;
#211661=ORIENTED_EDGE ( 'NONE', *, *, #180296, .F. ) ;
#211719=TOROIDAL_SURFACE ( 'NONE', #157572, 7.791421356237335338, 0.1000000000000000056 ) ;
#211735=LINE ( 'NONE', #134726, #187739 ) ;
#211761=CIRCLE ( 'NONE', #41094, 12.77499999999999503 ) ;
#211789=CARTESIAN_POINT ( 'NONE',  ( -21.37071067811865532, 67.92928932189387581, -182.2731074845244166 ) ) ;
#211818=EDGE_CURVE ( 'NONE', #193318, #239043, #157134, .T. ) ;
#211826=LINE ( 'NONE', #256016, #39256 ) ;
#211833=DIRECTION ( 'NONE',  ( 0.000000000000000000, -7.056502275159890043E-15, 1.000000000000000000 ) ) ;
#211849=CIRCLE ( 'NONE', #170373, 0.09999999999998898659 ) ;
#211878=CIRCLE ( 'NONE', #245196, 0.09999999999998898659 ) ;
#211892=EDGE_LOOP ( 'NONE', ( #88390, #194167, #19979, #165230, #160548, #122652 ) ) ;
#211915=FACE_OUTER_BOUND ( 'NONE', #125300, .T. ) ;
#211975=EDGE_CURVE ( 'NONE', #217568, #611, #116743, .T. ) ;
#211979=DIRECTION ( 'NONE',  ( 1.000000000000000000, 0.000000000000000000, 0.000000000000000000 ) ) ;
#211984=ADVANCED_FACE ( 'NONE', ( #143513 ), #180096, .T. ) ;
#211999=CARTESIAN_POINT ( 'NONE',  ( 23.25000000000000000, 85.00000000001251976, -179.9170766071767389 ) ) ;
#212028=AXIS2_PLACEMENT_3D ( 'NONE', #229304, #212316, #113197 ) ;
#212031=EDGE_LOOP ( 'NONE', ( #215633, #196508, #212951, #8764 ) ) ;
#212040=CARTESIAN_POINT ( 'NONE',  ( -18.59999999999999787, 64.25000000001264766, -196.5083017138704236 ) ) ;
#212048=DIRECTION ( 'NONE',  ( 0.000000000000000000, 0.000000000000000000, 1.000000000000000000 ) ) ;
#212065=EDGE_CURVE ( 'NONE', #87244, #84905, #141, .T. ) ;
#212070=ORIENTED_EDGE ( 'NONE', *, *, #127798, .F. ) ;
#212074=EDGE_CURVE ( 'NONE', #81149, #30084, #199666, .T. ) ;
#212076=ORIENTED_EDGE ( 'NONE', *, *, #116924, .T. ) ;
#212085=ORIENTED_EDGE ( 'NONE', *, *, #99075, .T. ) ;
#212117=DIRECTION ( 'NONE',  ( -1.000000000000000000, -0.000000000000000000, -0.000000000000000000 ) ) ;
#212122=ADVANCED_FACE ( 'NONE', ( #65263 ), #125247, .F. ) ;
#212147=CARTESIAN_POINT ( 'NONE',  ( -18.50000000000000000, 64.25000000001277556, -215.2731074845244450 ) ) ;
#212163=CARTESIAN_POINT ( 'NONE',  ( 20.94999999999999929, 70.60000000001254250, -182.4283735034374843 ) ) ;
#212164=AXIS2_PLACEMENT_3D ( 'NONE', #205903, #162956, #203348 ) ;
#212170=EDGE_CURVE ( 'NONE', #79652, #167877, #126529, .T. ) ;
#212190=EDGE_LOOP ( 'NONE', ( #56543, #238652, #96866, #226907 ) ) ;
#212212=AXIS2_PLACEMENT_3D ( 'NONE', #141730, #197854, #136587 ) ;
#212213=FACE_OUTER_BOUND ( 'NONE', #25191, .T. ) ;
#212284=EDGE_CURVE ( 'NONE', #189559, #141625, #206800, .T. ) ;
#212287=CARTESIAN_POINT ( 'NONE',  ( -20.85000000000000142, 68.97833521811233481, -166.1895420826271277 ) ) ;
#212289=DIRECTION ( 'NONE',  ( 0.000000000000000000, 0.000000000000000000, 1.000000000000000000 ) ) ;
#212299=VECTOR ( 'NONE', #129616, 1000.000000000000000 ) ;
#212316=DIRECTION ( 'NONE',  ( 0.000000000000000000, -6.240597636138643358E-14, -1.000000000000000000 ) ) ;
#212319=VECTOR ( 'NONE', #68199, 1000.000000000000000 ) ;
#212341=CARTESIAN_POINT ( 'NONE',  ( -18.59999999999999787, 66.65000000001259650, -191.3731074845244393 ) ) ;
#212357=DIRECTION ( 'NONE',  ( -1.000000000000000000, -0.000000000000000000, -0.000000000000000000 ) ) ;
#212367=CARTESIAN_POINT ( 'NONE',  ( -21.05000000000000071, 76.00000000001267608, -203.5231074845243597 ) ) ;
#212369=DIRECTION ( 'NONE',  ( 1.000000000000000000, 0.000000000000000000, 0.000000000000000000 ) ) ;
#212427=EDGE_CURVE ( 'NONE', #238502, #137554, #28122, .T. ) ;
#212430=EDGE_CURVE ( 'NONE', #252282, #52715, #120983, .T. ) ;
#212456=DIRECTION ( 'NONE',  ( 1.000000000000000000, -2.952720810173289112E-16, -2.061873921506763405E-30 ) ) ;
#212486=CARTESIAN_POINT ( 'NONE',  ( 19.58285714285715073, 65.61500148966121060, -195.8934228171345069 ) ) ;
#212510=VECTOR ( 'NONE', #178614, 1000.000000000000000 ) ;
#212511=CARTESIAN_POINT ( 'NONE',  ( -18.59999999999999787, 74.16465844978819177, -191.8679561919614116 ) ) ;
#212512=ORIENTED_EDGE ( 'NONE', *, *, #183782, .T. ) ;
#212557=DIRECTION ( 'NONE',  ( -1.836970198721029934E-16, -1.000000000000000000, -6.982962677686266711E-15 ) ) ;
#212575=CARTESIAN_POINT ( 'NONE',  ( -21.05000000000000071, 87.48912529308852015, -173.1231074845242688 ) ) ;
#212594=LINE ( 'NONE', #135589, #50737 ) ;
#212615=EDGE_CURVE ( 'NONE', #192558, #257053, #90447, .T. ) ;
#212625=ORIENTED_EDGE ( 'NONE', *, *, #183040, .T. ) ;
#212670=CARTESIAN_POINT ( 'NONE',  ( -23.15000000000000213, 76.00000000001267608, -203.5231074845243597 ) ) ;
#212674=CARTESIAN_POINT ( 'NONE',  ( -20.94999999999999929, 64.25000000001263345, -196.5083017138704236 ) ) ;
#212693=DIRECTION ( 'NONE',  ( 0.000000000000000000, 0.000000000000000000, 1.000000000000000000 ) ) ;
#212735=CARTESIAN_POINT ( 'NONE',  ( -23.15000000000000213, 76.00000000001267608, -203.5231074845243597 ) ) ;
#212789=EDGE_LOOP ( 'NONE', ( #176935, #193125, #90, #2113 ) ) ;
#212797=VERTEX_POINT ( 'NONE', #124506 ) ;
#212802=EDGE_CURVE ( 'NONE', #178394, #257053, #82759, .T. ) ;
#212804=DIRECTION ( 'NONE',  ( 0.000000000000000000, -6.982962677686266711E-15, 1.000000000000000000 ) ) ;
#212910=CARTESIAN_POINT ( 'NONE',  ( 20.94403535211772294, 65.69367753730709580, -164.5189238066348594 ) ) ;
#212922=CARTESIAN_POINT ( 'NONE',  ( 20.95132126680579887, 65.51005012986584575, -195.9527829460899113 ) ) ;
#212923=CARTESIAN_POINT ( 'NONE',  ( 18.57071067811864040, 65.82071067813119214, -182.1731074845244223 ) ) ;
#212936=ADVANCED_FACE ( 'NONE', ( #198894 ), #5909, .T. ) ;
#212951=ORIENTED_EDGE ( 'NONE', *, *, #125358, .T. ) ;
#212962=ORIENTED_EDGE ( 'NONE', *, *, #242280, .T. ) ;
#212967=CARTESIAN_POINT ( 'NONE',  ( -23.15000000000000213, 76.00000000001244871, -170.0231074845243597 ) ) ;
#212990=AXIS2_PLACEMENT_3D ( 'NONE', #199998, #40947, #99572 ) ;
#213012=CARTESIAN_POINT ( 'NONE',  ( 22.39999999999999503, 68.20922040163929978, -203.6231074845244109 ) ) ;
#213030=EDGE_CURVE ( 'NONE', #156620, #9837, #203054, .T. ) ;
#213052=CARTESIAN_POINT ( 'NONE',  ( -20.94999999999999929, 77.83534155023701828, -191.9679561919613491 ) ) ;
#213099=CARTESIAN_POINT ( 'NONE',  ( 20.94999999999999574, 76.00000000001267608, -203.5231074845243597 ) ) ;
#213106=VECTOR ( 'NONE', #244397, 1000.000000000000000 ) ;
#213162=AXIS2_PLACEMENT_3D ( 'NONE', #147452, #28845, #48348 ) ;
#213201=EDGE_LOOP ( 'NONE', ( #117653, #223034, #20309, #92671, #178825, #251848, #24966, #246338 ) ) ;
#213222=VECTOR ( 'NONE', #19746, 1000.000000000000000 ) ;
#213229=ADVANCED_FACE ( 'NONE', ( #143745 ), #161588, .F. ) ;
#213230=VECTOR ( 'NONE', #5232, 1000.000000000000000 ) ;
#213236=CARTESIAN_POINT ( 'NONE',  ( -20.64999999999999858, 74.00000000001259082, -190.2984855617622770 ) ) ;
#213260=DIRECTION ( 'NONE',  ( 0.000000000000000000, -0.9876197685951263461, 0.1568667991644794590 ) ) ;
#213320=VERTEX_POINT ( 'NONE', #49787 ) ;
#213348=CYLINDRICAL_SURFACE ( 'NONE', #151787, 0.09999999999999939493 ) ;
#213365=ORIENTED_EDGE ( 'NONE', *, *, #79299, .T. ) ;
#213371=ORIENTED_EDGE ( 'NONE', *, *, #210391, .T. ) ;
#213375=EDGE_CURVE ( 'NONE', #241009, #170452, #249064, .T. ) ;
#213431=CARTESIAN_POINT ( 'NONE',  ( 22.50000000000000000, 76.00000000001267608, -203.5231074845243597 ) ) ;
#213468=CARTESIAN_POINT ( 'NONE',  ( 23.24999999999999645, 70.40000000001253966, -182.4283735034374843 ) ) ;
#213478=EDGE_LOOP ( 'NONE', ( #92467, #8882, #178530 ) ) ;
#213487=ORIENTED_EDGE ( 'NONE', *, *, #35193, .F. ) ;
#213491=VERTEX_POINT ( 'NONE', #160480 ) ;
#213497=B_SPLINE_CURVE_WITH_KNOTS ( 'NONE', 3,
 ( #1247, #118673, #121263, #42971, #23436, #256817, #200756, #198183, #101612, #178661, #182496, #80781, #20862, #2538, #82055, #99057 ),
 .UNSPECIFIED., .F., .F.,
 ( 4, 3, 3, 3, 3, 4 ),
 ( 0.000000000000000000, 2.372700795694925591E-05, 5.739057815867077772E-05, 9.073899019181627494E-05, 0.0001243544287365772689, 0.0001585386695601308422 ),
 .UNSPECIFIED. ) ;
#213506=ORIENTED_EDGE ( 'NONE', *, *, #687, .F. ) ;
#213520=SHAPE_REPRESENTATION ( 'Injection Molded Chain Links 11', ( #2425 ), #239393 ) ;
#213522=DIRECTION ( 'NONE',  ( 0.000000000000000000, 0.9908441862701420355, 0.1350103645453197554 ) ) ;
#213552=DIRECTION ( 'NONE',  ( 1.000000000000000000, 0.000000000000000000, 0.000000000000000000 ) ) ;
#213553=EDGE_CURVE ( 'NONE', #184335, #221704, #157932, .T. ) ;
#213565=CIRCLE ( 'NONE', #205363, 11.80000000000000426 ) ;
#213574=DIRECTION ( 'NONE',  ( 1.000000000000000000, 0.000000000000000000, 0.000000000000000000 ) ) ;
#213593=EDGE_CURVE ( 'NONE', #195224, #8263, #220436, .T. ) ;
#213657=CARTESIAN_POINT ( 'NONE',  ( -23.25000000000000000, 74.08971962618075224, -182.6544753397233194 ) ) ;
#213747=ORIENTED_EDGE ( 'NONE', *, *, #220025, .F. ) ;
#213755=CARTESIAN_POINT ( 'NONE',  ( -23.25000000000000000, 76.00000000001246292, -172.1231074845243540 ) ) ;
#213765=ORIENTED_EDGE ( 'NONE', *, *, #38643, .F. ) ;
#213768=CARTESIAN_POINT ( 'NONE',  ( 20.94999999999999574, 74.83729825007462466, -195.6231074845243540 ) ) ;
#213786=CARTESIAN_POINT ( 'NONE',  ( 18.49999999999999289, 65.70729864261056719, -164.5657455973725121 ) ) ;
#213796=AXIS2_PLACEMENT_3D ( 'NONE', #89265, #206660, #167559 ) ;
#213808=VERTEX_POINT ( 'NONE', #236766 ) ;
#213814=FACE_OUTER_BOUND ( 'NONE', #100147, .T. ) ;
#213842=EDGE_CURVE ( 'NONE', #197295, #102120, #56823, .T. ) ;
#213903=EDGE_LOOP ( 'NONE', ( #230896, #32390 ) ) ;
#213909=AXIS2_PLACEMENT_3D ( 'NONE', #136542, #139089, #201664 ) ;
#213962=CARTESIAN_POINT ( 'NONE',  ( -21.05000000000000071, 76.00000000001267608, -203.5231074845243597 ) ) ;
#213978=ORIENTED_EDGE ( 'NONE', *, *, #3264, .T. ) ;
#213983=DIRECTION ( 'NONE',  ( -0.000000000000000000, -6.982962677686266711E-15, 1.000000000000000000 ) ) ;
#213989=DIRECTION ( 'NONE',  ( 1.000000000000000000, 0.000000000000000000, 0.000000000000000000 ) ) ;
#213992=ORIENTED_EDGE ( 'NONE', *, *, #160385, .F. ) ;
#213999=CARTESIAN_POINT ( 'NONE',  ( 22.48660254037844197, 64.35000000001267040, -203.5731074845244564 ) ) ;
#214003=AXIS2_PLACEMENT_3D ( 'NONE', #143536, #21060, #240086 ) ;
#214010=ORIENTED_EDGE ( 'NONE', *, *, #153677, .T. ) ;
#214011=DIRECTION ( 'NONE',  ( 0.7070776581709139474, 0.7071359030027652981, 2.946958787807621248E-14 ) ) ;
#214018=DIRECTION ( 'NONE',  ( -0.000000000000000000, 6.982962677686266711E-15, -1.000000000000000000 ) ) ;
#214019=EDGE_CURVE ( 'NONE', #9515, #139907, #226160, .T. ) ;
#214036=EDGE_LOOP ( 'NONE', ( #55892, #86314, #126618, #180849 ) ) ;
#214045=ORIENTED_EDGE ( 'NONE', *, *, #96917, .F. ) ;
#214054=EDGE_CURVE ( 'NONE', #139621, #38939, #215518, .T. ) ;
#214058=ORIENTED_EDGE ( 'NONE', *, *, #115647, .F. ) ;
#214071=AXIS2_PLACEMENT_3D ( 'NONE', #212735, #232308, #168506 ) ;
#214072=ORIENTED_EDGE ( 'NONE', *, *, #191902, .F. ) ;
#214094=AXIS2_PLACEMENT_3D ( 'NONE', #233544, #95298, #193130 ) ;
#214102=VERTEX_POINT ( 'NONE', #73582 ) ;
#214124=SPHERICAL_SURFACE ( 'NONE', #4949, 0.1000000000000000056 ) ;
#214131=LINE ( 'NONE', #253239, #77376 ) ;
#214143=DIRECTION ( 'NONE',  ( 1.000000000000000000, 0.000000000000000000, 0.000000000000000000 ) ) ;
#214145=EDGE_CURVE ( 'NONE', #64951, #10686, #98204, .T. ) ;
#214149=EDGE_CURVE ( 'NONE', #104276, #99797, #203040, .T. ) ;
#214155=AXIS2_PLACEMENT_3D ( 'NONE', #31527, #73217, #173628 ) ;
#214159=ORIENTED_EDGE ( 'NONE', *, *, #102892, .T. ) ;
#214170=DIRECTION ( 'NONE',  ( 0.000000000000000000, -0.9654727137038715545, -0.2605042016806676242 ) ) ;
#214202=CARTESIAN_POINT ( 'NONE',  ( 23.24999999999999645, 71.00000000001260503, -191.1178414656112921 ) ) ;
#214226=ORIENTED_EDGE ( 'NONE', *, *, #116918, .F. ) ;
#214239=EDGE_CURVE ( 'NONE', #165694, #183114, #175261, .T. ) ;
#214253=CARTESIAN_POINT ( 'NONE',  ( 18.49505832270841310, 85.43802806279552442, -196.3246343096304827 ) ) ;
#214254=EDGE_CURVE ( 'NONE', #41396, #254122, #176521, .T. ) ;
#214274=ORIENTED_EDGE ( 'NONE', *, *, #214019, .F. ) ;
#214289=CARTESIAN_POINT ( 'NONE',  ( -23.15000000000000213, 76.00000000001247713, -174.0231074845243882 ) ) ;
#214330=AXIS2_PLACEMENT_3D ( 'NONE', #10310, #166835, #92383 ) ;
#214335=ORIENTED_EDGE ( 'NONE', *, *, #81196, .T. ) ;
#214361=ORIENTED_EDGE ( 'NONE', *, *, #73646, .F. ) ;
#214399=DIRECTION ( 'NONE',  ( 0.000000000000000000, -7.026728003956695223E-15, 1.000000000000000000 ) ) ;
#214404=EDGE_LOOP ( 'NONE', ( #56800, #162110, #181288, #80903 ) ) ;
#214418=DIRECTION ( 'NONE',  ( -1.000000000000000000, 0.000000000000000000, -0.000000000000000000 ) ) ;
#214420=CARTESIAN_POINT ( 'NONE',  ( -18.59999999999999787, 64.35000000001264198, -196.6083017138704179 ) ) ;
#214425=AXIS2_PLACEMENT_3D ( 'NONE', #221633, #122575, #202099 ) ;
#214431=DIRECTION ( 'NONE',  ( -4.391705002472927119E-16, -1.000000000000000000, -7.026728003956683390E-15 ) ) ;
#214448=DIRECTION ( 'NONE',  ( 1.000000000000000000, -1.836970198721029934E-16, -1.601412966608202925E-30 ) ) ;
#214507=DIRECTION ( 'NONE',  ( 0.7071067811865475727, 0.7071067811865475727, 4.937700262164531476E-15 ) ) ;
#214512=DIRECTION ( 'NONE',  ( 0.000000000000000000, -7.056502275159890832E-15, 1.000000000000000000 ) ) ;
#214592=CARTESIAN_POINT ( 'NONE',  ( 20.94999999999999929, 67.22371710472015138, -194.9644784893834810 ) ) ;
#214651=CARTESIAN_POINT ( 'NONE',  ( 21.05000000000000071, 76.00000000001244871, -170.0231074845243597 ) ) ;
#214661=AXIS2_PLACEMENT_3D ( 'NONE', #43097, #160501, #20994 ) ;
#214672=ORIENTED_EDGE ( 'NONE', *, *, #102341, .T. ) ;
#214692=DIRECTION ( 'NONE',  ( 0.000000000000000000, -0.1568667991644355497, 0.9876197685951332295 ) ) ;
#214698=DIRECTION ( 'NONE',  ( 0.000000000000000000, 0.000000000000000000, 1.000000000000000000 ) ) ;
#214706=AXIS2_PLACEMENT_3D ( 'NONE', #42550, #162529, #221180 ) ;
#214717=DIRECTION ( 'NONE',  ( -1.000000000000000000, 0.000000000000000000, -0.000000000000000000 ) ) ;
#214718=DIRECTION ( 'NONE',  ( 0.000000000000000000, 1.000000000000000000, 6.352154140967427193E-15 ) ) ;
#214745=ADVANCED_FACE ( 'NONE', ( #58790 ), #202180, .F. ) ;
#214769=CARTESIAN_POINT ( 'NONE',  ( 18.59999999999999432, 77.16270174995064224, -195.4231074845243370 ) ) ;
#214786=ORIENTED_EDGE ( 'NONE', *, *, #91404, .T. ) ;
#214795=DIRECTION ( 'NONE',  ( 1.000000000000000000, 0.000000000000000000, 0.000000000000000000 ) ) ;
#214797=ORIENTED_EDGE ( 'NONE', *, *, #223124, .T. ) ;
#214802=AXIS2_PLACEMENT_3D ( 'NONE', #108984, #8621, #25618 ) ;
#214803=CIRCLE ( 'NONE', #160678, 0.09999999999999134581 ) ;
#214860=EDGE_CURVE ( 'NONE', #213808, #30344, #187768, .T. ) ;
#214880=CIRCLE ( 'NONE', #252458, 0.1000000000000028644 ) ;
#214933=EDGE_CURVE ( 'NONE', #130315, #216335, #75528, .T. ) ;
#214937=EDGE_LOOP ( 'NONE', ( #245867, #95475, #70241, #228317 ) ) ;
#214943=VECTOR ( 'NONE', #147442, 1000.000000000000000 ) ;
#214962=CYLINDRICAL_SURFACE ( 'NONE', #26894, 0.1000000000000033362 ) ;
#214992=CARTESIAN_POINT ( 'NONE',  ( 21.05000000000000071, 65.27628289530517236, -203.5231074845244166 ) ) ;
#215022=EDGE_CURVE ( 'NONE', #220769, #129083, #191641, .T. ) ;
#215043=CARTESIAN_POINT ( 'NONE',  ( -22.50485643085238863, 76.07878633908995880, -215.2729024236967916 ) ) ;
#215074=ADVANCED_FACE ( 'NONE', ( #234575 ), #120434, .T. ) ;
#215079=FACE_OUTER_BOUND ( 'NONE', #125641, .T. ) ;
#215090=ORIENTED_EDGE ( 'NONE', *, *, #3115, .T. ) ;
#215099=DIRECTION ( 'NONE',  ( 0.7071067811865475727, -0.7071067811865475727, -5.142139384388981164E-15 ) ) ;
#215117=CARTESIAN_POINT ( 'NONE',  ( 21.08621493067296271, 69.65070570884101642, -203.5793023240005084 ) ) ;
#215141=AXIS2_PLACEMENT_3D ( 'NONE', #46825, #229349, #91106 ) ;
#215203=DIRECTION ( 'NONE',  ( -0.000000000000000000, -0.8660254037844420383, 0.4999999999999943379 ) ) ;
#215210=DIRECTION ( 'NONE',  ( 0.000000000000000000, 0.000000000000000000, 1.000000000000000000 ) ) ;
#215232=CARTESIAN_POINT ( 'NONE',  ( 22.49999999999999645, 64.25043287652330548, -203.6239658536231900 ) ) ;
#215243=B_SPLINE_CURVE_WITH_KNOTS ( 'NONE', 3,
 ( #130549, #31491, #110997, #190555, #11919, #112293 ),
 .UNSPECIFIED., .F., .F.,
 ( 4, 2, 4 ),
 ( 0.000000000000000000, 0.0001895189928937423326, 0.0003790379857874846652 ),
 .UNSPECIFIED. ) ;
#215252=VECTOR ( 'NONE', #151840, 1000.000000000000000 ) ;
#215277=VERTEX_POINT ( 'NONE', #246139 ) ;
#215281=LINE ( 'NONE', #75781, #38411 ) ;
#215325=CARTESIAN_POINT ( 'NONE',  ( 20.94999999999999929, 84.73084112150795022, -193.9250327655399531 ) ) ;
#215343=ORIENTED_EDGE ( 'NONE', *, *, #208449, .F. ) ;
#215351=EDGE_CURVE ( 'NONE', #241281, #240431, #143899, .T. ) ;
#215375=ADVANCED_FACE ( 'NONE', ( #88306 ), #167913, .F. ) ;
#215386=DIRECTION ( 'NONE',  ( 0.000000000000000000, -7.086529944415886769E-15, 1.000000000000000000 ) ) ;
#215391=EDGE_CURVE ( 'NONE', #72316, #160017, #204245, .T. ) ;
#215397=EDGE_CURVE ( 'NONE', #236846, #114775, #229400, .T. ) ;
#215403=CARTESIAN_POINT ( 'NONE',  ( -18.59999999999999787, 64.35000000001264198, -196.5083017138704236 ) ) ;
#215404=CYLINDRICAL_SURFACE ( 'NONE', #90037, 0.09999999999999939493 ) ;
#215409=DIRECTION ( 'NONE',  ( 1.000000000000000000, 0.000000000000000000, 0.000000000000000000 ) ) ;
#215411=ADVANCED_FACE ( 'NONE', ( #11378 ), #4504, .T. ) ;
#215427=PLANE ( 'NONE',  #18092 ) ;
#215442=ORIENTED_EDGE ( 'NONE', *, *, #247571, .T. ) ;
#215454=DIRECTION ( 'NONE',  ( -1.000000000000000000, 0.000000000000000000, -0.000000000000000000 ) ) ;
#215471=ADVANCED_FACE ( 'NONE', ( #53058 ), #179329, .T. ) ;
#215491=DIRECTION ( 'NONE',  ( -1.000000000000000000, -0.000000000000000000, -0.000000000000000000 ) ) ;
#215492=DIRECTION ( 'NONE',  ( -0.000000000000000000, 6.982962677686266711E-15, -1.000000000000000000 ) ) ;
#215501=CARTESIAN_POINT ( 'NONE',  ( -22.50000000000000000, 64.35042919246788529, -203.6231074845244393 ) ) ;
#215510=DIRECTION ( 'NONE',  ( 0.000000000000000000, 0.000000000000000000, 1.000000000000000000 ) ) ;
#215518=CIRCLE ( 'NONE', #98967, 0.09999999999999939493 ) ;
#215520=FACE_OUTER_BOUND ( 'NONE', #20734, .T. ) ;
#215528=CARTESIAN_POINT ( 'NONE',  ( -20.64999999999999858, 85.40000000001252545, -179.9170766071767389 ) ) ;
#215533=CARTESIAN_POINT ( 'NONE',  ( -21.05000000000000071, 76.00000000001244871, -170.0231074845243597 ) ) ;
#215543=AXIS2_PLACEMENT_3D ( 'NONE', #104682, #219522, #145118 ) ;
#215629=AXIS2_PLACEMENT_3D ( 'NONE', #124151, #143689, #109688 ) ;
#215633=ORIENTED_EDGE ( 'NONE', *, *, #134121, .T. ) ;
#215672=FACE_OUTER_BOUND ( 'NONE', #176179, .T. ) ;
#215681=ADVANCED_FACE ( 'NONE', ( #107268 ), #30324, .T. ) ;
#215693=ADVANCED_FACE ( 'NONE', ( #87693 ), #47276, .F. ) ;
#215724=DIRECTION ( 'NONE',  ( -1.000000000000000000, 0.000000000000000000, -0.000000000000000000 ) ) ;
#215743=ORIENTED_EDGE ( 'NONE', *, *, #211653, .T. ) ;
#215762=CARTESIAN_POINT ( 'NONE',  ( -18.50000000000000000, 85.40000000001241176, -163.1084491415546438 ) ) ;
#215767=ORIENTED_EDGE ( 'NONE', *, *, #106778, .T. ) ;
#215770=CARTESIAN_POINT ( 'NONE',  ( 19.99999999999998934, 64.35000000001254250, -182.2731074845244450 ) ) ;
#215784=AXIS2_PLACEMENT_3D ( 'NONE', #197288, #154365, #138566 ) ;
#215785=EDGE_CURVE ( 'NONE', #31357, #60192, #128978, .T. ) ;
#215789=ORIENTED_EDGE ( 'NONE', *, *, #169125, .F. ) ;
#215826=EDGE_CURVE ( 'NONE', #14270, #217574, #33798, .T. ) ;
#215835=DIRECTION ( 'NONE',  ( -1.000000000000000000, 3.265361837132813093E-16, 2.280189983783949500E-30 ) ) ;
#215859=CARTESIAN_POINT ( 'NONE',  ( 21.05000000000000071, 85.00000000001261924, -193.6291383618718385 ) ) ;
#215868=VECTOR ( 'NONE', #215492, 1000.000000000000000 ) ;
#215954=DIRECTION ( 'NONE',  ( 0.7071067811865474617, -0.7071067811865474617, -4.937700262164531476E-15 ) ) ;
#215961=DIRECTION ( 'NONE',  ( -1.000000000000000000, -0.000000000000000000, -0.000000000000000000 ) ) ;
#215989=DIRECTION ( 'NONE',  ( 0.000000000000000000, 0.000000000000000000, 1.000000000000000000 ) ) ;
#215999=DIRECTION ( 'NONE',  ( 1.000000000000000000, 0.000000000000000000, 0.000000000000000000 ) ) ;
#216007=AXIS2_PLACEMENT_3D ( 'NONE', #51426, #110146, #190998 ) ;
#216040=CARTESIAN_POINT ( 'NONE',  ( 22.50000000000000000, 75.90000000001276703, -215.1726782920691505 ) ) ;
#216045=CARTESIAN_POINT ( 'NONE',  ( -21.05000000000000071, 74.16465844978819177, -191.9679561919613775 ) ) ;
#216060=VECTOR ( 'NONE', #61579, 1000.000000000000000 ) ;
#216066=CARTESIAN_POINT ( 'NONE',  ( -21.05000000000000071, 76.00000000001267608, -203.5231074845243597 ) ) ;
#216072=DIRECTION ( 'NONE',  ( -1.000000000000000000, -0.000000000000000000, -0.000000000000000000 ) ) ;
#216105=DIRECTION ( 'NONE',  ( 0.000000000000000000, 0.000000000000000000, -1.000000000000000000 ) ) ;
#216126=DIRECTION ( 'NONE',  ( 1.000000000000000000, 0.000000000000000000, 0.000000000000000000 ) ) ;
#216133=DIRECTION ( 'NONE',  ( 0.000000000000000000, -6.982962677686267499E-15, 1.000000000000000000 ) ) ;
#216158=TOROIDAL_SURFACE ( 'NONE', #16284, 0.2000000000000000111, 0.1000000000000000056 ) ;
#216164=( BOUNDED_SURFACE ( )  B_SPLINE_SURFACE ( 3, 2, ( 
 ( #245745, #149229, #227448 ),
 ( #4544, #123227, #5819 ),
 ( #164918, #147931, #28006 ),
 ( #226135, #67102, #228759 ),
 ( #9687, #125780, #205305 ),
 ( #85345, #86630, #187070 ) ),
 .UNSPECIFIED., .F., .F., .F. ) 
 B_SPLINE_SURFACE_WITH_KNOTS ( ( 4, 2, 4 ),
 ( 3, 3 ),
 ( 0.0001300404313046550988, 0.0003183318589266566725, 0.0005066232865486582733 ),
 ( 0.000000000000000000, 1.000000000000000000 ),
 .UNSPECIFIED. ) 
 GEOMETRIC_REPRESENTATION_ITEM ( )  RATIONAL_B_SPLINE_SURFACE ( (
 ( 1.000000000000000000, 0.7071067811865352493, 1.000000000000000000),
 ( 1.000000000000000000, 0.7625113560536035395, 1.000000000000000000),
 ( 1.000000000000000000, 0.8126073484694493754, 1.000000000000000000),
 ( 1.000000000000000000, 0.8923049332726276095, 1.000000000000000000),
 ( 1.000000000000000000, 0.9231914937774379215, 1.000000000000000000),
 ( 1.000000000000000000, 0.9238795325112713064, 1.000000000000000000) ) ) 
 REPRESENTATION_ITEM ( '' )  SURFACE ( )  );
#216168=DIRECTION ( 'NONE',  ( -1.000000000000000000, -7.304098846218163263E-16, 4.217023435051627211E-16 ) ) ;
#216217=ORIENTED_EDGE ( 'NONE', *, *, #159249, .F. ) ;
#216220=CARTESIAN_POINT ( 'NONE',  ( -22.57320508075686405, 64.25000000001267608, -203.5231074845243882 ) ) ;
#216227=CARTESIAN_POINT ( 'NONE',  ( -18.59999999999999787, 64.35000000001254250, -182.2731074845244450 ) ) ;
#216239=ORIENTED_EDGE ( 'NONE', *, *, #128672, .T. ) ;
#216246=AXIS2_PLACEMENT_3D ( 'NONE', #249692, #151898, #74934 ) ;
#216274=DIRECTION ( 'NONE',  ( 1.836970198721029934E-16, 1.000000000000000000, 6.982962677686266711E-15 ) ) ;
#216277=PLANE ( 'NONE',  #24288 ) ;
#216283=ORIENTED_EDGE ( 'NONE', *, *, #224505, .F. ) ;
#216301=AXIS2_PLACEMENT_3D ( 'NONE', #247774, #24904, #104385 ) ;
#216312=DIRECTION ( 'NONE',  ( 0.000000000000000000, 6.982962677686266711E-15, -1.000000000000000000 ) ) ;
#216321=FACE_OUTER_BOUND ( 'NONE', #222735, .T. ) ;
#216335=VERTEX_POINT ( 'NONE', #124556 ) ;
#216343=CARTESIAN_POINT ( 'NONE',  ( -18.59999999999999787, 68.97833521811233481, -166.3895420826271163 ) ) ;
#216355=ORIENTED_EDGE ( 'NONE', *, *, #22822, .T. ) ;
#216392=EDGE_CURVE ( 'NONE', #43634, #141625, #190968, .T. ) ;
#216396=CARTESIAN_POINT ( 'NONE',  ( 21.13498764882293557, 69.50438185653881362, -203.5247638792557154 ) ) ;
#216414=CIRCLE ( 'NONE', #29025, 0.5000000000000004441 ) ;
#216419=CARTESIAN_POINT ( 'NONE',  ( -21.05000000000000071, 77.83534155023700407, -191.9679561919613491 ) ) ;
#216441=CARTESIAN_POINT ( 'NONE',  ( 22.48970261584622321, 64.35000000001268461, -203.5784769727418393 ) ) ;
#216458=CIRCLE ( 'NONE', #29622, 12.77499999999999503 ) ;
#216472=TOROIDAL_SURFACE ( 'NONE', #158258, 1.900000000000002576, 0.1000000000000000056 ) ;
#216526=DIRECTION ( 'NONE',  ( 1.000000000000000000, 0.000000000000000000, 0.000000000000000000 ) ) ;
#216530=FACE_OUTER_BOUND ( 'NONE', #11225, .T. ) ;
#216531=CARTESIAN_POINT ( 'NONE',  ( -18.50000000000000000, 64.25000000001277556, -215.2731074845244450 ) ) ;
#216533=ORIENTED_EDGE ( 'NONE', *, *, #188983, .T. ) ;
#216548=ORIENTED_EDGE ( 'NONE', *, *, #204716, .T. ) ;
#216549=CARTESIAN_POINT ( 'NONE',  ( 20.95346350065193519, 67.11282275083814852, -195.0113755374890445 ) ) ;
#216551=EDGE_CURVE ( 'NONE', #248274, #17720, #80922, .T. ) ;
#216558=CIRCLE ( 'NONE', #145621, 0.09999999999999939493 ) ;
#216644=ORIENTED_EDGE ( 'NONE', *, *, #220465, .F. ) ;
#216666=CIRCLE ( 'NONE', #87471, 0.09999999999998898659 ) ;
#216686=DIRECTION ( 'NONE',  ( 0.000000000000000000, 0.9893560106964510714, -0.1455152366551481502 ) ) ;
#216688=ADVANCED_FACE ( 'NONE', ( #147330 ), #84299, .F. ) ;
#216698=DIRECTION ( 'NONE',  ( 1.000000000000000000, 0.000000000000000000, 0.000000000000000000 ) ) ;
#216699=CARTESIAN_POINT ( 'NONE',  ( -20.64999999999999858, 74.00000000001254818, -183.2477294072864709 ) ) ;
#216757=EDGE_LOOP ( 'NONE', ( #233722, #229597, #150896 ) ) ;
#216760=ORIENTED_EDGE ( 'NONE', *, *, #173563, .T. ) ;
#216770=CYLINDRICAL_SURFACE ( 'NONE', #141438, 0.09999999999998898659 ) ;
#216776=CIRCLE ( 'NONE', #16888, 0.09999999999998898659 ) ;
#216782=VERTEX_POINT ( 'NONE', #65221 ) ;
#216803=CARTESIAN_POINT ( 'NONE',  ( 21.05000000000000071, 70.60000000001254250, -182.4283735034374843 ) ) ;
#216804=EDGE_CURVE ( 'NONE', #196419, #143950, #192998, .T. ) ;
#216835=AXIS2_PLACEMENT_3D ( 'NONE', #63717, #48000, #143251 ) ;
#216845=DIRECTION ( 'NONE',  ( 0.000000000000000000, 7.086529944415886769E-15, -1.000000000000000000 ) ) ;
#216864=ORIENTED_EDGE ( 'NONE', *, *, #102974, .T. ) ;
#216874=VECTOR ( 'NONE', #14017, 1000.000000000000000 ) ;
#216885=DIRECTION ( 'NONE',  ( 0.000000000000000000, -6.982962677686266711E-15, 1.000000000000000000 ) ) ;
#216931=VECTOR ( 'NONE', #48699, 1000.000000000000000 ) ;
#216951=ORIENTED_EDGE ( 'NONE', *, *, #180656, .T. ) ;
#216968=DIRECTION ( 'NONE',  ( 0.000000000000000000, 6.982962677686266711E-15, -1.000000000000000000 ) ) ;
#216986=CARTESIAN_POINT ( 'NONE',  ( -18.40000000000000213, 85.68240343348880117, -163.3662641071115331 ) ) ;
#217000=ADVANCED_FACE ( 'NONE', ( #254118 ), #191014, .F. ) ;
#217005=ORIENTED_EDGE ( 'NONE', *, *, #120936, .T. ) ;
#217034=CARTESIAN_POINT ( 'NONE',  ( -20.00857864376270001, 66.85000000001254250, -182.3731074845244393 ) ) ;
#217036=VERTEX_POINT ( 'NONE', #98875 ) ;
#217038=DIRECTION ( 'NONE',  ( -1.000000000000000000, 0.000000000000000000, 0.000000000000000000 ) ) ;
#217040=DIRECTION ( 'NONE',  ( 2.342056488767301376E-15, 0.1350103645451835865, 0.9908441862701605762 ) ) ;
#217067=CIRCLE ( 'NONE', #204606, 11.64999999999999325 ) ;
#217085=ORIENTED_EDGE ( 'NONE', *, *, #87834, .T. ) ;
#217151=CARTESIAN_POINT ( 'NONE',  ( 23.15000000000000213, 87.65000000001246860, -173.1231074845242688 ) ) ;
#217160=VECTOR ( 'NONE', #212369, 1000.000000000000000 ) ;
#217195=CARTESIAN_POINT ( 'NONE',  ( -21.44999999999999929, 68.75000000001253397, -182.2731074845244166 ) ) ;
#217211=LINE ( 'NONE', #176845, #81148 ) ;
#217213=ORIENTED_EDGE ( 'NONE', *, *, #126454, .T. ) ;
#217248=EDGE_LOOP ( 'NONE', ( #229838, #245759, #137134 ) ) ;
#217295=LINE ( 'NONE', #81619, #113791 ) ;
#217329=AXIS2_PLACEMENT_3D ( 'NONE', #224082, #45457, #8904 ) ;
#217341=DIRECTION ( 'NONE',  ( 0.000000000000000000, -7.116814260417660624E-15, 1.000000000000000000 ) ) ;
#217347=ORIENTED_EDGE ( 'NONE', *, *, #113490, .T. ) ;
#217366=DIRECTION ( 'NONE',  ( 0.000000000000000000, 1.000000000000000000, 6.982962677686266711E-15 ) ) ;
#217401=DIRECTION ( 'NONE',  ( 1.000000000000000000, -0.000000000000000000, 0.000000000000000000 ) ) ;
#217434=ORIENTED_EDGE ( 'NONE', *, *, #167107, .F. ) ;
#217469=ORIENTED_EDGE ( 'NONE', *, *, #171564, .F. ) ;
#217508=CARTESIAN_POINT ( 'NONE',  ( 18.49999999999999645, 76.00000000001267608, -203.5231074845243597 ) ) ;
#217529=CARTESIAN_POINT ( 'NONE',  ( -20.94999999999999929, 64.35000000001251408, -176.8069731475025321 ) ) ;
#217546=CARTESIAN_POINT ( 'NONE',  ( 21.05000000000000071, 64.35000000001258513, -191.3731074845244393 ) ) ;
#217568=VERTEX_POINT ( 'NONE', #87999 ) ;
#217574=VERTEX_POINT ( 'NONE', #171458 ) ;
#217658=VECTOR ( 'NONE', #112840, 1000.000000000000000 ) ;
#217673=DIRECTION ( 'NONE',  ( 0.000000000000000000, 1.000000000000000000, 6.982962677686266711E-15 ) ) ;
#217687=ORIENTED_EDGE ( 'NONE', *, *, #251274, .T. ) ;
#217725=LINE ( 'NONE', #116093, #140972 ) ;
#217743=CIRCLE ( 'NONE', #13759, 0.09999999999999134581 ) ;
#217839=DIRECTION ( 'NONE',  ( -1.000000000000000000, -0.000000000000000000, -0.000000000000000000 ) ) ;
#217876=ORIENTED_EDGE ( 'NONE', *, *, #8912, .F. ) ;
#217894=ADVANCED_FACE ( 'NONE', ( #61743 ), #60238, .T. ) ;
#217915=DIRECTION ( 'NONE',  ( 1.000000000000000000, 0.000000000000000000, 0.000000000000000000 ) ) ;
#217916=CARTESIAN_POINT ( 'NONE',  ( 18.49999999999999645, 77.83534155023700407, -191.9679561919613491 ) ) ;
#217958=EDGE_CURVE ( 'NONE', #15440, #41155, #164700, .T. ) ;
#217973=DIRECTION ( 'NONE',  ( 1.000000000000000000, 0.000000000000000000, 0.000000000000000000 ) ) ;
#218062=VECTOR ( 'NONE', #173367, 1000.000000000000000 ) ;
#218066=EDGE_CURVE ( 'NONE', #184335, #52949, #126506, .T. ) ;
#218075=CARTESIAN_POINT ( 'NONE',  ( 21.05000000000000071, 76.00000000001244871, -170.0231074845243597 ) ) ;
#218091=CARTESIAN_POINT ( 'NONE',  ( -21.64999999999999858, 68.75000000001254818, -182.2731074845244166 ) ) ;
#218106=CIRCLE ( 'NONE', #163973, 11.80000000000000426 ) ;
#218129=AXIS2_PLACEMENT_3D ( 'NONE', #88529, #229361, #48136 ) ;
#218130=VERTEX_POINT ( 'NONE', #74628 ) ;
#218150=CARTESIAN_POINT ( 'NONE',  ( -18.59999999999999787, 74.26374286841520700, -191.9544551555068779 ) ) ;
#218154=ORIENTED_EDGE ( 'NONE', *, *, #92096, .F. ) ;
#218175=AXIS2_PLACEMENT_3D ( 'NONE', #205433, #144170, #228872 ) ;
#218181=CIRCLE ( 'NONE', #205719, 12.87499999999999822 ) ;
#218191=FACE_OUTER_BOUND ( 'NONE', #111720, .T. ) ;
#218193=VERTEX_POINT ( 'NONE', #14634 ) ;
#218204=CARTESIAN_POINT ( 'NONE',  ( 21.05000000000000071, 69.45934304831143891, -203.4231074845244223 ) ) ;
#218261=CARTESIAN_POINT ( 'NONE',  ( -22.39999999999999858, 64.25000000001269029, -203.5231074845244166 ) ) ;
#218266=SPHERICAL_SURFACE ( 'NONE', #126806, 0.1000000000000000056 ) ;
#218291=VERTEX_POINT ( 'NONE', #120175 ) ;
#218319=EDGE_CURVE ( 'NONE', #197295, #131701, #155757, .T. ) ;
#218320=VECTOR ( 'NONE', #127754, 1000.000000000000000 ) ;
#218324=AXIS2_PLACEMENT_3D ( 'NONE', #54423, #51837, #74031 ) ;
#218325=AXIS2_PLACEMENT_3D ( 'NONE', #83213, #47960, #205752 ) ;
#218429=VERTEX_POINT ( 'NONE', #51796 ) ;
#218433=VECTOR ( 'NONE', #127693, 1000.000000000000000 ) ;
#218441=DIRECTION ( 'NONE',  ( -1.000000000000000000, 2.952720810173289112E-16, 2.061873921506763405E-30 ) ) ;
#218470=AXIS2_PLACEMENT_3D ( 'NONE', #241468, #159373, #81083 ) ;
#218474=FACE_OUTER_BOUND ( 'NONE', #170679, .T. ) ;
#218498=DIRECTION ( 'NONE',  ( -3.265361837132813093E-16, -1.000000000000000000, -6.938893903907229955E-15 ) ) ;
#218501=ORIENTED_EDGE ( 'NONE', *, *, #144710, .F. ) ;
#218523=CARTESIAN_POINT ( 'NONE',  ( -20.94999999999999929, 70.10000000001267040, -193.3040077198679967 ) ) ;
#218528=DIRECTION ( 'NONE',  ( 0.000000000000000000, 0.000000000000000000, 1.000000000000000000 ) ) ;
#218566=DIRECTION ( 'NONE',  ( 1.000000000000000000, 0.000000000000000000, 0.000000000000000000 ) ) ;
#218574=CARTESIAN_POINT ( 'NONE',  ( 18.41815437325346494, 85.49870985315384075, -163.4191616457223404 ) ) ;
#218624=ADVANCED_FACE ( 'NONE', ( #197744 ), #21195, .T. ) ;
#218636=EDGE_LOOP ( 'NONE', ( #22796, #83494, #161095, #99156 ) ) ;
#218733=VERTEX_POINT ( 'NONE', #72378 ) ;
#218736=CARTESIAN_POINT ( 'NONE',  ( 21.04999999999999716, 65.37127968600823635, -191.3731074845244109 ) ) ;
#218747=LINE ( 'NONE', #143061, #156625 ) ;
#218770=ADVANCED_FACE ( 'NONE', ( #167630 ), #110113, .T. ) ;
#218776=CARTESIAN_POINT ( 'NONE',  ( -20.94999999999999929, 88.41227409416215721, -173.0231074845242745 ) ) ;
#218790=ORIENTED_EDGE ( 'NONE', *, *, #142385, .F. ) ;
#218798=ORIENTED_EDGE ( 'NONE', *, *, #46503, .T. ) ;
#218841=CARTESIAN_POINT ( 'NONE',  ( 21.05000000000000071, 65.57661458509973329, -196.0310555606543517 ) ) ;
#218856=ADVANCED_FACE ( 'NONE', ( #9812 ), #47780, .T. ) ;
#218862=ORIENTED_EDGE ( 'NONE', *, *, #218319, .F. ) ;
#218874=FACE_BOUND ( 'NONE', #29766, .T. ) ;
#218879=FACE_OUTER_BOUND ( 'NONE', #19147, .T. ) ;
#218900=DIRECTION ( 'NONE',  ( 0.000000000000000000, 0.000000000000000000, 1.000000000000000000 ) ) ;
#218903=DIRECTION ( 'NONE',  ( 0.000000000000000000, 6.938893903907222067E-15, -1.000000000000000000 ) ) ;
#218906=ORIENTED_EDGE ( 'NONE', *, *, #124741, .F. ) ;
#218949=CARTESIAN_POINT ( 'NONE',  ( -23.25000000000000000, 76.00000000001267608, -203.5231074845243597 ) ) ;
#218974=AXIS2_PLACEMENT_3D ( 'NONE', #171689, #88235, #148236 ) ;
#218977=DIRECTION ( 'NONE',  ( 0.000000000000000000, 6.982962677686266711E-15, -1.000000000000000000 ) ) ;
#218993=CIRCLE ( 'NONE', #214706, 0.09999999999999938105 ) ;
#218996=AXIS2_PLACEMENT_3D ( 'NONE', #175719, #253929, #196531 ) ;
#219007=CARTESIAN_POINT ( 'NONE',  ( 18.59999999999999076, 65.79142135624984178, -182.1731074845244223 ) ) ;
#219023=CARTESIAN_POINT ( 'NONE',  ( -21.98333005346336577, 76.00000000001273293, -210.8971828135810540 ) ) ;
#219045=CARTESIAN_POINT ( 'NONE',  ( 18.39999999999999858, 85.50000000001240608, -163.4229180933022576 ) ) ;
#219047=FACE_OUTER_BOUND ( 'NONE', #45376, .T. ) ;
#219070=ORIENTED_EDGE ( 'NONE', *, *, #81067, .F. ) ;
#219072=AXIS2_PLACEMENT_3D ( 'NONE', #132516, #136326, #232924 ) ;
#219123=VECTOR ( 'NONE', #138947, 1000.000000000000000 ) ;
#219153=CARTESIAN_POINT ( 'NONE',  ( 21.07928932188134397, 75.90110485435833709, -209.8516241409176928 ) ) ;
#219156=( BOUNDED_SURFACE ( )  B_SPLINE_SURFACE ( 3, 2, ( 
 ( #107229, #206344, #90216 ),
 ( #185491, #109790, #108517 ),
 ( #169823, #164651, #27739 ),
 ( #246730, #70707, #249330 ),
 ( #69412, #229749, #225861 ),
 ( #130645, #49824, #128088 ) ),
 .UNSPECIFIED., .F., .F., .F. ) 
 B_SPLINE_SURFACE_WITH_KNOTS ( ( 4, 2, 4 ),
 ( 3, 3 ),
 ( 0.0001300404313046710908, 0.0003183318589266637198, 0.0005066232865486563217 ),
 ( 0.000000000000000000, 1.000000000000000000 ),
 .UNSPECIFIED. ) 
 GEOMETRIC_REPRESENTATION_ITEM ( )  RATIONAL_B_SPLINE_SURFACE ( (
 ( 1.000000000000000000, 0.7071067811865475727, 1.000000000000000000),
 ( 1.000000000000000000, 0.7625113560532659207, 1.000000000000000000),
 ( 1.000000000000000000, 0.8126073484698599358, 1.000000000000000000),
 ( 1.000000000000000000, 0.8923049332723309579, 1.000000000000000000),
 ( 1.000000000000000000, 0.9231914937776042329, 1.000000000000000000),
 ( 1.000000000000000000, 0.9238795325112945100, 1.000000000000000000) ) ) 
 REPRESENTATION_ITEM ( '' )  SURFACE ( )  );
#219164=AXIS2_PLACEMENT_3D ( 'NONE', #243269, #35816, #210581 ) ;
#219181=CARTESIAN_POINT ( 'NONE',  ( 18.45139536634708932, 85.48608172029364027, -163.3825958667137002 ) ) ;
#219206=DIRECTION ( 'NONE',  ( 0.000000000000000000, 0.000000000000000000, -1.000000000000000000 ) ) ;
#219213=CARTESIAN_POINT ( 'NONE',  ( -23.15000000000000213, 87.48912529308852015, -173.1231074845242688 ) ) ;
#219221=AXIS2_PLACEMENT_3D ( 'NONE', #95321, #213989, #135715 ) ;
#219223=ORIENTED_EDGE ( 'NONE', *, *, #37969, .F. ) ;
#219241=ORIENTED_EDGE ( 'NONE', *, *, #49621, .F. ) ;
#219260=DIRECTION ( 'NONE',  ( 0.000000000000000000, 6.982962677686266711E-15, -1.000000000000000000 ) ) ;
#219298=EDGE_LOOP ( 'NONE', ( #35000, #244211, #53865, #74604 ) ) ;
#219299=EDGE_CURVE ( 'NONE', #254689, #215277, #243823, .T. ) ;
#219304=CYLINDRICAL_SURFACE ( 'NONE', #230572, 0.1000000000000028644 ) ;
#219327=CARTESIAN_POINT ( 'NONE',  ( 20.95325940946048249, 65.47660992931635349, -195.9586453552843466 ) ) ;
#219353=ORIENTED_EDGE ( 'NONE', *, *, #136604, .F. ) ;
#219390=CARTESIAN_POINT ( 'NONE',  ( 20.99551997958375082, 64.25000000001249134, -176.8714483468348533 ) ) ;
#219393=CIRCLE ( 'NONE', #248060, 11.69999999999998863 ) ;
#219399=ORIENTED_EDGE ( 'NONE', *, *, #191621, .F. ) ;
#219436=ORIENTED_EDGE ( 'NONE', *, *, #242116, .T. ) ;
#219448=ORIENTED_EDGE ( 'NONE', *, *, #175841, .T. ) ;
#219451=EDGE_CURVE ( 'NONE', #117271, #16498, #147920, .T. ) ;
#219519=DIRECTION ( 'NONE',  ( 1.000000000000000000, 0.000000000000000000, 0.000000000000000000 ) ) ;
#219522=DIRECTION ( 'NONE',  ( 0.000000000000000000, 0.8660254037844377084, 0.5000000000000016653 ) ) ;
#219548=CARTESIAN_POINT ( 'NONE',  ( 18.49999999999999645, 74.26374286841520700, -191.9544551555068779 ) ) ;
#219600=TOROIDAL_SURFACE ( 'NONE', #32195, 12.97499999999999609, 0.1000000000000000056 ) ;
#219606=DIRECTION ( 'NONE',  ( 0.000000000000000000, 0.000000000000000000, 1.000000000000000000 ) ) ;
#219651=CARTESIAN_POINT ( 'NONE',  ( -20.94999999999999929, 64.40000000001263913, -196.5949042542488883 ) ) ;
#219688=CIRCLE ( 'NONE', #257240, 0.09999999999999939493 ) ;
#219705=EDGE_CURVE ( 'NONE', #78372, #182093, #139692, .T. ) ;
#219716=AXIS2_PLACEMENT_3D ( 'NONE', #46178, #41077, #22801 ) ;
#219717=CARTESIAN_POINT ( 'NONE',  ( -21.44999999999999929, 68.85000000001254250, -182.2731074845244166 ) ) ;
#219724=ORIENTED_EDGE ( 'NONE', *, *, #11649, .T. ) ;
#219733=DIRECTION ( 'NONE',  ( 0.000000000000000000, 0.000000000000000000, 1.000000000000000000 ) ) ;
#219743=DIRECTION ( 'NONE',  ( -1.000000000000000000, 0.000000000000000000, -0.000000000000000000 ) ) ;
#219755=AXIS2_PLACEMENT_3D ( 'NONE', #178418, #98809, #59694 ) ;
#219767=CARTESIAN_POINT ( 'NONE',  ( 19.97071067695834046, 64.27928932305417220, -178.8468540517208396 ) ) ;
#219768=ADVANCED_FACE ( 'NONE', ( #250101 ), #202260, .T. ) ;
#219787=CARTESIAN_POINT ( 'NONE',  ( -21.40925344232282512, 69.34148114062223556, -203.6220576731440417 ) ) ;
#219830=CIRCLE ( 'NONE', #149135, 0.2000000000000057288 ) ;
#219882=ADVANCED_FACE ( 'NONE', ( #36204 ), #94862, .T. ) ;
#219892=AXIS2_PLACEMENT_3D ( 'NONE', #74820, #137306, #216845 ) ;
#219906=DIRECTION ( 'NONE',  ( -1.000000000000000000, 0.000000000000000000, -0.000000000000000000 ) ) ;
#219907=FACE_OUTER_BOUND ( 'NONE', #207022, .T. ) ;
#219909=DIRECTION ( 'NONE',  ( 0.000000000000000000, -6.938893903907222067E-15, 1.000000000000000000 ) ) ;
#219911=ORIENTED_EDGE ( 'NONE', *, *, #227326, .F. ) ;
#219934=EDGE_CURVE ( 'NONE', #180782, #223140, #72987, .T. ) ;
#219944=AXIS2_PLACEMENT_3D ( 'NONE', #236611, #217040, #160956 ) ;
#219955=ORIENTED_EDGE ( 'NONE', *, *, #37969, .T. ) ;
#219967=CARTESIAN_POINT ( 'NONE',  ( -21.05000000000000426, 69.52295361822282871, -203.4231074845244507 ) ) ;
#219970=VERTEX_POINT ( 'NONE', #30433 ) ;
#219984=CARTESIAN_POINT ( 'NONE',  ( -20.54999999999999716, 85.40000000001252545, -179.9170766071767389 ) ) ;
#219997=CIRCLE ( 'NONE', #199158, 0.09999999999999939493 ) ;
#220007=ORIENTED_EDGE ( 'NONE', *, *, #59897, .F. ) ;
#220010=CIRCLE ( 'NONE', #91025, 0.5000000000000004441 ) ;
#220025=EDGE_CURVE ( 'NONE', #80372, #230108, #81582, .T. ) ;
#220063=AXIS2_PLACEMENT_3D ( 'NONE', #46795, #205879, #5083 ) ;
#220072=CARTESIAN_POINT ( 'NONE',  ( -21.12757541349819590, 75.99483878420299732, -209.9964880557759273 ) ) ;
#220122=CARTESIAN_POINT ( 'NONE',  ( -20.94560253601877164, 64.25000000001250555, -177.0130239720093925 ) ) ;
#220139=LINE ( 'NONE', #100148, #134515 ) ;
#220153=CARTESIAN_POINT ( 'NONE',  ( 20.95595624212450048, 65.37610879691844445, -195.8934745703976432 ) ) ;
#220174=ORIENTED_EDGE ( 'NONE', *, *, #185100, .F. ) ;
#220194=CIRCLE ( 'NONE', #120268, 0.09999999999998898659 ) ;
#220210=CARTESIAN_POINT ( 'NONE',  ( -20.54999999999999716, 76.00000000001267608, -203.5231074845243597 ) ) ;
#220215=CIRCLE ( 'NONE', #70391, 0.09999999999998898659 ) ;
#220229=EDGE_LOOP ( 'NONE', ( #161673, #220632, #145569 ) ) ;
#220234=DIRECTION ( 'NONE',  ( -1.000000000000000000, 0.000000000000000000, 0.000000000000000000 ) ) ;
#220256=FACE_OUTER_BOUND ( 'NONE', #4988, .T. ) ;
#220264=CARTESIAN_POINT ( 'NONE',  ( 23.25000000000000000, 87.75000000001259082, -191.3731074845242688 ) ) ;
#220270=CARTESIAN_POINT ( 'NONE',  ( 18.49999999999999289, 65.58283456529608202, -178.6731074851066410 ) ) ;
#220284=AXIS2_PLACEMENT_3D ( 'NONE', #33341, #34607, #231515 ) ;
#220295=LINE ( 'NONE', #65051, #212510 ) ;
#220311=CYLINDRICAL_SURFACE ( 'NONE', #251359, 0.09999999999998898659 ) ;
#220317=DIRECTION ( 'NONE',  ( 0.000000000000000000, -1.186135710069610235E-15, 1.000000000000000000 ) ) ;
#220323=CARTESIAN_POINT ( 'NONE',  ( -20.64999999999999858, 84.66355140188177586, -193.9990063664569959 ) ) ;
#220335=CARTESIAN_POINT ( 'NONE',  ( -20.64999999999999858, 76.00000000001246292, -172.0231074845243597 ) ) ;
#220392=DIRECTION ( 'NONE',  ( 0.000000000000000000, 0.000000000000000000, -1.000000000000000000 ) ) ;
#220398=AXIS2_PLACEMENT_3D ( 'NONE', #176317, #216698, #255785 ) ;
#220401=DIRECTION ( 'NONE',  ( -0.1538461538461484146, -0.9880948137434723000, 0.000000000000000000 ) ) ;
#220412=CIRCLE ( 'NONE', #212028, 0.1000000000000028644 ) ;
#220429=ADVANCED_FACE ( 'NONE', ( #64105 ), #177532, .T. ) ;
#220435=CARTESIAN_POINT ( 'NONE',  ( -20.54999999999999716, 73.50000000001254818, -183.2477294072864709 ) ) ;
#220436=LINE ( 'NONE', #121367, #170161 ) ;
#220438=EDGE_CURVE ( 'NONE', #78303, #3356, #123505, .T. ) ;
#220442=ADVANCED_FACE ( 'NONE', ( #186630 ), #87496, .T. ) ;
#220456=ORIENTED_EDGE ( 'NONE', *, *, #129260, .F. ) ;
#220464=AXIS2_PLACEMENT_3D ( 'NONE', #154115, #152819, #111085 ) ;
#220465=EDGE_CURVE ( 'NONE', #247920, #6886, #32723, .T. ) ;
#220476=DIRECTION ( 'NONE',  ( -4.336808689941751890E-15, -0.8660254037844445918, -0.4999999999999897304 ) ) ;
#220491=ORIENTED_EDGE ( 'NONE', *, *, #147968, .F. ) ;
#220495=DIRECTION ( 'NONE',  ( 0.000000000000000000, -6.982962677686266711E-15, 1.000000000000000000 ) ) ;
#220503=ADVANCED_FACE ( 'NONE', ( #10561 ), #65063, .T. ) ;
#220538=LINE ( 'NONE', #252250, #128735 ) ;
#220545=AXIS2_PLACEMENT_3D ( 'NONE', #29872, #89797, #113221 ) ;
#220586=STYLED_ITEM ( 'NONE', ( #69801 ), #192084 ) ;
#220587=AXIS2_PLACEMENT_3D ( 'NONE', #59657, #80496, #235748 ) ;
#220612=DIRECTION ( 'NONE',  ( 0.000000000000000000, 6.982962677686266711E-15, -1.000000000000000000 ) ) ;
#220626=FACE_OUTER_BOUND ( 'NONE', #27660, .T. ) ;
#220629=DIRECTION ( 'NONE',  ( 0.000000000000000000, -1.000000000000000000, -6.982962677686265922E-15 ) ) ;
#220632=ORIENTED_EDGE ( 'NONE', *, *, #102341, .F. ) ;
#220645=ADVANCED_FACE ( 'NONE', ( #20844 ), #139466, .T. ) ;
#220646=EDGE_CURVE ( 'NONE', #65963, #29575, #231366, .T. ) ;
#220647=FACE_OUTER_BOUND ( 'NONE', #15003, .T. ) ;
#220673=CARTESIAN_POINT ( 'NONE',  ( 20.94999999999999929, 70.15000000001252545, -180.1556047088023149 ) ) ;
#220686=DIRECTION ( 'NONE',  ( 0.000000000000000000, -0.9915357197604982575, 0.1298341882519033486 ) ) ;
#220713=ADVANCED_FACE ( 'NONE', ( #2521 ), #1231, .T. ) ;
#220751=EDGE_CURVE ( 'NONE', #125507, #234183, #102896, .T. ) ;
#220769=VERTEX_POINT ( 'NONE', #27276 ) ;
#220785=ORIENTED_EDGE ( 'NONE', *, *, #53115, .T. ) ;
#220798=CARTESIAN_POINT ( 'NONE',  ( 21.05000000000000071, 69.58602111852471239, -203.4373083682504273 ) ) ;
#220814=AXIS2_PLACEMENT_3D ( 'NONE', #1035, #122304, #257904 ) ;
#220852=CARTESIAN_POINT ( 'NONE',  ( -21.59142135623730852, 68.15000000001253966, -182.3731074845244109 ) ) ;
#220880=DIRECTION ( 'NONE',  ( 1.000000000000000000, 0.000000000000000000, 0.000000000000000000 ) ) ;
#220897=AXIS2_PLACEMENT_3D ( 'NONE', #206861, #50330, #189868 ) ;
#220899=AXIS2_PLACEMENT_3D ( 'NONE', #37259, #78903, #235419 ) ;
#220938=ADVANCED_FACE ( 'NONE', ( #233165 ), #211015, .T. ) ;
#220954=B_SPLINE_CURVE_WITH_KNOTS ( 'NONE', 3,
 ( #16652, #195305, #118314, #81701, #238243, #76603, #219967, #19203 ),
 .UNSPECIFIED., .F., .F.,
 ( 4, 2, 2, 4 ),
 ( 0.000000000000000000, 9.550056980122538541E-05, 0.0001910011396024507708, 0.0003820022792049804173 ),
 .UNSPECIFIED. ) ;
#220964=VERTEX_POINT ( 'NONE', #89763 ) ;
#220971=CARTESIAN_POINT ( 'NONE',  ( 21.05000000000000071, 71.14953271029297355, -191.4888400755227167 ) ) ;
#221013=CARTESIAN_POINT ( 'NONE',  ( 20.22894356738409627, 66.72150177717490749, -195.2545845782749154 ) ) ;
#221019=AXIS2_PLACEMENT_3D ( 'NONE', #218949, #61168, #3762 ) ;
#221041=DIRECTION ( 'NONE',  ( 2.940209281316621016E-16, 1.000000000000000000, 9.408669700213187250E-15 ) ) ;
#221042=EDGE_LOOP ( 'NONE', ( #240296, #139894, #130012, #51099 ) ) ;
#221054=ADVANCED_FACE ( 'NONE', ( #96176 ), #252858, .T. ) ;
#221117=CIRCLE ( 'NONE', #137725, 0.09999999999998802902 ) ;
#221132=B_SPLINE_CURVE_WITH_KNOTS ( 'NONE', 3,
 ( #137166, #173786, #172497, #253252, #176320, #255788, #72074, #134576 ),
 .UNSPECIFIED., .F., .F.,
 ( 4, 2, 2, 4 ),
 ( 0.000000000000000000, 0.0002181133598169265018, 0.0003271700397253585820, 0.0004362267196337907163 ),
 .UNSPECIFIED. ) ;
#221138=CARTESIAN_POINT ( 'NONE',  ( 23.14999999999999503, 64.35000000001258513, -191.3731074845244393 ) ) ;
#221146=CARTESIAN_POINT ( 'NONE',  ( 18.50000000000000711, 85.42107434499938279, -163.1986354250934710 ) ) ;
#221154=VERTEX_POINT ( 'NONE', #43919 ) ;
#221168=AXIS2_PLACEMENT_3D ( 'NONE', #129406, #48579, #130684 ) ;
#221171=CARTESIAN_POINT ( 'NONE',  ( 22.43288208788031568, 75.99510014512738110, -215.1727593282434441 ) ) ;
#221180=DIRECTION ( 'NONE',  ( 0.000000000000000000, 0.1568667991644355497, -0.9876197685951332295 ) ) ;
#221189=ORIENTED_EDGE ( 'NONE', *, *, #123417, .F. ) ;
#221220=CIRCLE ( 'NONE', #17251, 0.09999999999998898659 ) ;
#221233=DIRECTION ( 'NONE',  ( 0.000000000000000000, 0.000000000000000000, 1.000000000000000000 ) ) ;
#221240=CIRCLE ( 'NONE', #75538, 0.09999999999998898659 ) ;
#221245=ORIENTED_EDGE ( 'NONE', *, *, #160181, .F. ) ;
#221272=EDGE_CURVE ( 'NONE', #9660, #213491, #165892, .T. ) ;
#221324=EDGE_CURVE ( 'NONE', #218733, #162124, #253041, .T. ) ;
#221351=ORIENTED_EDGE ( 'NONE', *, *, #226665, .F. ) ;
#221416=VECTOR ( 'NONE', #130482, 1000.000000000000000 ) ;
#221423=ORIENTED_EDGE ( 'NONE', *, *, #42712, .F. ) ;
#221462=ORIENTED_EDGE ( 'NONE', *, *, #219299, .T. ) ;
#221467=EDGE_LOOP ( 'NONE', ( #105781, #189951, #15690, #35550, #88613 ) ) ;
#221485=ORIENTED_EDGE ( 'NONE', *, *, #79965, .F. ) ;
#221505=LINE ( 'NONE', #182420, #66911 ) ;
#221512=CARTESIAN_POINT ( 'NONE',  ( 18.59999999999999076, 65.50857864377520912, -178.7731074845244166 ) ) ;
#221522=VERTEX_POINT ( 'NONE', #37215 ) ;
#221538=ADVANCED_FACE ( 'NONE', ( #244374 ), #146547, .T. ) ;
#221540=DIRECTION ( 'NONE',  ( 1.000000000000000000, 0.000000000000000000, 0.000000000000000000 ) ) ;
#221550=EDGE_CURVE ( 'NONE', #41396, #140330, #136507, .T. ) ;
#221576=SPHERICAL_SURFACE ( 'NONE', #76903, 0.1000000000000000056 ) ;
#221583=AXIS2_PLACEMENT_3D ( 'NONE', #143972, #126992, #223505 ) ;
#221633=CARTESIAN_POINT ( 'NONE',  ( -20.94999999999999929, 77.83534155023700407, -191.9679561919613491 ) ) ;
#221645=LINE ( 'NONE', #105530, #129401 ) ;
#221650=PLANE ( 'NONE',  #23979 ) ;
#221659=ORIENTED_EDGE ( 'NONE', *, *, #36201, .T. ) ;
#221679=CARTESIAN_POINT ( 'NONE',  ( -21.64999999999999858, 68.65000000001261071, -191.1731074845243938 ) ) ;
#221686=EDGE_CURVE ( 'NONE', #195224, #91774, #78251, .T. ) ;
#221704=VERTEX_POINT ( 'NONE', #90436 ) ;
#221743=ORIENTED_EDGE ( 'NONE', *, *, #143716, .T. ) ;
#221752=SPHERICAL_SURFACE ( 'NONE', #233494, 0.1000000000000000056 ) ;
#221772=VERTEX_POINT ( 'NONE', #78250 ) ;
#221828=DIRECTION ( 'NONE',  ( 0.000000000000000000, 0.000000000000000000, -1.000000000000000000 ) ) ;
#221860=DIRECTION ( 'NONE',  ( 0.000000000000000000, 0.000000000000000000, 1.000000000000000000 ) ) ;
#221868=EDGE_CURVE ( 'NONE', #6746, #27052, #20025, .T. ) ;
#221871=ORIENTED_EDGE ( 'NONE', *, *, #256831, .F. ) ;
#221884=LINE ( 'NONE', #185354, #70739 ) ;
#221891=EDGE_CURVE ( 'NONE', #128423, #242182, #228305, .T. ) ;
#221892=DIRECTION ( 'NONE',  ( -1.000000000000000000, 0.000000000000000000, -0.000000000000000000 ) ) ;
#221896=ORIENTED_EDGE ( 'NONE', *, *, #235535, .F. ) ;
#221899=TOROIDAL_SURFACE ( 'NONE', #238491, 0.2000000000000000111, 0.1000000000000000056 ) ;
#221916=CARTESIAN_POINT ( 'NONE',  ( 18.59999999999999432, 77.16270174995064224, -195.5231074845243313 ) ) ;
#221968=CIRCLE ( 'NONE', #209520, 4.049999999999998046 ) ;
#221972=ORIENTED_EDGE ( 'NONE', *, *, #107138, .F. ) ;
#221976=VECTOR ( 'NONE', #223132, 1000.000000000000000 ) ;
#221988=CARTESIAN_POINT ( 'NONE',  ( -18.50000000000000000, 85.40000000001263913, -196.2258477248610120 ) ) ;
#222024=DIRECTION ( 'NONE',  ( 0.000000000000000000, -7.026728003956695223E-15, 1.000000000000000000 ) ) ;
#222040=DIRECTION ( 'NONE',  ( 0.000000000000000000, 0.000000000000000000, -1.000000000000000000 ) ) ;
#222065=DIRECTION ( 'NONE',  ( 1.000000000000000000, -0.000000000000000000, 0.000000000000000000 ) ) ;
#222066=CIRCLE ( 'NONE', #113763, 0.8750000000000007772 ) ;
#222083=CIRCLE ( 'NONE', #43067, 0.2000000000000057288 ) ;
#222092=FACE_OUTER_BOUND ( 'NONE', #195943, .T. ) ;
#222097=EDGE_LOOP ( 'NONE', ( #79705, #11044, #188892, #141092 ) ) ;
#222127=ORIENTED_EDGE ( 'NONE', *, *, #102304, .F. ) ;
#222131=CARTESIAN_POINT ( 'NONE',  ( 20.94999999999999929, 76.00000000001247713, -174.1231074845243540 ) ) ;
#222152=CIRCLE ( 'NONE', #168067, 0.09999999999998898659 ) ;
#222222=CARTESIAN_POINT ( 'NONE',  ( 20.94999999999999929, 76.00000000001244871, -170.0231074845243597 ) ) ;
#222277=CARTESIAN_POINT ( 'NONE',  ( 20.97217846901852312, 67.12455827530294528, -195.0218798005872145 ) ) ;
#222305=ORIENTED_EDGE ( 'NONE', *, *, #54911, .F. ) ;
#222307=CARTESIAN_POINT ( 'NONE',  ( -22.39999999999999858, 76.10085836911147794, -215.2726746080137445 ) ) ;
#222314=CARTESIAN_POINT ( 'NONE',  ( 20.01093837587850288, 64.25000000001250555, -178.7687100499268240 ) ) ;
#222322=CARTESIAN_POINT ( 'NONE',  ( -20.94999999999999929, 68.97833521811233481, -166.1895420826271277 ) ) ;
#222338=VERTEX_POINT ( 'NONE', #42673 ) ;
#222341=TOROIDAL_SURFACE ( 'NONE', #164135, 0.2000000000000000111, 0.1000000000000000056 ) ;
#222363=CARTESIAN_POINT ( 'NONE',  ( -20.93302460841142931, 65.68434038414410736, -164.4866880726065972 ) ) ;
#222381=ORIENTED_EDGE ( 'NONE', *, *, #145636, .F. ) ;
#222410=AXIS2_PLACEMENT_3D ( 'NONE', #30828, #110333, #225128 ) ;
#222415=ORIENTED_EDGE ( 'NONE', *, *, #99075, .F. ) ;
#222426=ADVANCED_FACE ( 'NONE', ( #102615 ), #223859, .T. ) ;
#222430=ORIENTED_EDGE ( 'NONE', *, *, #159249, .T. ) ;
#222431=ORIENTED_EDGE ( 'NONE', *, *, #147450, .T. ) ;
#222456=EDGE_CURVE ( 'NONE', #115127, #247461, #232603, .T. ) ;
#222478=AXIS2_PLACEMENT_3D ( 'NONE', #199143, #217401, #17924 ) ;
#222496=CARTESIAN_POINT ( 'NONE',  ( 20.85000000000000142, 76.00000000001239187, -162.2231074845243768 ) ) ;
#222507=ORIENTED_EDGE ( 'NONE', *, *, #97780, .T. ) ;
#222521=VECTOR ( 'NONE', #139000, 1000.000000000000000 ) ;
#222541=EDGE_CURVE ( 'NONE', #90288, #63948, #249864, .T. ) ;
#222601=ORIENTED_EDGE ( 'NONE', *, *, #88866, .T. ) ;
#222604=CIRCLE ( 'NONE', #85224, 1.900000000000012790 ) ;
#222616=DIRECTION ( 'NONE',  ( 0.000000000000000000, 0.000000000000000000, -1.000000000000000000 ) ) ;
#222626=ORIENTED_EDGE ( 'NONE', *, *, #96917, .T. ) ;
#222641=AXIS2_PLACEMENT_3D ( 'NONE', #17961, #200466, #97477 ) ;
#222653=ORIENTED_EDGE ( 'NONE', *, *, #203975, .F. ) ;
#222655=TOROIDAL_SURFACE ( 'NONE', #118651, 0.6000000000000013101, 0.1000000000000000056 ) ;
#222667=DIRECTION ( 'NONE',  ( -0.000000000000000000, -0.1298341882519953583, -0.9915357197604862671 ) ) ;
#222683=CYLINDRICAL_SURFACE ( 'NONE', #177544, 0.09999999999998898659 ) ;
#222695=ORIENTED_EDGE ( 'NONE', *, *, #214254, .F. ) ;
#222709=DIRECTION ( 'NONE',  ( 0.000000000000000000, 0.000000000000000000, 1.000000000000000000 ) ) ;
#222735=EDGE_LOOP ( 'NONE', ( #38172, #55449, #41906, #142447 ) ) ;
#222746=ORIENTED_EDGE ( 'NONE', *, *, #249878, .T. ) ;
#222798=CARTESIAN_POINT ( 'NONE',  ( 20.94999999999999929, 74.16465844978819177, -191.9679561919613775 ) ) ;
#222799=CARTESIAN_POINT ( 'NONE',  ( 18.52928932188133970, 65.72071067813116940, -178.8731074845244109 ) ) ;
#222811=MECHANICAL_DESIGN_GEOMETRIC_PRESENTATION_REPRESENTATION('',(#243672),#160315);
#222821=CARTESIAN_POINT ( 'NONE',  ( -18.50000000000000000, 76.00000000001267608, -203.5231074845243597 ) ) ;
#222823=CYLINDRICAL_SURFACE ( 'NONE', #30681, 0.09999999999999939493 ) ;
#222828=AXIS2_PLACEMENT_3D ( 'NONE', #113206, #71543, #191495 ) ;
#222857=DIRECTION ( 'NONE',  ( -1.000000000000000000, -0.000000000000000000, -0.000000000000000000 ) ) ;
#222887=VECTOR ( 'NONE', #177761, 999.9999999999998863 ) ;
#222903=LINE ( 'NONE', #202076, #153896 ) ;
#222904=CARTESIAN_POINT ( 'NONE',  ( 21.08750232978087524, 65.27513661400244871, -191.2942493115248510 ) ) ;
#222906=CARTESIAN_POINT ( 'NONE',  ( -18.54118089899630561, 85.46353763186074559, -196.4745298866561711 ) ) ;
#222914=DIRECTION ( 'NONE',  ( 0.000000000000000000, -1.000000000000000000, 0.000000000000000000 ) ) ;
#222938=ORIENTED_EDGE ( 'NONE', *, *, #238282, .F. ) ;
#222953=CARTESIAN_POINT ( 'NONE',  ( 20.94999999999999929, 67.22371710472012296, -191.3731074845244109 ) ) ;
#222984=CIRCLE ( 'NONE', #18970, 0.09999999999999939493 ) ;
#222993=ORIENTED_EDGE ( 'NONE', *, *, #164632, .T. ) ;
#222996=VERTEX_POINT ( 'NONE', #232599 ) ;
#222997=FACE_OUTER_BOUND ( 'NONE', #185437, .T. ) ;
#222999=VERTEX_POINT ( 'NONE', #87889 ) ;
#223004=EDGE_CURVE ( 'NONE', #230108, #116223, #133470, .T. ) ;
#223010=ORIENTED_EDGE ( 'NONE', *, *, #242280, .F. ) ;
#223011=CIRCLE ( 'NONE', #94027, 11.80000000000000426 ) ;
#223034=ORIENTED_EDGE ( 'NONE', *, *, #71539, .T. ) ;
#223035=DIRECTION ( 'NONE',  ( 0.000000000000000000, 0.000000000000000000, 1.000000000000000000 ) ) ;
#223050=CARTESIAN_POINT ( 'NONE',  ( -21.04999999999999716, 76.08574093704612551, -209.9369337733373015 ) ) ;
#223068=FACE_OUTER_BOUND ( 'NONE', #8438, .T. ) ;
#223083=FACE_OUTER_BOUND ( 'NONE', #109486, .T. ) ;
#223092=AXIS2_PLACEMENT_3D ( 'NONE', #47393, #128241, #205185 ) ;
#223099=DIRECTION ( 'NONE',  ( 0.7071067811865474617, -0.7071067811865474617, -5.142139384388980375E-15 ) ) ;
#223101=AXIS2_PLACEMENT_3D ( 'NONE', #93763, #216274, #211154 ) ;
#223124=EDGE_CURVE ( 'NONE', #82861, #167877, #65775, .T. ) ;
#223132=DIRECTION ( 'NONE',  ( 1.000000000000000000, 0.000000000000000000, 0.000000000000000000 ) ) ;
#223140=VERTEX_POINT ( 'NONE', #56476 ) ;
#223149=EDGE_CURVE ( 'NONE', #139621, #218429, #223976, .T. ) ;
#223166=ADVANCED_FACE ( 'NONE', ( #250397 ), #71791, .T. ) ;
#223176=CARTESIAN_POINT ( 'NONE',  ( 20.95545211741311320, 65.41358668846868341, -195.9369606249361198 ) ) ;
#223190=DIRECTION ( 'NONE',  ( 0.000000000000000000, 0.000000000000000000, -1.000000000000000000 ) ) ;
#223194=ORIENTED_EDGE ( 'NONE', *, *, #44962, .T. ) ;
#223206=LINE ( 'NONE', #95871, #95651 ) ;
#223270=ORIENTED_EDGE ( 'NONE', *, *, #23743, .T. ) ;
#223297=DIRECTION ( 'NONE',  ( 0.000000000000000000, 0.000000000000000000, 1.000000000000000000 ) ) ;
#223342=ORIENTED_EDGE ( 'NONE', *, *, #159089, .F. ) ;
#223353=LINE ( 'NONE', #124281, #84577 ) ;
#223376=CARTESIAN_POINT ( 'NONE',  ( -20.54999999999999716, 74.00000000001254818, -183.2477294072864709 ) ) ;
#223381=DIRECTION ( 'NONE',  ( -6.938893903907222856E-15, -1.000000000000000000, -7.272083257015735086E-15 ) ) ;
#223400=DIRECTION ( 'NONE',  ( 0.7071359030028288029, 0.000000000000000000, 0.7070776581708504427 ) ) ;
#223428=ORIENTED_EDGE ( 'NONE', *, *, #48219, .F. ) ;
#223495=VECTOR ( 'NONE', #174915, 1000.000000000000000 ) ;
#223505=DIRECTION ( 'NONE',  ( 1.000000000000000000, 0.000000000000000000, 0.000000000000000000 ) ) ;
#223516=ORIENTED_EDGE ( 'NONE', *, *, #219451, .T. ) ;
#223527=LINE ( 'NONE', #243104, #164886 ) ;
#223533=DIRECTION ( 'NONE',  ( -0.000000000000000000, 6.982962677686266711E-15, -1.000000000000000000 ) ) ;
#223534=DIRECTION ( 'NONE',  ( 1.000000000000000000, 0.000000000000000000, 0.000000000000000000 ) ) ;
#223547=FACE_OUTER_BOUND ( 'NONE', #178576, .T. ) ;
#223559=AXIS2_PLACEMENT_3D ( 'NONE', #223376, #242947, #126865 ) ;
#223577=CARTESIAN_POINT ( 'NONE',  ( 20.97438252431638972, 67.07457649393661825, -195.0507367955136431 ) ) ;
#223583=EDGE_LOOP ( 'NONE', ( #24166, #236606, #238253 ) ) ;
#223622=ORIENTED_EDGE ( 'NONE', *, *, #251186, .T. ) ;
#223640=DIRECTION ( 'NONE',  ( 0.000000000000000000, 0.000000000000000000, 1.000000000000000000 ) ) ;
#223651=ORIENTED_EDGE ( 'NONE', *, *, #66632, .T. ) ;
#223652=VERTEX_POINT ( 'NONE', #132238 ) ;
#223659=CARTESIAN_POINT ( 'NONE',  ( -18.59999999999999787, 68.97833521811233481, -166.1895420826271277 ) ) ;
#223665=CARTESIAN_POINT ( 'NONE',  ( -20.85000000000000142, 65.66751761918722252, -164.4282609406112670 ) ) ;
#223693=ORIENTED_EDGE ( 'NONE', *, *, #126464, .T. ) ;
#223699=VERTEX_POINT ( 'NONE', #34457 ) ;
#223718=DIRECTION ( 'NONE',  ( 3.469446951953728416E-14, 0.8660254037844343777, -0.5000000000000074385 ) ) ;
#223719=CARTESIAN_POINT ( 'NONE',  ( -23.25000000000000000, 87.48912529308852015, -173.1231074845242688 ) ) ;
#223731=ORIENTED_EDGE ( 'NONE', *, *, #198397, .T. ) ;
#223732=CIRCLE ( 'NONE', #252967, 7.791421356237338003 ) ;
#223769=ORIENTED_EDGE ( 'NONE', *, *, #61159, .T. ) ;
#223777=CYLINDRICAL_SURFACE ( 'NONE', #115897, 0.1000000000000028644 ) ;
#223806=CARTESIAN_POINT ( 'NONE',  ( 20.94999999999999574, 77.85102823015347440, -191.8691942151018566 ) ) ;
#223851=VERTEX_POINT ( 'NONE', #62971 ) ;
#223859=CYLINDRICAL_SURFACE ( 'NONE', #7725, 0.09999999999999939493 ) ;
#223888=ORIENTED_EDGE ( 'NONE', *, *, #32590, .T. ) ;
#223921=AXIS2_PLACEMENT_3D ( 'NONE', #179118, #78675, #199948 ) ;
#223944=EDGE_CURVE ( 'NONE', #247736, #130315, #62054, .T. ) ;
#223965=ADVANCED_FACE ( 'NONE', ( #87655 ), #219156, .T. ) ;
#223976=CIRCLE ( 'NONE', #219892, 11.75000000000001066 ) ;
#224020=DIRECTION ( 'NONE',  ( 0.000000000000000000, -0.008583690987162452199, -0.9999631594459053030 ) ) ;
#224026=VECTOR ( 'NONE', #8601, 1000.000000000000000 ) ;
#224040=VECTOR ( 'NONE', #191563, 1000.000000000000000 ) ;
#224066=FACE_OUTER_BOUND ( 'NONE', #79703, .T. ) ;
#224074=DIRECTION ( 'NONE',  ( 1.000000000000000000, 0.000000000000000000, 0.000000000000000000 ) ) ;
#224082=CARTESIAN_POINT ( 'NONE',  ( 21.05000000000000071, 71.00000000001260503, -191.1178414656112921 ) ) ;
#224088=CARTESIAN_POINT ( 'NONE',  ( 18.53691006697079757, 65.69784844286159853, -178.8209087672253474 ) ) ;
#224089=FACE_OUTER_BOUND ( 'NONE', #105094, .T. ) ;
#224111=EDGE_CURVE ( 'NONE', #3356, #78303, #78770, .T. ) ;
#224117=CARTESIAN_POINT ( 'NONE',  ( -23.25000000000000000, 77.83585931145600512, -158.5186683157258187 ) ) ;
#224171=ORIENTED_EDGE ( 'NONE', *, *, #33761, .F. ) ;
#224179=DIRECTION ( 'NONE',  ( 1.000000000000000000, -3.265361837132813093E-16, -2.280189983783949500E-30 ) ) ;
#224189=CARTESIAN_POINT ( 'NONE',  ( 21.07189867249812210, 65.27501972991944967, -191.3106560422477003 ) ) ;
#224201=DIRECTION ( 'NONE',  ( -1.000000000000000000, 0.000000000000000000, -0.000000000000000000 ) ) ;
#224317=CARTESIAN_POINT ( 'NONE',  ( -18.50000000000000000, 85.40000000001241176, -163.1410656363516125 ) ) ;
#224334=CARTESIAN_POINT ( 'NONE',  ( 18.40000000000000213, 85.51932773110506503, -196.5501311079649724 ) ) ;
#224350=CARTESIAN_POINT ( 'NONE',  ( -22.39999999999999858, 68.20922040163927136, -203.5231074845243882 ) ) ;
#224358=AXIS2_PLACEMENT_3D ( 'NONE', #65675, #6985, #69552 ) ;
#224427=CARTESIAN_POINT ( 'NONE',  ( 18.49999999999999645, 74.16465844978819177, -191.9679561919613775 ) ) ;
#224435=DIRECTION ( 'NONE',  ( 1.734723475976817507E-14, -6.982962677686266711E-15, 1.000000000000000000 ) ) ;
#224448=CARTESIAN_POINT ( 'NONE',  ( -23.15000000000000213, 71.65000000001253966, -182.3731074845244109 ) ) ;
#224505=EDGE_CURVE ( 'NONE', #197295, #255597, #12365, .T. ) ;
#224589=VERTEX_POINT ( 'NONE', #200584 ) ;
#224591=VECTOR ( 'NONE', #182308, 1000.000000000000000 ) ;
#224600=CIRCLE ( 'NONE', #178865, 0.09999999999998802902 ) ;
#224635=AXIS2_PLACEMENT_3D ( 'NONE', #31453, #133089, #110952 ) ;
#224689=DIRECTION ( 'NONE',  ( -1.000000000000000000, -0.000000000000000000, -0.000000000000000000 ) ) ;
#224709=CIRCLE ( 'NONE', #33229, 0.2000000000000057288 ) ;
#224768=CARTESIAN_POINT ( 'NONE',  ( -18.59117750673697245, 65.66751761918722252, -164.4282609406112670 ) ) ;
#224770=DIRECTION ( 'NONE',  ( 1.000000000000000000, 0.000000000000000000, 0.000000000000000000 ) ) ;
#224784=DIRECTION ( 'NONE',  ( 1.000000000000000000, 0.000000000000000000, 0.000000000000000000 ) ) ;
#224787=EDGE_CURVE ( 'NONE', #34288, #160017, #224709, .T. ) ;
#224800=CARTESIAN_POINT ( 'NONE',  ( -20.64999999999999858, 68.75000000001260503, -191.1731074845243938 ) ) ;
#224842=CARTESIAN_POINT ( 'NONE',  ( 21.11344571971183015, 65.38212097649690691, -191.2770865921224015 ) ) ;
#224863=CARTESIAN_POINT ( 'NONE',  ( 20.44999100639871514, 65.56028929680083195, -195.7640317585554044 ) ) ;
#224926=CARTESIAN_POINT ( 'NONE',  ( -18.59999999999999787, 77.83585931145600512, -158.5186683157258187 ) ) ;
#224936=AXIS2_PLACEMENT_3D ( 'NONE', #147151, #165454, #244971 ) ;
#224964=EDGE_LOOP ( 'NONE', ( #235848, #105394, #233614, #114294 ) ) ;
#224980=DIRECTION ( 'NONE',  ( -1.000000000000000000, 0.000000000000000000, -0.000000000000000000 ) ) ;
#225010=CIRCLE ( 'NONE', #204172, 0.09999999999999939493 ) ;
#225015=LINE ( 'NONE', #125923, #194103 ) ;
#225021=DIRECTION ( 'NONE',  ( 0.000000000000000000, 0.000000000000000000, -1.000000000000000000 ) ) ;
#225053=CIRCLE ( 'NONE', #175067, 0.09999999999998898659 ) ;
#225080=EDGE_CURVE ( 'NONE', #213808, #71516, #41776, .T. ) ;
#225094=DIRECTION ( 'NONE',  ( 0.000000000000000000, -0.4999999999999088507, 0.8660254037844913322 ) ) ;
#225113=CARTESIAN_POINT ( 'NONE',  ( 20.99142135623731065, 64.40000000001248281, -176.9513107147999449 ) ) ;
#225128=DIRECTION ( 'NONE',  ( 0.000000000000000000, 0.000000000000000000, 1.000000000000000000 ) ) ;
#225131=DIRECTION ( 'NONE',  ( -1.000000000000000000, -0.000000000000000000, 0.000000000000000000 ) ) ;
#225132=ORIENTED_EDGE ( 'NONE', *, *, #212284, .T. ) ;
#225144=DIRECTION ( 'NONE',  ( 1.296989514748957922E-15, 0.9887567792719351711, -0.1495327102803594987 ) ) ;
#225168=ORIENTED_EDGE ( 'NONE', *, *, #211559, .F. ) ;
#225176=CARTESIAN_POINT ( 'NONE',  ( 21.00000000000000000, 66.25000000001260503, -191.2731074845244166 ) ) ;
#225233=AXIS2_PLACEMENT_3D ( 'NONE', #105041, #107652, #184622 ) ;
#225266=ORIENTED_EDGE ( 'NONE', *, *, #47322, .F. ) ;
#225268=DIRECTION ( 'NONE',  ( -1.000000000000000000, 0.000000000000000000, -0.000000000000000000 ) ) ;
#225287=EDGE_LOOP ( 'NONE', ( #8884, #9816, #52286, #233057 ) ) ;
#225319=ORIENTED_EDGE ( 'NONE', *, *, #200583, .T. ) ;
#225325=CARTESIAN_POINT ( 'NONE',  ( -22.39999999999999858, 64.35000000001268461, -203.5231074845244166 ) ) ;
#225334=EDGE_LOOP ( 'NONE', ( #26057, #167914, #129779, #244872 ) ) ;
#225342=FACE_OUTER_BOUND ( 'NONE', #67227, .T. ) ;
#225348=VERTEX_POINT ( 'NONE', #251916 ) ;
#225364=AXIS2_PLACEMENT_3D ( 'NONE', #60765, #85440, #165017 ) ;
#225369=AXIS2_PLACEMENT_3D ( 'NONE', #29542, #109030, #30819 ) ;
#225370=CARTESIAN_POINT ( 'NONE',  ( -21.05000000000000071, 76.00000000001270450, -207.8231074845243143 ) ) ;
#225404=DIRECTION ( 'NONE',  ( 0.000000000000000000, 0.1350103645451835865, 0.9908441862701605762 ) ) ;
#225407=ADVANCED_FACE ( 'NONE', ( #24895 ), #221752, .T. ) ;
#225408=ORIENTED_EDGE ( 'NONE', *, *, #99625, .T. ) ;
#225412=CARTESIAN_POINT ( 'NONE',  ( -20.54999999999999716, 66.65000000001259650, -191.2731074845244166 ) ) ;
#225458=DIRECTION ( 'NONE',  ( 1.000000000000000000, 0.000000000000000000, 0.000000000000000000 ) ) ;
#225462=CARTESIAN_POINT ( 'NONE',  ( -18.46902351632711969, 85.50947011869349978, -196.5366535502670047 ) ) ;
#225488=DIRECTION ( 'NONE',  ( 0.000000000000000000, 0.000000000000000000, 1.000000000000000000 ) ) ;
#225490=ORIENTED_EDGE ( 'NONE', *, *, #155726, .F. ) ;
#225508=ORIENTED_EDGE ( 'NONE', *, *, #98431, .T. ) ;
#225529=EDGE_LOOP ( 'NONE', ( #32565, #227382, #175276, #216644 ) ) ;
#225536=DIRECTION ( 'NONE',  ( 1.000000000000000000, 0.000000000000000000, 0.000000000000000000 ) ) ;
#225557=AXIS2_PLACEMENT_3D ( 'NONE', #166814, #122532, #34669 ) ;
#225572=ORIENTED_EDGE ( 'NONE', *, *, #203008, .T. ) ;
#225579=VERTEX_POINT ( 'NONE', #7892 ) ;
#225600=CARTESIAN_POINT ( 'NONE',  ( 21.05000000000000071, 65.27628289530507288, -191.3731074845244393 ) ) ;
#225603=CARTESIAN_POINT ( 'NONE',  ( -21.00219873199078435, 64.39461131213606393, -196.6104600562298401 ) ) ;
#225612=ADVANCED_FACE ( 'NONE', ( #245212 ), #76004, .T. ) ;
#225618=DIRECTION ( 'NONE',  ( -1.000000000000000000, -0.000000000000000000, -0.000000000000000000 ) ) ;
#225648=CARTESIAN_POINT ( 'NONE',  ( 21.05000000000000071, 74.16465844978819177, -191.9679561919613775 ) ) ;
#225669=VECTOR ( 'NONE', #137548, 1000.000000000000000 ) ;
#225725=FACE_OUTER_BOUND ( 'NONE', #61634, .T. ) ;
#225746=ORIENTED_EDGE ( 'NONE', *, *, #46503, .F. ) ;
#225768=DIRECTION ( 'NONE',  ( 0.000000000000000000, 0.000000000000000000, -1.000000000000000000 ) ) ;
#225774=EDGE_LOOP ( 'NONE', ( #211427, #180070, #255383, #250964 ) ) ;
#225819=VERTEX_POINT ( 'NONE', #242316 ) ;
#225835=CARTESIAN_POINT ( 'NONE',  ( 23.14999999999999858, 70.50000000001253397, -182.4283735034374843 ) ) ;
#225855=ORIENTED_EDGE ( 'NONE', *, *, #34449, .F. ) ;
#225861=CARTESIAN_POINT ( 'NONE',  ( -21.05000000000000071, 69.74115727647347285, -203.5551211777124934 ) ) ;
#225873=DIRECTION ( 'NONE',  ( 0.000000000000000000, 0.000000000000000000, 1.000000000000000000 ) ) ;
#225888=ORIENTED_EDGE ( 'NONE', *, *, #185717, .T. ) ;
#225912=DIRECTION ( 'NONE',  ( 1.000000000000000000, -0.000000000000000000, 0.000000000000000000 ) ) ;
#225920=CARTESIAN_POINT ( 'NONE',  ( 21.05000000000000071, 67.22371710472012296, -191.3731074845244109 ) ) ;
#225947=CARTESIAN_POINT ( 'NONE',  ( -18.50000000000000000, 70.65875701002110532, -213.3297576910124178 ) ) ;
#225984=FACE_OUTER_BOUND ( 'NONE', #65567, .T. ) ;
#225987=LINE ( 'NONE', #47367, #200196 ) ;
#226019=FACE_OUTER_BOUND ( 'NONE', #133855, .T. ) ;
#226032=CARTESIAN_POINT ( 'NONE',  ( -18.50211644919735576, 65.69792220476374212, -164.5335554128461979 ) ) ;
#226039=CIRCLE ( 'NONE', #47165, 0.09999999999998898659 ) ;
#226113=EDGE_LOOP ( 'NONE', ( #47521, #166150, #183022, #67604 ) ) ;
#226128=CARTESIAN_POINT ( 'NONE',  ( 20.30531438145591139, 65.90309893892256810, -195.7270896772506035 ) ) ;
#226135=CARTESIAN_POINT ( 'NONE',  ( 21.09107601085585770, 75.96069283529571692, -209.8869854598850679 ) ) ;
#226138=ORIENTED_EDGE ( 'NONE', *, *, #166921, .F. ) ;
#226160=LINE ( 'NONE', #26742, #157879 ) ;
#226161=EDGE_CURVE ( 'NONE', #124945, #58661, #217295, .T. ) ;
#226175=VERTEX_POINT ( 'NONE', #141627 ) ;
#226219=VERTEX_POINT ( 'NONE', #56924 ) ;
#226237=EDGE_CURVE ( 'NONE', #203708, #41142, #196990, .T. ) ;
#226242=ORIENTED_EDGE ( 'NONE', *, *, #255479, .F. ) ;
#226261=VECTOR ( 'NONE', #17143, 1000.000000000000000 ) ;
#226277=AXIS2_PLACEMENT_3D ( 'NONE', #19850, #41982, #99340 ) ;
#226290=VERTEX_POINT ( 'NONE', #223719 ) ;
#226301=CARTESIAN_POINT ( 'NONE',  ( 18.46921299892754931, 85.50937817783642458, -196.5365287751538403 ) ) ;
#226317=ORIENTED_EDGE ( 'NONE', *, *, #119205, .T. ) ;
#226329=CARTESIAN_POINT ( 'NONE',  ( 20.94999999999999574, 77.83534155023700407, -191.8679561919613832 ) ) ;
#226337=EDGE_CURVE ( 'NONE', #94509, #10056, #34911, .T. ) ;
#226342=DIRECTION ( 'NONE',  ( 0.000000000000000000, 1.000000000000000000, 0.000000000000000000 ) ) ;
#226354=AXIS2_PLACEMENT_3D ( 'NONE', #148884, #70653, #151459 ) ;
#226355=DIRECTION ( 'NONE',  ( -7.304098846217948299E-16, -1.000000000000000000, 0.000000000000000000 ) ) ;
#226368=CIRCLE ( 'NONE', #113962, 0.09999999999999939493 ) ;
#226373=AXIS2_PLACEMENT_3D ( 'NONE', #188455, #90627, #55328 ) ;
#226378=EDGE_CURVE ( 'NONE', #229015, #165380, #193107, .T. ) ;
#226420=DIRECTION ( 'NONE',  ( 0.000000000000000000, -1.509041004344873323E-14, 1.000000000000000000 ) ) ;
#226430=DIRECTION ( 'NONE',  ( -1.000000000000000000, 0.000000000000000000, -0.000000000000000000 ) ) ;
#226432=VECTOR ( 'NONE', #199982, 1000.000000000000000 ) ;
#226469=DIRECTION ( 'NONE',  ( -1.000000000000000000, 0.000000000000000000, -0.000000000000000000 ) ) ;
#226489=VERTEX_POINT ( 'NONE', #174079 ) ;
#226501=ADVANCED_FACE ( 'NONE', ( #231456 ), #71100, .T. ) ;
#226536=ORIENTED_EDGE ( 'NONE', *, *, #187402, .T. ) ;
#226538=EDGE_CURVE ( 'NONE', #87244, #59994, #184698, .T. ) ;
#226546=EDGE_CURVE ( 'NONE', #163056, #120584, #69818, .T. ) ;
#226552=DIRECTION ( 'NONE',  ( 0.000000000000000000, 0.000000000000000000, -1.000000000000000000 ) ) ;
#226579=AXIS2_PLACEMENT_3D ( 'NONE', #90131, #133136, #131845 ) ;
#226606=AXIS2_PLACEMENT_3D ( 'NONE', #229698, #64518, #241864 ) ;
#226615=DIRECTION ( 'NONE',  ( 0.000000000000000000, 0.000000000000000000, -1.000000000000000000 ) ) ;
#226623=CARTESIAN_POINT ( 'NONE',  ( -23.25000000000000000, 84.59626168225550202, -179.4732350016745954 ) ) ;
#226641=EDGE_LOOP ( 'NONE', ( #135110, #239147, #39773, #127720 ) ) ;
#226665=EDGE_CURVE ( 'NONE', #64951, #254689, #14044, .T. ) ;
#226668=ORIENTED_EDGE ( 'NONE', *, *, #211818, .F. ) ;
#226672=EDGE_CURVE ( 'NONE', #133625, #161032, #84899, .T. ) ;
#226699=ORIENTED_EDGE ( 'NONE', *, *, #238282, .T. ) ;
#226711=CARTESIAN_POINT ( 'NONE',  ( -20.94999999999999929, 70.15000000001266756, -193.3906102602464330 ) ) ;
#226717=CARTESIAN_POINT ( 'NONE',  ( 20.94999999999999574, 69.45000000001260787, -193.6792853948412869 ) ) ;
#226776=LINE ( 'NONE', #48139, #218433 ) ;
#226795=DIRECTION ( 'NONE',  ( 1.000000000000000000, 0.000000000000000000, -0.000000000000000000 ) ) ;
#226819=ADVANCED_FACE ( 'NONE', ( #37958 ), #100442, .T. ) ;
#226825=EDGE_LOOP ( 'NONE', ( #113070, #165506, #35812, #56410, #38830 ) ) ;
#226833=CARTESIAN_POINT ( 'NONE',  ( -23.15000000000000213, 64.35000000001275566, -215.2731074845244450 ) ) ;
#226849=EDGE_LOOP ( 'NONE', ( #31, #243464, #137169, #22850 ) ) ;
#226877=ORIENTED_EDGE ( 'NONE', *, *, #255199, .F. ) ;
#226897=DIRECTION ( 'NONE',  ( -3.265361837132813093E-16, -1.000000000000000000, -6.982962677686266711E-15 ) ) ;
#226903=ORIENTED_EDGE ( 'NONE', *, *, #133915, .T. ) ;
#226907=ORIENTED_EDGE ( 'NONE', *, *, #122388, .F. ) ;
#226918=CARTESIAN_POINT ( 'NONE',  ( -20.94999999999999929, 64.25000000001264766, -196.6815067946272961 ) ) ;
#226920=ORIENTED_EDGE ( 'NONE', *, *, #197737, .T. ) ;
#226934=ADVANCED_FACE ( 'NONE', ( #144721 ), #123902, .T. ) ;
#227009=DIRECTION ( 'NONE',  ( -1.000000000000000000, -0.000000000000000000, -0.000000000000000000 ) ) ;
#227058=DIRECTION ( 'NONE',  ( 0.000000000000000000, -6.982962677686266711E-15, 1.000000000000000000 ) ) ;
#227067=VERTEX_POINT ( 'NONE', #98499 ) ;
#227070=CIRCLE ( 'NONE', #56366, 0.09999999999998898659 ) ;
#227101=ORIENTED_EDGE ( 'NONE', *, *, #26090, .F. ) ;
#227162=CIRCLE ( 'NONE', #177130, 0.09999999999998898659 ) ;
#227169=DIRECTION ( 'NONE',  ( 0.000000000000000000, 0.000000000000000000, -1.000000000000000000 ) ) ;
#227176=ORIENTED_EDGE ( 'NONE', *, *, #14964, .F. ) ;
#227181=CARTESIAN_POINT ( 'NONE',  ( -20.94999999999999929, 87.65000000001245439, -170.0231074845242745 ) ) ;
#227188=ADVANCED_FACE ( 'NONE', ( #37313 ), #213348, .F. ) ;
#227196=ORIENTED_EDGE ( 'NONE', *, *, #55615, .F. ) ;
#227206=ORIENTED_EDGE ( 'NONE', *, *, #227825, .F. ) ;
#227226=DIRECTION ( 'NONE',  ( 1.000000000000000000, 0.000000000000000000, 0.000000000000000000 ) ) ;
#227242=ADVANCED_FACE ( 'NONE', ( #196672 ), #239249, .F. ) ;
#227248=DIRECTION ( 'NONE',  ( -0.000000000000000000, 1.000000000000000000, 6.352154140967427193E-15 ) ) ;
#227249=AXIS2_PLACEMENT_3D ( 'NONE', #69566, #109949, #242080 ) ;
#227257=LINE ( 'NONE', #108599, #48646 ) ;
#227267=CYLINDRICAL_SURFACE ( 'NONE', #186758, 12.87499999999999822 ) ;
#227269=CARTESIAN_POINT ( 'NONE',  ( 20.04142135623730070, 64.35000000001254250, -182.1731074845244507 ) ) ;
#227274=CIRCLE ( 'NONE', #214802, 0.09999999999998708533 ) ;
#227280=EDGE_CURVE ( 'NONE', #41259, #209479, #130912, .T. ) ;
#227298=DIRECTION ( 'NONE',  ( 1.000000000000000000, -2.952720810173289112E-16, -2.061873921506763405E-30 ) ) ;
#227313=DIRECTION ( 'NONE',  ( 0.000000000000000000, 1.000000000000000000, 6.982962677686266711E-15 ) ) ;
#227326=EDGE_CURVE ( 'NONE', #50255, #12967, #195428, .T. ) ;
#227330=DIRECTION ( 'NONE',  ( 1.000000000000000000, 0.000000000000000000, 0.000000000000000000 ) ) ;
#227334=ORIENTED_EDGE ( 'NONE', *, *, #217958, .F. ) ;
#227336=DIRECTION ( 'NONE',  ( -1.000000000000000000, 0.000000000000000000, 0.000000000000000000 ) ) ;
#227346=CARTESIAN_POINT ( 'NONE',  ( -18.55807992284872299, 65.67101464000555211, -164.4404391622479977 ) ) ;
#227359=ADVANCED_FACE ( 'NONE', ( #75486 ), #214962, .F. ) ;
#227380=ORIENTED_EDGE ( 'NONE', *, *, #3641, .T. ) ;
#227382=ORIENTED_EDGE ( 'NONE', *, *, #63070, .F. ) ;
#227412=VECTOR ( 'NONE', #181440, 1000.000000000000000 ) ;
#227442=EDGE_LOOP ( 'NONE', ( #95388, #186496, #157907 ) ) ;
#227448=CARTESIAN_POINT ( 'NONE',  ( 21.05000000000000071, 76.10000000001272724, -210.0637644362255969 ) ) ;
#227459=ORIENTED_EDGE ( 'NONE', *, *, #25997, .T. ) ;
#227479=ORIENTED_EDGE ( 'NONE', *, *, #109038, .F. ) ;
#227495=VERTEX_POINT ( 'NONE', #170445 ) ;
#227557=ADVANCED_FACE ( 'NONE', ( #167854 ), #222655, .T. ) ;
#227584=ORIENTED_EDGE ( 'NONE', *, *, #127522, .F. ) ;
#227600=CARTESIAN_POINT ( 'NONE',  ( -21.05000000000000071, 87.65000000001266756, -200.5231074845242745 ) ) ;
#227601=FACE_OUTER_BOUND ( 'NONE', #94658, .T. ) ;
#227602=CARTESIAN_POINT ( 'NONE',  ( 18.43565242384934422, 85.51932773110506503, -196.5501311079650009 ) ) ;
#227611=CARTESIAN_POINT ( 'NONE',  ( 22.39999999999999503, 76.00000000001273293, -211.3138870828977360 ) ) ;
#227646=DIRECTION ( 'NONE',  ( -1.000000000000000000, 2.952720810173289112E-16, 2.061873921506763405E-30 ) ) ;
#227655=ADVANCED_FACE ( 'NONE', ( #158555 ), #196365, .F. ) ;
#227666=AXIS2_PLACEMENT_3D ( 'NONE', #45264, #167809, #169103 ) ;
#227674=VERTEX_POINT ( 'NONE', #19011 ) ;
#227690=AXIS2_PLACEMENT_3D ( 'NONE', #167292, #249381, #169880 ) ;
#227740=ADVANCED_FACE ( 'NONE', ( #200226 ), #166268, .F. ) ;
#227754=EDGE_LOOP ( 'NONE', ( #223516, #228237, #12467, #150623 ) ) ;
#227800=VERTEX_POINT ( 'NONE', #30597 ) ;
#227819=ORIENTED_EDGE ( 'NONE', *, *, #96691, .T. ) ;
#227823=VECTOR ( 'NONE', #105310, 1000.000000000000000 ) ;
#227825=EDGE_CURVE ( 'NONE', #158664, #16270, #28037, .T. ) ;
#227889=CARTESIAN_POINT ( 'NONE',  ( -22.00356870071802007, 75.99999999998983924, -210.7773498462519797 ) ) ;
#227894=EDGE_LOOP ( 'NONE', ( #14812, #182037, #204672, #67880 ) ) ;
#227938=AXIS2_PLACEMENT_3D ( 'NONE', #222222, #178005, #181845 ) ;
#227941=ORIENTED_EDGE ( 'NONE', *, *, #184909, .T. ) ;
#227948=CARTESIAN_POINT ( 'NONE',  ( -23.25000000000000000, 87.75000000001267608, -203.5231074845243029 ) ) ;
#227949=DIRECTION ( 'NONE',  ( 0.000000000000000000, 1.000000000000000000, 0.000000000000000000 ) ) ;
#227953=SPHERICAL_SURFACE ( 'NONE', #50057, 0.1000000000000000056 ) ;
#227975=CARTESIAN_POINT ( 'NONE',  ( 18.59999999999999076, 74.16465844978819177, -191.9679561919613775 ) ) ;
#227976=DIRECTION ( 'NONE',  ( 1.000000000000000000, 0.000000000000000000, -0.000000000000000000 ) ) ;
#228011=AXIS2_PLACEMENT_3D ( 'NONE', #185380, #184091, #225768 ) ;
#228015=DIRECTION ( 'NONE',  ( 0.000000000000000000, 1.000000000000000000, 6.352154140967427193E-15 ) ) ;
#228043=DIRECTION ( 'NONE',  ( -3.265361837132813093E-16, -1.000000000000000000, -7.026728003956683390E-15 ) ) ;
#228059=CARTESIAN_POINT ( 'NONE',  ( -18.60000000000000853, 85.36424052760351344, -196.3428589026835596 ) ) ;
#228104=AXIS2_PLACEMENT_3D ( 'NONE', #78778, #59193, #25268 ) ;
#228132=FACE_OUTER_BOUND ( 'NONE', #48319, .T. ) ;
#228133=VERTEX_POINT ( 'NONE', #227181 ) ;
#228142=VECTOR ( 'NONE', #25292, 999.9999999999998863 ) ;
#228144=DIRECTION ( 'NONE',  ( 1.000000000000000000, 0.000000000000000000, 0.000000000000000000 ) ) ;
#228147=VERTEX_POINT ( 'NONE', #31592 ) ;
#228204=ORIENTED_EDGE ( 'NONE', *, *, #180296, .T. ) ;
#228215=CARTESIAN_POINT ( 'NONE',  ( -21.05439746398122836, 64.25000000001264766, -196.5331909970394406 ) ) ;
#228229=FACE_OUTER_BOUND ( 'NONE', #149960, .T. ) ;
#228230=ADVANCED_FACE ( 'NONE', ( #190657 ), #126805, .T. ) ;
#228237=ORIENTED_EDGE ( 'NONE', *, *, #3264, .F. ) ;
#228240=CARTESIAN_POINT ( 'NONE',  ( -21.05000000000000071, 77.16270174995064224, -195.5231074845243313 ) ) ;
#228248=LINE ( 'NONE', #208694, #150780 ) ;
#228286=EDGE_CURVE ( 'NONE', #117188, #4716, #19376, .T. ) ;
#228305=CIRCLE ( 'NONE', #182523, 0.1000000000000072220 ) ;
#228317=ORIENTED_EDGE ( 'NONE', *, *, #116149, .F. ) ;
#228338=VERTEX_POINT ( 'NONE', #164022 ) ;
#228362=ADVANCED_FACE ( 'NONE', ( #47903, #162749 ), #205694, .T. ) ;
#228379=CYLINDRICAL_SURFACE ( 'NONE', #44772, 0.09999999999999939493 ) ;
#228388=EDGE_CURVE ( 'NONE', #611, #177234, #143923, .T. ) ;
#228403=VERTEX_POINT ( 'NONE', #182310 ) ;
#228438=ORIENTED_EDGE ( 'NONE', *, *, #76527, .T. ) ;
#228460=ORIENTED_EDGE ( 'NONE', *, *, #17066, .T. ) ;
#228491=AXIS2_PLACEMENT_3D ( 'NONE', #143038, #86911, #226420 ) ;
#228516=EDGE_CURVE ( 'NONE', #241603, #156110, #35799, .T. ) ;
#228517=VECTOR ( 'NONE', #159634, 1000.000000000000000 ) ;
#228562=ORIENTED_EDGE ( 'NONE', *, *, #122809, .F. ) ;
#228587=ORIENTED_EDGE ( 'NONE', *, *, #202443, .T. ) ;
#228653=CARTESIAN_POINT ( 'NONE',  ( 18.49999999999999289, 65.67426406872445455, -178.6731074845244223 ) ) ;
#228673=VERTEX_POINT ( 'NONE', #119457 ) ;
#228697=ORIENTED_EDGE ( 'NONE', *, *, #166110, .T. ) ;
#228712=ORIENTED_EDGE ( 'NONE', *, *, #45558, .T. ) ;
#228722=CIRCLE ( 'NONE', #78834, 0.09999999999999939493 ) ;
#228736=CARTESIAN_POINT ( 'NONE',  ( -20.64999999999999858, 85.40000000001262492, -193.6291383618718385 ) ) ;
#228745=EDGE_LOOP ( 'NONE', ( #75507, #144576, #98765, #14042 ) ) ;
#228746=TOROIDAL_SURFACE ( 'NONE', #103617, 11.90000000000000213, 0.1000000000000000056 ) ;
#228748=DIRECTION ( 'NONE',  ( 0.000000000000000000, 0.000000000000000000, 1.000000000000000000 ) ) ;
#228759=CARTESIAN_POINT ( 'NONE',  ( 21.05000000000000071, 76.02138556595068053, -209.8280685972093522 ) ) ;
#228774=DIRECTION ( 'NONE',  ( 0.000000000000000000, -6.982962677686266711E-15, 1.000000000000000000 ) ) ;
#228804=FACE_OUTER_BOUND ( 'NONE', #14423, .T. ) ;
#228809=CARTESIAN_POINT ( 'NONE',  ( -21.05000000000000071, 77.83534155023700407, -191.9679561919613491 ) ) ;
#228815=CIRCLE ( 'NONE', #3947, 0.8750000000000007772 ) ;
#228840=ORIENTED_EDGE ( 'NONE', *, *, #56042, .F. ) ;
#228842=ADVANCED_FACE ( 'NONE', ( #163712 ), #65003, .T. ) ;
#228852=CARTESIAN_POINT ( 'NONE',  ( -21.55000000000000426, 68.29142135624991283, -191.1731074845243938 ) ) ;
#228864=AXIS2_PLACEMENT_3D ( 'NONE', #180566, #77574, #140126 ) ;
#228872=DIRECTION ( 'NONE',  ( 0.000000000000000000, 1.000000000000000000, 0.000000000000000000 ) ) ;
#228898=ADVANCED_FACE ( 'NONE', ( #252216 ), #177475, .F. ) ;
#228949=CARTESIAN_POINT ( 'NONE',  ( 21.05000000000000071, 69.35000000001259934, -191.3731074845244109 ) ) ;
#229015=VERTEX_POINT ( 'NONE', #79981 ) ;
#229062=CARTESIAN_POINT ( 'NONE',  ( 18.59999999999999787, 86.35479209693788505, -176.2665665014505407 ) ) ;
#229087=DIRECTION ( 'NONE',  ( 0.000000000000000000, 0.000000000000000000, 1.000000000000000000 ) ) ;
#229110=CARTESIAN_POINT ( 'NONE',  ( 21.93340585971889212, 68.67585297715770309, -203.5231074845244166 ) ) ;
#229141=CIRCLE ( 'NONE', #120834, 7.899999999999990585 ) ;
#229168=ORIENTED_EDGE ( 'NONE', *, *, #184548, .F. ) ;
#229183=CARTESIAN_POINT ( 'NONE',  ( -21.07016717457011268, 76.00000000001274714, -209.8440483226252411 ) ) ;
#229203=VERTEX_POINT ( 'NONE', #83819 ) ;
#229248=FACE_OUTER_BOUND ( 'NONE', #78031, .T. ) ;
#229304=CARTESIAN_POINT ( 'NONE',  ( -23.15000000000000213, 64.35000000001249987, -177.0379132551784096 ) ) ;
#229314=TOROIDAL_SURFACE ( 'NONE', #220899, 11.65000000000000036, 0.1000000000000000056 ) ;
#229331=CIRCLE ( 'NONE', #129360, 0.09999999999999939493 ) ;
#229336=LINE ( 'NONE', #154947, #255934 ) ;
#229349=DIRECTION ( 'NONE',  ( 1.000000000000000000, -0.000000000000000000, 0.000000000000000000 ) ) ;
#229361=DIRECTION ( 'NONE',  ( 1.000000000000000000, 0.000000000000000000, 0.000000000000000000 ) ) ;
#229396=CARTESIAN_POINT ( 'NONE',  ( -18.59999999999999787, 64.35000000001264198, -196.5083017138704236 ) ) ;
#229400=CIRCLE ( 'NONE', #116954, 0.09999999999998898659 ) ;
#229430=CARTESIAN_POINT ( 'NONE',  ( 19.99999999999998934, 64.25000000001253397, -182.1731074845244507 ) ) ;
#229434=EDGE_LOOP ( 'NONE', ( #222601, #205262, #53793 ) ) ;
#229473=ORIENTED_EDGE ( 'NONE', *, *, #182176, .F. ) ;
#229481=FACE_OUTER_BOUND ( 'NONE', #249793, .T. ) ;
#229483=FACE_OUTER_BOUND ( 'NONE', #204807, .T. ) ;
#229536=ORIENTED_EDGE ( 'NONE', *, *, #35440, .F. ) ;
#229577=AXIS2_PLACEMENT_3D ( 'NONE', #189386, #66867, #167282 ) ;
#229590=DIRECTION ( 'NONE',  ( 0.000000000000000000, 5.956132106358139644E-15, -1.000000000000000000 ) ) ;
#229597=ORIENTED_EDGE ( 'NONE', *, *, #110386, .T. ) ;
#229695=CARTESIAN_POINT ( 'NONE',  ( 21.05000000000000071, 71.00000000001253397, -182.4283735034374843 ) ) ;
#229698=CARTESIAN_POINT ( 'NONE',  ( -20.64999999999999858, 71.65000000001253966, -182.3731074845244109 ) ) ;
#229701=LINE ( 'NONE', #14527, #223495 ) ;
#229716=ORIENTED_EDGE ( 'NONE', *, *, #57682, .F. ) ;
#229739=DIRECTION ( 'NONE',  ( 0.000000000000000000, 0.000000000000000000, 1.000000000000000000 ) ) ;
#229749=CARTESIAN_POINT ( 'NONE',  ( -21.04999999999988347, 69.69982018209628905, -203.5745903664068521 ) ) ;
#229769=ORIENTED_EDGE ( 'NONE', *, *, #38779, .T. ) ;
#229779=ORIENTED_EDGE ( 'NONE', *, *, #57861, .F. ) ;
#229806=LINE ( 'NONE', #26492, #24281 ) ;
#229826=DIRECTION ( 'NONE',  ( -1.000000000000000000, -0.000000000000000000, -0.000000000000000000 ) ) ;
#229838=ORIENTED_EDGE ( 'NONE', *, *, #63809, .F. ) ;
#229852=AXIS2_PLACEMENT_3D ( 'NONE', #218776, #160130, #196653 ) ;
#229855=ORIENTED_EDGE ( 'NONE', *, *, #108829, .T. ) ;
#229876=CARTESIAN_POINT ( 'NONE',  ( 21.14999999999999503, 76.00000000001267608, -203.5231074845243597 ) ) ;
#229880=ORIENTED_EDGE ( 'NONE', *, *, #146211, .T. ) ;
#229895=( BOUNDED_SURFACE ( )  B_SPLINE_SURFACE ( 3, 2, ( 
 ( #222799, #125015, #241121 ),
 ( #44196, #144549, #123727 ),
 ( #224088, #141986, #23369 ),
 ( #139407, #182426, #41636 ),
 ( #140708, #242371, #220270 ),
 ( #221512, #199427, #178591 ) ),
 .UNSPECIFIED., .F., .F., .F. ) 
 B_SPLINE_SURFACE_WITH_KNOTS ( ( 4, 2, 4 ),
 ( 3, 3 ),
 ( 3.141592653589783346, 3.926990816987233845, 4.712388980384684345 ),
 ( 0.000000000000000000, 1.000000000000000000 ),
 .UNSPECIFIED. ) 
 GEOMETRIC_REPRESENTATION_ITEM ( )  RATIONAL_B_SPLINE_SURFACE ( (
 ( 1.000000000000000000, 0.9238795325112774126, 1.000000000000000000),
 ( 1.000000000000000000, 0.9240297172244186230, 1.000000000000000000),
 ( 1.000000000000000000, 0.9038128468038687524, 1.000000000000000000),
 ( 1.000000000000000000, 0.8282379607649484887, 1.000000000000000000),
 ( 1.000000000000000000, 0.7727932973490982960, 1.000000000000000000),
 ( 1.000000000000000000, 0.7071067811866457165, 1.000000000000000000) ) ) 
 REPRESENTATION_ITEM ( '' )  SURFACE ( )  );
#229904=DIRECTION ( 'NONE',  ( 0.000000000000000000, 0.000000000000000000, 1.000000000000000000 ) ) ;
#229906=DIRECTION ( 'NONE',  ( -1.000000000000000000, 2.952720810173289112E-16, 2.061873921506763405E-30 ) ) ;
#229943=CARTESIAN_POINT ( 'NONE',  ( -20.94999999999999929, 68.97833521811233481, -166.3895420826271163 ) ) ;
#229992=LINE ( 'NONE', #168792, #212299 ) ;
#230013=CARTESIAN_POINT ( 'NONE',  ( 20.51284917709620359, 65.68911337716731680, -195.8506342989327038 ) ) ;
#230041=EDGE_CURVE ( 'NONE', #48255, #54936, #84488, .T. ) ;
#230042=EDGE_LOOP ( 'NONE', ( #228438, #141588, #50810, #46945 ) ) ;
#230071=VERTEX_POINT ( 'NONE', #104077 ) ;
#230088=ORIENTED_EDGE ( 'NONE', *, *, #181829, .T. ) ;
#230108=VERTEX_POINT ( 'NONE', #69803 ) ;
#230114=ORIENTED_EDGE ( 'NONE', *, *, #79147, .F. ) ;
#230122=ORIENTED_EDGE ( 'NONE', *, *, #141247, .T. ) ;
#230132=DIRECTION ( 'NONE',  ( 1.000000000000000000, 0.000000000000000000, 0.000000000000000000 ) ) ;
#230185=DIRECTION ( 'NONE',  ( 1.000000000000000000, -2.952720810173289112E-16, -2.061873921506763405E-30 ) ) ;
#230210=CIRCLE ( 'NONE', #72009, 0.1000000000000141609 ) ;
#230275=DIRECTION ( 'NONE',  ( 0.000000000000000000, 1.000000000000000000, 0.000000000000000000 ) ) ;
#230292=CYLINDRICAL_SURFACE ( 'NONE', #43465, 0.09999999999999939493 ) ;
#230336=EDGE_CURVE ( 'NONE', #210483, #87546, #100850, .T. ) ;
#230341=VERTEX_POINT ( 'NONE', #117886 ) ;
#230353=ORIENTED_EDGE ( 'NONE', *, *, #182440, .T. ) ;
#230356=DIRECTION ( 'NONE',  ( 0.000000000000000000, -6.982962677686266711E-15, 1.000000000000000000 ) ) ;
#230381=ORIENTED_EDGE ( 'NONE', *, *, #161425, .T. ) ;
#230397=AXIS2_PLACEMENT_3D ( 'NONE', #121529, #139754, #24990 ) ;
#230398=CARTESIAN_POINT ( 'NONE',  ( -21.05000000000000071, 87.48912529308871910, -200.5231074845242745 ) ) ;
#230433=ORIENTED_EDGE ( 'NONE', *, *, #255406, .T. ) ;
#230449=ORIENTED_EDGE ( 'NONE', *, *, #68496, .F. ) ;
#230488=EDGE_CURVE ( 'NONE', #183114, #50587, #69471, .T. ) ;
#230524=LINE ( 'NONE', #74044, #207026 ) ;
#230538=ADVANCED_FACE ( 'NONE', ( #151618 ), #188150, .F. ) ;
#230541=FACE_OUTER_BOUND ( 'NONE', #128444, .T. ) ;
#230545=LINE ( 'NONE', #233132, #82034 ) ;
#230562=AXIS2_PLACEMENT_3D ( 'NONE', #207376, #246482, #147387 ) ;
#230572=AXIS2_PLACEMENT_3D ( 'NONE', #120253, #21141, #100608 ) ;
#230617=ORIENTED_EDGE ( 'NONE', *, *, #118562, .T. ) ;
#230625=CARTESIAN_POINT ( 'NONE',  ( -23.15000000000000213, 73.40000000001276703, -215.2731074845243882 ) ) ;
#230632=EDGE_LOOP ( 'NONE', ( #66025, #19479, #174281, #224171 ) ) ;
#230669=CARTESIAN_POINT ( 'NONE',  ( -23.25000000000000000, 73.40000000001253966, -183.2477294072864709 ) ) ;
#230691=CARTESIAN_POINT ( 'NONE',  ( -20.94999999999999929, 77.16412189325360771, -162.1082593989527254 ) ) ;
#230736=AXIS2_PLACEMENT_3D ( 'NONE', #205909, #208506, #27322 ) ;
#230738=CARTESIAN_POINT ( 'NONE',  ( 23.15000000000000213, 85.00000000001251976, -179.9170766071767389 ) ) ;
#230742=CIRCLE ( 'NONE', #126679, 12.97499999999998721 ) ;
#230743=ORIENTED_EDGE ( 'NONE', *, *, #214149, .T. ) ;
#230762=ORIENTED_EDGE ( 'NONE', *, *, #74158, .T. ) ;
#230773=AXIS2_PLACEMENT_3D ( 'NONE', #24028, #184352, #46130 ) ;
#230776=LINE ( 'NONE', #194226, #249023 ) ;
#230810=AXIS2_PLACEMENT_3D ( 'NONE', #195738, #113605, #193157 ) ;
#230833=DIRECTION ( 'NONE',  ( -1.000000000000000000, -0.000000000000000000, -0.000000000000000000 ) ) ;
#230834=ORIENTED_EDGE ( 'NONE', *, *, #18643, .T. ) ;
#230848=DIRECTION ( 'NONE',  ( -1.000000000000000000, -0.000000000000000000, -0.000000000000000000 ) ) ;
#230864=EDGE_CURVE ( 'NONE', #52949, #10056, #11198, .T. ) ;
#230879=ORIENTED_EDGE ( 'NONE', *, *, #172767, .F. ) ;
#230896=ORIENTED_EDGE ( 'NONE', *, *, #153407, .T. ) ;
#230934=DIRECTION ( 'NONE',  ( 0.000000000000000000, -6.938893903907222067E-15, 1.000000000000000000 ) ) ;
#230948=CARTESIAN_POINT ( 'NONE',  ( -20.94999999999999929, 77.16270174995064224, -195.4231074845243370 ) ) ;
#230952=EDGE_CURVE ( 'NONE', #18724, #108178, #53056, .T. ) ;
#230966=ORIENTED_EDGE ( 'NONE', *, *, #225080, .T. ) ;
#231007=ADVANCED_FACE ( 'NONE', ( #19731 ), #140963, .F. ) ;
#231047=VERTEX_POINT ( 'NONE', #123966 ) ;
#231054=AXIS2_PLACEMENT_3D ( 'NONE', #12952, #93743, #170770 ) ;
#231065=CARTESIAN_POINT ( 'NONE',  ( 23.14999999999999503, 69.55000000001277272, -215.2731074845244166 ) ) ;
#231086=CIRCLE ( 'NONE', #22981, 0.09999999999999939493 ) ;
#231103=DIRECTION ( 'NONE',  ( 0.000000000000000000, 0.000000000000000000, -1.000000000000000000 ) ) ;
#231157=FACE_OUTER_BOUND ( 'NONE', #70935, .T. ) ;
#231164=AXIS2_PLACEMENT_3D ( 'NONE', #134357, #17016, #54823 ) ;
#231183=CARTESIAN_POINT ( 'NONE',  ( 18.49999999999999645, 77.83585931145600512, -158.5186683157258187 ) ) ;
#231185=DIRECTION ( 'NONE',  ( 2.557131231893037478E-16, 0.8660254037844420383, -0.4999999999999942824 ) ) ;
#231210=CARTESIAN_POINT ( 'NONE',  ( -23.15000000000000213, 85.60000000001252829, -179.9170766071767389 ) ) ;
#231231=CARTESIAN_POINT ( 'NONE',  ( -21.14999999999999858, 76.00000000001267608, -203.5231074845243597 ) ) ;
#231250=CIRCLE ( 'NONE', #14779, 0.09999999999998898659 ) ;
#231251=VECTOR ( 'NONE', #7163, 1000.000000000000000 ) ;
#231265=ADVANCED_FACE ( 'NONE', ( #173402, #53401 ), #35163, .T. ) ;
#231276=ORIENTED_EDGE ( 'NONE', *, *, #47224, .T. ) ;
#231286=DIRECTION ( 'NONE',  ( 0.000000000000000000, -6.517943393102675675E-15, 1.000000000000000000 ) ) ;
#231325=EDGE_CURVE ( 'NONE', #69740, #46643, #41563, .T. ) ;
#231346=ORIENTED_EDGE ( 'NONE', *, *, #212430, .T. ) ;
#231353=ORIENTED_EDGE ( 'NONE', *, *, #212074, .F. ) ;
#231366=B_SPLINE_CURVE_WITH_KNOTS ( 'NONE', 3,
 ( #160362, #237306, #80767, #22124, #241164, #216441, #58637 ),
 .UNSPECIFIED., .F., .F.,
 ( 4, 3, 4 ),
 ( 0.000000000000000000, 3.357501770814703122E-05, 5.199112466349482939E-05 ),
 .UNSPECIFIED. ) ;
#231374=ORIENTED_EDGE ( 'NONE', *, *, #169386, .T. ) ;
#231383=EDGE_CURVE ( 'NONE', #224589, #135929, #165705, .T. ) ;
#231389=DIRECTION ( 'NONE',  ( 0.000000000000000000, 0.9915357197604982575, -0.1298341882519033486 ) ) ;
#231415=AXIS2_PLACEMENT_3D ( 'NONE', #65131, #3884, #40486 ) ;
#231456=FACE_OUTER_BOUND ( 'NONE', #1414, .T. ) ;
#231511=CIRCLE ( 'NONE', #189809, 7.899999999999990585 ) ;
#231515=DIRECTION ( 'NONE',  ( 1.000000000000000000, 0.000000000000000000, 0.000000000000000000 ) ) ;
#231534=ORIENTED_EDGE ( 'NONE', *, *, #52889, .T. ) ;
#231540=DIRECTION ( 'NONE',  ( 0.000000000000000000, -1.000000000000000000, 0.000000000000000000 ) ) ;
#231595=EDGE_CURVE ( 'NONE', #218193, #135203, #219830, .T. ) ;
#231608=CARTESIAN_POINT ( 'NONE',  ( 23.14999999999999858, 70.40000000001261071, -191.1178414656113205 ) ) ;
#231609=ORIENTED_EDGE ( 'NONE', *, *, #126837, .T. ) ;
#231614=AXIS2_PLACEMENT_3D ( 'NONE', #223659, #240671, #62051 ) ;
#231694=VECTOR ( 'NONE', #214448, 1000.000000000000000 ) ;
#231711=EDGE_CURVE ( 'NONE', #53690, #146901, #28544, .T. ) ;
#231720=CARTESIAN_POINT ( 'NONE',  ( -23.15000000000000213, 74.00000000001254818, -183.2477294072864709 ) ) ;
#231754=FACE_OUTER_BOUND ( 'NONE', #113825, .T. ) ;
#231763=DIRECTION ( 'NONE',  ( -0.000000000000000000, 1.000000000000000000, 6.982962677686266711E-15 ) ) ;
#231771=EDGE_CURVE ( 'NONE', #196072, #119302, #32630, .T. ) ;
#231825=EDGE_CURVE ( 'NONE', #63242, #199384, #21669, .T. ) ;
#231853=CARTESIAN_POINT ( 'NONE',  ( -23.15000000000000213, 71.65000000001259650, -191.1731074845243654 ) ) ;
#231904=DIRECTION ( 'NONE',  ( -1.000000000000000000, 1.836970198721029934E-16, 1.601412966608202925E-30 ) ) ;
#231907=CIRCLE ( 'NONE', #119469, 11.64999999999999325 ) ;
#231929=ORIENTED_EDGE ( 'NONE', *, *, #26073, .T. ) ;
#231991=DIRECTION ( 'NONE',  ( 0.000000000000000000, 0.4999999999999088507, -0.8660254037844913322 ) ) ;
#232001=VECTOR ( 'NONE', #160859, 1000.000000000000000 ) ;
#232016=DIRECTION ( 'NONE',  ( -0.000000000000000000, 0.4791956752371485107, 0.8777080977375185666 ) ) ;
#232018=ORIENTED_EDGE ( 'NONE', *, *, #228286, .T. ) ;
#232039=VERTEX_POINT ( 'NONE', #237532 ) ;
#232056=FACE_OUTER_BOUND ( 'NONE', #12688, .T. ) ;
#232073=AXIS2_PLACEMENT_3D ( 'NONE', #138128, #201982, #97707 ) ;
#232089=CARTESIAN_POINT ( 'NONE',  ( 18.50596464788227280, 65.69367753730708159, -164.5189238066348594 ) ) ;
#232126=EDGE_CURVE ( 'NONE', #242379, #181359, #7837, .T. ) ;
#232136=ORIENTED_EDGE ( 'NONE', *, *, #13517, .T. ) ;
#232154=FACE_OUTER_BOUND ( 'NONE', #169826, .T. ) ;
#232165=EDGE_CURVE ( 'NONE', #97927, #67516, #70402, .T. ) ;
#232255=CARTESIAN_POINT ( 'NONE',  ( 21.14999999999999503, 76.10000000001276987, -215.1726782920691505 ) ) ;
#232291=CARTESIAN_POINT ( 'NONE',  ( 20.95443524775735256, 67.12144573613981891, -194.9893852089242898 ) ) ;
#232295=EDGE_CURVE ( 'NONE', #188235, #141837, #49522, .T. ) ;
#232300=VECTOR ( 'NONE', #117807, 1000.000000000000114 ) ;
#232308=DIRECTION ( 'NONE',  ( 1.000000000000000000, 0.000000000000000000, 0.000000000000000000 ) ) ;
#232334=ORIENTED_EDGE ( 'NONE', *, *, #93748, .F. ) ;
#232348=EDGE_LOOP ( 'NONE', ( #51279, #1424, #51659, #168479 ) ) ;
#232362=EDGE_LOOP ( 'NONE', ( #141533, #9104, #103048, #58479 ) ) ;
#232374=ORIENTED_EDGE ( 'NONE', *, *, #127465, .F. ) ;
#232400=EDGE_CURVE ( 'NONE', #252282, #183838, #157908, .T. ) ;
#232406=ORIENTED_EDGE ( 'NONE', *, *, #211818, .T. ) ;
#232418=CARTESIAN_POINT ( 'NONE',  ( -23.25000000000000000, 64.35000000001254250, -182.1731074845244507 ) ) ;
#232434=CARTESIAN_POINT ( 'NONE',  ( 23.14999999999999858, 78.00000000001244871, -170.0231074845243313 ) ) ;
#232449=CARTESIAN_POINT ( 'NONE',  ( -20.94999999999999929, 77.13501884592258762, -162.3061306010920362 ) ) ;
#232493=CARTESIAN_POINT ( 'NONE',  ( 20.89192007715128341, 65.67101464000555211, -164.4404391622479977 ) ) ;
#232507=CARTESIAN_POINT ( 'NONE',  ( -21.14999999999999858, 76.10000000001276987, -215.1726782920691505 ) ) ;
#232509=CYLINDRICAL_SURFACE ( 'NONE', #140573, 0.1000000000000026007 ) ;
#232530=CIRCLE ( 'NONE', #7071, 0.09999999999998898659 ) ;
#232531=ORIENTED_EDGE ( 'NONE', *, *, #53846, .F. ) ;
#232557=DIRECTION ( 'NONE',  ( -0.000000000000000000, 6.982962677686266711E-15, -1.000000000000000000 ) ) ;
#232586=VECTOR ( 'NONE', #2793, 1000.000000000000000 ) ;
#232599=CARTESIAN_POINT ( 'NONE',  ( 18.59999999999999432, 74.83729825007462466, -195.5231074845243597 ) ) ;
#232603=CIRCLE ( 'NONE', #228491, 12.87499999999999822 ) ;
#232698=AXIS2_PLACEMENT_3D ( 'NONE', #91286, #189096, #169578 ) ;
#232730=ADVANCED_FACE ( 'NONE', ( #219907 ), #8027, .F. ) ;
#232740=ORIENTED_EDGE ( 'NONE', *, *, #175324, .T. ) ;
#232757=CARTESIAN_POINT ( 'NONE',  ( -23.25000000000000000, 71.75000000001253397, -182.3731074845244109 ) ) ;
#232767=CARTESIAN_POINT ( 'NONE',  ( -18.59999999999999787, 76.00000000001244871, -170.0231074845243597 ) ) ;
#232795=DIRECTION ( 'NONE',  ( -0.000000000000000000, -1.000000000000000000, -6.982962677686266711E-15 ) ) ;
#232796=CIRCLE ( 'NONE', #195386, 0.09999999999999344136 ) ;
#232799=ADVANCED_FACE ( 'NONE', ( #65970 ), #133100, .F. ) ;
#232852=DIRECTION ( 'NONE',  ( -0.000000000000000000, -6.982962677686266711E-15, 1.000000000000000000 ) ) ;
#232901=DIRECTION ( 'NONE',  ( 1.000000000000000000, 0.000000000000000000, 0.000000000000000000 ) ) ;
#232921=DIRECTION ( 'NONE',  ( 0.000000000000000000, 0.000000000000000000, 1.000000000000000000 ) ) ;
#232923=ORIENTED_EDGE ( 'NONE', *, *, #140315, .T. ) ;
#232924=DIRECTION ( 'NONE',  ( 0.000000000000000000, 0.000000000000000000, 1.000000000000000000 ) ) ;
#232929=CARTESIAN_POINT ( 'NONE',  ( -23.15000000000000213, 73.40000000001259650, -190.2984855617622770 ) ) ;
#232959=ORIENTED_EDGE ( 'NONE', *, *, #89287, .F. ) ;
#232997=ADVANCED_FACE ( 'NONE', ( #211915 ), #88067, .T. ) ;
#233021=CIRCLE ( 'NONE', #120597, 11.74999999999999645 ) ;
#233032=ADVANCED_FACE ( 'NONE', ( #227601 ), #216472, .F. ) ;
#233057=ORIENTED_EDGE ( 'NONE', *, *, #97780, .F. ) ;
#233060=VERTEX_POINT ( 'NONE', #89365 ) ;
#233090=ADVANCED_FACE ( 'NONE', ( #114068 ), #245529, .F. ) ;
#233110=DIRECTION ( 'NONE',  ( -0.000000000000000000, 6.982962677686266711E-15, -1.000000000000000000 ) ) ;
#233116=DIRECTION ( 'NONE',  ( 1.000000000000000000, 0.000000000000000000, 0.000000000000000000 ) ) ;
#233122=ORIENTED_EDGE ( 'NONE', *, *, #149709, .T. ) ;
#233127=CARTESIAN_POINT ( 'NONE',  ( -20.54999999999999716, 71.65000000001256808, -186.7731074845243882 ) ) ;
#233128=DIRECTION ( 'NONE',  ( -1.000000000000000000, 3.265361837132813093E-16, 2.280189983783949500E-30 ) ) ;
#233132=CARTESIAN_POINT ( 'NONE',  ( -21.05000000000000071, 74.16465844978819177, -191.8679561919614116 ) ) ;
#233165=FACE_OUTER_BOUND ( 'NONE', #135806, .T. ) ;
#233171=AXIS2_PLACEMENT_3D ( 'NONE', #241517, #62877, #164560 ) ;
#233192=AXIS2_PLACEMENT_3D ( 'NONE', #184652, #244626, #68576 ) ;
#233224=DIRECTION ( 'NONE',  ( 0.000000000000000000, -7.116814260417693756E-15, 1.000000000000000000 ) ) ;
#233247=CARTESIAN_POINT ( 'NONE',  ( 22.47071067811865319, 75.90090754531013317, -211.2431822290224090 ) ) ;
#233248=VERTEX_POINT ( 'NONE', #46086 ) ;
#233345=CARTESIAN_POINT ( 'NONE',  ( 21.05000000000000071, 70.15000000001266756, -193.3906102602464330 ) ) ;
#233353=DIRECTION ( 'NONE',  ( 0.000000000000000000, -2.775557561562888827E-14, 1.000000000000000000 ) ) ;
#233373=VERTEX_POINT ( 'NONE', #231183 ) ;
#233381=CARTESIAN_POINT ( 'NONE',  ( 18.58222699835054570, 65.66799936921584901, -164.4299399888601272 ) ) ;
#233387=ORIENTED_EDGE ( 'NONE', *, *, #131256, .T. ) ;
#233417=CARTESIAN_POINT ( 'NONE',  ( 21.05000000000000071, 76.00000000001247713, -174.0231074845243882 ) ) ;
#233418=CARTESIAN_POINT ( 'NONE',  ( 21.05000000000000071, 76.00000000001259082, -190.5481074845243654 ) ) ;
#233419=CARTESIAN_POINT ( 'NONE',  ( -20.00857864376270001, 66.65000000001253966, -182.3731074845244393 ) ) ;
#233462=ORIENTED_EDGE ( 'NONE', *, *, #180589, .T. ) ;
#233494=AXIS2_PLACEMENT_3D ( 'NONE', #122707, #257006, #182676 ) ;
#233499=AXIS2_PLACEMENT_3D ( 'NONE', #177286, #254201, #237230 ) ;
#233507=DIRECTION ( 'NONE',  ( 0.000000000000000000, -6.982962677686266711E-15, 1.000000000000000000 ) ) ;
#233527=CARTESIAN_POINT ( 'NONE',  ( 22.49999999999999645, 64.35042919246788529, -203.6231074845244393 ) ) ;
#233540=ORIENTED_EDGE ( 'NONE', *, *, #198549, .F. ) ;
#233544=CARTESIAN_POINT ( 'NONE',  ( 20.94999999999999929, 69.55000000001261640, -193.5060803140843859 ) ) ;
#233553=DIRECTION ( 'NONE',  ( -2.952720810173289112E-16, -1.000000000000000000, -6.982962677686266711E-15 ) ) ;
#233573=AXIS2_PLACEMENT_3D ( 'NONE', #121005, #161402, #178411 ) ;
#233614=ORIENTED_EDGE ( 'NONE', *, *, #204837, .F. ) ;
#233634=CARTESIAN_POINT ( 'NONE',  ( 22.39999999999999503, 76.10000000001276987, -215.1726782920691505 ) ) ;
#233654=ORIENTED_EDGE ( 'NONE', *, *, #150565, .F. ) ;
#233683=ORIENTED_EDGE ( 'NONE', *, *, #135882, .T. ) ;
#233695=CARTESIAN_POINT ( 'NONE',  ( -23.25000000000000000, 84.59626168225560150, -194.0729799673740104 ) ) ;
#233697=EDGE_CURVE ( 'NONE', #18425, #160419, #111882, .T. ) ;
#233722=ORIENTED_EDGE ( 'NONE', *, *, #111288, .F. ) ;
#233758=CARTESIAN_POINT ( 'NONE',  ( -22.39999999999999858, 64.35000000001268461, -203.6231074845244393 ) ) ;
#233765=ADVANCED_FACE ( 'NONE', ( #230541 ), #51870, .F. ) ;
#233799=TOROIDAL_SURFACE ( 'NONE', #42245, 11.70000000000000107, 0.1000000000000000056 ) ;
#233819=DIRECTION ( 'NONE',  ( 0.000000000000000000, 0.9999176327611370985, -0.01283462868041286391 ) ) ;
#233848=CARTESIAN_POINT ( 'NONE',  ( -21.14999999999999858, 69.45934304831143891, -203.4231074845244223 ) ) ;
#233880=DIRECTION ( 'NONE',  ( 1.000000000000000000, 0.000000000000000000, 0.000000000000000000 ) ) ;
#233911=DIRECTION ( 'NONE',  ( 0.000000000000000000, -6.608470384673536035E-15, 1.000000000000000000 ) ) ;
#233912=CIRCLE ( 'NONE', #92258, 4.049999999999998046 ) ;
#233930=DIRECTION ( 'NONE',  ( 1.000000000000000000, 0.000000000000000000, 0.000000000000000000 ) ) ;
#233939=EDGE_LOOP ( 'NONE', ( #104516, #205827, #56544, #211661 ) ) ;
#233950=DIRECTION ( 'NONE',  ( -1.000000000000000000, -0.000000000000000000, -0.000000000000000000 ) ) ;
#233960=AXIS2_PLACEMENT_3D ( 'NONE', #41929, #165726, #127868 ) ;
#233965=ORIENTED_EDGE ( 'NONE', *, *, #200583, .F. ) ;
#234058=DIRECTION ( 'NONE',  ( 7.304098846218134667E-16, 1.000000000000000000, 6.982962677686267499E-15 ) ) ;
#234100=DIRECTION ( 'NONE',  ( 1.000000000000000000, 0.000000000000000000, 0.000000000000000000 ) ) ;
#234108=AXIS2_PLACEMENT_3D ( 'NONE', #130769, #154239, #235018 ) ;
#234128=DIRECTION ( 'NONE',  ( 1.000000000000000000, -7.304098846218134667E-16, -5.100424963727255829E-30 ) ) ;
#234144=FACE_OUTER_BOUND ( 'NONE', #24003, .T. ) ;
#234183=VERTEX_POINT ( 'NONE', #208113 ) ;
#234184=CARTESIAN_POINT ( 'NONE',  ( 22.39999999999999858, 68.20922040163929978, -203.6231074845244109 ) ) ;
#234185=ORIENTED_EDGE ( 'NONE', *, *, #190420, .T. ) ;
#234218=CARTESIAN_POINT ( 'NONE',  ( -20.15000000000000568, 66.70857864377522617, -182.3731074845244393 ) ) ;
#234248=AXIS2_PLACEMENT_3D ( 'NONE', #91762, #73511, #231286 ) ;
#234250=AXIS2_PLACEMENT_3D ( 'NONE', #209940, #93818, #174700 ) ;
#234251=FACE_OUTER_BOUND ( 'NONE', #512, .T. ) ;
#234255=DIRECTION ( 'NONE',  ( 0.000000000000000000, 0.000000000000000000, 1.000000000000000000 ) ) ;
#234282=DIRECTION ( 'NONE',  ( 0.000000000000000000, -6.982962677686266711E-15, 1.000000000000000000 ) ) ;
#234320=EDGE_LOOP ( 'NONE', ( #28612, #29045, #165045, #75178 ) ) ;
#234338=SPHERICAL_SURFACE ( 'NONE', #218324, 0.1000000000000000056 ) ;
#234353=FACE_OUTER_BOUND ( 'NONE', #240737, .T. ) ;
#234370=DIRECTION ( 'NONE',  ( 0.000000000000000000, 0.1350103645451974088, -0.9908441862701587999 ) ) ;
#234457=ORIENTED_EDGE ( 'NONE', *, *, #149709, .F. ) ;
#234461=VERTEX_POINT ( 'NONE', #22754 ) ;
#234466=ADVANCED_FACE ( 'NONE', ( #104794 ), #85232, .T. ) ;
#234477=EDGE_LOOP ( 'NONE', ( #228204, #130577, #28300, #95575, #100673, #206545, #131880, #190989, #138938, #160832, #196544 ) ) ;
#234490=CARTESIAN_POINT ( 'NONE',  ( -21.07928932188134041, 69.67148334361938566, -203.6220026301787982 ) ) ;
#234524=EDGE_CURVE ( 'NONE', #115598, #203961, #138202, .T. ) ;
#234545=CARTESIAN_POINT ( 'NONE',  ( -20.85000000000000142, 76.00000000001244871, -170.0231074845243597 ) ) ;
#234549=ADVANCED_FACE ( 'NONE', ( #236040 ), #121279, .F. ) ;
#234575=FACE_OUTER_BOUND ( 'NONE', #173114, .T. ) ;
#234609=CARTESIAN_POINT ( 'NONE',  ( -21.05000000000000071, 74.75000000001261924, -195.5231074845243597 ) ) ;
#234626=DIRECTION ( 'NONE',  ( -1.000000000000000000, 3.265361837132813093E-16, 2.280189983783949500E-30 ) ) ;
#234649=DIRECTION ( 'NONE',  ( 0.000000000000000000, 0.000000000000000000, 1.000000000000000000 ) ) ;
#234658=CARTESIAN_POINT ( 'NONE',  ( -20.94999999999999929, 87.65000000001266756, -200.4231074845242802 ) ) ;
#234684=DIRECTION ( 'NONE',  ( 1.000000000000000000, 0.000000000000000000, 0.000000000000000000 ) ) ;
#234694=EDGE_CURVE ( 'NONE', #44671, #230071, #192282, .T. ) ;
#234698=DIRECTION ( 'NONE',  ( 0.000000000000000000, -6.982962677686266711E-15, 1.000000000000000000 ) ) ;
#234732=DIRECTION ( 'NONE',  ( -5.603264701231743991E-32, -7.172728831056617961E-15, 1.000000000000000000 ) ) ;
#234737=DIRECTION ( 'NONE',  ( -0.000000000000000000, 0.8700118002898356018, -0.4930308989875170078 ) ) ;
#234741=ADVANCED_FACE ( 'NONE', ( #193728 ), #233799, .F. ) ;
#234768=DIRECTION ( 'NONE',  ( -1.000000000000000000, 0.000000000000000000, 0.000000000000000000 ) ) ;
#234796=CARTESIAN_POINT ( 'NONE',  ( -21.14999999999999858, 64.25000000001263345, -196.7392418215462726 ) ) ;
#234812=FACE_OUTER_BOUND ( 'NONE', #181742, .T. ) ;
#234820=TOROIDAL_SURFACE ( 'NONE', #230736, 0.2000000000000000111, 0.1000000000000000056 ) ;
#234831=CIRCLE ( 'NONE', #138914, 0.09999999999998898659 ) ;
#234888=ORIENTED_EDGE ( 'NONE', *, *, #65070, .T. ) ;
#234893=AXIS2_PLACEMENT_3D ( 'NONE', #215859, #191216, #210748 ) ;
#234948=AXIS2_PLACEMENT_3D ( 'NONE', #86284, #124174, #160751 ) ;
#234957=ORIENTED_EDGE ( 'NONE', *, *, #211235, .F. ) ;
#234963=FACE_OUTER_BOUND ( 'NONE', #213201, .T. ) ;
#234998=ORIENTED_EDGE ( 'NONE', *, *, #158035, .F. ) ;
#235007=CIRCLE ( 'NONE', #214155, 3.900000000000000799 ) ;
#235018=DIRECTION ( 'NONE',  ( 0.000000000000000000, -6.938893903907222067E-15, 1.000000000000000000 ) ) ;
#235019=VERTEX_POINT ( 'NONE', #26667 ) ;
#235040=CYLINDRICAL_SURFACE ( 'NONE', #182648, 11.75000000000001066 ) ;
#235057=EDGE_CURVE ( 'NONE', #200485, #34176, #246967, .T. ) ;
#235058=DIRECTION ( 'NONE',  ( 1.000000000000000000, 0.000000000000000000, 0.000000000000000000 ) ) ;
#235060=AXIS2_PLACEMENT_3D ( 'NONE', #74760, #118990, #198511 ) ;
#235079=CARTESIAN_POINT ( 'NONE',  ( 22.40000000000010516, 76.00000000001371347, -215.2735403769832487 ) ) ;
#235107=FACE_OUTER_BOUND ( 'NONE', #230042, .T. ) ;
#235121=VECTOR ( 'NONE', #223533, 1000.000000000000000 ) ;
#235124=CARTESIAN_POINT ( 'NONE',  ( 20.94999999999999929, 69.15387683765983695, -166.2853812176745691 ) ) ;
#235130=AXIS2_PLACEMENT_3D ( 'NONE', #179483, #257644, #38671 ) ;
#235150=ORIENTED_EDGE ( 'NONE', *, *, #32326, .F. ) ;
#235164=CARTESIAN_POINT ( 'NONE',  ( 23.14999999999999858, 76.00000000001244871, -170.0231074845243597 ) ) ;
#235177=ORIENTED_EDGE ( 'NONE', *, *, #99625, .F. ) ;
#235211=VERTEX_POINT ( 'NONE', #76038 ) ;
#235216=VERTEX_POINT ( 'NONE', #235124 ) ;
#235218=FACE_OUTER_BOUND ( 'NONE', #141384, .T. ) ;
#235229=CARTESIAN_POINT ( 'NONE',  ( -21.44999999999999929, 68.65000000001253966, -182.2731074845244166 ) ) ;
#235283=DIRECTION ( 'NONE',  ( 1.000000000000000000, 0.000000000000000000, 0.000000000000000000 ) ) ;
#235338=LINE ( 'NONE', #215770, #162803 ) ;
#235366=CARTESIAN_POINT ( 'NONE',  ( 20.85000000000000142, 77.83585931145600512, -158.5186683157258187 ) ) ;
#235419=DIRECTION ( 'NONE',  ( 0.000000000000000000, -7.086529944415886769E-15, 1.000000000000000000 ) ) ;
#235423=DIRECTION ( 'NONE',  ( 3.616040088954490704E-32, 7.105427357601001859E-15, -1.000000000000000000 ) ) ;
#235439=DIRECTION ( 'NONE',  ( 0.000000000000000000, -7.272083257015735086E-15, 1.000000000000000000 ) ) ;
#235480=AXIS2_PLACEMENT_3D ( 'NONE', #72183, #73481, #137264 ) ;
#235535=EDGE_CURVE ( 'NONE', #20407, #188235, #15795, .T. ) ;
#235538=CIRCLE ( 'NONE', #202245, 0.9750000000000036415 ) ;
#235547=TOROIDAL_SURFACE ( 'NONE', #135776, 4.149999999999999467, 0.1000000000000000056 ) ;
#235559=ORIENTED_EDGE ( 'NONE', *, *, #214239, .F. ) ;
#235574=ORIENTED_EDGE ( 'NONE', *, *, #77080, .T. ) ;
#235588=FACE_OUTER_BOUND ( 'NONE', #36042, .T. ) ;
#235603=CARTESIAN_POINT ( 'NONE',  ( 22.47110162079220785, 75.97120258721007247, -215.1730434212086891 ) ) ;
#235607=DIRECTION ( 'NONE',  ( 0.000000000000000000, 6.982962677686266711E-15, -1.000000000000000000 ) ) ;
#235653=CARTESIAN_POINT ( 'NONE',  ( 21.03675099975492202, 67.12481996722777922, -191.1975653477463766 ) ) ;
#235677=CIRCLE ( 'NONE', #19209, 0.09999999999998898659 ) ;
#235679=EDGE_CURVE ( 'NONE', #79652, #68241, #26145, .T. ) ;
#235694=CIRCLE ( 'NONE', #123281, 0.09999999999998898659 ) ;
#235721=CIRCLE ( 'NONE', #65041, 4.049999999999998046 ) ;
#235728=CARTESIAN_POINT ( 'NONE',  ( 20.94999999999999929, 85.40000000001262492, -193.6291383618718385 ) ) ;
#235748=DIRECTION ( 'NONE',  ( 0.000000000000000000, -0.8660254037844377084, -0.5000000000000016653 ) ) ;
#235751=DIRECTION ( 'NONE',  ( -1.000000000000000000, -0.000000000000000000, -0.000000000000000000 ) ) ;
#235781=CARTESIAN_POINT ( 'NONE',  ( -22.37643362114956602, 75.90091862633136088, -211.1488974784827519 ) ) ;
#235802=DIRECTION ( 'NONE',  ( 0.000000000000000000, 0.000000000000000000, 1.000000000000000000 ) ) ;
#235848=ORIENTED_EDGE ( 'NONE', *, *, #161702, .T. ) ;
#235853=AXIS2_PLACEMENT_3D ( 'NONE', #253053, #95270, #34054 ) ;
#235862=LINE ( 'NONE', #136760, #82141 ) ;
#235873=EDGE_LOOP ( 'NONE', ( #241079, #85760, #179307, #107227 ) ) ;
#235898=DIRECTION ( 'NONE',  ( 0.000000000000000000, -6.853228547068871147E-15, 1.000000000000000000 ) ) ;
#235904=DIRECTION ( 'NONE',  ( 2.694716079187273439E-16, 1.000000000000000000, 6.467318590049456648E-15 ) ) ;
#235981=CARTESIAN_POINT ( 'NONE',  ( -20.00857864376270001, 66.85000000001259934, -191.1731074845244223 ) ) ;
#236015=LINE ( 'NONE', #254279, #75533 ) ;
#236018=AXIS2_PLACEMENT_3D ( 'NONE', #78399, #140970, #44435 ) ;
#236032=ORIENTED_EDGE ( 'NONE', *, *, #194612, .T. ) ;
#236040=FACE_OUTER_BOUND ( 'NONE', #195137, .T. ) ;
#236048=DIRECTION ( 'NONE',  ( 0.000000000000000000, -0.4999999999999088507, -0.8660254037844913322 ) ) ;
#236049=VECTOR ( 'NONE', #41917, 999.9999999999998863 ) ;
#236078=DIRECTION ( 'NONE',  ( 0.000000000000000000, -6.982962677686266711E-15, 1.000000000000000000 ) ) ;
#236090=CARTESIAN_POINT ( 'NONE',  ( 21.33487959338958717, 69.27444184810150318, -203.5231074845243882 ) ) ;
#236092=AXIS2_PLACEMENT_3D ( 'NONE', #137343, #112673, #35727 ) ;
#236095=DIRECTION ( 'NONE',  ( -2.952720810173289112E-16, -1.000000000000000000, -6.982962677686266711E-15 ) ) ;
#236114=CARTESIAN_POINT ( 'NONE',  ( 20.95083306685154056, 67.08315735812242053, -195.0457826312660643 ) ) ;
#236149=ORIENTED_EDGE ( 'NONE', *, *, #191498, .F. ) ;
#236153=ORIENTED_EDGE ( 'NONE', *, *, #104644, .F. ) ;
#236155=ORIENTED_EDGE ( 'NONE', *, *, #248326, .T. ) ;
#236163=CIRCLE ( 'NONE', #140277, 0.1000000000000028644 ) ;
#236191=CARTESIAN_POINT ( 'NONE',  ( -22.49806830649814415, 64.35011034517360429, -203.6005718008499628 ) ) ;
#236213=SPHERICAL_SURFACE ( 'NONE', #173255, 0.1000000000000000056 ) ;
#236222=ORIENTED_EDGE ( 'NONE', *, *, #1473, .F. ) ;
#236231=CARTESIAN_POINT ( 'NONE',  ( 21.12230431290520016, 75.99479014832370183, -209.9806741378173456 ) ) ;
#236269=VERTEX_POINT ( 'NONE', #49120 ) ;
#236270=CIRCLE ( 'NONE', #169685, 0.09999999999999939493 ) ;
#236284=CARTESIAN_POINT ( 'NONE',  ( -23.15000000000000213, 85.00000000001251976, -179.3170766071767446 ) ) ;
#236295=EDGE_CURVE ( 'NONE', #35186, #137948, #22571, .T. ) ;
#236324=CIRCLE ( 'NONE', #15604, 0.09999999999998898659 ) ;
#236326=ADVANCED_FACE ( 'NONE', ( #70001 ), #149539, .T. ) ;
#236336=ORIENTED_EDGE ( 'NONE', *, *, #55290, .F. ) ;
#236342=CARTESIAN_POINT ( 'NONE',  ( 21.05000000000000071, 76.00000000001244871, -170.0231074845243597 ) ) ;
#236347=ADVANCED_FACE ( 'NONE', ( #1971 ), #81491, .F. ) ;
#236356=AXIS2_PLACEMENT_3D ( 'NONE', #144031, #8402, #205287 ) ;
#236362=CYLINDRICAL_SURFACE ( 'NONE', #153233, 0.09999999999999939493 ) ;
#236378=ORIENTED_EDGE ( 'NONE', *, *, #252819, .F. ) ;
#236393=AXIS2_PLACEMENT_3D ( 'NONE', #140476, #47785, #110344 ) ;
#236401=DIRECTION ( 'NONE',  ( 1.000000000000000000, 0.000000000000000000, 0.000000000000000000 ) ) ;
#236414=ORIENTED_EDGE ( 'NONE', *, *, #249854, .F. ) ;
#236429=CARTESIAN_POINT ( 'NONE',  ( -18.39999999999999858, 85.50000000001263345, -196.4910380878246485 ) ) ;
#236438=ORIENTED_EDGE ( 'NONE', *, *, #54827, .F. ) ;
#236441=CARTESIAN_POINT ( 'NONE',  ( 21.05000000000000071, 87.39257802171813694, -173.0970570643562212 ) ) ;
#236444=FACE_OUTER_BOUND ( 'NONE', #26846, .T. ) ;
#236474=DIRECTION ( 'NONE',  ( 0.000000000000000000, 0.9915357197604982575, -0.1298341882519033486 ) ) ;
#236512=CIRCLE ( 'NONE', #124119, 0.09999999999998898659 ) ;
#236537=EDGE_CURVE ( 'NONE', #8118, #239144, #22769, .T. ) ;
#236606=ORIENTED_EDGE ( 'NONE', *, *, #128282, .T. ) ;
#236608=VECTOR ( 'NONE', #162521, 1000.000000000000000 ) ;
#236611=CARTESIAN_POINT ( 'NONE',  ( 18.59999999999999432, 77.63717271298298783, -191.9409541190523214 ) ) ;
#236618=DIRECTION ( 'NONE',  ( 6.938893903907991995E-14, 0.000000000000000000, -1.000000000000000000 ) ) ;
#236650=CARTESIAN_POINT ( 'NONE',  ( 20.94999999999999929, 76.00000000001244871, -170.0231074845243597 ) ) ;
#236651=DIRECTION ( 'NONE',  ( -1.000000000000000000, 0.000000000000000000, 0.000000000000000000 ) ) ;
#236659=DIRECTION ( 'NONE',  ( 1.000000000000000000, 0.000000000000000000, 0.000000000000000000 ) ) ;
#236662=ORIENTED_EDGE ( 'NONE', *, *, #47565, .T. ) ;
#236678=ADVANCED_FACE ( 'NONE', ( #142161 ), #120070, .T. ) ;
#236686=DIRECTION ( 'NONE',  ( -1.000000000000000000, 7.304098846218135653E-16, 4.639676173203994055E-30 ) ) ;
#236722=B_SPLINE_CURVE_WITH_KNOTS ( 'NONE', 3,
 ( #64559, #65844, #200229, #124553 ),
 .UNSPECIFIED., .F., .F.,
 ( 4, 4 ),
 ( 3.469446951953614189E-18, 0.0001058379652594603572 ),
 .UNSPECIFIED. ) ;
#236766=CARTESIAN_POINT ( 'NONE',  ( -20.94999999999999929, 87.48912529308871910, -200.5231074845242745 ) ) ;
#236781=DIRECTION ( 'NONE',  ( 1.000000000000000000, 0.000000000000000000, 0.000000000000000000 ) ) ;
#236783=DIRECTION ( 'NONE',  ( -0.7071067811865475727, 0.7071067811865475727, 4.937700262164531476E-15 ) ) ;
#236839=ORIENTED_EDGE ( 'NONE', *, *, #40743, .T. ) ;
#236840=VERTEX_POINT ( 'NONE', #140890 ) ;
#236846=VERTEX_POINT ( 'NONE', #144718 ) ;
#236874=DIRECTION ( 'NONE',  ( -2.827886303505248766E-16, -0.8660254037844377084, -0.5000000000000015543 ) ) ;
#236875=AXIS2_PLACEMENT_3D ( 'NONE', #142610, #43544, #205152 ) ;
#236908=VERTEX_POINT ( 'NONE', #165600 ) ;
#236913=VERTEX_POINT ( 'NONE', #203433 ) ;
#236916=AXIS2_PLACEMENT_3D ( 'NONE', #186673, #127974, #47118 ) ;
#236949=CARTESIAN_POINT ( 'NONE',  ( 20.95512820512820440, 67.12384868372447499, -191.3731074845244109 ) ) ;
#236960=EDGE_CURVE ( 'NONE', #8263, #83828, #85248, .T. ) ;
#237005=FACE_OUTER_BOUND ( 'NONE', #218636, .T. ) ;
#237030=CARTESIAN_POINT ( 'NONE',  ( 23.14999999999999858, 76.00000000001244871, -170.0231074845243597 ) ) ;
#237050=CYLINDRICAL_SURFACE ( 'NONE', #68800, 0.1000000000000028644 ) ;
#237077=CIRCLE ( 'NONE', #57989, 7.800000000000001599 ) ;
#237100=DIRECTION ( 'NONE',  ( 0.000000000000000000, -0.9908441862701791170, 0.1350103645450472789 ) ) ;
#237135=ORIENTED_EDGE ( 'NONE', *, *, #127016, .F. ) ;
#237141=CARTESIAN_POINT ( 'NONE',  ( 21.05000000000000071, 65.43728505328415679, -196.0663053788799743 ) ) ;
#237155=ORIENTED_EDGE ( 'NONE', *, *, #230336, .F. ) ;
#237180=DIRECTION ( 'NONE',  ( 0.000000000000000000, 6.982962677686266711E-15, -1.000000000000000000 ) ) ;
#237185=CIRCLE ( 'NONE', #124753, 0.09999999999998898659 ) ;
#237196=ORIENTED_EDGE ( 'NONE', *, *, #87986, .F. ) ;
#237210=CARTESIAN_POINT ( 'NONE',  ( 18.59999999999996945, 65.66751761918722252, -164.4282609406112670 ) ) ;
#237213=EDGE_CURVE ( 'NONE', #225348, #94509, #160507, .T. ) ;
#237227=DIRECTION ( 'NONE',  ( 0.000000000000000000, -6.547589603894034005E-15, 1.000000000000000000 ) ) ;
#237230=DIRECTION ( 'NONE',  ( 0.000000000000000000, 0.000000000000000000, 1.000000000000000000 ) ) ;
#237278=CARTESIAN_POINT ( 'NONE',  ( -1.739115166359751801E-14, 64.35000000001259934, -191.2731074845244450 ) ) ;
#237302=EDGE_CURVE ( 'NONE', #226175, #241424, #60494, .T. ) ;
#237305=CARTESIAN_POINT ( 'NONE',  ( 21.05000000000000071, 76.00000000001267608, -203.5231074845243597 ) ) ;
#237306=CARTESIAN_POINT ( 'NONE',  ( 22.49999999999999645, 64.35023708198076520, -203.6119174609113713 ) ) ;
#237321=DIRECTION ( 'NONE',  ( -1.387778780781345459E-13, -0.4999999999999088507, -0.8660254037844913322 ) ) ;
#237323=FACE_OUTER_BOUND ( 'NONE', #107674, .T. ) ;
#237397=CARTESIAN_POINT ( 'NONE',  ( -20.07928932188135107, 66.77928932189388433, -182.2731074845244166 ) ) ;
#237430=AXIS2_PLACEMENT_3D ( 'NONE', #242038, #43851, #105054 ) ;
#237446=CIRCLE ( 'NONE', #145284, 0.5000000000000004441 ) ;
#237452=EDGE_CURVE ( 'NONE', #71853, #223851, #143720, .T. ) ;
#237499=LINE ( 'NONE', #97949, #213222 ) ;
#237515=DIRECTION ( 'NONE',  ( 0.000000000000000000, -1.000000000000000000, -6.982962677686265922E-15 ) ) ;
#237532=CARTESIAN_POINT ( 'NONE',  ( -21.05000000000000071, 69.74218538953657287, -203.6208977758331855 ) ) ;
#237562=CIRCLE ( 'NONE', #241643, 0.1000000000000046685 ) ;
#237568=DIRECTION ( 'NONE',  ( 0.000000000000000000, 0.000000000000000000, 1.000000000000000000 ) ) ;
#237571=CARTESIAN_POINT ( 'NONE',  ( -23.25000000000000000, 64.25000000001244871, -170.0231074845244166 ) ) ;
#237591=CYLINDRICAL_SURFACE ( 'NONE', #171088, 0.1000000000000026007 ) ;
#237600=EDGE_CURVE ( 'NONE', #251509, #81897, #189879, .T. ) ;
#237639=DIRECTION ( 'NONE',  ( 1.000000000000000000, 0.000000000000000000, 0.000000000000000000 ) ) ;
#237670=CIRCLE ( 'NONE', #29403, 12.87499999999999822 ) ;
#237682=AXIS2_PLACEMENT_3D ( 'NONE', #196956, #41778, #18334 ) ;
#237739=ORIENTED_EDGE ( 'NONE', *, *, #197398, .F. ) ;
#237759=ORIENTED_EDGE ( 'NONE', *, *, #39594, .T. ) ;
#237786=EDGE_CURVE ( 'NONE', #161922, #71516, #110767, .T. ) ;
#237796=CIRCLE ( 'NONE', #96126, 0.09999999999998898659 ) ;
#237810=DIRECTION ( 'NONE',  ( 1.000000000000000000, 0.000000000000000000, 0.000000000000000000 ) ) ;
#237812=DIRECTION ( 'NONE',  ( 3.616040088954490704E-32, 7.105427357601001859E-15, -1.000000000000000000 ) ) ;
#237817=CARTESIAN_POINT ( 'NONE',  ( 21.14999999999999503, 76.00000000001271871, -209.7731074845243597 ) ) ;
#237826=CARTESIAN_POINT ( 'NONE',  ( 20.94999999999999929, 77.83534155023701828, -191.9679561919613491 ) ) ;
#237864=ORIENTED_EDGE ( 'NONE', *, *, #31148, .F. ) ;
#237869=VECTOR ( 'NONE', #184027, 1000.000000000000000 ) ;
#237870=EDGE_LOOP ( 'NONE', ( #153052, #41322, #239887, #7196 ) ) ;
#237906=DIRECTION ( 'NONE',  ( 1.000000000000000000, 0.000000000000000000, 0.000000000000000000 ) ) ;
#237954=ORIENTED_EDGE ( 'NONE', *, *, #18813, .F. ) ;
#238056=DIRECTION ( 'NONE',  ( 0.000000000000000000, 0.000000000000000000, -1.000000000000000000 ) ) ;
#238074=ORIENTED_EDGE ( 'NONE', *, *, #139725, .F. ) ;
#238088=ADVANCED_FACE ( 'NONE', ( #41017 ), #78806, .T. ) ;
#238127=CARTESIAN_POINT ( 'NONE',  ( -20.94999999999999929, 64.35000000001251408, -176.8069731475025321 ) ) ;
#238128=LINE ( 'NONE', #59462, #222521 ) ;
#238145=CARTESIAN_POINT ( 'NONE',  ( 18.40916198585734165, 85.50000000001240608, -163.4229178527016586 ) ) ;
#238154=DIRECTION ( 'NONE',  ( 0.000000000000000000, -0.2605042016806647931, -0.9654727137038724427 ) ) ;
#238167=DIRECTION ( 'NONE',  ( -1.000000000000000000, 0.000000000000000000, 0.000000000000000000 ) ) ;
#238183=TOROIDAL_SURFACE ( 'NONE', #217329, 0.4000000000000012990, 0.1000000000000000056 ) ;
#238187=CIRCLE ( 'NONE', #142504, 0.09999999999998898659 ) ;
#238195=CIRCLE ( 'NONE', #196503, 6.329289321881370611 ) ;
#238203=CARTESIAN_POINT ( 'NONE',  ( -21.05000000000000071, 74.83729825007462466, -195.5231074845243597 ) ) ;
#238243=CARTESIAN_POINT ( 'NONE',  ( -21.05000000000000782, 69.66772772607704667, -203.4855714212387738 ) ) ;
#238253=ORIENTED_EDGE ( 'NONE', *, *, #174070, .F. ) ;
#238282=EDGE_CURVE ( 'NONE', #192523, #204747, #248184, .T. ) ;
#238301=CARTESIAN_POINT ( 'NONE',  ( 20.94999999999999929, 76.00000000001239187, -162.2231074845243768 ) ) ;
#238302=DIRECTION ( 'NONE',  ( 0.000000000000000000, 0.9908441862701791170, -0.1350103645450472789 ) ) ;
#238336=CARTESIAN_POINT ( 'NONE',  ( 20.94999999999999574, 65.52661458509973613, -195.9444530202758870 ) ) ;
#238342=ADVANCED_FACE ( 'NONE', ( #70857 ), #128240, .F. ) ;
#238351=CARTESIAN_POINT ( 'NONE',  ( -22.47071067811865319, 75.90090754531013317, -211.2431822290224090 ) ) ;
#238410=EDGE_CURVE ( 'NONE', #236269, #185078, #56376, .T. ) ;
#238455=DIRECTION ( 'NONE',  ( 0.000000000000000000, -6.467318590049456648E-15, 1.000000000000000000 ) ) ;
#238491=AXIS2_PLACEMENT_3D ( 'NONE', #19137, #115678, #59513 ) ;
#238502=VERTEX_POINT ( 'NONE', #173830 ) ;
#238520=CARTESIAN_POINT ( 'NONE',  ( -23.15000000000000213, 64.35000000001258513, -191.3731074845244393 ) ) ;
#238544=DIRECTION ( 'NONE',  ( -1.000000000000000000, 0.000000000000000000, -0.000000000000000000 ) ) ;
#238549=DIRECTION ( 'NONE',  ( 0.000000000000000000, 0.000000000000000000, 1.000000000000000000 ) ) ;
#238556=DIRECTION ( 'NONE',  ( 0.000000000000000000, 0.01283462868040404978, 0.9999176327611370985 ) ) ;
#238559=ORIENTED_EDGE ( 'NONE', *, *, #10285, .T. ) ;
#238565=EDGE_CURVE ( 'NONE', #162952, #154016, #190268, .T. ) ;
#238626=EDGE_CURVE ( 'NONE', #106612, #189559, #44548, .T. ) ;
#238652=ORIENTED_EDGE ( 'NONE', *, *, #189624, .F. ) ;
#238717=EDGE_CURVE ( 'NONE', #188520, #70041, #198617, .T. ) ;
#238723=EDGE_LOOP ( 'NONE', ( #147311, #16849, #162942 ) ) ;
#238751=TOROIDAL_SURFACE ( 'NONE', #126318, 0.2000000000000000111, 0.1000000000000000056 ) ;
#238757=ORIENTED_EDGE ( 'NONE', *, *, #44148, .T. ) ;
#238800=CARTESIAN_POINT ( 'NONE',  ( 23.15000000000000213, 87.48912529308852015, -173.1231074845242688 ) ) ;
#238806=VECTOR ( 'NONE', #247381, 1000.000000000000000 ) ;
#238900=FACE_OUTER_BOUND ( 'NONE', #55481, .T. ) ;
#238901=LINE ( 'NONE', #40732, #81672 ) ;
#238915=DIRECTION ( 'NONE',  ( 0.000000000000000000, 0.000000000000000000, 1.000000000000000000 ) ) ;
#238916=FACE_OUTER_BOUND ( 'NONE', #174202, .T. ) ;
#238930=DIRECTION ( 'NONE',  ( 0.000000000000000000, -1.000000000000000000, -6.860497997771532351E-15 ) ) ;
#238943=ADVANCED_FACE ( 'NONE', ( #36569 ), #82071, .F. ) ;
#238962=DIRECTION ( 'NONE',  ( 0.000000000000000000, -6.982962677686266711E-15, 1.000000000000000000 ) ) ;
#238982=CARTESIAN_POINT ( 'NONE',  ( 20.94999999999999929, 85.00000000001251976, -179.9170766071767389 ) ) ;
#239009=CARTESIAN_POINT ( 'NONE',  ( -18.50000000000000000, 85.32100840337396619, -196.2871692354464415 ) ) ;
#239043=VERTEX_POINT ( 'NONE', #178639 ) ;
#239078=AXIS2_PLACEMENT_3D ( 'NONE', #22503, #186702, #220686 ) ;
#239087=CARTESIAN_POINT ( 'NONE',  ( 21.04999999999999716, 69.70076908992579945, -203.6215449845244052 ) ) ;
#239088=CARTESIAN_POINT ( 'NONE',  ( 18.39999999999999858, 85.50000000001263345, -196.4910380878246201 ) ) ;
#239111=AXIS2_PLACEMENT_3D ( 'NONE', #192122, #31776, #132128 ) ;
#239144=VERTEX_POINT ( 'NONE', #170651 ) ;
#239147=ORIENTED_EDGE ( 'NONE', *, *, #223944, .T. ) ;
#239175=CARTESIAN_POINT ( 'NONE',  ( -20.64999999999999858, 68.85000000001259934, -191.2731074845244166 ) ) ;
#239176=VERTEX_POINT ( 'NONE', #88462 ) ;
#239189=DIRECTION ( 'NONE',  ( 0.000000000000000000, 0.000000000000000000, 1.000000000000000000 ) ) ;
#239199=VECTOR ( 'NONE', #204465, 1000.000000000000000 ) ;
#239210=CARTESIAN_POINT ( 'NONE',  ( 21.05000000000000071, 77.36087058720467269, -195.4501095574333931 ) ) ;
#239214=DIRECTION ( 'NONE',  ( 0.000000000000000000, 1.000000000000000000, 7.272083257015735086E-15 ) ) ;
#239218=CIRCLE ( 'NONE', #60141, 0.09999999999998898659 ) ;
#239249=TOROIDAL_SURFACE ( 'NONE', #176718, 0.4000000000000012990, 0.1000000000000000056 ) ;
#239260=EDGE_LOOP ( 'NONE', ( #63094, #51353, #40359, #199451 ) ) ;
#239277=DIRECTION ( 'NONE',  ( 1.000000000000000000, -1.836970198721029934E-16, -1.282749433769087582E-30 ) ) ;
#239302=ORIENTED_EDGE ( 'NONE', *, *, #245343, .F. ) ;
#239311=CARTESIAN_POINT ( 'NONE',  ( -21.44999999999999929, 68.65000000001261071, -191.1731074845243938 ) ) ;
#239315=DIRECTION ( 'NONE',  ( 2.952720810173289112E-16, 1.000000000000000000, 1.261617073437673512E-14 ) ) ;
#239326=CIRCLE ( 'NONE', #231164, 0.1000000000000118433 ) ;
#239346=CIRCLE ( 'NONE', #60276, 0.09999999999999939493 ) ;
#239367=CARTESIAN_POINT ( 'NONE',  ( -21.17356465864818560, 69.57719687377097273, -203.6220187255382541 ) ) ;
#239381=CARTESIAN_POINT ( 'NONE',  ( 21.05000000000000071, 76.03753606329841830, -209.8553797584600602 ) ) ;
#239393=( GEOMETRIC_REPRESENTATION_CONTEXT ( 3 ) GLOBAL_UNCERTAINTY_ASSIGNED_CONTEXT ( ( #193744 ) ) GLOBAL_UNIT_ASSIGNED_CONTEXT ( ( #47303, #246803, #29099 ) ) REPRESENTATION_CONTEXT ( 'NONE', 'WORKASPACE' ) );
#239420=VERTEX_POINT ( 'NONE', #229943 ) ;
#239426=EDGE_LOOP ( 'NONE', ( #185507, #244540, #202170, #92169 ) ) ;
#239437=ORIENTED_EDGE ( 'NONE', *, *, #99329, .F. ) ;
#239444=DIRECTION ( 'NONE',  ( 0.000000000000000000, 0.000000000000000000, 1.000000000000000000 ) ) ;
#239461=DIRECTION ( 'NONE',  ( -1.000000000000000000, -0.000000000000000000, -0.000000000000000000 ) ) ;
#239471=VERTEX_POINT ( 'NONE', #244672 ) ;
#239473=ORIENTED_EDGE ( 'NONE', *, *, #159806, .T. ) ;
#239485=FACE_OUTER_BOUND ( 'NONE', #158637, .T. ) ;
#239489=DIRECTION ( 'NONE',  ( 1.000000000000000000, -7.304098846218134667E-16, -4.639676173203993355E-30 ) ) ;
#239494=LINE ( 'NONE', #63397, #22744 ) ;
#239511=VERTEX_POINT ( 'NONE', #210397 ) ;
#239512=CARTESIAN_POINT ( 'NONE',  ( -23.15000000000000213, 76.00000000001244871, -170.0231074845243597 ) ) ;
#239518=AXIS2_PLACEMENT_3D ( 'NONE', #81435, #619, #201409 ) ;
#239531=DIRECTION ( 'NONE',  ( 0.000000000000000000, 6.982962677686266711E-15, -1.000000000000000000 ) ) ;
#239532=LINE ( 'NONE', #162576, #150723 ) ;
#239548=DIRECTION ( 'NONE',  ( 0.000000000000000000, -6.982962677686266711E-15, 1.000000000000000000 ) ) ;
#239556=DIRECTION ( 'NONE',  ( 0.000000000000000000, 0.000000000000000000, 1.000000000000000000 ) ) ;
#239582=DIRECTION ( 'NONE',  ( 0.000000000000000000, 0.000000000000000000, 1.000000000000000000 ) ) ;
#239595=ORIENTED_EDGE ( 'NONE', *, *, #93748, .T. ) ;
#239607=CARTESIAN_POINT ( 'NONE',  ( 23.14999999999999858, 80.00000000001244871, -170.0231074845243313 ) ) ;
#239626=AXIS2_PLACEMENT_3D ( 'NONE', #140185, #218441, #239315 ) ;
#239629=EDGE_CURVE ( 'NONE', #93986, #81149, #65896, .T. ) ;
#239633=ADVANCED_FACE ( 'NONE', ( #98102 ), #236362, .F. ) ;
#239659=CIRCLE ( 'NONE', #127222, 0.1000000000000028644 ) ;
#239671=ORIENTED_EDGE ( 'NONE', *, *, #223124, .F. ) ;
#239683=DIRECTION ( 'NONE',  ( 4.239556034732056743E-17, 0.1298341882519953860, 0.9915357197604862671 ) ) ;
#239686=CARTESIAN_POINT ( 'NONE',  ( -21.04386569057572132, 64.25000000001250555, -176.8802701327438456 ) ) ;
#239702=EDGE_CURVE ( 'NONE', #109096, #228673, #99397, .T. ) ;
#239737=VECTOR ( 'NONE', #192704, 1000.000000000000000 ) ;
#239757=AXIS2_PLACEMENT_3D ( 'NONE', #50596, #170626, #31095 ) ;
#239824=DIRECTION ( 'NONE',  ( 0.000000000000000000, 0.000000000000000000, -1.000000000000000000 ) ) ;
#239830=DIRECTION ( 'NONE',  ( -1.000000000000000000, 1.836970198721029934E-16, 1.282749433769087582E-30 ) ) ;
#239859=ORIENTED_EDGE ( 'NONE', *, *, #203008, .F. ) ;
#239887=ORIENTED_EDGE ( 'NONE', *, *, #96387, .F. ) ;
#239932=ORIENTED_EDGE ( 'NONE', *, *, #42350, .T. ) ;
#239953=FACE_OUTER_BOUND ( 'NONE', #174859, .T. ) ;
#239986=AXIS2_PLACEMENT_3D ( 'NONE', #130355, #31308, #207354 ) ;
#240001=ORIENTED_EDGE ( 'NONE', *, *, #57912, .T. ) ;
#240021=CIRCLE ( 'NONE', #210782, 0.09999999999998898659 ) ;
#240022=AXIS2_PLACEMENT_3D ( 'NONE', #44692, #87639, #223297 ) ;
#240086=DIRECTION ( 'NONE',  ( 1.000000000000000000, 0.000000000000000000, 0.000000000000000000 ) ) ;
#240119=LINE ( 'NONE', #101854, #160206 ) ;
#240140=EDGE_CURVE ( 'NONE', #246415, #83828, #23459, .T. ) ;
#240166=DIRECTION ( 'NONE',  ( 1.000000000000000000, 0.000000000000000000, 0.000000000000000000 ) ) ;
#240170=EDGE_CURVE ( 'NONE', #178668, #204747, #153426, .T. ) ;
#240289=CARTESIAN_POINT ( 'NONE',  ( 23.14999999999999503, 64.25000000001253397, -182.1731074845244507 ) ) ;
#240296=ORIENTED_EDGE ( 'NONE', *, *, #197316, .T. ) ;
#240305=ORIENTED_EDGE ( 'NONE', *, *, #171624, .F. ) ;
#240324=ORIENTED_EDGE ( 'NONE', *, *, #244203, .T. ) ;
#240341=DIRECTION ( 'NONE',  ( -0.000000000000000000, 1.000000000000000000, 6.982962677686266711E-15 ) ) ;
#240348=CARTESIAN_POINT ( 'NONE',  ( 20.85000000000000142, 76.00000000001244871, -170.0231074845243597 ) ) ;
#240358=ORIENTED_EDGE ( 'NONE', *, *, #214933, .T. ) ;
#240364=EDGE_LOOP ( 'NONE', ( #19468, #43028, #256704, #109229, #179629 ) ) ;
#240369=CIRCLE ( 'NONE', #207045, 0.1000000000000028644 ) ;
#240384=AXIS2_PLACEMENT_3D ( 'NONE', #11800, #250379, #167029 ) ;
#240402=EDGE_CURVE ( 'NONE', #205515, #102606, #182819, .T. ) ;
#240414=ORIENTED_EDGE ( 'NONE', *, *, #36987, .T. ) ;
#240421=CARTESIAN_POINT ( 'NONE',  ( 20.85000000000000142, 87.65000000001244018, -170.0231074845242745 ) ) ;
#240431=VERTEX_POINT ( 'NONE', #38839 ) ;
#240432=ORIENTED_EDGE ( 'NONE', *, *, #14198, .T. ) ;
#240483=CARTESIAN_POINT ( 'NONE',  ( -21.05000000000000071, 77.83534155023700407, -191.8679561919613832 ) ) ;
#240515=LINE ( 'NONE', #61882, #162168 ) ;
#240551=EDGE_LOOP ( 'NONE', ( #148330, #89317, #17977, #37429, #66359 ) ) ;
#240567=ORIENTED_EDGE ( 'NONE', *, *, #111949, .F. ) ;
#240577=AXIS2_PLACEMENT_3D ( 'NONE', #211999, #50315, #209406 ) ;
#240595=ORIENTED_EDGE ( 'NONE', *, *, #88616, .T. ) ;
#240596=EDGE_CURVE ( 'NONE', #19071, #51100, #203256, .T. ) ;
#240671=DIRECTION ( 'NONE',  ( -1.000000000000000000, 0.000000000000000000, -0.000000000000000000 ) ) ;
#240673=CYLINDRICAL_SURFACE ( 'NONE', #6880, 0.09999999999999939493 ) ;
#240701=ORIENTED_EDGE ( 'NONE', *, *, #219299, .F. ) ;
#240734=CARTESIAN_POINT ( 'NONE',  ( 18.58725287972269058, 85.56662691070425808, -163.2006026787589974 ) ) ;
#240737=EDGE_LOOP ( 'NONE', ( #237135, #117114, #216760, #45095 ) ) ;
#240816=B_SPLINE_CURVE_WITH_KNOTS ( 'NONE', 3,
 ( #118968, #99364, #178969, #133391, #212922, #34313, #14750, #219327, #184056, #82359, #143644, #44561, #65395, #223176, #199799, #180227, #124105, #1558, #139780, #40739, #120278, #203624 ),
 .UNSPECIFIED., .F., .F.,
 ( 4, 3, 3, 3, 3, 3, 3, 4 ),
 ( 0.000000000000000000, 7.307836821087015899E-06, 4.161455748548358328E-05, 7.576591810647013904E-05, 0.0001098090429817646371, 0.0001438003617351047054, 0.0001777914035423768207, 0.0002117966137402968007 ),
 .UNSPECIFIED. ) ;
#240869=LINE ( 'NONE', #80458, #247243 ) ;
#240906=DIRECTION ( 'NONE',  ( 0.000000000000000000, -7.272083257015735086E-15, 1.000000000000000000 ) ) ;
#240921=CARTESIAN_POINT ( 'NONE',  ( -21.07928932188134041, 75.90110485435833709, -209.8516241409176644 ) ) ;
#240940=ORIENTED_EDGE ( 'NONE', *, *, #202364, .F. ) ;
#240974=DIRECTION ( 'NONE',  ( 0.000000000000000000, -7.026728003956695223E-15, 1.000000000000000000 ) ) ;
#241009=VERTEX_POINT ( 'NONE', #50073 ) ;
#241020=AXIS2_PLACEMENT_3D ( 'NONE', #55436, #175446, #201083 ) ;
#241023=ORIENTED_EDGE ( 'NONE', *, *, #172568, .F. ) ;
#241054=AXIS2_PLACEMENT_3D ( 'NONE', #226711, #149780, #31133 ) ;
#241057=EDGE_CURVE ( 'NONE', #230071, #99483, #219997, .T. ) ;
#241079=ORIENTED_EDGE ( 'NONE', *, *, #49607, .T. ) ;
#241102=CARTESIAN_POINT ( 'NONE',  ( 21.05000000000000071, 65.51556651037091683, -196.0663016830324636 ) ) ;
#241120=AXIS2_PLACEMENT_3D ( 'NONE', #47163, #186717, #167175 ) ;
#241121=CARTESIAN_POINT ( 'NONE',  ( 18.49999999999999289, 65.79142135624982757, -178.8731074845244109 ) ) ;
#241135=AXIS2_PLACEMENT_3D ( 'NONE', #255503, #19530, #238556 ) ;
#241164=CARTESIAN_POINT ( 'NONE',  ( 22.49231231312462853, 64.35001509633539740, -203.5841603721258082 ) ) ;
#241195=CIRCLE ( 'NONE', #45546, 0.2000000000000057288 ) ;
#241199=VECTOR ( 'NONE', #102140, 1000.000000000000000 ) ;
#241213=CARTESIAN_POINT ( 'NONE',  ( 21.14261333020286671, 65.28430735075768609, -191.2731074845242176 ) ) ;
#241238=ADVANCED_FACE ( 'NONE', ( #12260 ), #113903, .T. ) ;
#241266=AXIS2_PLACEMENT_3D ( 'NONE', #131476, #32411, #53224 ) ;
#241271=CARTESIAN_POINT ( 'NONE',  ( 21.05000000000000071, 76.00000000001267608, -203.5231074845243597 ) ) ;
#241281=VERTEX_POINT ( 'NONE', #126414 ) ;
#241315=CARTESIAN_POINT ( 'NONE',  ( 21.05000000000000071, 67.22371735104150048, -195.0355151060044534 ) ) ;
#241325=( BOUNDED_SURFACE ( )  B_SPLINE_SURFACE ( 3, 2, ( 
 ( #53094, #192619, #28447 ),
 ( #252570, #227889, #71405 ),
 ( #50507, #109210, #29723 ),
 ( #188755, #229183, #209610 ) ),
 .UNSPECIFIED., .F., .F., .F. ) 
 B_SPLINE_SURFACE_WITH_KNOTS ( ( 4, 4 ),
 ( 3, 3 ),
 ( -1.908195823574487804E-17, 0.001979672783031562362 ),
 ( 0.000000000000000000, 1.000000000000000000 ),
 .UNSPECIFIED. ) 
 GEOMETRIC_REPRESENTATION_ITEM ( )  RATIONAL_B_SPLINE_SURFACE ( (
 ( 1.000000000000000000, 0.7103081912008383236, 1.000000000000000000),
 ( 1.000000000000000000, 0.7104998333557640544, 1.000000000000000000),
 ( 1.000000000000000000, 0.7107238315756078118, 1.000000000000000000),
 ( 1.000000000000000000, 0.7110073749539294052, 1.000000000000000000) ) ) 
 REPRESENTATION_ITEM ( '' )  SURFACE ( )  );
#241351=CARTESIAN_POINT ( 'NONE',  ( 20.85000000000000142, 69.01799029515598249, -166.3269553662681233 ) ) ;
#241370=SPHERICAL_SURFACE ( 'NONE', #203832, 0.1000000000000000056 ) ;
#241382=VERTEX_POINT ( 'NONE', #163002 ) ;
#241424=VERTEX_POINT ( 'NONE', #230669 ) ;
#241441=DIRECTION ( 'NONE',  ( 0.000000000000000000, -2.775557561562888827E-14, 1.000000000000000000 ) ) ;
#241467=CARTESIAN_POINT ( 'NONE',  ( 18.59999999999999076, 74.75000000001260503, -195.5231074845243597 ) ) ;
#241468=CARTESIAN_POINT ( 'NONE',  ( 20.94999999999999574, 74.75000000001261924, -195.6231074845243540 ) ) ;
#241470=ORIENTED_EDGE ( 'NONE', *, *, #171852, .F. ) ;
#241491=DIRECTION ( 'NONE',  ( -1.000000000000000000, 0.000000000000000000, 0.000000000000000000 ) ) ;
#241496=DIRECTION ( 'NONE',  ( 0.000000000000000000, 0.000000000000000000, -1.000000000000000000 ) ) ;
#241517=CARTESIAN_POINT ( 'NONE',  ( -22.59999999999999787, 64.35042919246788529, -203.6231074845244393 ) ) ;
#241522=DIRECTION ( 'NONE',  ( 0.000000000000000000, 7.026728003956695223E-15, -1.000000000000000000 ) ) ;
#241533=EDGE_LOOP ( 'NONE', ( #242566, #199794, #54664, #179821 ) ) ;
#241559=EDGE_CURVE ( 'NONE', #200926, #63948, #41144, .T. ) ;
#241574=CARTESIAN_POINT ( 'NONE',  ( -18.59999999999999787, 69.06610602788607878, -166.2374616501508342 ) ) ;
#241585=AXIS2_PLACEMENT_3D ( 'NONE', #137196, #94211, #36852 ) ;
#241598=EDGE_LOOP ( 'NONE', ( #243023, #86279, #43687 ) ) ;
#241603=VERTEX_POINT ( 'NONE', #226329 ) ;
#241627=ORIENTED_EDGE ( 'NONE', *, *, #246787, .F. ) ;
#241635=DIRECTION ( 'NONE',  ( -1.000000000000000000, 0.000000000000000000, -0.000000000000000000 ) ) ;
#241643=AXIS2_PLACEMENT_3D ( 'NONE', #10204, #131410, #91005 ) ;
#241689=ORIENTED_EDGE ( 'NONE', *, *, #173941, .T. ) ;
#241694=CYLINDRICAL_SURFACE ( 'NONE', #129102, 0.09999999999999939493 ) ;
#241721=EDGE_CURVE ( 'NONE', #152244, #20407, #170282, .T. ) ;
#241797=EDGE_CURVE ( 'NONE', #218429, #30910, #138720, .T. ) ;
#241821=ORIENTED_EDGE ( 'NONE', *, *, #84902, .F. ) ;
#241825=ORIENTED_EDGE ( 'NONE', *, *, #94119, .F. ) ;
#241839=EDGE_CURVE ( 'NONE', #115598, #32552, #145342, .T. ) ;
#241854=EDGE_CURVE ( 'NONE', #144388, #197466, #252050, .T. ) ;
#241864=DIRECTION ( 'NONE',  ( 1.000000000000000000, 0.000000000000000000, 0.000000000000000000 ) ) ;
#241895=FACE_OUTER_BOUND ( 'NONE', #67715, .T. ) ;
#241901=CARTESIAN_POINT ( 'NONE',  ( 19.75857864376269291, 64.35000000001251408, -178.7731074845244450 ) ) ;
#241918=ORIENTED_EDGE ( 'NONE', *, *, #178455, .F. ) ;
#241937=AXIS2_PLACEMENT_3D ( 'NONE', #220971, #144005, #183159 ) ;
#241954=CARTESIAN_POINT ( 'NONE',  ( -18.59999999999999787, 66.85000000001275566, -215.2731074845244166 ) ) ;
#242000=ADVANCED_FACE ( 'NONE', ( #288 ), #216770, .T. ) ;
#242013=DIRECTION ( 'NONE',  ( -3.265361837132813093E-16, -1.000000000000000000, -6.982962677686266711E-15 ) ) ;
#242035=DIRECTION ( 'NONE',  ( -1.000000000000000000, -0.000000000000000000, -0.000000000000000000 ) ) ;
#242036=LINE ( 'NONE', #2132, #210623 ) ;
#242038=CARTESIAN_POINT ( 'NONE',  ( 21.14999999999999858, 76.10000000001272724, -210.0637644362255969 ) ) ;
#242047=CARTESIAN_POINT ( 'NONE',  ( 21.11101077988997332, 69.57631526528663812, -203.5383927534386999 ) ) ;
#242062=AXIS2_PLACEMENT_3D ( 'NONE', #17887, #234370, #213522 ) ;
#242067=ORIENTED_EDGE ( 'NONE', *, *, #71845, .T. ) ;
#242080=DIRECTION ( 'NONE',  ( 1.000000000000000000, 0.000000000000000000, 0.000000000000000000 ) ) ;
#242084=ORIENTED_EDGE ( 'NONE', *, *, #32952, .T. ) ;
#242116=EDGE_CURVE ( 'NONE', #172693, #104276, #221884, .T. ) ;
#242161=VERTEX_POINT ( 'NONE', #125389 ) ;
#242176=LINE ( 'NONE', #257840, #199898 ) ;
#242182=VERTEX_POINT ( 'NONE', #146214 ) ;
#242186=ADVANCED_FACE ( 'NONE', ( #186654 ), #8014, .F. ) ;
#242198=DIRECTION ( 'NONE',  ( 0.000000000000000000, 6.608470384673536035E-15, -1.000000000000000000 ) ) ;
#242199=CARTESIAN_POINT ( 'NONE',  ( -23.15000000000000213, 87.65000000001246860, -173.1231074845242688 ) ) ;
#242204=CARTESIAN_POINT ( 'NONE',  ( -22.49999999999999645, 64.25043287652330548, -203.6239658536231900 ) ) ;
#242207=AXIS2_PLACEMENT_3D ( 'NONE', #257331, #157031, #81289 ) ;
#242252=EDGE_LOOP ( 'NONE', ( #230879, #204329, #210305, #194457 ) ) ;
#242255=CARTESIAN_POINT ( 'NONE',  ( -2.995603634470891112E-16, 87.75000000001253397, -182.2731074845242745 ) ) ;
#242269=ORIENTED_EDGE ( 'NONE', *, *, #220751, .F. ) ;
#242280=EDGE_CURVE ( 'NONE', #11922, #136223, #245505, .T. ) ;
#242297=DIRECTION ( 'NONE',  ( 1.000000000000000000, 0.000000000000000000, 0.000000000000000000 ) ) ;
#242316=CARTESIAN_POINT ( 'NONE',  ( -21.14999999999999858, 76.10085836911147794, -215.2726746080137445 ) ) ;
#242326=DIRECTION ( 'NONE',  ( 0.000000000000000000, 7.109473446599835262E-15, -1.000000000000000000 ) ) ;
#242329=ORIENTED_EDGE ( 'NONE', *, *, #140464, .T. ) ;
#242337=ORIENTED_EDGE ( 'NONE', *, *, #108829, .F. ) ;
#242365=DIRECTION ( 'NONE',  ( 0.000000000000000000, 6.982962677686266711E-15, -1.000000000000000000 ) ) ;
#242367=DIRECTION ( 'NONE',  ( 1.000000000000000000, -0.000000000000000000, 0.000000000000000000 ) ) ;
#242371=CARTESIAN_POINT ( 'NONE',  ( 18.49999999999716849, 65.55993210786937198, -178.7559897356427712 ) ) ;
#242379=VERTEX_POINT ( 'NONE', #255541 ) ;
#242383=LINE ( 'NONE', #127585, #52275 ) ;
#242414=EDGE_LOOP ( 'NONE', ( #99868, #240358, #93706, #241825 ) ) ;
#242421=CIRCLE ( 'NONE', #84151, 0.09999999999998898659 ) ;
#242441=CIRCLE ( 'NONE', #221583, 0.09999999999999939493 ) ;
#242442=ORIENTED_EDGE ( 'NONE', *, *, #61257, .F. ) ;
#242472=FACE_OUTER_BOUND ( 'NONE', #223583, .T. ) ;
#242500=ORIENTED_EDGE ( 'NONE', *, *, #45244, .T. ) ;
#242545=DIRECTION ( 'NONE',  ( -1.000000000000000000, 0.000000000000000000, 0.000000000000000000 ) ) ;
#242552=CARTESIAN_POINT ( 'NONE',  ( 21.00000000000000000, 66.25000000001260503, -191.2731074845244166 ) ) ;
#242556=ORIENTED_EDGE ( 'NONE', *, *, #22333, .F. ) ;
#242561=DIRECTION ( 'NONE',  ( 1.000000000000000000, -0.000000000000000000, 0.000000000000000000 ) ) ;
#242566=ORIENTED_EDGE ( 'NONE', *, *, #52196, .T. ) ;
#242577=CARTESIAN_POINT ( 'NONE',  ( 20.94999999999999929, 71.00000000001253397, -182.4283735034374843 ) ) ;
#242664=LINE ( 'NONE', #203549, #120583 ) ;
#242715=CARTESIAN_POINT ( 'NONE',  ( -23.15000000000000213, 85.00000000001251976, -179.9170766071767389 ) ) ;
#242733=DIRECTION ( 'NONE',  ( 2.952720810173289112E-16, 1.000000000000000000, 6.467318590049456648E-15 ) ) ;
#242751=CARTESIAN_POINT ( 'NONE',  ( -18.59999999999999787, 68.97833521811233481, -166.1895420826271277 ) ) ;
#242757=CYLINDRICAL_SURFACE ( 'NONE', #106025, 0.09999999999999939493 ) ;
#242775=CARTESIAN_POINT ( 'NONE',  ( -23.15000000000000213, 74.07476635515273244, -182.7533510176504876 ) ) ;
#242778=CARTESIAN_POINT ( 'NONE',  ( -22.45372860728439690, 75.98507938046427057, -215.1729046192282340 ) ) ;
#242780=DIRECTION ( 'NONE',  ( 1.000000000000000000, -0.000000000000000000, 0.000000000000000000 ) ) ;
#242807=CARTESIAN_POINT ( 'NONE',  ( -21.64999999999999858, 68.65000000001261071, -191.2731074845244166 ) ) ;
#242889=VECTOR ( 'NONE', #209557, 1000.000000000000000 ) ;
#242890=ORIENTED_EDGE ( 'NONE', *, *, #166865, .T. ) ;
#242908=SPHERICAL_SURFACE ( 'NONE', #149133, 0.1000000000000000056 ) ;
#242947=DIRECTION ( 'NONE',  ( -1.000000000000000000, 0.000000000000000000, -0.000000000000000000 ) ) ;
#242953=VECTOR ( 'NONE', #122866, 999.9999999999998863 ) ;
#242983=CARTESIAN_POINT ( 'NONE',  ( -21.05000000000000071, 87.65000000001246860, -172.9231074845242802 ) ) ;
#242993=EDGE_CURVE ( 'NONE', #110754, #50587, #145894, .T. ) ;
#243023=ORIENTED_EDGE ( 'NONE', *, *, #110386, .F. ) ;
#243041=DIRECTION ( 'NONE',  ( -1.000000000000000000, -0.000000000000000000, -0.000000000000000000 ) ) ;
#243075=PLANE ( 'NONE',  #249648 ) ;
#243104=CARTESIAN_POINT ( 'NONE',  ( -21.05000000000000071, 74.26374286841520700, -191.9544551555068779 ) ) ;
#243125=ORIENTED_EDGE ( 'NONE', *, *, #223004, .F. ) ;
#243133=EDGE_LOOP ( 'NONE', ( #45098, #124894, #178628, #248250 ) ) ;
#243137=DIRECTION ( 'NONE',  ( -1.000000000000000000, 2.952720810173289112E-16, 2.061873921506763405E-30 ) ) ;
#243138=EDGE_CURVE ( 'NONE', #166912, #150964, #75195, .T. ) ;
#243155=DIRECTION ( 'NONE',  ( -1.000000000000000000, 0.000000000000000000, -0.000000000000000000 ) ) ;
#243157=AXIS2_PLACEMENT_3D ( 'NONE', #232255, #128004, #9327 ) ;
#243178=EDGE_CURVE ( 'NONE', #90063, #199384, #79614, .T. ) ;
#243186=CARTESIAN_POINT ( 'NONE',  ( 19.75857864376269291, 64.25000000001250555, -178.6731074845244507 ) ) ;
#243219=VERTEX_POINT ( 'NONE', #148167 ) ;
#243269=CARTESIAN_POINT ( 'NONE',  ( 23.25000000000000000, 85.00000000001261924, -193.6291383618718385 ) ) ;
#243297=CIRCLE ( 'NONE', #126793, 0.09999999999998898659 ) ;
#243321=VECTOR ( 'NONE', #49923, 1000.000000000000000 ) ;
#243329=CARTESIAN_POINT ( 'NONE',  ( 21.07971444708685738, 69.67020791838612581, -203.6109309208423213 ) ) ;
#243330=DIRECTION ( 'NONE',  ( 1.000000000000000000, 0.000000000000000000, 0.000000000000000000 ) ) ;
#243392=ORIENTED_EDGE ( 'NONE', *, *, #130877, .T. ) ;
#243405=EDGE_CURVE ( 'NONE', #91407, #116470, #29593, .T. ) ;
#243411=EDGE_CURVE ( 'NONE', #151569, #654, #129526, .T. ) ;
#243449=CARTESIAN_POINT ( 'NONE',  ( 18.49999999999998934, 69.35000000001259934, -191.1731074845243938 ) ) ;
#243464=ORIENTED_EDGE ( 'NONE', *, *, #215397, .T. ) ;
#243470=DIRECTION ( 'NONE',  ( 0.000000000000000000, 6.938893903907030216E-14, -1.000000000000000000 ) ) ;
#243478=CARTESIAN_POINT ( 'NONE',  ( -21.08078803292166725, 75.92081401285503262, -209.8561204489615193 ) ) ;
#243494=DIRECTION ( 'NONE',  ( 0.000000000000000000, -7.086529944415886769E-15, 1.000000000000000000 ) ) ;
#243503=CARTESIAN_POINT ( 'NONE',  ( 20.94999999999999929, 76.00000000001260503, -190.6481074845243597 ) ) ;
#243536=EDGE_LOOP ( 'NONE', ( #48034, #153359, #225572, #118021 ) ) ;
#243544=CARTESIAN_POINT ( 'NONE',  ( -21.14999999999999858, 76.10000000001272724, -210.0637644362255969 ) ) ;
#243639=DIRECTION ( 'NONE',  ( -1.000000000000000000, 0.000000000000000000, -0.000000000000000000 ) ) ;
#243672=STYLED_ITEM ( 'NONE', ( #251949 ), #26624 ) ;
#243683=B_SPLINE_CURVE_WITH_KNOTS ( 'NONE', 3,
 ( #23017, #80360, #179516, #821, #221171, #17837, #157404, #102486, #235603, #62123, #119539, #19133, #59510, #159955, #182069, #216040 ),
 .UNSPECIFIED., .F., .F.,
 ( 4, 3, 3, 3, 3, 4 ),
 ( 0.000000000000000000, 2.209833635978099498E-05, 5.595056164119025226E-05, 8.979992002654954499E-05, 0.0001236482757198867745, 0.0001574984039362969023 ),
 .UNSPECIFIED. ) ;
#243686=CARTESIAN_POINT ( 'NONE',  ( 18.59999999999999076, 74.16465844978819177, -191.9679561919613775 ) ) ;
#243690=ORIENTED_EDGE ( 'NONE', *, *, #85585, .F. ) ;
#243701=ADVANCED_FACE ( 'NONE', ( #182541 ), #106816, .F. ) ;
#243712=CIRCLE ( 'NONE', #214661, 0.5999999999999894307 ) ;
#243751=CARTESIAN_POINT ( 'NONE',  ( -20.85000000000000497, 64.25000000001250555, -176.9422547304831426 ) ) ;
#243752=CIRCLE ( 'NONE', #6419, 0.09999999999998898659 ) ;
#243753=CARTESIAN_POINT ( 'NONE',  ( 20.94999999999999929, 69.35000000001259934, -191.3731074845244109 ) ) ;
#243760=CARTESIAN_POINT ( 'NONE',  ( 20.94999999999999574, 74.73821383144760944, -195.4366085209788935 ) ) ;
#243770=DIRECTION ( 'NONE',  ( 0.000000000000000000, -1.000000000000000000, -6.982962677686265922E-15 ) ) ;
#243772=ORIENTED_EDGE ( 'NONE', *, *, #27924, .T. ) ;
#243782=CARTESIAN_POINT ( 'NONE',  ( -21.14999999999999858, 69.45934304831143891, -203.5231074845243882 ) ) ;
#243783=CYLINDRICAL_SURFACE ( 'NONE', #122568, 0.09999999999999939493 ) ;
#243789=CIRCLE ( 'NONE', #239518, 0.1000000000000070832 ) ;
#243795=EDGE_CURVE ( 'NONE', #246161, #196907, #211070, .T. ) ;
#243800=CARTESIAN_POINT ( 'NONE',  ( 18.39999999999999858, 85.51932773110506503, -196.5501311079649724 ) ) ;
#243801=DIRECTION ( 'NONE',  ( 1.000000000000000000, 0.000000000000000000, 0.000000000000000000 ) ) ;
#243823=LINE ( 'NONE', #246403, #251951 ) ;
#243835=AXIS2_PLACEMENT_3D ( 'NONE', #198323, #19708, #99206 ) ;
#243839=CIRCLE ( 'NONE', #181326, 2.100000000000004530 ) ;
#243853=ORIENTED_EDGE ( 'NONE', *, *, #230336, .T. ) ;
#243867=DIRECTION ( 'NONE',  ( -0.000000000000000000, 6.982962677686266711E-15, -1.000000000000000000 ) ) ;
#243886=CARTESIAN_POINT ( 'NONE',  ( 18.46905048506371472, 85.47374425739481296, -163.3471211922688724 ) ) ;
#243940=DIRECTION ( 'NONE',  ( -0.000000000000000000, -6.982962677686266711E-15, 1.000000000000000000 ) ) ;
#243998=DIRECTION ( 'NONE',  ( -1.000000000000000000, -0.000000000000000000, -0.000000000000000000 ) ) ;
#244019=TOROIDAL_SURFACE ( 'NONE', #135685, 0.2000000000000000111, 0.1000000000000000056 ) ;
#244106=AXIS2_PLACEMENT_3D ( 'NONE', #204391, #6196, #240974 ) ;
#244107=CARTESIAN_POINT ( 'NONE',  ( -23.15000000000000213, 76.00000000001246292, -172.1231074845243540 ) ) ;
#244118=TOROIDAL_SURFACE ( 'NONE', #131703, 0.4000000000000012990, 0.1000000000000000056 ) ;
#244123=ORIENTED_EDGE ( 'NONE', *, *, #162823, .F. ) ;
#244126=DIRECTION ( 'NONE',  ( 1.000000000000000000, 0.000000000000000000, 0.000000000000000000 ) ) ;
#244184=CARTESIAN_POINT ( 'NONE',  ( -18.59999999999999787, 68.97833521811233481, -166.1895420826271277 ) ) ;
#244203=EDGE_CURVE ( 'NONE', #137582, #99703, #32145, .T. ) ;
#244210=AXIS2_PLACEMENT_3D ( 'NONE', #224448, #164500, #221860 ) ;
#244211=ORIENTED_EDGE ( 'NONE', *, *, #14198, .F. ) ;
#244232=CARTESIAN_POINT ( 'NONE',  ( -18.59999999999999787, 77.83585931145600512, -158.4186683157258244 ) ) ;
#244233=LINE ( 'NONE', #20082, #167157 ) ;
#244302=CYLINDRICAL_SURFACE ( 'NONE', #14854, 0.09999999999998898659 ) ;
#244326=EDGE_LOOP ( 'NONE', ( #90642, #8642, #157471, #123274 ) ) ;
#244337=CARTESIAN_POINT ( 'NONE',  ( -22.39999999999999858, 76.00000000001273293, -211.3138870828977645 ) ) ;
#244356=B_SPLINE_CURVE_WITH_KNOTS ( 'NONE', 3,
 ( #156733, #112452, #236231, #57579, #133288, #53743, #191998, #13340 ),
 .UNSPECIFIED., .F., .F.,
 ( 4, 2, 2, 4 ),
 ( 0.000000000000000000, 0.0001306511400391301332, 0.0001959767100586967854, 0.0002613022800782634106 ),
 .UNSPECIFIED. ) ;
#244374=FACE_OUTER_BOUND ( 'NONE', #130084, .T. ) ;
#244378=EDGE_CURVE ( 'NONE', #151955, #228147, #254905, .T. ) ;
#244386=VECTOR ( 'NONE', #79674, 1000.000000000000000 ) ;
#244397=DIRECTION ( 'NONE',  ( -1.000000000000000000, -7.304098846218164250E-16, 4.217023435051628197E-16 ) ) ;
#244407=CARTESIAN_POINT ( 'NONE',  ( 21.09793522318408066, 65.27537548979982773, -191.2838166135473728 ) ) ;
#244436=CARTESIAN_POINT ( 'NONE',  ( 20.12481660106788439, 66.47365600773768790, -195.2969658154282229 ) ) ;
#244438=ORIENTED_EDGE ( 'NONE', *, *, #209753, .T. ) ;
#244449=ORIENTED_EDGE ( 'NONE', *, *, #116198, .T. ) ;
#244465=CARTESIAN_POINT ( 'NONE',  ( 21.11345278033224560, 67.11787792664171093, -191.2770853137656104 ) ) ;
#244494=ORIENTED_EDGE ( 'NONE', *, *, #30355, .F. ) ;
#244521=CARTESIAN_POINT ( 'NONE',  ( -20.94788355080264353, 65.69792220476374212, -164.5335554128461979 ) ) ;
#244528=VERTEX_POINT ( 'NONE', #185754 ) ;
#244540=ORIENTED_EDGE ( 'NONE', *, *, #172767, .T. ) ;
#244564=CARTESIAN_POINT ( 'NONE',  ( 18.50000000000000355, 85.40000000001239755, -163.1410656363516125 ) ) ;
#244565=VECTOR ( 'NONE', #144333, 1000.000000000000000 ) ;
#244586=ORIENTED_EDGE ( 'NONE', *, *, #162717, .F. ) ;
#244592=FACE_OUTER_BOUND ( 'NONE', #49082, .T. ) ;
#244593=CARTESIAN_POINT ( 'NONE',  ( -20.12071067811865888, 66.67928932189394686, -191.1731074845244223 ) ) ;
#244599=DIRECTION ( 'NONE',  ( 1.000000000000000000, -0.000000000000000000, 0.000000000000000000 ) ) ;
#244609=DIRECTION ( 'NONE',  ( 0.000000000000000000, -6.982962677686266711E-15, 1.000000000000000000 ) ) ;
#244626=DIRECTION ( 'NONE',  ( 1.000000000000000000, 0.000000000000000000, 0.000000000000000000 ) ) ;
#244627=CIRCLE ( 'NONE', #169673, 0.1000000000000026007 ) ;
#244672=CARTESIAN_POINT ( 'NONE',  ( -23.25000000000000000, 85.60000000001252829, -179.9170766071767389 ) ) ;
#244682=AXIS2_PLACEMENT_3D ( 'NONE', #190148, #154888, #132746 ) ;
#244717=ORIENTED_EDGE ( 'NONE', *, *, #125358, .F. ) ;
#244754=ADVANCED_FACE ( 'NONE', ( #51336 ), #248293, .F. ) ;
#244787=ORIENTED_EDGE ( 'NONE', *, *, #158432, .F. ) ;
#244867=EDGE_CURVE ( 'NONE', #97945, #38825, #201640, .T. ) ;
#244872=ORIENTED_EDGE ( 'NONE', *, *, #85555, .F. ) ;
#244895=VECTOR ( 'NONE', #237906, 1000.000000000000000 ) ;
#244921=ORIENTED_EDGE ( 'NONE', *, *, #212802, .F. ) ;
#244923=CARTESIAN_POINT ( 'NONE',  ( 22.47071067811865319, 75.90090754531013317, -211.2431822290224090 ) ) ;
#244925=DIRECTION ( 'NONE',  ( 1.000000000000000000, -3.265361837132813093E-16, -2.280189983783949500E-30 ) ) ;
#244938=DIRECTION ( 'NONE',  ( 1.000000000000000000, -2.952720810173289112E-16, -2.061873921506763405E-30 ) ) ;
#244946=AXIS2_PLACEMENT_3D ( 'NONE', #190607, #214011, #254384 ) ;
#244971=DIRECTION ( 'NONE',  ( -1.000000000000000000, 0.000000000000000000, 0.000000000000000000 ) ) ;
#245027=ORIENTED_EDGE ( 'NONE', *, *, #7283, .F. ) ;
#245083=TOROIDAL_SURFACE ( 'NONE', #49454, 7.800000000000000711, 0.1000000000000000056 ) ;
#245196=AXIS2_PLACEMENT_3D ( 'NONE', #212575, #13092, #136867 ) ;
#245212=FACE_OUTER_BOUND ( 'NONE', #89338, .T. ) ;
#245243=ADVANCED_FACE ( 'NONE', ( #92314 ), #188854, .F. ) ;
#245266=PLANE ( 'NONE',  #79271 ) ;
#245300=DIRECTION ( 'NONE',  ( -1.000000000000000000, 0.000000000000000000, 0.000000000000000000 ) ) ;
#245303=CARTESIAN_POINT ( 'NONE',  ( 21.05000000000000071, 87.48912529308852015, -173.1231074845242688 ) ) ;
#245314=DIRECTION ( 'NONE',  ( 1.000000000000000000, 0.000000000000000000, 0.000000000000000000 ) ) ;
#245343=EDGE_CURVE ( 'NONE', #247011, #151569, #139255, .T. ) ;
#245360=DIRECTION ( 'NONE',  ( -1.000000000000000000, 0.000000000000000000, 0.000000000000000000 ) ) ;
#245370=CARTESIAN_POINT ( 'NONE',  ( -22.41119224318417125, 76.00000000001276135, -215.1726782920691505 ) ) ;
#245385=ORIENTED_EDGE ( 'NONE', *, *, #244378, .T. ) ;
#245392=CARTESIAN_POINT ( 'NONE',  ( 21.14999999999998082, 87.75000000001267608, -203.5231074845243029 ) ) ;
#245412=ORIENTED_EDGE ( 'NONE', *, *, #203376, .T. ) ;
#245505=CIRCLE ( 'NONE', #224635, 0.2000000000000057288 ) ;
#245521=CARTESIAN_POINT ( 'NONE',  ( -23.25000000000000000, 71.85000000001254250, -182.2731074845243882 ) ) ;
#245524=PLANE ( 'NONE',  #153104 ) ;
#245529=TOROIDAL_SURFACE ( 'NONE', #153992, 1.900000000000002576, 0.1000000000000000056 ) ;
#245548=CARTESIAN_POINT ( 'NONE',  ( 20.94999999999999574, 87.65000000001265335, -200.4231074845242802 ) ) ;
#245557=CARTESIAN_POINT ( 'NONE',  ( -21.05000000000000071, 76.00000000001242029, -165.9231074845243654 ) ) ;
#245560=DIRECTION ( 'NONE',  ( 1.000000000000000000, -3.265361837132813093E-16, -2.280189983783949500E-30 ) ) ;
#245568=EDGE_CURVE ( 'NONE', #670, #81505, #221132, .T. ) ;
#245635=DIRECTION ( 'NONE',  ( 1.000000000000000000, 0.000000000000000000, 0.000000000000000000 ) ) ;
#245637=CARTESIAN_POINT ( 'NONE',  ( -20.94999999999999929, 75.74389420792046224, -203.5580039261966760 ) ) ;
#245642=CIRCLE ( 'NONE', #162269, 11.64999999999999325 ) ;
#245649=CIRCLE ( 'NONE', #45731, 2.000000000000001776 ) ;
#245658=DIRECTION ( 'NONE',  ( 0.000000000000000000, 0.000000000000000000, 1.000000000000000000 ) ) ;
#245733=CARTESIAN_POINT ( 'NONE',  ( 20.97565083910961548, 65.52538259873381321, -195.9451643079358973 ) ) ;
#245745=CARTESIAN_POINT ( 'NONE',  ( 21.15000000000000213, 76.00000000001271871, -210.0637644362255969 ) ) ;
#245759=ORIENTED_EDGE ( 'NONE', *, *, #166766, .T. ) ;
#245767=AXIS2_PLACEMENT_3D ( 'NONE', #24962, #26236, #86163 ) ;
#245779=FACE_OUTER_BOUND ( 'NONE', #28744, .T. ) ;
#245855=CARTESIAN_POINT ( 'NONE',  ( 18.49999999999999645, 74.13328508995527955, -191.7704322382423641 ) ) ;
#245864=FACE_OUTER_BOUND ( 'NONE', #166858, .T. ) ;
#245867=ORIENTED_EDGE ( 'NONE', *, *, #158411, .T. ) ;
#245879=EDGE_CURVE ( 'NONE', #125024, #51335, #237077, .T. ) ;
#245929=AXIS2_PLACEMENT_3D ( 'NONE', #18069, #1046, #200560 ) ;
#246030=DIRECTION ( 'NONE',  ( 0.000000000000000000, 7.026728003956695223E-15, -1.000000000000000000 ) ) ;
#246035=CARTESIAN_POINT ( 'NONE',  ( 21.00000000000000000, 66.25000000001253397, -182.3731074845244393 ) ) ;
#246073=CARTESIAN_POINT ( 'NONE',  ( -23.15000000000000213, 64.25000000001269029, -203.5231074845244166 ) ) ;
#246081=CIRCLE ( 'NONE', #204361, 11.80000000000000426 ) ;
#246135=AXIS2_PLACEMENT_3D ( 'NONE', #111986, #166849, #208524 ) ;
#246139=CARTESIAN_POINT ( 'NONE',  ( -21.52071067811865746, 68.22071067813125467, -191.1731074845243938 ) ) ;
#246155=CARTESIAN_POINT ( 'NONE',  ( -18.59999999999999787, 74.83729825007462466, -195.5231074845243597 ) ) ;
#246161=VERTEX_POINT ( 'NONE', #37787 ) ;
#246171=ADVANCED_FACE ( 'NONE', ( #162872 ), #18203, .T. ) ;
#246204=ADVANCED_FACE ( 'NONE', ( #224089 ), #45465, .F. ) ;
#246219=CARTESIAN_POINT ( 'NONE',  ( 21.14999999999999503, 76.00000000001267608, -203.5231074845243597 ) ) ;
#246247=ORIENTED_EDGE ( 'NONE', *, *, #146286, .T. ) ;
#246276=EDGE_CURVE ( 'NONE', #213320, #65963, #245642, .T. ) ;
#246278=VERTEX_POINT ( 'NONE', #85840 ) ;
#246338=ORIENTED_EDGE ( 'NONE', *, *, #107267, .T. ) ;
#246342=CARTESIAN_POINT ( 'NONE',  ( 22.57320508075688537, 64.35000000001268461, -203.5231074845244166 ) ) ;
#246355=CARTESIAN_POINT ( 'NONE',  ( -21.05000000000000071, 74.83729825007462466, -195.4231074845243654 ) ) ;
#246364=ADVANCED_FACE ( 'NONE', ( #169309 ), #74808, .F. ) ;
#246372=CIRCLE ( 'NONE', #187936, 0.5000000000000004441 ) ;
#246380=DIRECTION ( 'NONE',  ( -0.000000000000000000, 6.982962677686266711E-15, -1.000000000000000000 ) ) ;
#246403=CARTESIAN_POINT ( 'NONE',  ( -21.52071067811865746, 68.22071067813118361, -182.2731074845244166 ) ) ;
#246415=VERTEX_POINT ( 'NONE', #193975 ) ;
#246422=AXIS2_PLACEMENT_3D ( 'NONE', #68916, #192699, #32371 ) ;
#246423=LINE ( 'NONE', #229430, #187498 ) ;
#246425=ORIENTED_EDGE ( 'NONE', *, *, #126464, .F. ) ;
#246426=DIRECTION ( 'NONE',  ( -1.000000000000000000, 3.265361837132813093E-16, 2.280189983783949500E-30 ) ) ;
#246427=ORIENTED_EDGE ( 'NONE', *, *, #158679, .F. ) ;
#246443=DIRECTION ( 'NONE',  ( -0.000000000000000000, 1.000000000000000000, 8.717686153663073805E-15 ) ) ;
#246446=CARTESIAN_POINT ( 'NONE',  ( -20.85000000000000142, 77.83585931145600512, -158.4186683157258244 ) ) ;
#246463=DIRECTION ( 'NONE',  ( 1.000000000000000000, -3.265361837132813093E-16, -2.280189983783949500E-30 ) ) ;
#246465=CARTESIAN_POINT ( 'NONE',  ( 18.49999999999999289, 65.79142135625006915, -215.2731074845244450 ) ) ;
#246466=CARTESIAN_POINT ( 'NONE',  ( 18.42595409746872903, 85.49999981257734305, -196.5237451327744225 ) ) ;
#246476=ORIENTED_EDGE ( 'NONE', *, *, #60833, .T. ) ;
#246479=CARTESIAN_POINT ( 'NONE',  ( -21.05000000000000071, 64.35000000001264198, -196.7392418215462726 ) ) ;
#246482=DIRECTION ( 'NONE',  ( -1.000000000000000000, 0.000000000000000000, -0.000000000000000000 ) ) ;
#246512=LINE ( 'NONE', #91305, #70921 ) ;
#246519=LINE ( 'NONE', #48322, #256070 ) ;
#246566=EDGE_LOOP ( 'NONE', ( #38649, #242890, #119564 ) ) ;
#246658=ADVANCED_FACE ( 'NONE', ( #28192 ), #208232, .T. ) ;
#246681=CARTESIAN_POINT ( 'NONE',  ( 21.14999999999999503, 87.65000000001275282, -215.2731074845242745 ) ) ;
#246723=ORIENTED_EDGE ( 'NONE', *, *, #5955, .T. ) ;
#246730=CARTESIAN_POINT ( 'NONE',  ( -21.09107601085562322, 69.63612202465219525, -203.5624146492413900 ) ) ;
#246771=EDGE_CURVE ( 'NONE', #79128, #57467, #116634, .T. ) ;
#246781=DIRECTION ( 'NONE',  ( -0.000000000000000000, 1.000000000000000000, 6.982962677686267499E-15 ) ) ;
#246787=EDGE_CURVE ( 'NONE', #83828, #241603, #66763, .T. ) ;
#246803=( NAMED_UNIT ( * ) PLANE_ANGLE_UNIT ( ) SI_UNIT ( $, .RADIAN. ) );
#246836=ORIENTED_EDGE ( 'NONE', *, *, #82498, .F. ) ;
#246862=ORIENTED_EDGE ( 'NONE', *, *, #54337, .F. ) ;
#246884=CIRCLE ( 'NONE', #17933, 0.1000000000000118433 ) ;
#246902=ORIENTED_EDGE ( 'NONE', *, *, #221550, .T. ) ;
#246917=EDGE_LOOP ( 'NONE', ( #152241, #173462, #86962, #204332 ) ) ;
#246919=CARTESIAN_POINT ( 'NONE',  ( 21.14999999999999503, 87.75000000001264766, -200.6231074845242688 ) ) ;
#246951=EDGE_CURVE ( 'NONE', #38969, #116223, #175145, .T. ) ;
#246967=LINE ( 'NONE', #207882, #213106 ) ;
#246973=EDGE_CURVE ( 'NONE', #32434, #97945, #125205, .T. ) ;
#246977=CARTESIAN_POINT ( 'NONE',  ( 22.32929514600007792, 68.42135243463620498, -203.6221831626383221 ) ) ;
#246982=VERTEX_POINT ( 'NONE', #6675 ) ;
#246983=DIRECTION ( 'NONE',  ( 0.000000000000000000, 6.982962677686266711E-15, -1.000000000000000000 ) ) ;
#247011=VERTEX_POINT ( 'NONE', #207470 ) ;
#247025=ORIENTED_EDGE ( 'NONE', *, *, #2906, .F. ) ;
#247026=CARTESIAN_POINT ( 'NONE',  ( -22.39999999999999858, 76.00000000001273293, -215.2735403769829645 ) ) ;
#247045=EDGE_LOOP ( 'NONE', ( #137592, #163704, #240567, #147356 ) ) ;
#247081=CARTESIAN_POINT ( 'NONE',  ( -20.92356734117541706, 65.68026841930954163, -164.4725740131889893 ) ) ;
#247090=TOROIDAL_SURFACE ( 'NONE', #230562, 11.65000000000000036, 0.1000000000000000056 ) ;
#247092=EDGE_CURVE ( 'NONE', #138354, #184002, #216776, .T. ) ;
#247101=AXIS2_PLACEMENT_3D ( 'NONE', #248078, #8202, #48589 ) ;
#247139=DIRECTION ( 'NONE',  ( 0.000000000000000000, 0.000000000000000000, -1.000000000000000000 ) ) ;
#247143=ORIENTED_EDGE ( 'NONE', *, *, #162322, .F. ) ;
#247165=EDGE_CURVE ( 'NONE', #59053, #116446, #250104, .T. ) ;
#247180=ORIENTED_EDGE ( 'NONE', *, *, #79147, .T. ) ;
#247201=EDGE_CURVE ( 'NONE', #56486, #207747, #146219, .T. ) ;
#247210=CARTESIAN_POINT ( 'NONE',  ( 21.14999999999999503, 76.10000000001276987, -215.1726782920691505 ) ) ;
#247243=VECTOR ( 'NONE', #84288, 1000.000000000000000 ) ;
#247281=CARTESIAN_POINT ( 'NONE',  ( -21.53699400380208928, 69.21228820681695026, -203.5231074845244450 ) ) ;
#247328=CARTESIAN_POINT ( 'NONE',  ( 21.05000000000000071, 85.00000000001251976, -179.4170766071767389 ) ) ;
#247351=FACE_OUTER_BOUND ( 'NONE', #23000, .T. ) ;
#247381=DIRECTION ( 'NONE',  ( 1.000000000000000000, 0.000000000000000000, 0.000000000000000000 ) ) ;
#247416=AXIS2_PLACEMENT_3D ( 'NONE', #33143, #47504, #207907 ) ;
#247419=ORIENTED_EDGE ( 'NONE', *, *, #136394, .T. ) ;
#247421=ORIENTED_EDGE ( 'NONE', *, *, #77527, .F. ) ;
#247451=FACE_OUTER_BOUND ( 'NONE', #147905, .T. ) ;
#247461=VERTEX_POINT ( 'NONE', #70235 ) ;
#247462=DIRECTION ( 'NONE',  ( 0.000000000000000000, -1.000000000000000000, -6.982962677686265922E-15 ) ) ;
#247571=EDGE_CURVE ( 'NONE', #191888, #12967, #138007, .T. ) ;
#247582=LINE ( 'NONE', #68968, #141152 ) ;
#247607=AXIS2_PLACEMENT_3D ( 'NONE', #108618, #106020, #214143 ) ;
#247616=CARTESIAN_POINT ( 'NONE',  ( -18.39999999999999858, 85.51932773110506503, -196.5501311079649724 ) ) ;
#247641=ORIENTED_EDGE ( 'NONE', *, *, #106778, .F. ) ;
#247654=EDGE_CURVE ( 'NONE', #129211, #247920, #246372, .T. ) ;
#247684=CARTESIAN_POINT ( 'NONE',  ( -18.50000000000000000, 77.16412189325360771, -162.1082593989527254 ) ) ;
#247699=ORIENTED_EDGE ( 'NONE', *, *, #95387, .F. ) ;
#247706=EDGE_CURVE ( 'NONE', #78372, #123921, #8862, .T. ) ;
#247711=ADVANCED_FACE ( 'NONE', ( #194023 ), #133930, .F. ) ;
#247736=VERTEX_POINT ( 'NONE', #53204 ) ;
#247750=CARTESIAN_POINT ( 'NONE',  ( -20.94999999999999929, 87.65000000001246860, -173.1231074845242688 ) ) ;
#247751=CARTESIAN_POINT ( 'NONE',  ( 18.49999999999999645, 85.32100840337396619, -196.2871692354464415 ) ) ;
#247761=CIRCLE ( 'NONE', #122880, 0.09999999999998898659 ) ;
#247764=ORIENTED_EDGE ( 'NONE', *, *, #89681, .T. ) ;
#247774=CARTESIAN_POINT ( 'NONE',  ( -18.59999999999999787, 64.35000000001264198, -196.5083017138704236 ) ) ;
#247784=ORIENTED_EDGE ( 'NONE', *, *, #247201, .F. ) ;
#247830=EDGE_CURVE ( 'NONE', #210147, #213808, #221220, .T. ) ;
#247831=EDGE_CURVE ( 'NONE', #6886, #162124, #254528, .T. ) ;
#247834=AXIS2_PLACEMENT_3D ( 'NONE', #243449, #64810, #127362 ) ;
#247877=CARTESIAN_POINT ( 'NONE',  ( 21.05000000000000071, 65.57661458509971908, -196.0310555606543517 ) ) ;
#247903=CARTESIAN_POINT ( 'NONE',  ( -23.15000000000000213, 76.00000000001244871, -170.0231074845243597 ) ) ;
#247920=VERTEX_POINT ( 'NONE', #163864 ) ;
#247951=CARTESIAN_POINT ( 'NONE',  ( -21.05000000000000426, 64.40000000001263913, -196.5949042542488883 ) ) ;
#247957=DIRECTION ( 'NONE',  ( 0.000000000000000000, -2.775557561562888827E-14, 1.000000000000000000 ) ) ;
#247994=EDGE_LOOP ( 'NONE', ( #76500, #61074, #150819, #65436 ) ) ;
#248012=ORIENTED_EDGE ( 'NONE', *, *, #41407, .T. ) ;
#248041=CARTESIAN_POINT ( 'NONE',  ( 21.05000000000000071, 76.10000000001272724, -210.0637644362255969 ) ) ;
#248060=AXIS2_PLACEMENT_3D ( 'NONE', #16004, #215454, #36859 ) ;
#248071=CARTESIAN_POINT ( 'NONE',  ( 19.97071067811864609, 64.27928932189385591, -178.8731074845244393 ) ) ;
#248078=CARTESIAN_POINT ( 'NONE',  ( -20.64999999999999858, 85.00000000001251976, -179.9170766071767389 ) ) ;
#248089=FACE_OUTER_BOUND ( 'NONE', #86651, .T. ) ;
#248091=VERTEX_POINT ( 'NONE', #54166 ) ;
#248105=ORIENTED_EDGE ( 'NONE', *, *, #190420, .F. ) ;
#248129=ADVANCED_FACE ( 'NONE', ( #72475 ), #192387, .F. ) ;
#248154=CARTESIAN_POINT ( 'NONE',  ( 23.14999999999999858, 76.00000000001244871, -170.0231074845243597 ) ) ;
#248160=EDGE_CURVE ( 'NONE', #32552, #83659, #38466, .T. ) ;
#248170=FACE_OUTER_BOUND ( 'NONE', #214404, .T. ) ;
#248184=LINE ( 'NONE', #89097, #173556 ) ;
#248192=DIRECTION ( 'NONE',  ( -0.000000000000000000, 6.982962677686266711E-15, -1.000000000000000000 ) ) ;
#248194=CYLINDRICAL_SURFACE ( 'NONE', #120112, 0.09999999999999939493 ) ;
#248207=CARTESIAN_POINT ( 'NONE',  ( -18.50000324121759121, 65.70692517833286672, -164.5644653378303985 ) ) ;
#248250=ORIENTED_EDGE ( 'NONE', *, *, #153951, .F. ) ;
#248274=VERTEX_POINT ( 'NONE', #4463 ) ;
#248293=PLANE ( 'NONE',  #247416 ) ;
#248302=CARTESIAN_POINT ( 'NONE',  ( 23.14999999999999858, 76.00000000001267608, -203.5231074845243597 ) ) ;
#248326=EDGE_CURVE ( 'NONE', #202321, #91017, #242441, .T. ) ;
#248336=AXIS2_PLACEMENT_3D ( 'NONE', #4629, #84125, #163730 ) ;
#248337=DIRECTION ( 'NONE',  ( 1.000000000000000000, 0.000000000000000000, 0.000000000000000000 ) ) ;
#248357=EDGE_LOOP ( 'NONE', ( #255121, #85940, #42165, #97572 ) ) ;
#248383=CARTESIAN_POINT ( 'NONE',  ( -20.64999999999999858, 76.00000000001243450, -168.1231074845243540 ) ) ;
#248421=SURFACE_SIDE_STYLE ('',( #128474 ) ) ;
#248429=ADVANCED_FACE ( 'NONE', ( #108715 ), #188249, .T. ) ;
#248430=CARTESIAN_POINT ( 'NONE',  ( -18.50000000000000000, 85.48068669529139640, -163.0819923157664562 ) ) ;
#248437=ORIENTED_EDGE ( 'NONE', *, *, #203723, .F. ) ;
#248468=DIRECTION ( 'NONE',  ( 1.000000000000000000, 0.000000000000000000, 0.000000000000000000 ) ) ;
#248486=CIRCLE ( 'NONE', #73723, 0.09999999999999971412 ) ;
#248499=DIRECTION ( 'NONE',  ( 1.000000000000000000, -7.304098846218135653E-16, -5.100424963727256530E-30 ) ) ;
#248526=B_SPLINE_CURVE_WITH_KNOTS ( 'NONE', 3,
 ( #83577, #181448, #163167, #84855, #6635, #24949, #2773, #161891 ),
 .UNSPECIFIED., .F., .F.,
 ( 4, 2, 2, 4 ),
 ( 0.000000000000000000, 0.0001094981963948483966, 0.0002189963927896967932, 0.0004379927855793893038 ),
 .UNSPECIFIED. ) ;
#248551=VERTEX_POINT ( 'NONE', #35635 ) ;
#248602=EDGE_CURVE ( 'NONE', #133625, #144953, #104519, .T. ) ;
#248625=TOROIDAL_SURFACE ( 'NONE', #90408, 7.791421356237316687, 0.1000000000000000056 ) ;
#248636=ORIENTED_EDGE ( 'NONE', *, *, #86878, .F. ) ;
#248640=DIRECTION ( 'NONE',  ( 0.000000000000000000, 0.000000000000000000, -1.000000000000000000 ) ) ;
#248668=CARTESIAN_POINT ( 'NONE',  ( -23.15000000000000213, 84.66355140188167638, -179.5472086025916099 ) ) ;
#248671=ORIENTED_EDGE ( 'NONE', *, *, #171624, .T. ) ;
#248684=EDGE_CURVE ( 'NONE', #206261, #68241, #71402, .T. ) ;
#248709=CARTESIAN_POINT ( 'NONE',  ( -18.59999999999999787, 70.65875701002109111, -213.3297576910124178 ) ) ;
#248738=DIRECTION ( 'NONE',  ( 1.000000000000000000, 0.000000000000000000, 0.000000000000000000 ) ) ;
#248742=CYLINDRICAL_SURFACE ( 'NONE', #136391, 0.09999999999998898659 ) ;
#248786=ORIENTED_EDGE ( 'NONE', *, *, #80032, .T. ) ;
#248807=DIRECTION ( 'NONE',  ( -1.000000000000000000, -0.000000000000000000, -0.000000000000000000 ) ) ;
#248818=VECTOR ( 'NONE', #156142, 1000.000000000000000 ) ;
#248820=EDGE_LOOP ( 'NONE', ( #127342, #222746, #148071 ) ) ;
#248829=EDGE_LOOP ( 'NONE', ( #90543, #151837, #171252, #4841 ) ) ;
#248833=DIRECTION ( 'NONE',  ( 1.000000000000000000, -0.000000000000000000, 0.000000000000000000 ) ) ;
#248850=EDGE_LOOP ( 'NONE', ( #73924, #24544, #126229, #1997 ) ) ;
#248861=VECTOR ( 'NONE', #83670, 1000.000000000000000 ) ;
#248866=DIRECTION ( 'NONE',  ( 0.000000000000000000, -7.056502275159890832E-15, 1.000000000000000000 ) ) ;
#248918=ORIENTED_EDGE ( 'NONE', *, *, #178039, .T. ) ;
#248927=CARTESIAN_POINT ( 'NONE',  ( -20.94999999999999929, 87.75000000001247713, -173.1231074845242688 ) ) ;
#248946=CARTESIAN_POINT ( 'NONE',  ( 22.01447462590973458, 75.90096299995320805, -210.7869076857542439 ) ) ;
#248958=ORIENTED_EDGE ( 'NONE', *, *, #155539, .T. ) ;
#248981=AXIS2_PLACEMENT_3D ( 'NONE', #255887, #233819, #13490 ) ;
#249023=VECTOR ( 'NONE', #10435, 1000.000000000000000 ) ;
#249064=CIRCLE ( 'NONE', #244946, 0.1000000000000021289 ) ;
#249088=ORIENTED_EDGE ( 'NONE', *, *, #94340, .T. ) ;
#249098=CIRCLE ( 'NONE', #28352, 0.1000000000000033223 ) ;
#249112=FACE_OUTER_BOUND ( 'NONE', #109303, .T. ) ;
#249158=ORIENTED_EDGE ( 'NONE', *, *, #155993, .T. ) ;
#249162=CARTESIAN_POINT ( 'NONE',  ( -21.70464131381649509, 68.90464198104483273, -203.5231074845243882 ) ) ;
#249185=DIRECTION ( 'NONE',  ( 0.000000000000000000, -1.000000000000000000, -6.982962677686265922E-15 ) ) ;
#249236=ORIENTED_EDGE ( 'NONE', *, *, #209931, .T. ) ;
#249272=DIRECTION ( 'NONE',  ( 0.000000000000000000, -6.982962677686266711E-15, 1.000000000000000000 ) ) ;
#249303=EDGE_CURVE ( 'NONE', #20109, #132574, #129814, .T. ) ;
#249319=ORIENTED_EDGE ( 'NONE', *, *, #94119, .T. ) ;
#249330=CARTESIAN_POINT ( 'NONE',  ( -21.05000000000000071, 69.69503888732768360, -203.5017219185864406 ) ) ;
#249359=VECTOR ( 'NONE', #255538, 1000.000000000000114 ) ;
#249381=DIRECTION ( 'NONE',  ( 1.000000000000000000, 0.000000000000000000, 0.000000000000000000 ) ) ;
#249392=DIRECTION ( 'NONE',  ( 0.000000000000000000, 0.000000000000000000, 1.000000000000000000 ) ) ;
#249405=DIRECTION ( 'NONE',  ( 1.000000000000000000, 0.000000000000000000, 0.000000000000000000 ) ) ;
#249445=AXIS2_PLACEMENT_3D ( 'NONE', #1468, #99274, #22352 ) ;
#249458=AXIS2_PLACEMENT_3D ( 'NONE', #95714, #237810, #136104 ) ;
#249476=AXIS2_PLACEMENT_3D ( 'NONE', #54872, #51004, #251804 ) ;
#249479=CYLINDRICAL_SURFACE ( 'NONE', #57785, 0.1000000000000072220 ) ;
#249483=DIRECTION ( 'NONE',  ( 1.000000000000000000, 0.000000000000000000, 0.000000000000000000 ) ) ;
#249485=FACE_OUTER_BOUND ( 'NONE', #257088, .T. ) ;
#249510=DIRECTION ( 'NONE',  ( 0.000000000000000000, -1.000000000000000000, -6.982962677686265922E-15 ) ) ;
#249579=DIRECTION ( 'NONE',  ( 0.000000000000000000, 1.000000000000000000, 6.982962677686266711E-15 ) ) ;
#249593=CARTESIAN_POINT ( 'NONE',  ( 20.12518398540832010, 66.02491127934493420, -195.5264392320576974 ) ) ;
#249617=ORIENTED_EDGE ( 'NONE', *, *, #247654, .T. ) ;
#249618=ORIENTED_EDGE ( 'NONE', *, *, #64702, .F. ) ;
#249648=AXIS2_PLACEMENT_3D ( 'NONE', #63142, #64451, #143968 ) ;
#249649=ORIENTED_EDGE ( 'NONE', *, *, #68585, .T. ) ;
#249652=ORIENTED_EDGE ( 'NONE', *, *, #22098, .T. ) ;
#249660=ORIENTED_EDGE ( 'NONE', *, *, #22934, .T. ) ;
#249686=( BOUNDED_CURVE ( )  B_SPLINE_CURVE ( 3, ( #201441, #101010, #140168, #183186 ),
 .UNSPECIFIED., .F., .F. ) 
 B_SPLINE_CURVE_WITH_KNOTS ( ( 4, 4 ),
 ( 3.141592653589793116, 4.712388980384689674 ),
 .UNSPECIFIED. ) 
 CURVE ( )  GEOMETRIC_REPRESENTATION_ITEM ( )  RATIONAL_B_SPLINE_CURVE ( ( 1.000000000000000000, 0.8047378541243649375, 0.8047378541243649375, 1.000000000000000000 ) ) 
 REPRESENTATION_ITEM ( '' )  );
#249692=CARTESIAN_POINT ( 'NONE',  ( 21.14999999999999858, 76.10000000001268461, -203.5231074845243597 ) ) ;
#249694=VERTEX_POINT ( 'NONE', #24045 ) ;
#249699=DIRECTION ( 'NONE',  ( 0.000000000000000000, 0.9908441862701791170, 0.1350103645450472789 ) ) ;
#249734=ORIENTED_EDGE ( 'NONE', *, *, #238626, .F. ) ;
#249782=CARTESIAN_POINT ( 'NONE',  ( 22.39999999999999503, 64.35000000001267040, -203.6231074845244393 ) ) ;
#249793=EDGE_LOOP ( 'NONE', ( #148013, #99113, #107631, #125235 ) ) ;
#249822=CARTESIAN_POINT ( 'NONE',  ( -21.05000000000000071, 77.16270174995064224, -195.4231074845243370 ) ) ;
#249833=ORIENTED_EDGE ( 'NONE', *, *, #182176, .T. ) ;
#249844=ADVANCED_FACE ( 'NONE', ( #168724 ), #10895, .F. ) ;
#249845=ADVANCED_FACE ( 'NONE', ( #109971 ), #46261, .T. ) ;
#249854=EDGE_CURVE ( 'NONE', #133612, #176502, #63347, .T. ) ;
#249864=LINE ( 'NONE', #71248, #140590 ) ;
#249866=CARTESIAN_POINT ( 'NONE',  ( 20.94999999999999929, 77.16412189325360771, -162.1082593989527254 ) ) ;
#249878=EDGE_CURVE ( 'NONE', #68808, #77018, #242421, .T. ) ;
#249887=EDGE_CURVE ( 'NONE', #110167, #171376, #193397, .T. ) ;
#249902=AXIS2_PLACEMENT_3D ( 'NONE', #212287, #210990, #216105 ) ;
#249956=CARTESIAN_POINT ( 'NONE',  ( 22.00411653962159519, 68.74655713164250415, -203.6221455902930302 ) ) ;
#250020=DIRECTION ( 'NONE',  ( -0.000000000000000000, -1.000000000000000000, -6.982962677686266711E-15 ) ) ;
#250032=ADVANCED_FACE ( 'NONE', ( #220647 ), #65411, .T. ) ;
#250036=CARTESIAN_POINT ( 'NONE',  ( -23.15000000000000213, 80.83132476063549632, -186.5534105423255653 ) ) ;
#250051=EDGE_CURVE ( 'NONE', #222999, #9515, #155179, .T. ) ;
#250101=FACE_OUTER_BOUND ( 'NONE', #96645, .T. ) ;
#250104=CIRCLE ( 'NONE', #204285, 2.000000000000001776 ) ;
#250171=AXIS2_PLACEMENT_3D ( 'NONE', #207575, #8086, #13225 ) ;
#250177=EDGE_LOOP ( 'NONE', ( #19974, #143404, #190868, #69529 ) ) ;
#250240=DIRECTION ( 'NONE',  ( -1.000000000000000000, 0.000000000000000000, -0.000000000000000000 ) ) ;
#250357=ORIENTED_EDGE ( 'NONE', *, *, #146679, .F. ) ;
#250379=DIRECTION ( 'NONE',  ( 1.000000000000000000, 0.000000000000000000, 0.000000000000000000 ) ) ;
#250397=FACE_OUTER_BOUND ( 'NONE', #134072, .T. ) ;
#250427=CARTESIAN_POINT ( 'NONE',  ( -21.64999999999999858, 68.65000000001253966, -182.2731074845244166 ) ) ;
#250435=DIRECTION ( 'NONE',  ( 1.000000000000000000, 0.000000000000000000, 0.000000000000000000 ) ) ;
#250439=CARTESIAN_POINT ( 'NONE',  ( -22.47071067811865319, 75.90090754531013317, -211.2431822290224090 ) ) ;
#250450=DIRECTION ( 'NONE',  ( 0.000000000000000000, -6.982962677686266711E-15, 1.000000000000000000 ) ) ;
#250477=CARTESIAN_POINT ( 'NONE',  ( 20.85000000000000142, 69.06610602788607878, -166.2374616501508342 ) ) ;
#250478=AXIS2_PLACEMENT_3D ( 'NONE', #124832, #46549, #25724 ) ;
#250485=EDGE_LOOP ( 'NONE', ( #67384, #56743, #123713 ) ) ;
#250523=AXIS2_PLACEMENT_3D ( 'NONE', #198768, #159662, #239189 ) ;
#250559=EDGE_LOOP ( 'NONE', ( #177279, #175845, #85795, #189417 ) ) ;
#250581=ORIENTED_EDGE ( 'NONE', *, *, #129260, .T. ) ;
#250604=VERTEX_POINT ( 'NONE', #113210 ) ;
#250623=EDGE_CURVE ( 'NONE', #202942, #139907, #246884, .T. ) ;
#250633=DIRECTION ( 'NONE',  ( -1.000000000000000000, -0.000000000000000000, -0.000000000000000000 ) ) ;
#250641=ORIENTED_EDGE ( 'NONE', *, *, #123417, .T. ) ;
#250650=AXIS2_PLACEMENT_3D ( 'NONE', #7620, #244938, #147114 ) ;
#250667=ORIENTED_EDGE ( 'NONE', *, *, #241797, .F. ) ;
#250682=EDGE_CURVE ( 'NONE', #55154, #129211, #196997, .T. ) ;
#250715=DIRECTION ( 'NONE',  ( 0.000000000000000000, -7.116814260417668513E-15, 1.000000000000000000 ) ) ;
#250719=DIRECTION ( 'NONE',  ( -1.000000000000000000, 2.952720810173289112E-16, 2.061873921506763405E-30 ) ) ;
#250720=CARTESIAN_POINT ( 'NONE',  ( -18.59999999999999787, 64.35000000001259934, -191.3731074845244393 ) ) ;
#250734=ORIENTED_EDGE ( 'NONE', *, *, #53115, .F. ) ;
#250760=DIRECTION ( 'NONE',  ( 1.000000000000000000, 0.000000000000000000, 0.000000000000000000 ) ) ;
#250766=DIRECTION ( 'NONE',  ( -1.000000000000000000, 0.000000000000000000, -0.000000000000000000 ) ) ;
#250771=EDGE_CURVE ( 'NONE', #247011, #103860, #240869, .T. ) ;
#250809=CARTESIAN_POINT ( 'NONE',  ( 21.05000000000000071, 65.27628289530507288, -191.3731074845244393 ) ) ;
#250868=CARTESIAN_POINT ( 'NONE',  ( 18.59999999999999076, 69.55000000001261640, -193.5060803140843859 ) ) ;
#250896=LINE ( 'NONE', #167548, #215252 ) ;
#250909=DIRECTION ( 'NONE',  ( -1.000000000000000000, -0.000000000000000000, -0.000000000000000000 ) ) ;
#250918=AXIS2_PLACEMENT_3D ( 'NONE', #60569, #17589, #214512 ) ;
#250920=DIRECTION ( 'NONE',  ( 0.000000000000000000, 6.982962677686266711E-15, -1.000000000000000000 ) ) ;
#250924=EDGE_LOOP ( 'NONE', ( #170525, #204688, #106620, #208460 ) ) ;
#250959=DIRECTION ( 'NONE',  ( -1.000000000000000000, -0.000000000000000000, -0.000000000000000000 ) ) ;
#250964=ORIENTED_EDGE ( 'NONE', *, *, #212170, .T. ) ;
#250983=ORIENTED_EDGE ( 'NONE', *, *, #149765, .T. ) ;
#251038=EDGE_CURVE ( 'NONE', #100336, #17038, #254641, .T. ) ;
#251077=DIRECTION ( 'NONE',  ( -1.000000000000000000, 0.000000000000000000, 0.000000000000000000 ) ) ;
#251083=DIRECTION ( 'NONE',  ( 0.000000000000000000, 0.000000000000000000, 1.000000000000000000 ) ) ;
#251088=CARTESIAN_POINT ( 'NONE',  ( -21.05000000000000071, 64.37928932189399234, -196.6546908321834053 ) ) ;
#251095=CARTESIAN_POINT ( 'NONE',  ( -18.59999999999999787, 77.86671491006991630, -191.7704322382423356 ) ) ;
#251132=ORIENTED_EDGE ( 'NONE', *, *, #41407, .F. ) ;
#251142=CARTESIAN_POINT ( 'NONE',  ( -18.50000000000000355, 77.26327546522965406, -162.1212428177779543 ) ) ;
#251186=EDGE_CURVE ( 'NONE', #172803, #109697, #59989, .T. ) ;
#251214=AXIS2_PLACEMENT_3D ( 'NONE', #16432, #115499, #58076 ) ;
#251230=LINE ( 'NONE', #119454, #109786 ) ;
#251264=ORIENTED_EDGE ( 'NONE', *, *, #211653, .F. ) ;
#251274=EDGE_CURVE ( 'NONE', #166912, #252901, #68385, .T. ) ;
#251298=EDGE_CURVE ( 'NONE', #115598, #185078, #84908, .T. ) ;
#251305=CYLINDRICAL_SURFACE ( 'NONE', #95169, 0.09999999999998898659 ) ;
#251332=EDGE_CURVE ( 'NONE', #252282, #173853, #118279, .T. ) ;
#251338=EDGE_LOOP ( 'NONE', ( #223769, #117871, #144215, #184323 ) ) ;
#251359=AXIS2_PLACEMENT_3D ( 'NONE', #161635, #41680, #100322 ) ;
#251390=CARTESIAN_POINT ( 'NONE',  ( -23.25000000000000000, 77.25000000001239187, -162.2226267301092548 ) ) ;
#251402=DIRECTION ( 'NONE',  ( 0.000000000000000000, -7.429790795770644761E-15, 1.000000000000000000 ) ) ;
#251419=DIRECTION ( 'NONE',  ( 0.000000000000000000, 0.000000000000000000, 1.000000000000000000 ) ) ;
#251423=EDGE_CURVE ( 'NONE', #162455, #242379, #59992, .T. ) ;
#251474=DIRECTION ( 'NONE',  ( 0.000000000000000000, 0.1568667991644355497, -0.9876197685951332295 ) ) ;
#251481=DIRECTION ( 'NONE',  ( -7.304098846218134667E-16, 1.000000000000000000, 6.982962677686267499E-15 ) ) ;
#251509=VERTEX_POINT ( 'NONE', #35355 ) ;
#251512=DIRECTION ( 'NONE',  ( 0.000000000000000000, -7.086529944415886769E-15, 1.000000000000000000 ) ) ;
#251513=ADVANCED_FACE ( 'NONE', ( #204640 ), #243783, .T. ) ;
#251549=CARTESIAN_POINT ( 'NONE',  ( -20.85000000000000142, 69.15387683765983695, -166.2853812176745691 ) ) ;
#251566=CIRCLE ( 'NONE', #39224, 0.09999999999999939493 ) ;
#251593=EDGE_LOOP ( 'NONE', ( #185974, #201068, #80946, #188670, #75763 ) ) ;
#251625=CARTESIAN_POINT ( 'NONE',  ( 18.60000000000000497, 76.00000000001267608, -203.5231074845243597 ) ) ;
#251652=ADVANCED_FACE ( 'NONE', ( #207242 ), #31200, .T. ) ;
#251686=TOROIDAL_SURFACE ( 'NONE', #214094, 0.2000000000000000111, 0.1000000000000000056 ) ;
#251705=EDGE_LOOP ( 'NONE', ( #116561, #206896, #221245, #171629 ) ) ;
#251727=CARTESIAN_POINT ( 'NONE',  ( -23.15000000000000213, 76.00000000001267608, -203.5231074845243597 ) ) ;
#251731=EDGE_CURVE ( 'NONE', #27052, #220964, #76747, .T. ) ;
#251756=DIRECTION ( 'NONE',  ( 0.000000000000000000, 0.9654727137038715545, -0.2605042016806676242 ) ) ;
#251778=ORIENTED_EDGE ( 'NONE', *, *, #162498, .T. ) ;
#251803=CARTESIAN_POINT ( 'NONE',  ( -22.50000000000000000, 76.00000000001271871, -209.7731074845243597 ) ) ;
#251804=DIRECTION ( 'NONE',  ( 0.000000000000000000, 0.8660254037844420383, -0.4999999999999943379 ) ) ;
#251808=LINE ( 'NONE', #247951, #118110 ) ;
#251810=CIRCLE ( 'NONE', #1993, 12.97499999999998721 ) ;
#251838=ORIENTED_EDGE ( 'NONE', *, *, #31148, .T. ) ;
#251848=ORIENTED_EDGE ( 'NONE', *, *, #79460, .T. ) ;
#251871=ORIENTED_EDGE ( 'NONE', *, *, #251423, .T. ) ;
#251894=DIRECTION ( 'NONE',  ( 1.734723475976817507E-14, 1.000000000000000000, 6.982962677686266711E-15 ) ) ;
#251895=ORIENTED_EDGE ( 'NONE', *, *, #59499, .T. ) ;
#251916=CARTESIAN_POINT ( 'NONE',  ( -20.54999999999999716, 74.05981308412469843, -182.8522266955776843 ) ) ;
#251918=EDGE_LOOP ( 'NONE', ( #29319, #43287, #247180 ) ) ;
#251937=ORIENTED_EDGE ( 'NONE', *, *, #246771, .T. ) ;
#251949=PRESENTATION_STYLE_ASSIGNMENT (( #133295 ) ) ;
#251951=VECTOR ( 'NONE', #67761, 1000.000000000000000 ) ;
#251965=VERTEX_POINT ( 'NONE', #41441 ) ;
#252003=DIRECTION ( 'NONE',  ( 1.000000000000000000, 0.000000000000000000, 0.000000000000000000 ) ) ;
#252022=EDGE_CURVE ( 'NONE', #32434, #38825, #76931, .T. ) ;
#252025=CARTESIAN_POINT ( 'NONE',  ( 20.94999675878240808, 65.70692517833285251, -164.5644653378303985 ) ) ;
#252032=CIRCLE ( 'NONE', #214425, 0.09999999999998898659 ) ;
#252050=LINE ( 'NONE', #254593, #62161 ) ;
#252062=AXIS2_PLACEMENT_3D ( 'NONE', #2325, #23219, #182277 ) ;
#252146=VECTOR ( 'NONE', #107453, 1000.000000000000114 ) ;
#252148=VERTEX_POINT ( 'NONE', #111658 ) ;
#252179=EDGE_LOOP ( 'NONE', ( #70961, #40243, #113746, #41281 ) ) ;
#252194=VERTEX_POINT ( 'NONE', #137619 ) ;
#252204=EDGE_CURVE ( 'NONE', #178668, #2919, #197912, .T. ) ;
#252216=FACE_OUTER_BOUND ( 'NONE', #227754, .T. ) ;
#252242=ORIENTED_EDGE ( 'NONE', *, *, #63068, .T. ) ;
#252250=CARTESIAN_POINT ( 'NONE',  ( -20.94999999999999929, 64.30000000001250271, -176.7781056340430723 ) ) ;
#252277=LINE ( 'NONE', #31987, #181984 ) ;
#252280=VECTOR ( 'NONE', #78940, 1000.000000000000000 ) ;
#252281=ORIENTED_EDGE ( 'NONE', *, *, #155308, .T. ) ;
#252282=VERTEX_POINT ( 'NONE', #41137 ) ;
#252326=DIRECTION ( 'NONE',  ( 0.000000000000000000, -6.938893903907222067E-15, 1.000000000000000000 ) ) ;
#252327=ADVANCED_FACE ( 'NONE', ( #59348 ), #118837, .T. ) ;
#252339=EDGE_CURVE ( 'NONE', #225348, #148199, #56448, .T. ) ;
#252347=AXIS2_PLACEMENT_3D ( 'NONE', #109587, #71782, #70512 ) ;
#252355=ADVANCED_FACE ( 'NONE', ( #22860 ), #102328, .T. ) ;
#252367=DIRECTION ( 'NONE',  ( 0.000000000000000000, 0.000000000000000000, 1.000000000000000000 ) ) ;
#252373=CARTESIAN_POINT ( 'NONE',  ( 18.59999999999999787, 74.13328508995527955, -191.7704322382423641 ) ) ;
#252380=CARTESIAN_POINT ( 'NONE',  ( 18.49999999999999289, 69.15387683765983695, -166.2853812176745691 ) ) ;
#252392=ADVANCED_FACE ( 'NONE', ( #142757 ), #97937, .F. ) ;
#252425=EDGE_LOOP ( 'NONE', ( #231929, #41881, #77668, #62061 ) ) ;
#252447=DIRECTION ( 'NONE',  ( 0.000000000000000000, 6.982962677686266711E-15, -1.000000000000000000 ) ) ;
#252458=AXIS2_PLACEMENT_3D ( 'NONE', #101483, #83218, #160253 ) ;
#252486=ORIENTED_EDGE ( 'NONE', *, *, #54337, .T. ) ;
#252491=EDGE_CURVE ( 'NONE', #100958, #131701, #65806, .T. ) ;
#252497=ORIENTED_EDGE ( 'NONE', *, *, #195922, .F. ) ;
#252524=CARTESIAN_POINT ( 'NONE',  ( -21.55000000000000071, 68.65000000001253966, -182.3731074845244109 ) ) ;
#252534=AXIS2_PLACEMENT_3D ( 'NONE', #130219, #205914, #28624 ) ;
#252535=CARTESIAN_POINT ( 'NONE',  ( -20.64999999999999858, 74.00000000001254818, -182.8477294072864652 ) ) ;
#252545=VECTOR ( 'NONE', #91254, 1000.000000000000000 ) ;
#252570=CARTESIAN_POINT ( 'NONE',  ( -22.00411653889199570, 75.90096189422563100, -210.7765503521646622 ) ) ;
#252596=TOROIDAL_SURFACE ( 'NONE', #19385, 11.65000000000000036, 0.1000000000000000056 ) ;
#252617=CARTESIAN_POINT ( 'NONE',  ( -21.05000000000000071, 76.00000000001273293, -210.0637644362255685 ) ) ;
#252676=CARTESIAN_POINT ( 'NONE',  ( -20.54999999999999716, 73.60000000001254250, -183.2477294072864709 ) ) ;
#252702=ORIENTED_EDGE ( 'NONE', *, *, #106997, .F. ) ;
#252707=DIRECTION ( 'NONE',  ( 0.000000000000000000, 0.8700118002898393765, -0.4930308989875104575 ) ) ;
#252715=CIRCLE ( 'NONE', #27917, 4.049999999999998046 ) ;
#252735=ORIENTED_EDGE ( 'NONE', *, *, #180589, .F. ) ;
#252792=AXIS2_PLACEMENT_3D ( 'NONE', #191999, #53745, #249392 ) ;
#252808=EDGE_CURVE ( 'NONE', #4716, #177211, #164795, .T. ) ;
#252810=CARTESIAN_POINT ( 'NONE',  ( -23.25000000000000000, 85.60000000001262777, -193.6291383618718385 ) ) ;
#252819=EDGE_CURVE ( 'NONE', #170452, #28569, #143670, .T. ) ;
#252834=CIRCLE ( 'NONE', #240384, 0.09999999999998898659 ) ;
#252858=TOROIDAL_SURFACE ( 'NONE', #115482, 11.65000000000000036, 0.1000000000000000056 ) ;
#252873=EDGE_CURVE ( 'NONE', #2919, #43634, #235694, .T. ) ;
#252879=DIRECTION ( 'NONE',  ( 0.000000000000000000, -6.517943393102675675E-15, 1.000000000000000000 ) ) ;
#252886=EDGE_LOOP ( 'NONE', ( #112806, #88354, #133806, #55397 ) ) ;
#252893=DIRECTION ( 'NONE',  ( 0.000000000000000000, -6.982962677686266711E-15, 1.000000000000000000 ) ) ;
#252901=VERTEX_POINT ( 'NONE', #254258 ) ;
#252906=CARTESIAN_POINT ( 'NONE',  ( 18.55807992284871588, 65.67101464000555211, -164.4404391622479977 ) ) ;
#252919=DIRECTION ( 'NONE',  ( -1.000000000000000000, 0.000000000000000000, 0.000000000000000000 ) ) ;
#252948=CARTESIAN_POINT ( 'NONE',  ( -21.55000000000000426, 68.25000000001253397, -182.2731074845244166 ) ) ;
#252967=AXIS2_PLACEMENT_3D ( 'NONE', #146659, #250909, #150550 ) ;
#252974=ORIENTED_EDGE ( 'NONE', *, *, #27732, .T. ) ;
#252989=ORIENTED_EDGE ( 'NONE', *, *, #143997, .F. ) ;
#253002=AXIS2_PLACEMENT_3D ( 'NONE', #57265, #101509, #39029 ) ;
#253008=AXIS2_PLACEMENT_3D ( 'NONE', #200080, #116680, #176682 ) ;
#253013=EDGE_LOOP ( 'NONE', ( #236032, #119249, #25699, #17736 ) ) ;
#253014=DIRECTION ( 'NONE',  ( -4.391705002472927119E-16, -1.000000000000000000, -7.026728003956683390E-15 ) ) ;
#253041=CIRCLE ( 'NONE', #240577, 0.6000000000000033085 ) ;
#253052=ORIENTED_EDGE ( 'NONE', *, *, #181833, .F. ) ;
#253053=CARTESIAN_POINT ( 'NONE',  ( 23.14999999999999858, 76.00000000001244871, -170.0231074845243597 ) ) ;
#253065=CARTESIAN_POINT ( 'NONE',  ( -23.25000000000000000, 64.35000000001275566, -215.2731074845244450 ) ) ;
#253078=CIRCLE ( 'NONE', #219755, 0.09999999999998898659 ) ;
#253107=DIRECTION ( 'NONE',  ( 0.000000000000000000, -1.411300455031978166E-14, 1.000000000000000000 ) ) ;
#253114=AXIS2_PLACEMENT_3D ( 'NONE', #245637, #5709, #146512 ) ;
#253171=AXIS2_PLACEMENT_3D ( 'NONE', #14728, #89093, #128234 ) ;
#253185=AXIS2_PLACEMENT_3D ( 'NONE', #1128, #61124, #130076 ) ;
#253192=DIRECTION ( 'NONE',  ( -1.000000000000000000, 0.000000000000000000, 0.000000000000000000 ) ) ;
#253218=ORIENTED_EDGE ( 'NONE', *, *, #77853, .F. ) ;
#253223=ORIENTED_EDGE ( 'NONE', *, *, #243411, .F. ) ;
#253239=CARTESIAN_POINT ( 'NONE',  ( -18.50000000000000000, 64.25000000001254818, -182.1731074845244507 ) ) ;
#253248=EDGE_CURVE ( 'NONE', #52715, #192523, #140246, .T. ) ;
#253252=CARTESIAN_POINT ( 'NONE',  ( 18.54286124688534443, 85.62391757881020737, -163.2819051526615510 ) ) ;
#253257=DIRECTION ( 'NONE',  ( -0.000000000000000000, 1.000000000000000000, 6.982962677686266711E-15 ) ) ;
#253260=FACE_OUTER_BOUND ( 'NONE', #23872, .T. ) ;
#253272=EDGE_CURVE ( 'NONE', #10849, #122787, #164970, .T. ) ;
#253280=DIRECTION ( 'NONE',  ( 0.000000000000000000, -0.2605042016806740079, 0.9654727137038698892 ) ) ;
#253320=CIRCLE ( 'NONE', #207557, 0.1000000000000028644 ) ;
#253345=FACE_OUTER_BOUND ( 'NONE', #53780, .T. ) ;
#253356=DIRECTION ( 'NONE',  ( 0.000000000000000000, 0.000000000000000000, 1.000000000000000000 ) ) ;
#253384=EDGE_CURVE ( 'NONE', #226219, #154016, #43741, .T. ) ;
#253394=CARTESIAN_POINT ( 'NONE',  ( 20.85000000000000142, 64.25000000001249134, -176.8069731475025321 ) ) ;
#253417=ORIENTED_EDGE ( 'NONE', *, *, #157775, .F. ) ;
#253464=DIRECTION ( 'NONE',  ( -1.000000000000000000, 2.952720810173289112E-16, 2.061873921506763405E-30 ) ) ;
#253495=DIRECTION ( 'NONE',  ( 0.000000000000000000, 0.000000000000000000, -1.000000000000000000 ) ) ;
#253519=CARTESIAN_POINT ( 'NONE',  ( -23.25000000000000000, 76.00000000001244871, -170.0231074845243597 ) ) ;
#253523=CARTESIAN_POINT ( 'NONE',  ( 21.14999999999999858, 64.35000000001258513, -191.2731074845244450 ) ) ;
#253527=ORIENTED_EDGE ( 'NONE', *, *, #139135, .F. ) ;
#253553=ORIENTED_EDGE ( 'NONE', *, *, #26308, .F. ) ;
#253555=VERTEX_POINT ( 'NONE', #17449 ) ;
#253560=CARTESIAN_POINT ( 'NONE',  ( -20.85000000000000142, 64.25000000001244871, -170.0231074845244166 ) ) ;
#253579=CARTESIAN_POINT ( 'NONE',  ( 23.15000000000000213, 84.66355140188167638, -179.5472086025916099 ) ) ;
#253585=VERTEX_POINT ( 'NONE', #40902 ) ;
#253607=CIRCLE ( 'NONE', #137106, 0.09999999999999939493 ) ;
#253645=DIRECTION ( 'NONE',  ( 0.000000000000000000, 0.000000000000000000, 1.000000000000000000 ) ) ;
#253657=CARTESIAN_POINT ( 'NONE',  ( 20.94999999999999929, 87.48912529308852015, -173.1231074845242688 ) ) ;
#253668=ADVANCED_FACE ( 'NONE', ( #4292 ), #35448, .T. ) ;
#253678=DIRECTION ( 'NONE',  ( -1.000000000000000000, 0.000000000000000000, -0.000000000000000000 ) ) ;
#253709=CYLINDRICAL_SURFACE ( 'NONE', #133043, 0.09999999999998898659 ) ;
#253712=EDGE_LOOP ( 'NONE', ( #183707, #125800, #193515 ) ) ;
#253725=FACE_OUTER_BOUND ( 'NONE', #97511, .T. ) ;
#253731=AXIS2_PLACEMENT_3D ( 'NONE', #216699, #66623, #86147 ) ;
#253760=DIRECTION ( 'NONE',  ( 1.000000000000000000, 0.000000000000000000, 0.000000000000000000 ) ) ;
#253769=ORIENTED_EDGE ( 'NONE', *, *, #153621, .F. ) ;
#253827=CIRCLE ( 'NONE', #33142, 7.800000000000001599 ) ;
#253907=ORIENTED_EDGE ( 'NONE', *, *, #114112, .T. ) ;
#253918=DIRECTION ( 'NONE',  ( 1.000000000000000000, 0.000000000000000000, 0.000000000000000000 ) ) ;
#253929=DIRECTION ( 'NONE',  ( 0.000000000000000000, -6.982962677686266711E-15, 1.000000000000000000 ) ) ;
#253989=FACE_OUTER_BOUND ( 'NONE', #77026, .T. ) ;
#253996=EDGE_CURVE ( 'NONE', #252194, #171376, #121421, .T. ) ;
#254067=EDGE_LOOP ( 'NONE', ( #116220, #142930, #54955, #178895 ) ) ;
#254107=EDGE_CURVE ( 'NONE', #105519, #205739, #173381, .T. ) ;
#254116=CARTESIAN_POINT ( 'NONE',  ( 23.14999999999998437, 76.00000000001267608, -203.5231074845243597 ) ) ;
#254118=FACE_OUTER_BOUND ( 'NONE', #57219, .T. ) ;
#254122=VERTEX_POINT ( 'NONE', #163098 ) ;
#254167=ORIENTED_EDGE ( 'NONE', *, *, #133915, .F. ) ;
#254174=DIRECTION ( 'NONE',  ( 1.000000000000000000, 0.000000000000000000, 0.000000000000000000 ) ) ;
#254179=CARTESIAN_POINT ( 'NONE',  ( 18.50000972452444969, 65.70673848567014375, -164.5638252334829872 ) ) ;
#254182=EDGE_CURVE ( 'NONE', #179110, #121258, #70435, .T. ) ;
#254196=ORIENTED_EDGE ( 'NONE', *, *, #53365, .T. ) ;
#254201=DIRECTION ( 'NONE',  ( 1.000000000000000000, 0.000000000000000000, 0.000000000000000000 ) ) ;
#254209=EDGE_CURVE ( 'NONE', #233373, #109083, #2632, .T. ) ;
#254220=CARTESIAN_POINT ( 'NONE',  ( 21.05000000000000071, 76.00000000001244871, -170.0231074845243597 ) ) ;
#254232=AXIS2_PLACEMENT_3D ( 'NONE', #64084, #240166, #40712 ) ;
#254248=ORIENTED_EDGE ( 'NONE', *, *, #66275, .F. ) ;
#254258=CARTESIAN_POINT ( 'NONE',  ( -23.15000000000000213, 74.07476635515278929, -190.7928639513982318 ) ) ;
#254278=LINE ( 'NONE', #37846, #18600 ) ;
#254279=CARTESIAN_POINT ( 'NONE',  ( 18.59999999999999076, 77.25000000001263345, -195.5231074845243313 ) ) ;
#254283=ADVANCED_FACE ( 'NONE', ( #232056 ), #7874, .F. ) ;
#254286=EDGE_CURVE ( 'NONE', #24117, #217574, #235677, .T. ) ;
#254315=DIRECTION ( 'NONE',  ( 0.000000000000000000, 0.4999999999999943379, 0.8660254037844420383 ) ) ;
#254334=CARTESIAN_POINT ( 'NONE',  ( 22.49533356619864577, 64.34999999370857893, -203.5882300648472381 ) ) ;
#254335=ORIENTED_EDGE ( 'NONE', *, *, #49621, .T. ) ;
#254339=AXIS2_PLACEMENT_3D ( 'NONE', #53808, #17262, #252003 ) ;
#254355=EDGE_CURVE ( 'NONE', #221154, #252282, #74281, .T. ) ;
#254384=DIRECTION ( 'NONE',  ( 0.7071359030027593029, -0.7070776581709197206, 0.000000000000000000 ) ) ;
#254406=DIRECTION ( 'NONE',  ( 0.000000000000000000, -0.008583690987162452199, 0.9999631594459053030 ) ) ;
#254407=EDGE_LOOP ( 'NONE', ( #216355, #181534, #5963, #187112 ) ) ;
#254411=ORIENTED_EDGE ( 'NONE', *, *, #109609, .T. ) ;
#254429=AXIS2_PLACEMENT_3D ( 'NONE', #102747, #183602, #127475 ) ;
#254439=DIRECTION ( 'NONE',  ( 1.000000000000000000, 0.000000000000000000, 0.000000000000000000 ) ) ;
#254443=ORIENTED_EDGE ( 'NONE', *, *, #80765, .T. ) ;
#254447=ADVANCED_FACE ( 'NONE', ( #5911 ), #202842, .T. ) ;
#254459=CARTESIAN_POINT ( 'NONE',  ( 23.14999999999999858, 76.00000000001244871, -170.0231074845243597 ) ) ;
#254462=DIRECTION ( 'NONE',  ( 0.000000000000000000, -0.8660254037844377084, -0.5000000000000016653 ) ) ;
#254524=EDGE_CURVE ( 'NONE', #125487, #59470, #202546, .T. ) ;
#254528=CIRCLE ( 'NONE', #50524, 0.09999999999999939493 ) ;
#254555=ORIENTED_EDGE ( 'NONE', *, *, #241797, .T. ) ;
#254558=FACE_OUTER_BOUND ( 'NONE', #3351, .T. ) ;
#254571=DIRECTION ( 'NONE',  ( 1.000000000000000000, 0.000000000000000000, 0.000000000000000000 ) ) ;
#254590=ORIENTED_EDGE ( 'NONE', *, *, #200678, .T. ) ;
#254593=CARTESIAN_POINT ( 'NONE',  ( -18.50000000000000000, 64.35000000001276987, -215.2731074845244450 ) ) ;
#254595=CARTESIAN_POINT ( 'NONE',  ( -20.85000000000000142, 77.85161776048127535, -158.4199177649206831 ) ) ;
#254603=AXIS2_PLACEMENT_3D ( 'NONE', #77973, #40453, #101628 ) ;
#254613=ADVANCED_FACE ( 'NONE', ( #114007 ), #131012, .T. ) ;
#254628=CARTESIAN_POINT ( 'NONE',  ( 18.50000000000000711, 85.41920976342188965, -196.2753380217653785 ) ) ;
#254641=LINE ( 'NONE', #218091, #9744 ) ;
#254653=FACE_BOUND ( 'NONE', #33555, .T. ) ;
#254689=VERTEX_POINT ( 'NONE', #60451 ) ;
#254700=ADVANCED_FACE ( 'NONE', ( #160870 ), #119164, .F. ) ;
#254706=ORIENTED_EDGE ( 'NONE', *, *, #1998, .F. ) ;
#254768=ADVANCED_FACE ( 'NONE', ( #26494 ), #23937, .F. ) ;
#254770=DIRECTION ( 'NONE',  ( 1.000000000000000000, 0.000000000000000000, 0.000000000000000000 ) ) ;
#254794=EDGE_CURVE ( 'NONE', #71381, #91407, #140366, .T. ) ;
#254833=ORIENTED_EDGE ( 'NONE', *, *, #247092, .T. ) ;
#254841=CONICAL_SURFACE ( 'NONE', #34368, 4.299999999999970512, 0.7853981633974466137 ) ;
#254857=SPHERICAL_SURFACE ( 'NONE', #159493, 0.1000000000000000056 ) ;
#254905=CIRCLE ( 'NONE', #192616, 4.150000000000001243 ) ;
#254913=ORIENTED_EDGE ( 'NONE', *, *, #188171, .T. ) ;
#254920=CARTESIAN_POINT ( 'NONE',  ( 18.49999999999999289, 68.97833521811233481, -166.1895420826271277 ) ) ;
#254944=DIRECTION ( 'NONE',  ( 0.000000000000000000, -6.982962677686266711E-15, 1.000000000000000000 ) ) ;
#254975=ORIENTED_EDGE ( 'NONE', *, *, #41038, .F. ) ;
#254977=DIRECTION ( 'NONE',  ( 0.000000000000000000, -1.000000000000000000, -6.982962677686265922E-15 ) ) ;
#255004=EDGE_CURVE ( 'NONE', #156136, #139303, #181, .T. ) ;
#255027=LINE ( 'NONE', #230398, #209549 ) ;
#255041=ORIENTED_EDGE ( 'NONE', *, *, #113490, .F. ) ;
#255056=ORIENTED_EDGE ( 'NONE', *, *, #100263, .T. ) ;
#255066=ORIENTED_EDGE ( 'NONE', *, *, #112755, .F. ) ;
#255101=AXIS2_PLACEMENT_3D ( 'NONE', #165620, #31269, #149909 ) ;
#255113=EDGE_CURVE ( 'NONE', #221772, #88021, #182701, .T. ) ;
#255121=ORIENTED_EDGE ( 'NONE', *, *, #19651, .F. ) ;
#255157=ADVANCED_FACE ( 'NONE', ( #223083 ), #57802, .F. ) ;
#255199=EDGE_CURVE ( 'NONE', #148199, #126474, #11777, .T. ) ;
#255244=TOROIDAL_SURFACE ( 'NONE', #55347, 2.100000000000002309, 0.1000000000000000056 ) ;
#255261=CARTESIAN_POINT ( 'NONE',  ( 21.97500000000000497, 66.25000000001253397, -182.2731074845244450 ) ) ;
#255284=TOROIDAL_SURFACE ( 'NONE', #68082, 4.149999999999999467, 0.1000000000000000056 ) ;
#255346=DIRECTION ( 'NONE',  ( 0.000000000000000000, 0.8660254037844281605, -0.5000000000000185407 ) ) ;
#255360=LINE ( 'NONE', #52065, #218062 ) ;
#255383=ORIENTED_EDGE ( 'NONE', *, *, #112755, .T. ) ;
#255396=CARTESIAN_POINT ( 'NONE',  ( -22.57848426163147693, 76.00426432929585019, -215.2731657914146410 ) ) ;
#255404=CARTESIAN_POINT ( 'NONE',  ( -20.85000000000000142, 68.97833521811233481, -166.3895420826271163 ) ) ;
#255406=EDGE_CURVE ( 'NONE', #100484, #15467, #19459, .T. ) ;
#255434=VERTEX_POINT ( 'NONE', #18166 ) ;
#255437=DIRECTION ( 'NONE',  ( -1.000000000000000000, 2.952720810173289112E-16, 2.061873921506763405E-30 ) ) ;
#255438=PLANE ( 'NONE',  #253002 ) ;
#255448=VERTEX_POINT ( 'NONE', #195548 ) ;
#255479=EDGE_CURVE ( 'NONE', #164247, #46606, #67618, .T. ) ;
#255503=CARTESIAN_POINT ( 'NONE',  ( 22.39999999999999858, 75.90000000001273861, -211.3138870828977360 ) ) ;
#255538=DIRECTION ( 'NONE',  ( -0.7071067811865474617, 0.7071067811865474617, 4.937700262164531476E-15 ) ) ;
#255541=CARTESIAN_POINT ( 'NONE',  ( -23.25000000000000000, 64.35000000001258513, -191.3731074845244393 ) ) ;
#255574=ORIENTED_EDGE ( 'NONE', *, *, #50288, .T. ) ;
#255583=VERTEX_POINT ( 'NONE', #126241 ) ;
#255597=VERTEX_POINT ( 'NONE', #160277 ) ;
#255681=ORIENTED_EDGE ( 'NONE', *, *, #140030, .F. ) ;
#255702=CIRCLE ( 'NONE', #138995, 0.09999999999999939493 ) ;
#255712=CARTESIAN_POINT ( 'NONE',  ( -22.50000000000000000, 64.35023708198076520, -203.6119174609113713 ) ) ;
#255722=CIRCLE ( 'NONE', #155833, 0.1000000000000070832 ) ;
#255733=CARTESIAN_POINT ( 'NONE',  ( -2.995603634470891112E-16, 69.35000000001254250, -182.2731074845244166 ) ) ;
#255736=FACE_OUTER_BOUND ( 'NONE', #222097, .T. ) ;
#255749=EDGE_CURVE ( 'NONE', #193233, #182596, #174417, .T. ) ;
#255769=DIRECTION ( 'NONE',  ( -0.000000000000000000, -0.01283462868040327436, 0.9999176327611370985 ) ) ;
#255773=DIRECTION ( 'NONE',  ( 0.000000000000000000, 0.000000000000000000, 1.000000000000000000 ) ) ;
#255775=CARTESIAN_POINT ( 'NONE',  ( 21.14999999999999858, 76.00000000001267608, -203.4231074845243654 ) ) ;
#255783=CIRCLE ( 'NONE', #10125, 0.09999999999998898659 ) ;
#255785=DIRECTION ( 'NONE',  ( 0.000000000000000000, -7.056502275159890043E-15, 1.000000000000000000 ) ) ;
#255788=CARTESIAN_POINT ( 'NONE',  ( 18.47149038651512143, 85.67145715801912331, -163.3503211497859127 ) ) ;
#255826=SPHERICAL_SURFACE ( 'NONE', #28446, 0.1000000000000000056 ) ;
#255851=ADVANCED_FACE ( 'NONE', ( #193941 ), #221899, .T. ) ;
#255865=ORIENTED_EDGE ( 'NONE', *, *, #113348, .T. ) ;
#255873=EDGE_CURVE ( 'NONE', #3432, #62026, #141650, .T. ) ;
#255887=CARTESIAN_POINT ( 'NONE',  ( -22.39999999999999858, 75.90000000001273861, -211.3138870828977645 ) ) ;
#255905=LINE ( 'NONE', #119029, #788 ) ;
#255910=CARTESIAN_POINT ( 'NONE',  ( 20.96077737575317457, 64.37609936600755134, -176.8823155274176315 ) ) ;
#255920=ORIENTED_EDGE ( 'NONE', *, *, #135086, .F. ) ;
#255934=VECTOR ( 'NONE', #72848, 1000.000000000000000 ) ;
#255950=EDGE_LOOP ( 'NONE', ( #148091, #28091, #253417, #230114 ) ) ;
#255953=ORIENTED_EDGE ( 'NONE', *, *, #69411, .T. ) ;
#255979=ORIENTED_EDGE ( 'NONE', *, *, #210839, .T. ) ;
#256011=ORIENTED_EDGE ( 'NONE', *, *, #42712, .T. ) ;
#256014=ADVANCED_FACE ( 'NONE', ( #253260 ), #201080, .F. ) ;
#256016=CARTESIAN_POINT ( 'NONE',  ( 20.94999999999999574, 74.75000000001261924, -195.5231074845243597 ) ) ;
#256041=CARTESIAN_POINT ( 'NONE',  ( 21.05000000000000071, 70.15000000001252545, -180.1556047088023149 ) ) ;
#256070=VECTOR ( 'NONE', #104420, 1000.000000000000000 ) ;
#256077=ORIENTED_EDGE ( 'NONE', *, *, #209196, .F. ) ;
#256108=VERTEX_POINT ( 'NONE', #7266 ) ;
#256161=EDGE_CURVE ( 'NONE', #108178, #139621, #178911, .T. ) ;
#256193=LINE ( 'NONE', #118037, #184852 ) ;
#256203=ADVANCED_FACE ( 'NONE', ( #141041 ), #215427, .F. ) ;
#256232=CARTESIAN_POINT ( 'NONE',  ( -23.15000000000000213, 64.35000000001249987, -177.0379132551784096 ) ) ;
#256252=DIRECTION ( 'NONE',  ( 0.000000000000000000, 0.000000000000000000, -1.000000000000000000 ) ) ;
#256278=EDGE_LOOP ( 'NONE', ( #21891, #35050, #223342, #68218 ) ) ;
#256297=ORIENTED_EDGE ( 'NONE', *, *, #43716, .F. ) ;
#256362=FACE_OUTER_BOUND ( 'NONE', #120518, .T. ) ;
#256382=DIRECTION ( 'NONE',  ( 0.000000000000000000, 0.9654727137038715545, -0.2605042016806676242 ) ) ;
#256467=ADVANCED_FACE ( 'NONE', ( #182285 ), #97149, .F. ) ;
#256481=DIRECTION ( 'NONE',  ( 1.000000000000000000, 0.000000000000000000, 0.000000000000000000 ) ) ;
#256492=DIRECTION ( 'NONE',  ( -3.469446951953995998E-14, 0.000000000000000000, -1.000000000000000000 ) ) ;
#256523=CIRCLE ( 'NONE', #219164, 0.6000000000000033085 ) ;
#256530=DIRECTION ( 'NONE',  ( -1.000000000000000000, 0.000000000000000000, 0.000000000000000000 ) ) ;
#256534=DIRECTION ( 'NONE',  ( 0.000000000000000000, 6.982962677686266711E-15, -1.000000000000000000 ) ) ;
#256547=CARTESIAN_POINT ( 'NONE',  ( 20.94999999999999929, 69.55000000001261640, -193.5060803140843859 ) ) ;
#256588=ORIENTED_EDGE ( 'NONE', *, *, #212284, .F. ) ;
#256606=ORIENTED_EDGE ( 'NONE', *, *, #22098, .F. ) ;
#256616=FACE_OUTER_BOUND ( 'NONE', #108953, .T. ) ;
#256637=CARTESIAN_POINT ( 'NONE',  ( 21.05000000000000071, 87.75000000001246292, -172.9231074845242802 ) ) ;
#256641=CARTESIAN_POINT ( 'NONE',  ( 21.05000000000000071, 65.27628289530510131, -195.8581939154368285 ) ) ;
#256665=DIRECTION ( 'NONE',  ( 1.000000000000000000, -0.000000000000000000, 0.000000000000000000 ) ) ;
#256678=VERTEX_POINT ( 'NONE', #36378 ) ;
#256683=FACE_OUTER_BOUND ( 'NONE', #5269, .T. ) ;
#256704=ORIENTED_EDGE ( 'NONE', *, *, #211019, .F. ) ;
#256706=DIRECTION ( 'NONE',  ( -1.000000000000000000, -0.000000000000000000, -0.000000000000000000 ) ) ;
#256720=EDGE_LOOP ( 'NONE', ( #253218, #199465, #75303, #183610 ) ) ;
#256772=DIRECTION ( 'NONE',  ( 1.000000000000000000, 0.000000000000000000, 0.000000000000000000 ) ) ;
#256817=CARTESIAN_POINT ( 'NONE',  ( 21.05995757104869881, 67.22461075529132302, -191.3282023615332150 ) ) ;
#256831=EDGE_CURVE ( 'NONE', #54825, #137582, #35110, .T. ) ;
#256832=AXIS2_PLACEMENT_3D ( 'NONE', #92884, #169916, #73366 ) ;
#256847=CARTESIAN_POINT ( 'NONE',  ( -20.94999999999999929, 61.95000000001248708, -175.5368025552853624 ) ) ;
#256848=DIRECTION ( 'NONE',  ( -1.000000000000000000, 0.000000000000000000, -0.000000000000000000 ) ) ;
#256887=CARTESIAN_POINT ( 'NONE',  ( 21.70464131381650219, 68.90464198104483273, -203.5231074845243882 ) ) ;
#256916=DIRECTION ( 'NONE',  ( 0.000000000000000000, -6.352154140967427193E-15, 1.000000000000000000 ) ) ;
#256917=VECTOR ( 'NONE', #179784, 1000.000000000000000 ) ;
#256939=AXIS2_PLACEMENT_3D ( 'NONE', #28141, #163783, #24286 ) ;
#256972=ORIENTED_EDGE ( 'NONE', *, *, #157717, .F. ) ;
#256981=CARTESIAN_POINT ( 'NONE',  ( 21.05000000000000071, 76.00000000001243450, -168.1231074845243540 ) ) ;
#256994=VERTEX_POINT ( 'NONE', #85699 ) ;
#257006=DIRECTION ( 'NONE',  ( 0.000000000000000000, -1.000000000000000000, -6.982962677686265922E-15 ) ) ;
#257009=ADVANCED_FACE ( 'NONE', ( #30939 ), #99558, .F. ) ;
#257041=LINE ( 'NONE', #191, #22386 ) ;
#257051=LINE ( 'NONE', #173774, #198198 ) ;
#257053=VERTEX_POINT ( 'NONE', #248668 ) ;
#257065=ORIENTED_EDGE ( 'NONE', *, *, #7283, .T. ) ;
#257076=TOROIDAL_SURFACE ( 'NONE', #65588, 7.800000000000000711, 0.1000000000000000056 ) ;
#257088=EDGE_LOOP ( 'NONE', ( #15351, #3660, #82940 ) ) ;
#257136=DIRECTION ( 'NONE',  ( 0.000000000000000000, -6.308085367188367561E-15, 1.000000000000000000 ) ) ;
#257155=DIRECTION ( 'NONE',  ( 0.000000000000000000, -0.1568667991644355497, 0.9876197685951332295 ) ) ;
#257171=CYLINDRICAL_SURFACE ( 'NONE', #154084, 11.75000000000001066 ) ;
#257240=AXIS2_PLACEMENT_3D ( 'NONE', #46018, #23926, #227226 ) ;
#257241=CARTESIAN_POINT ( 'NONE',  ( 21.05000000000000071, 76.00000000001267608, -203.5231074845243597 ) ) ;
#257258=VECTOR ( 'NONE', #167484, 1000.000000000000000 ) ;
#257283=DIRECTION ( 'NONE',  ( -1.000000000000000000, 0.000000000000000000, 0.000000000000000000 ) ) ;
#257291=CARTESIAN_POINT ( 'NONE',  ( 22.39999999999999503, 76.10085836911147794, -215.2726746080137445 ) ) ;
#257300=ADVANCED_FACE ( 'NONE', ( #78982 ), #72845, .T. ) ;
#257301=CARTESIAN_POINT ( 'NONE',  ( 21.05000000000000071, 69.45934304831145312, -203.5231074845243882 ) ) ;
#257325=DIRECTION ( 'NONE',  ( 1.000000000000000000, 0.000000000000000000, 0.000000000000000000 ) ) ;
#257328=VERTEX_POINT ( 'NONE', #46295 ) ;
#257331=CARTESIAN_POINT ( 'NONE',  ( -18.50000000000000000, 85.50000000001277556, -215.2731074845243029 ) ) ;
#257334=PLANE ( 'NONE',  #61930 ) ;
#257335=CARTESIAN_POINT ( 'NONE',  ( 21.05000000000000071, 76.00000000001270450, -207.8231074845243711 ) ) ;
#257346=DIRECTION ( 'NONE',  ( 0.000000000000000000, -0.6728971962617102953, 0.7397360091702507301 ) ) ;
#257347=CARTESIAN_POINT ( 'NONE',  ( -18.40000000000000213, 85.50000000001242029, -163.1009576351939074 ) ) ;
#257350=DIRECTION ( 'NONE',  ( 0.000000000000000000, -1.000000000000000000, -6.982962677686265922E-15 ) ) ;
#257391=DIRECTION ( 'NONE',  ( 0.000000000000000000, -1.000000000000000000, -6.982962677686266711E-15 ) ) ;
#257412=DIRECTION ( 'NONE',  ( 0.000000000000000000, 0.000000000000000000, 1.000000000000000000 ) ) ;
#257424=ORIENTED_EDGE ( 'NONE', *, *, #102978, .T. ) ;
#257477=VECTOR ( 'NONE', #57964, 1000.000000000000000 ) ;
#257508=DIRECTION ( 'NONE',  ( 0.000000000000000000, -8.338584948901395817E-15, 1.000000000000000000 ) ) ;
#257514=ORIENTED_EDGE ( 'NONE', *, *, #146304, .T. ) ;
#257534=DIRECTION ( 'NONE',  ( 0.000000000000000000, -0.4930308989875170078, -0.8700118002898356018 ) ) ;
#257554=SPHERICAL_SURFACE ( 'NONE', #210441, 0.1000000000000000056 ) ;
#257555=VERTEX_POINT ( 'NONE', #160526 ) ;
#257629=VERTEX_POINT ( 'NONE', #224317 ) ;
#257633=DIRECTION ( 'NONE',  ( 1.000000000000000000, 0.000000000000000000, 0.000000000000000000 ) ) ;
#257644=DIRECTION ( 'NONE',  ( 0.000000000000000000, 6.982962677686266711E-15, -1.000000000000000000 ) ) ;
#257655=CARTESIAN_POINT ( 'NONE',  ( 18.36493879433276177, 85.50000080620296217, -163.1009588241743984 ) ) ;
#257692=ORIENTED_EDGE ( 'NONE', *, *, #150360, .F. ) ;
#257711=ORIENTED_EDGE ( 'NONE', *, *, #204957, .F. ) ;
#257763=CARTESIAN_POINT ( 'NONE',  ( 21.14999999999999503, 76.10000000001276987, -215.1726782920691505 ) ) ;
#257787=CARTESIAN_POINT ( 'NONE',  ( -23.15000000000000213, 64.25000000001253397, -182.1731074845244507 ) ) ;
#257799=DIRECTION ( 'NONE',  ( 6.484947573744954877E-15, -0.9274965247785555977, 0.3738317757009190223 ) ) ;
#257840=CARTESIAN_POINT ( 'NONE',  ( -21.05000000000000071, 70.10000000001267040, -193.3040077198679967 ) ) ;
#257877=CIRCLE ( 'NONE', #28849, 0.4000000000000114575 ) ;
#257887=DIRECTION ( 'NONE',  ( -1.000000000000000000, 0.000000000000000000, 0.000000000000000000 ) ) ;
#257904=DIRECTION ( 'NONE',  ( 0.000000000000000000, 6.467318590049456648E-15, -1.000000000000000000 ) ) ;
#257917=VECTOR ( 'NONE', #76875, 1000.000000000000000 ) ;
#257918=AXIS2_PLACEMENT_3D ( 'NONE', #93313, #232852, #90734 ) ;
#257935=VERTEX_POINT ( 'NONE', #75541 ) ;
#257951=ADVANCED_FACE ( 'NONE', ( #124921 ), #100182, .F. ) ;
#257958=CARTESIAN_POINT ( 'NONE',  ( -20.54999999999999716, 87.75000000001253397, -182.3731074845242972 ) ) ;
#257986=CARTESIAN_POINT ( 'NONE',  ( -18.59999999999999787, 66.75000000001260503, -191.2731074845244166 ) ) ;
#258022=CARTESIAN_POINT ( 'NONE',  ( 21.46681500598285197, 76.00000000001273293, -210.3806186439483099 ) ) ;
#258037=CARTESIAN_POINT ( 'NONE',  ( -23.15000000000000213, 73.40000000001253966, -183.2477294072864709 ) ) ;
#258048=CIRCLE ( 'NONE', #187190, 0.1000000000000072220 ) ;
#258062=AXIS2_PLACEMENT_3D ( 'NONE', #205822, #87146, #187573 ) ;
#258089=DIRECTION ( 'NONE',  ( 0.000000000000000000, -7.116814260417693756E-15, 1.000000000000000000 ) ) ;
ENDSEC;
END-ISO-10303-21;
